ISO-10303-21;
HEADER;
FILE_DESCRIPTION (('STEP AP214'),
    '1' );
FILE_NAME ('straight bevel gear(output)_iso_ISO - Straight bevel gear 2M 47GT 48PT 20PA 5FW ---47O25H120MD16.0N.step',
    '2026-10-08T08:02:49',
    ( '' ),
    ( '' ),
    'SwSTEP 2.0',
    'SolidWorks 2026',
    '' );
FILE_SCHEMA (( 'AUTOMOTIVE_DESIGN' ));
ENDSEC;

DATA;
#6=ORIENTED_EDGE ( 'NONE', *, *, #7694, .T. ) ;
#7=CARTESIAN_POINT ( 'NONE',  ( 0.5848930533535030563, -19.57496322689467760, 42.61565319285014652 ) ) ;
#10=CARTESIAN_POINT ( 'NONE',  ( 5.910764540655177868, -13.99299321836483045, 14.44636214622763681 ) ) ;
#14=VERTEX_POINT ( 'NONE', #34229 ) ;
#19=CARTESIAN_POINT ( 'NONE',  ( 0.8560838555295158248, -34.16988317699912159, -32.13708010619451727 ) ) ;
#23=CARTESIAN_POINT ( 'NONE',  ( 1.092182651088189127, 25.48667707440418440, 33.27447183874333803 ) ) ;
#30=CARTESIAN_POINT ( 'NONE',  ( 0.9789233960466694473, -22.43936322751809342, -35.39508023406433068 ) ) ;
#33=CARTESIAN_POINT ( 'NONE',  ( 0.5806925824938499181, 45.08220210717423271, 12.91578164539256335 ) ) ;
#37=CARTESIAN_POINT ( 'NONE',  ( 0.8560838555295223751, -26.00596412780120303, -39.03924517540328765 ) ) ;
#40=CARTESIAN_POINT ( 'NONE',  ( 0.5832655196449135770, 40.46492986189638685, -23.70284021473238667 ) ) ;
#44=CYLINDRICAL_SURFACE ( 'NONE', #23607, 12.50000000000000000 ) ;
#45=CARTESIAN_POINT ( 'NONE',  ( 2.528190830796654964, -23.59892530385130627, 34.71807685711083025 ) ) ;
#61=VERTEX_POINT ( 'NONE', #2846 ) ;
#62=B_SPLINE_CURVE_WITH_KNOTS ( 'NONE', 3,
 ( #7041, #45606, #7993, #3579, #27403, #31488 ),
 .UNSPECIFIED., .F., .F.,
 ( 4, 2, 4 ),
 ( 1.216335680627485354E-16, 0.0002448718616795927711, 0.0004897437233590629189 ),
 .UNSPECIFIED. ) ;
#65=EDGE_CURVE ( 'NONE', #40254, #5752, #47059, .T. ) ;
#67=ORIENTED_EDGE ( 'NONE', *, *, #12959, .F. ) ;
#78=ORIENTED_EDGE ( 'NONE', *, *, #56716, .F. ) ;
#80=DIRECTION ( 'NONE',  ( 0.07906939808003035641, -0.7873210066866034307, 0.6114520935586490458 ) ) ;
#86=ORIENTED_EDGE ( 'NONE', *, *, #4568, .F. ) ;
#88=CARTESIAN_POINT ( 'NONE',  ( 1.231276596079887264, -16.87422718933211030, 38.37365278131431268 ) ) ;
#89=CARTESIAN_POINT ( 'NONE',  ( 0.7764146366350301864, -30.95828368181982881, -35.23670167801082442 ) ) ;
#95=ORIENTED_EDGE ( 'NONE', *, *, #30971, .T. ) ;
#100=CARTESIAN_POINT ( 'NONE',  ( 3.238018933889920792, 11.66219248059495683, 6.587925235854416250 ) ) ;
#102=FACE_OUTER_BOUND ( 'NONE', #56108, .T. ) ;
#105=LINE ( 'NONE', #9217, #17995 ) ;
#107=CARTESIAN_POINT ( 'NONE',  ( 0.5782707292762442330, -44.06349990951357398, -16.06687055502457540 ) ) ;
#108=CARTESIAN_POINT ( 'NONE',  ( 0.9787464366903551038, 41.90826471085239291, 0.1770361985267714100 ) ) ;
#110=ORIENTED_EDGE ( 'NONE', *, *, #11013, .T. ) ;
#123=ORIENTED_EDGE ( 'NONE', *, *, #51983, .T. ) ;
#126=DIRECTION ( 'NONE',  ( 0.07906939808003035641, 0.6497517485244377333, -0.7560229464617442829 ) ) ;
#129=VERTEX_POINT ( 'NONE', #54848 ) ;
#130=DIRECTION ( 'NONE',  ( -1.000000000000000000, -0.000000000000000000, -0.000000000000000000 ) ) ;
#142=CARTESIAN_POINT ( 'NONE',  ( 4.958415959904820092, 24.01335991616949883, 38.55596580763011616 ) ) ;
#143=VECTOR ( 'NONE', #45056, 1000.000000000000114 ) ;
#150=CARTESIAN_POINT ( 'NONE',  ( 2.528190830796656741, -41.94888846746666644, 1.595271919470088395 ) ) ;
#151=ORIENTED_EDGE ( 'NONE', *, *, #60540, .T. ) ;
#153=CARTESIAN_POINT ( 'NONE',  ( 0.6064782688330876415, 5.400824873672297244, -46.58503554901177779 ) ) ;
#154=CARTESIAN_POINT ( 'NONE',  ( 0.7056313189692692278, -13.08832644501797837, 45.03825434923295745 ) ) ;
#160=CARTESIAN_POINT ( 'NONE',  ( 4.956445790444011124, -16.41925925744418180, -44.13554095710700409 ) ) ;
#161=CARTESIAN_POINT ( 'NONE',  ( 0.9754292589017227177, -37.66327352597247824, -18.37948024844710559 ) ) ;
#167=ORIENTED_EDGE ( 'NONE', *, *, #37298, .F. ) ;
#172=B_SPLINE_CURVE_WITH_KNOTS ( 'NONE', 3,
 ( #49055, #11162, #20259, #6410, #20862, #40000, #59053, #16169, #54340, #30550, #21165, #49661, #35596, #54656, #11784, #30863, #49979, #45304, #2348 ),
 .UNSPECIFIED., .F., .F.,
 ( 4, 3, 3, 3, 3, 3, 4 ),
 ( 6.939740885162003740E-18, 0.0002732106629380659556, 0.0004098138914053819915, 0.0005464171197651502675, 0.0006830203481512588017, 0.0008196235766963637414, 0.001011968216111144630 ),
 .UNSPECIFIED. ) ;
#173=EDGE_CURVE ( 'NONE', #14818, #35927, #7295, .T. ) ;
#183=CARTESIAN_POINT ( 'NONE',  ( 0.5806925824938499181, 28.25565086187788921, -37.42780459384738379 ) ) ;
#188=CARTESIAN_POINT ( 'NONE',  ( 0.6845945791218034371, -45.78817307429869743, -10.19066863517858579 ) ) ;
#197=CARTESIAN_POINT ( 'NONE',  ( 0.9772918015221170318, 28.83491956217883967, -30.41190999581177223 ) ) ;
#206=EDGE_CURVE ( 'NONE', #20518, #58874, #57008, .T. ) ;
#210=DIRECTION ( 'NONE',  ( 1.000000000000000000, -0.000000000000000000, -0.000000000000000000 ) ) ;
#213=CARTESIAN_POINT ( 'NONE',  ( 5.910764540655177868, -1.997730036635376738, -20.01275376278557161 ) ) ;
#214=CARTESIAN_POINT ( 'NONE',  ( 0.5817216825391113844, -25.61650133936588603, -39.28141814315932123 ) ) ;
#217=VERTEX_POINT ( 'NONE', #13200 ) ;
#232=ORIENTED_EDGE ( 'NONE', *, *, #53084, .F. ) ;
#233=CARTESIAN_POINT ( 'NONE',  ( 4.291220156522059348, -21.76365521422086147, 41.78196152674276931 ) ) ;
#238=ORIENTED_EDGE ( 'NONE', *, *, #9253, .F. ) ;
#241=CARTESIAN_POINT ( 'NONE',  ( 2.618530812446115519, -21.05599821100534186, -42.02822537933690938 ) ) ;
#252=CARTESIAN_POINT ( 'NONE',  ( 0.9754292580325143458, 38.80678078702572265, -15.82280733156209784 ) ) ;
#254=CARTESIAN_POINT ( 'NONE',  ( 0.9789889208857682767, 38.62063605787587051, 16.27210399817645126 ) ) ;
#260=CARTESIAN_POINT ( 'NONE',  ( 0.9769922540276056999, -41.15456160972863131, 7.914140117357955084 ) ) ;
#263=CARTESIAN_POINT ( 'NONE',  ( 0.5837157313716003770, 4.784661690600440664, -46.65130304813069273 ) ) ;
#270=CARTESIAN_POINT ( 'NONE',  ( 3.782542959838391727, 11.41479611462064980, -40.45911866388357936 ) ) ;
#272=CARTESIAN_POINT ( 'NONE',  ( 0.5797568599927143129, 40.66629966594037171, -23.35545718137295168 ) ) ;
#279=CARTESIAN_POINT ( 'NONE',  ( 5.895881250540457863, 16.57931246612949394, -11.38657454016544968 ) ) ;
#284=CARTESIAN_POINT ( 'NONE',  ( 4.960386119450151732, 7.741275488564681950, -43.06401187166018474 ) ) ;
#285=CARTESIAN_POINT ( 'NONE',  ( 5.838029081930957709, 35.04472919977139611, 31.66910187339719940 ) ) ;
#289=FACE_OUTER_BOUND ( 'NONE', #54400, .T. ) ;
#290=ORIENTED_EDGE ( 'NONE', *, *, #8641, .T. ) ;
#296=B_SPLINE_CURVE_WITH_KNOTS ( 'NONE', 3,
 ( #42728, #61184, #18606, #18304, #13602, #32708 ),
 .UNSPECIFIED., .F., .F.,
 ( 4, 2, 4 ),
 ( 1.217335034318563839E-16, 0.0002448718616795921206, 0.0004897437233590624852 ),
 .UNSPECIFIED. ) ;
#299=CARTESIAN_POINT ( 'NONE',  ( 4.956445790443988031, 47.01859095792194410, 2.605792484304518375 ) ) ;
#300=ORIENTED_EDGE ( 'NONE', *, *, #3443, .F. ) ;
#301=CARTESIAN_POINT ( 'NONE',  ( 4.962356264823601926, -41.65024625884322518, 6.040909239515423579 ) ) ;
#304=FACE_OUTER_BOUND ( 'NONE', #29189, .T. ) ;
#308=CARTESIAN_POINT ( 'NONE',  ( 0.5837157313716025975, 40.30294267679386877, 23.97727831037320456 ) ) ;
#312=CARTESIAN_POINT ( 'NONE',  ( 0.5817217712918332229, 16.42911102810642632, 43.92401694784443578 ) ) ;
#313=ORIENTED_EDGE ( 'NONE', *, *, #32073, .T. ) ;
#319=CARTESIAN_POINT ( 'NONE',  ( 0.5806925824938502512, 46.40146083665138832, -6.791670970259978013 ) ) ;
#321=ORIENTED_EDGE ( 'NONE', *, *, #58759, .F. ) ;
#322=CARTESIAN_POINT ( 'NONE',  ( 1.157643937452369043, 25.52398866004628886, 33.24948537160511108 ) ) ;
#325=CARTESIAN_POINT ( 'NONE',  ( 0.9788927965476030835, -34.63124975320486953, -23.60112609946664008 ) ) ;
#328=CARTESIAN_POINT ( 'NONE',  ( 0.9790724872846759963, -22.51621571723094561, -35.34621959639500233 ) ) ;
#330=EDGE_CURVE ( 'NONE', #57580, #41543, #34967, .T. ) ;
#339=ADVANCED_FACE ( 'NONE', ( #24744 ), #40840, .F. ) ;
#342=CARTESIAN_POINT ( 'NONE',  ( 0.5797568665920704856, 46.55714410835498995, 5.626512336762159450 ) ) ;
#343=CARTESIAN_POINT ( 'NONE',  ( -69.95594261585600293, 0.000000000000000000, -12.50000000000000000 ) ) ;
#346=CARTESIAN_POINT ( 'NONE',  ( 0.8554163680231738898, 33.26717477998096228, -33.08323677136228724 ) ) ;
#347=CARTESIAN_POINT ( 'NONE',  ( 0.5834584762367746036, -1.749022159738321536, 46.86338560644049522 ) ) ;
#349=CARTESIAN_POINT ( 'NONE',  ( 0.5835871038041865466, 45.26563263149099470, -12.25793438440576821 ) ) ;
#350=LINE ( 'NONE', #10092, #1144 ) ;
#354=CARTESIAN_POINT ( 'NONE',  ( 5.894904586330512508, -20.11291651039286066, -0.001227847351197789826 ) ) ;
#366=ORIENTED_EDGE ( 'NONE', *, *, #38922, .T. ) ;
#371=VERTEX_POINT ( 'NONE', #31845 ) ;
#372=CARTESIAN_POINT ( 'NONE',  ( 2.618530812446111078, 9.522253559614041407, 46.03317799527443555 ) ) ;
#378=CARTESIAN_POINT ( 'NONE',  ( 0.9783242366443567484, -39.67693573533197338, 13.49352662801158331 ) ) ;
#388=ORIENTED_EDGE ( 'NONE', *, *, #42181, .T. ) ;
#390=CARTESIAN_POINT ( 'NONE',  ( 3.782625744892854414, -16.11616831265073557, 38.82663033297269806 ) ) ;
#397=EDGE_CURVE ( 'NONE', #43088, #32860, #59563, .T. ) ;
#414=B_SPLINE_CURVE_WITH_KNOTS ( 'NONE', 3,
 ( #40927, #35601, #2041, #21474, #2662, #7043 ),
 .UNSPECIFIED., .F., .F.,
 ( 4, 2, 4 ),
 ( 3.471140604459641645E-18, 0.0002291459268755710208, 0.0004582918537511385722 ),
 .UNSPECIFIED. ) ;
#415=CONICAL_SURFACE ( 'NONE', #48459, 42.08604991992415023, 1.569615340895231137 ) ;
#417=CARTESIAN_POINT ( 'NONE',  ( 1.000433927950263424, 3.539116715176812367, -41.75994888082603751 ) ) ;
#425=CARTESIAN_POINT ( 'NONE',  ( 5.895881250540457863, -15.78174954617507453, -12.46852288244697071 ) ) ;
#432=CARTESIAN_POINT ( 'NONE',  ( 0.8560838555295158248, -14.76796170096741534, 44.52280473286123907 ) ) ;
#433=CARTESIAN_POINT ( 'NONE',  ( 4.958415959904820980, -16.79601473596579453, 42.20305489904562535 ) ) ;
#436=DIRECTION ( 'NONE',  ( -1.000000000000000000, -0.000000000000000000, -0.000000000000000000 ) ) ;
#440=FACE_OUTER_BOUND ( 'NONE', #59744, .T. ) ;
#442=ORIENTED_EDGE ( 'NONE', *, *, #38279, .F. ) ;
#443=CARTESIAN_POINT ( 'NONE',  ( 4.962356264823608143, 39.61238188121388504, 14.21600504921214814 ) ) ;
#453=CARTESIAN_POINT ( 'NONE',  ( 1.231276596079887264, 33.41651732065550817, 25.31033664684050777 ) ) ;
#455=CARTESIAN_POINT ( 'NONE',  ( 0.5824936645240066380, 17.19419371894991500, -43.63024044622647324 ) ) ;
#458=FACE_OUTER_BOUND ( 'NONE', #15532, .T. ) ;
#468=FACE_OUTER_BOUND ( 'NONE', #1447, .T. ) ;
#477=CARTESIAN_POINT ( 'NONE',  ( 0.8554163680231708922, 28.56078411578483056, -37.22213163970263139 ) ) ;
#482=CARTESIAN_POINT ( 'NONE',  ( 4.962356264823602814, 39.61238188121407688, -14.21600504921160812 ) ) ;
#486=EDGE_CURVE ( 'NONE', #49719, #55841, #52030, .T. ) ;
#492=CARTESIAN_POINT ( 'NONE',  ( 4.956445790443998689, -17.42806872899825521, 43.74700527484080936 ) ) ;
#493=CARTESIAN_POINT ( 'NONE',  ( 0.9754292589017224957, -40.94879475388736267, 8.917604784878262691 ) ) ;
#499=CARTESIAN_POINT ( 'NONE',  ( 0.9789233960466690032, 41.51700863864244440, 5.716180589452370064 ) ) ;
#500=CARTESIAN_POINT ( 'NONE',  ( 5.894904586330512508, -15.78536547177706773, 12.46401416013601171 ) ) ;
#502=CARTESIAN_POINT ( 'NONE',  ( 5.895881250540457863, 10.82621851909522803, 16.95053610317680892 ) ) ;
#504=CARTESIAN_POINT ( 'NONE',  ( 4.956445790444004018, -47.08764048036452721, -0.5405220916603282744 ) ) ;
#506=CARTESIAN_POINT ( 'NONE',  ( 5.895881250540457863, 19.71075194021738852, 4.001742065590625508 ) ) ;
#510=CARTESIAN_POINT ( 'NONE',  ( 4.956445790443991584, 39.12691469763999663, 26.20348443209871903 ) ) ;
#511=DIRECTION ( 'NONE',  ( -0.07906939808003034253, -0.7447223275783662055, -0.6626738904570801392 ) ) ;
#525=ORIENTED_EDGE ( 'NONE', *, *, #29778, .F. ) ;
#532=B_SPLINE_CURVE_WITH_KNOTS ( 'NONE', 3,
 ( #47179, #28362, #4227, #47482 ),
 .UNSPECIFIED., .F., .F.,
 ( 4, 4 ),
 ( 0.000000000000000000, 0.005004948556313794893 ),
 .UNSPECIFIED. ) ;
#533=ADVANCED_FACE ( 'NONE', ( #9251 ), #17209, .F. ) ;
#535=CARTESIAN_POINT ( 'NONE',  ( 4.962356264823598373, -19.84272732133986139, 37.11471096901200895 ) ) ;
#537=EDGE_CURVE ( 'NONE', #3024, #29827, #532, .T. ) ;
#539=VERTEX_POINT ( 'NONE', #4530 ) ;
#543=FACE_OUTER_BOUND ( 'NONE', #2482, .T. ) ;
#544=CARTESIAN_POINT ( 'NONE',  ( 5.895596859100789899, -4.659086063546006073, 19.56581458219818259 ) ) ;
#550=CARTESIAN_POINT ( 'NONE',  ( 1.000110580585049425, 40.58939401150527004, -10.43640630440781258 ) ) ;
#555=CARTESIAN_POINT ( 'NONE',  ( 5.910764540655177868, 0.6875337509668891789, -20.10046108452351987 ) ) ;
#556=CARTESIAN_POINT ( 'NONE',  ( 0.9772918015221170318, 35.84507786591080958, -21.71329658383247363 ) ) ;
#559=EDGE_LOOP ( 'NONE', ( #5677, #4763, #51928, #14978 ) ) ;
#561=EDGE_CURVE ( 'NONE', #53916, #49170, #12131, .T. ) ;
#567=ADVANCED_FACE ( 'NONE', ( #52778 ), #57973, .F. ) ;
#569=CARTESIAN_POINT ( 'NONE',  ( 4.962356264823608143, 0.000000000000000000, 0.000000000000000000 ) ) ;
#573=CARTESIAN_POINT ( 'NONE',  ( 0.9790850452238877288, -27.09605925476339294, -31.97093841484085885 ) ) ;
#574=CARTESIAN_POINT ( 'NONE',  ( 0.5806925824938499181, 5.237374507879953178, -46.60249210726582447 ) ) ;
#576=ORIENTED_EDGE ( 'NONE', *, *, #47910, .T. ) ;
#589=FACE_OUTER_BOUND ( 'NONE', #57216, .T. ) ;
#591=CARTESIAN_POINT ( 'NONE',  ( 0.9787464366903563251, -34.65110827157835161, 23.57190464179372569 ) ) ;
#595=CARTESIAN_POINT ( 'NONE',  ( 0.5804410086790514622, -38.97211966759181934, 26.09010809617888427 ) ) ;
#603=CARTESIAN_POINT ( 'NONE',  ( 0.8554163680231738898, 36.24698750680799009, 29.78861141095913112 ) ) ;
#624=( BOUNDED_SURFACE ( )  B_SPLINE_SURFACE ( 3, 1, ( 
 ( #9004, #37856 ),
 ( #26963, #2518 ),
 ( #41390, #56916 ),
 ( #21644, #47233 ) ),
 .UNSPECIFIED., .F., .F., .F. ) 
 B_SPLINE_SURFACE_WITH_KNOTS ( ( 4, 4 ),
 ( 2, 2 ),
 ( 0.000000000000000000, 1.000000000000000000 ),
 ( 0.000000000000000000, 1.000000000000000000 ),
 .UNSPECIFIED. ) 
 GEOMETRIC_REPRESENTATION_ITEM ( )  RATIONAL_B_SPLINE_SURFACE ( (
 ( 1.000000000000000000, 1.000000000000000000),
 ( 0.9952954269826590483, 0.8620686068821307169),
 ( 0.9952954269826590483, 0.8620686068821307169),
 ( 1.000000000000000000, 1.000000000000000000) ) ) 
 REPRESENTATION_ITEM ( '' )  SURFACE ( )  );
#639=EDGE_CURVE ( 'NONE', #7531, #35778, #49498, .T. ) ;
#654=CARTESIAN_POINT ( 'NONE',  ( 5.917102823773431552, 5.950457534745815735, 19.21150106521946910 ) ) ;
#665=FACE_OUTER_BOUND ( 'NONE', #5662, .T. ) ;
#674=CARTESIAN_POINT ( 'NONE',  ( 0.9790850452238870627, -1.349767895839444121, 41.88693658995079261 ) ) ;
#676=ORIENTED_EDGE ( 'NONE', *, *, #35823, .T. ) ;
#695=DIRECTION ( 'NONE',  ( -1.000000000000000000, -0.000000000000000000, -0.000000000000000000 ) ) ;
#698=EDGE_LOOP ( 'NONE', ( #12368, #22476, #25732, #52712 ) ) ;
#701=CARTESIAN_POINT ( 'NONE',  ( 5.910764540655178756, -9.651974367318080894, 17.64484710281723068 ) ) ;
#704=ORIENTED_EDGE ( 'NONE', *, *, #30101, .T. ) ;
#706=CARTESIAN_POINT ( 'NONE',  ( 4.956445790444022670, -4.175462451061590308, -46.90526157542895191 ) ) ;
#707=DIRECTION ( 'NONE',  ( 0.000000000000000000, 0.000000000000000000, 1.000000000000000000 ) ) ;
#713=CARTESIAN_POINT ( 'NONE',  ( 5.838029081930957709, -22.71741985886527715, -41.41236401256216482 ) ) ;
#715=VERTEX_POINT ( 'NONE', #55863 ) ;
#734=CARTESIAN_POINT ( 'NONE',  ( 5.894904586330512508, 12.98639672351314189, 15.35848013968732140 ) ) ;
#766=CARTESIAN_POINT ( 'NONE',  ( 0.5824935313925968527, -45.88237815356815474, 9.697708596715390428 ) ) ;
#779=CARTESIAN_POINT ( 'NONE',  ( 0.5806925824938499181, 46.89268439822727430, -0.5463627657667492477 ) ) ;
#781=CARTESIAN_POINT ( 'NONE',  ( 0.9762797500689124330, -40.96497924994810091, -8.842808390835211085 ) ) ;
#785=ORIENTED_EDGE ( 'NONE', *, *, #4685, .F. ) ;
#788=VECTOR ( 'NONE', #13466, 1000.000000000000114 ) ;
#789=VERTEX_POINT ( 'NONE', #46810 ) ;
#791=CARTESIAN_POINT ( 'NONE',  ( 0.5797568665920712627, -0.9380854118316781509, 46.88651516547137987 ) ) ;
#794=B_SPLINE_CURVE_WITH_KNOTS ( 'NONE', 3,
 ( #8782, #27896, #8163, #37018, #46401, #3447 ),
 .UNSPECIFIED., .F., .F.,
 ( 4, 2, 4 ),
 ( 1.051843754078492886E-17, 0.0002448709889506574819, 0.0004897419779013044471 ),
 .UNSPECIFIED. ) ;
#795=ORIENTED_EDGE ( 'NONE', *, *, #6044, .T. ) ;
#798=CARTESIAN_POINT ( 'NONE',  ( 1.231276596079881047, 40.19859528295886975, 11.88905834349143653 ) ) ;
#827=CARTESIAN_POINT ( 'NONE',  ( 0.9762797500689124330, -26.66896101499549587, -32.32787193067855469 ) ) ;
#831=( BOUNDED_SURFACE ( )  B_SPLINE_SURFACE ( 3, 1, ( 
 ( #41675, #17861 ),
 ( #21625, #46373 ),
 ( #50730, #27252 ),
 ( #60738, #2807 ) ),
 .UNSPECIFIED., .F., .F., .F. ) 
 B_SPLINE_SURFACE_WITH_KNOTS ( ( 4, 4 ),
 ( 2, 2 ),
 ( 0.000000000000000000, 1.000000000000000000 ),
 ( 0.000000000000000000, 1.000000000000000000 ),
 .UNSPECIFIED. ) 
 GEOMETRIC_REPRESENTATION_ITEM ( )  RATIONAL_B_SPLINE_SURFACE ( (
 ( 1.000000000000000000, 1.000000000000000000),
 ( 0.9729067724841187204, 0.9999501103223794596),
 ( 0.9729067724841187204, 0.9999501103223794596),
 ( 1.000000000000000000, 1.000000000000000000) ) ) 
 REPRESENTATION_ITEM ( '' )  SURFACE ( )  );
#832=CARTESIAN_POINT ( 'NONE',  ( 0.9789889208857702751, -6.875788487547667138, 41.34075991944121142 ) ) ;
#834=CARTESIAN_POINT ( 'NONE',  ( 0.9762797500689124330, 28.76866969768027715, -30.47438972336406238 ) ) ;
#835=CARTESIAN_POINT ( 'NONE',  ( 4.958415959904818315, -35.95869674887519807, -27.75204644607441296 ) ) ;
#840=FACE_OUTER_BOUND ( 'NONE', #26080, .T. ) ;
#847=CARTESIAN_POINT ( 'NONE',  ( 0.5797568665920715958, -38.30338252035704016, 27.05690662476175490 ) ) ;
#862=ORIENTED_EDGE ( 'NONE', *, *, #14237, .T. ) ;
#863=CARTESIAN_POINT ( 'NONE',  ( 5.917102823773431552, 19.00193826451960888, 6.589086449814391955 ) ) ;
#864=CARTESIAN_POINT ( 'NONE',  ( 5.894904586330512508, -4.661384928609073164, 19.56529842882492076 ) ) ;
#867=EDGE_CURVE ( 'NONE', #47641, #16356, #52484, .T. ) ;
#869=CARTESIAN_POINT ( 'NONE',  ( 5.896782393890504181, 14.91246379622012874, 13.49609241241464375 ) ) ;
#872=CARTESIAN_POINT ( 'NONE',  ( 3.238018933889920792, -13.17791601574921145, 2.397920317590518824 ) ) ;
#876=CARTESIAN_POINT ( 'NONE',  ( 0.8560838555295223751, -46.85553835019177882, -2.220666565569921591 ) ) ;
#892=ORIENTED_EDGE ( 'NONE', *, *, #60788, .T. ) ;
#893=CARTESIAN_POINT ( 'NONE',  ( 0.9762797500689124330, -40.96497924994810091, -8.842808390835211085 ) ) ;
#895=ORIENTED_EDGE ( 'NONE', *, *, #36444, .F. ) ;
#902=ORIENTED_EDGE ( 'NONE', *, *, #5659, .F. ) ;
#908=CARTESIAN_POINT ( 'NONE',  ( 1.000110580585051201, -41.76694666412394241, -3.455379737181916600 ) ) ;
#919=FACE_OUTER_BOUND ( 'NONE', #8044, .T. ) ;
#928=CARTESIAN_POINT ( 'NONE',  ( 1.000110580585050091, 38.32249311736364916, 16.96478717937593572 ) ) ;
#932=ORIENTED_EDGE ( 'NONE', *, *, #47477, .F. ) ;
#934=VECTOR ( 'NONE', #9923, 999.9999999999998863 ) ;
#935=EDGE_LOOP ( 'NONE', ( #31985, #2475, #19862, #53772 ) ) ;
#946=CARTESIAN_POINT ( 'NONE',  ( 0.5837800005270550319, 40.34941272192465078, 23.89895712447661680 ) ) ;
#949=CARTESIAN_POINT ( 'NONE',  ( 0.5806925824938502512, 32.20670061096268455, -34.08739940358283604 ) ) ;
#955=CARTESIAN_POINT ( 'NONE',  ( 4.962356264823609031, -20.60668162140307658, 36.69605251817252878 ) ) ;
#960=CARTESIAN_POINT ( 'NONE',  ( 0.9780303403264759554, -12.72545693111817400, -39.92996818542863480 ) ) ;
#963=CARTESIAN_POINT ( 'NONE',  ( 0.7056759521544929692, -39.13842014767732280, 25.84439779644466384 ) ) ;
#969=EDGE_CURVE ( 'NONE', #49966, #55475, #35315, .T. ) ;
#975=VECTOR ( 'NONE', #8436, 1000.000000000000227 ) ;
#981=CARTESIAN_POINT ( 'NONE',  ( 0.5806925824938494740, -1.020860314013172454, 46.88475452172951918 ) ) ;
#982=EDGE_CURVE ( 'NONE', #10729, #25288, #1299, .T. ) ;
#984=ORIENTED_EDGE ( 'NONE', *, *, #31684, .F. ) ;
#993=B_SPLINE_CURVE_WITH_KNOTS ( 'NONE', 3,
 ( #7007, #34629, #29915, #16436 ),
 .UNSPECIFIED., .F., .F.,
 ( 4, 4 ),
 ( 0.000000000000000000, 0.004447772540403792038 ),
 .UNSPECIFIED. ) ;
#999=CARTESIAN_POINT ( 'NONE',  ( 4.956445790444027111, 8.365049606152357597, -46.34181691762039179 ) ) ;
#1000=ORIENTED_EDGE ( 'NONE', *, *, #47037, .T. ) ;
#1015=CARTESIAN_POINT ( 'NONE',  ( 5.895596859100789899, -7.232071727009982354, -18.76766692340500242 ) ) ;
#1022=CARTESIAN_POINT ( 'NONE',  ( 2.282803330402978670, 45.63374208672272658, -11.13815472237010695 ) ) ;
#1035=CARTESIAN_POINT ( 'NONE',  ( 3.782625744892853081, -19.24499441524892518, -37.37470125702732560 ) ) ;
#1038=DIRECTION ( 'NONE',  ( 0.000000000000000000, 0.000000000000000000, 1.000000000000000000 ) ) ;
#1039=B_SPLINE_CURVE_WITH_KNOTS ( 'NONE', 3,
 ( #22633, #61430, #38919, #57348 ),
 .UNSPECIFIED., .F., .F.,
 ( 4, 4 ),
 ( 1.226634733346699349E-18, 0.004042984057420973693 ),
 .UNSPECIFIED. ) ;
#1042=EDGE_CURVE ( 'NONE', #26356, #28755, #19522, .T. ) ;
#1050=CARTESIAN_POINT ( 'NONE',  ( 4.962356264823601926, 34.44911810793277596, -24.17630781256817940 ) ) ;
#1054=CARTESIAN_POINT ( 'NONE',  ( 0.7056759521544955227, 45.45046072100352319, -11.57602908451353585 ) ) ;
#1065=CARTESIAN_POINT ( 'NONE',  ( 1.091591847532191073, 36.45402868198649315, -20.68484430226018489 ) ) ;
#1074=CARTESIAN_POINT ( 'NONE',  ( 1.000433927950263646, 33.29480191618684159, 25.45338568864124795 ) ) ;
#1077=CARTESIAN_POINT ( 'NONE',  ( 4.962356264823608143, 0.000000000000000000, 0.000000000000000000 ) ) ;
#1080=CARTESIAN_POINT ( 'NONE',  ( 0.8560838555295223751, -34.16988317699956923, 32.13708010619405542 ) ) ;
#1085=CARTESIAN_POINT ( 'NONE',  ( 0.9754292589017198312, -30.68784786461271352, 28.54090854078868844 ) ) ;
#1089=CARTESIAN_POINT ( 'NONE',  ( 3.661933894777877896, -12.12681416997633121, -45.44855930652273912 ) ) ;
#1090=CARTESIAN_POINT ( 'NONE',  ( 5.896782393890504181, -13.97772289704270676, -14.46199673252280249 ) ) ;
#1092=ORIENTED_EDGE ( 'NONE', *, *, #34956, .T. ) ;
#1107=EDGE_CURVE ( 'NONE', #42042, #20290, #49545, .T. ) ;
#1109=CARTESIAN_POINT ( 'NONE',  ( 4.291220156522059348, 18.92432707711549256, -43.14230918696924277 ) ) ;
#1110=CARTESIAN_POINT ( 'NONE',  ( 0.7764146366350254125, 45.46540463260674159, 11.52985061752779394 ) ) ;
#1116=EDGE_CURVE ( 'NONE', #39908, #48550, #49093, .T. ) ;
#1122=CARTESIAN_POINT ( 'NONE',  ( 0.7056313189692690058, 16.06732225071473508, -44.06347466609102526 ) ) ;
#1125=CARTESIAN_POINT ( 'NONE',  ( 0.5804410086790514622, -45.84731009780851707, -9.876437042313495951 ) ) ;
#1130=CARTESIAN_POINT ( 'NONE',  ( 4.291220156522060236, -47.09990378333908723, -0.9940125280393553586 ) ) ;
#1133=CARTESIAN_POINT ( 'NONE',  ( 4.956445790444002242, -36.61936279692601204, 29.60676136436992678 ) ) ;
#1135=ORIENTED_EDGE ( 'NONE', *, *, #2307, .F. ) ;
#1141=CARTESIAN_POINT ( 'NONE',  ( 4.960386119450139297, 41.48529788082155534, 13.90706742673822838 ) ) ;
#1142=CARTESIAN_POINT ( 'NONE',  ( 1.157644175074338921, -41.23316702885658458, 7.538448928632200285 ) ) ;
#1144=VECTOR ( 'NONE', #29188, 1000.000000000000000 ) ;
#1148=DIRECTION ( 'NONE',  ( 0.07906939808003035641, 0.2876259487683096583, 0.9544733332484420796 ) ) ;
#1154=ORIENTED_EDGE ( 'NONE', *, *, #29107, .T. ) ;
#1158=CARTESIAN_POINT ( 'NONE',  ( 0.5835226383429259478, -34.65813563702828759, 31.59202603049256908 ) ) ;
#1162=CARTESIAN_POINT ( 'NONE',  ( 0.8554163680231720024, -44.61245466728215092, -14.52357950615188642 ) ) ;
#1163=CARTESIAN_POINT ( 'NONE',  ( 0.9769922540276050338, 40.30057869606137899, 11.49760461351358209 ) ) ;
#1170=CARTESIAN_POINT ( 'NONE',  ( 4.960386119450136633, 7.741275488564100193, 43.06401187166027711 ) ) ;
#1171=ORIENTED_EDGE ( 'NONE', *, *, #26743, .F. ) ;
#1183=VECTOR ( 'NONE', #23803, 1000.000000000000000 ) ;
#1187=CARTESIAN_POINT ( 'NONE',  ( 0.9784957157296363395, -31.23728338876063049, -27.93859666272861375 ) ) ;
#1191=CARTESIAN_POINT ( 'NONE',  ( 0.9787464366903556590, -26.92194882595154226, -32.11763790043268330 ) ) ;
#1193=ORIENTED_EDGE ( 'NONE', *, *, #12418, .F. ) ;
#1195=CARTESIAN_POINT ( 'NONE',  ( 0.6845945791218023269, 28.51769667890508586, 37.24442907125723679 ) ) ;
#1197=ORIENTED_EDGE ( 'NONE', *, *, #37868, .F. ) ;
#1198=ADVANCED_FACE ( 'NONE', ( #22914 ), #35941, .F. ) ;
#1205=CARTESIAN_POINT ( 'NONE',  ( 4.960386119450149955, -10.60034705332619431, 42.45078452774905742 ) ) ;
#1208=DIRECTION ( 'NONE',  ( -0.07906939808003035641, 0.8535645278111612111, -0.5149520629629237289 ) ) ;
#1211=ADVANCED_FACE ( 'NONE', ( #23215 ), #34056, .F. ) ;
#1215=CARTESIAN_POINT ( 'NONE',  ( 3.238018933889920792, -8.435922058907767251, -10.40397574889937182 ) ) ;
#1218=CARTESIAN_POINT ( 'NONE',  ( 5.896782393890504181, 12.98055409426303441, 15.36331026452057813 ) ) ;
#1219=DIRECTION ( 'NONE',  ( 0.000000000000000000, 0.000000000000000000, 1.000000000000000000 ) ) ;
#1228=EDGE_CURVE ( 'NONE', #21594, #10282, #26979, .T. ) ;
#1229=DIRECTION ( 'NONE',  ( 0.000000000000000000, 0.000000000000000000, -1.000000000000000000 ) ) ;
#1230=ORIENTED_EDGE ( 'NONE', *, *, #16681, .T. ) ;
#1231=CARTESIAN_POINT ( 'NONE',  ( 4.962356264823598373, -24.61258717641114657, 34.13877780978559429 ) ) ;
#1239=ORIENTED_EDGE ( 'NONE', *, *, #35443, .F. ) ;
#1250=ORIENTED_EDGE ( 'NONE', *, *, #39355, .F. ) ;
#1251=CARTESIAN_POINT ( 'NONE',  ( 4.960386119450149955, -43.42409617054094895, 5.365103581847332492 ) ) ;
#1255=EDGE_LOOP ( 'NONE', ( #52868, #40210, #7155, #49299 ) ) ;
#1260=EDGE_CURVE ( 'NONE', #26356, #29096, #28406, .T. ) ;
#1261=( BOUNDED_SURFACE ( )  B_SPLINE_SURFACE ( 3, 1, ( 
 ( #23943, #43376 ),
 ( #19562, #4803 ),
 ( #734, #10776 ),
 ( #15169, #29554 ) ),
 .UNSPECIFIED., .F., .F., .F. ) 
 B_SPLINE_SURFACE_WITH_KNOTS ( ( 4, 4 ),
 ( 2, 2 ),
 ( 0.000000000000000000, 1.000000000000000000 ),
 ( 0.000000000000000000, 1.000000000000000000 ),
 .UNSPECIFIED. ) 
 GEOMETRIC_REPRESENTATION_ITEM ( )  RATIONAL_B_SPLINE_SURFACE ( (
 ( 1.000000000000000000, 1.000000000000000000),
 ( 0.9729067724841187204, 0.9999501103223794596),
 ( 0.9729067724841187204, 0.9999501103223794596),
 ( 1.000000000000000000, 1.000000000000000000) ) ) 
 REPRESENTATION_ITEM ( '' )  SURFACE ( )  );
#1273=CARTESIAN_POINT ( 'NONE',  ( 0.7764146366350237471, 46.59651770594938114, 5.367030030502223603 ) ) ;
#1279=CARTESIAN_POINT ( 'NONE',  ( 4.962356264823609919, 39.89814050050791394, -13.39305724859256763 ) ) ;
#1287=DIRECTION ( 'NONE',  ( -1.000000000000000000, -0.000000000000000000, -0.000000000000000000 ) ) ;
#1295=ORIENTED_EDGE ( 'NONE', *, *, #60687, .F. ) ;
#1296=ORIENTED_EDGE ( 'NONE', *, *, #57741, .T. ) ;
#1299=LINE ( 'NONE', #19836, #50083 ) ;
#1304=EDGE_LOOP ( 'NONE', ( #45179, #2061, #25588, #25077 ) ) ;
#1311=CARTESIAN_POINT ( 'NONE',  ( 4.956445790444022670, -4.175462451061590308, -46.90526157542895191 ) ) ;
#1312=CARTESIAN_POINT ( 'NONE',  ( 0.5806925824938499181, -14.41498975133639426, 44.62544602368059543 ) ) ;
#1318=CARTESIAN_POINT ( 'NONE',  ( 4.956445790444041322, 46.03642002599030292, -9.908889005849065512 ) ) ;
#1328=CARTESIAN_POINT ( 'NONE',  ( 0.9787284016396621267, -39.65084253017462146, -13.57006579114940870 ) ) ;
#1331=CARTESIAN_POINT ( 'NONE',  ( 0.9780106845699487739, 15.35453589240238870, -38.99448004505720178 ) ) ;
#1336=CARTESIAN_POINT ( 'NONE',  ( 0.9788927965476035276, 9.577372930391250705, -40.79963897369664494 ) ) ;
#1343=FACE_OUTER_BOUND ( 'NONE', #51667, .T. ) ;
#1354=CARTESIAN_POINT ( 'NONE',  ( 1.157644175074339365, -27.68781125088666428, 31.47042077275824568 ) ) ;
#1358=FACE_OUTER_BOUND ( 'NONE', #43017, .T. ) ;
#1368=FACE_OUTER_BOUND ( 'NONE', #44704, .T. ) ;
#1373=EDGE_CURVE ( 'NONE', #30313, #7742, #20985, .T. ) ;
#1375=ADVANCED_FACE ( 'NONE', ( #304 ), #29263, .F. ) ;
#1382=CARTESIAN_POINT ( 'NONE',  ( 4.962356264823603702, 37.36413190407388640, -19.36897635181878030 ) ) ;
#1388=CARTESIAN_POINT ( 'NONE',  ( 0.6845945791218023269, -8.654967045697796735, -46.10312425586610630 ) ) ;
#1391=CARTESIAN_POINT ( 'NONE',  ( 0.5817217712918331118, -14.32834839058178389, 44.65348123502227651 ) ) ;
#1393=CARTESIAN_POINT ( 'NONE',  ( 4.958415959904820092, 43.07243048339554292, -14.42115411732696195 ) ) ;
#1397=CARTESIAN_POINT ( 'NONE',  ( 5.896782393890504181, 10.81700609697900894, -16.95636948099241792 ) ) ;
#1402=ORIENTED_EDGE ( 'NONE', *, *, #22563, .F. ) ;
#1403=CARTESIAN_POINT ( 'NONE',  ( 1.231276596079887264, -13.22565419921979313, -39.77887431816952102 ) ) ;
#1414=VERTEX_POINT ( 'NONE', #55901 ) ;
#1416=CARTESIAN_POINT ( 'NONE',  ( 0.9775691876210979014, 41.48266884170315194, 5.960024728101428693 ) ) ;
#1428=ADVANCED_FACE ( 'NONE', ( #13320 ), #35699, .F. ) ;
#1432=CARTESIAN_POINT ( 'NONE',  ( 0.8560838555295223751, -29.58154842764516701, 36.40473632241573654 ) ) ;
#1438=CARTESIAN_POINT ( 'NONE',  ( 4.956445790443988919, 44.65954324082213134, 14.93530206124989945 ) ) ;
#1441=EDGE_LOOP ( 'NONE', ( #60485, #13982, #14945, #61799 ) ) ;
#1443=CARTESIAN_POINT ( 'NONE',  ( 3.782625744892851749, 30.43998245888566245, 28.99388852840778341 ) ) ;
#1447=EDGE_LOOP ( 'NONE', ( #2708, #42694, #34709, #41037 ) ) ;
#1448=EDGE_CURVE ( 'NONE', #42568, #34245, #40424, .T. ) ;
#1459=CARTESIAN_POINT ( 'NONE',  ( 0.9762797500689124330, 4.697980241569248427, -41.64437257103928403 ) ) ;
#1462=CARTESIAN_POINT ( 'NONE',  ( 0.8554163680231816613, 40.82560365045065254, 23.11872746688558067 ) ) ;
#1463=ADVANCED_FACE ( 'NONE', ( #56515 ), #12099, .F. ) ;
#1466=VERTEX_POINT ( 'NONE', #41840 ) ;
#1469=ORIENTED_EDGE ( 'NONE', *, *, #537, .F. ) ;
#1472=EDGE_CURVE ( 'NONE', #22620, #59460, #15009, .T. ) ;
#1482=CARTESIAN_POINT ( 'NONE',  ( 3.238018933889920792, 5.069615556373155307, 12.39784217024205759 ) ) ;
#1491=CARTESIAN_POINT ( 'NONE',  ( 0.9789233960466698914, -26.95685022293044142, -32.08839280629113944 ) ) ;
#1499=FACE_OUTER_BOUND ( 'NONE', #22375, .T. ) ;
#1500=CIRCLE ( 'NONE', #4484, 42.08604991992415023 ) ;
#1504=CARTESIAN_POINT ( 'NONE',  ( 5.895881250540457863, -13.98558879082075634, -14.45444526027788434 ) ) ;
#1520=CARTESIAN_POINT ( 'NONE',  ( 5.896278296736517710, -17.30792457686182573, 10.24513184180886682 ) ) ;
#1531=CARTESIAN_POINT ( 'NONE',  ( 4.962356264823608143, -36.43094049105388166, 21.07183363638861096 ) ) ;
#1533=ADVANCED_FACE ( 'NONE', ( #29246 ), #1261, .F. ) ;
#1545=CARTESIAN_POINT ( 'NONE',  ( 0.9788927965476030835, 20.01615798422175985, -36.81969625326166096 ) ) ;
#1547=( BOUNDED_SURFACE ( )  B_SPLINE_SURFACE ( 3, 1, ( 
 ( #61067, #18804 ),
 ( #3740, #18180 ),
 ( #37928, #3133 ),
 ( #55750, #22261 ) ),
 .UNSPECIFIED., .F., .F., .F. ) 
 B_SPLINE_SURFACE_WITH_KNOTS ( ( 4, 4 ),
 ( 2, 2 ),
 ( 0.000000000000000000, 1.000000000000000000 ),
 ( 0.000000000000000000, 1.000000000000000000 ),
 .UNSPECIFIED. ) 
 GEOMETRIC_REPRESENTATION_ITEM ( )  RATIONAL_B_SPLINE_SURFACE ( (
 ( 1.000000000000000000, 1.000000000000000000),
 ( 0.7282232189291693025, 0.9929344683865674037),
 ( 0.7282232189291693025, 0.9929344683865674037),
 ( 1.000000000000000000, 1.000000000000000000) ) ) 
 REPRESENTATION_ITEM ( '' )  SURFACE ( )  );
#1550=CARTESIAN_POINT ( 'NONE',  ( 5.895596859100789899, 3.341829471546786667, 19.83331437242874884 ) ) ;
#1553=CARTESIAN_POINT ( 'NONE',  ( 0.8560838555295223751, -39.18289055412714106, -25.78902716088815694 ) ) ;
#1555=ORIENTED_EDGE ( 'NONE', *, *, #11372, .T. ) ;
#1560=CARTESIAN_POINT ( 'NONE',  ( 0.8560838555295223751, 46.60258007729417784, 5.345312359546021241 ) ) ;
#1567=LINE ( 'NONE', #59511, #60713 ) ;
#1573=CARTESIAN_POINT ( 'NONE',  ( 0.9780106845699501061, 41.57531628521707745, -5.274876514156579432 ) ) ;
#1575=B_SPLINE_CURVE_WITH_KNOTS ( 'NONE', 3,
 ( #38696, #9539, #61528, #5438, #43710, #19895 ),
 .UNSPECIFIED., .F., .F.,
 ( 4, 2, 4 ),
 ( 6.619851161367215630E-18, 0.0002291472222819954021, 0.0004582944445639841905 ),
 .UNSPECIFIED. ) ;
#1576=ADVANCED_FACE ( 'NONE', ( #43068 ), #18483, .F. ) ;
#1577=CARTESIAN_POINT ( 'NONE',  ( 4.962356264823603702, 17.31942680647464528, -38.35717733303005161 ) ) ;
#1581=CARTESIAN_POINT ( 'NONE',  ( 5.896782393890504181, -17.30187591025968530, 10.25529994022543079 ) ) ;
#1592=CARTESIAN_POINT ( 'NONE',  ( 0.5804410086790514622, 46.89585601637879364, 0.5463884574786330717 ) ) ;
#1593=ORIENTED_EDGE ( 'NONE', *, *, #60869, .F. ) ;
#1595=CARTESIAN_POINT ( 'NONE',  ( 0.8554163680231708922, 36.24698750680798298, 29.78861141095913467 ) ) ;
#1611=CARTESIAN_POINT ( 'NONE',  ( 2.528100132419515589, -37.99744774289700899, -17.84510419296803718 ) ) ;
#1620=VECTOR ( 'NONE', #38965, 1000.000000000000114 ) ;
#1621=CARTESIAN_POINT ( 'NONE',  ( 0.9754292580325141238, -37.13786007973355652, -19.41923828583751899 ) ) ;
#1622=DIRECTION ( 'NONE',  ( 0.07906939808003035641, -0.9968364091521051407, -0.008074879317899854095 ) ) ;
#1625=ORIENTED_EDGE ( 'NONE', *, *, #59196, .T. ) ;
#1628=CARTESIAN_POINT ( 'NONE',  ( 2.282803330402965791, -46.76237730313502539, -4.447131256914662600 ) ) ;
#1631=ORIENTED_EDGE ( 'NONE', *, *, #9264, .F. ) ;
#1634=CARTESIAN_POINT ( 'NONE',  ( 0.9754292589017217185, 41.45298143524652090, -6.162612840702018424 ) ) ;
#1637=ORIENTED_EDGE ( 'NONE', *, *, #43667, .F. ) ;
#1643=CARTESIAN_POINT ( 'NONE',  ( 1.231276596079887264, -18.40965318903149495, -37.66113965983570466 ) ) ;
#1652=CARTESIAN_POINT ( 'NONE',  ( 0.8554163680231708922, -34.17638377241205916, -32.14312158693720534 ) ) ;
#1655=CARTESIAN_POINT ( 'NONE',  ( 3.238018933889920792, 6.676852487597082053, -11.61150865419828193 ) ) ;
#1662=ORIENTED_EDGE ( 'NONE', *, *, #36726, .T. ) ;
#1666=CARTESIAN_POINT ( 'NONE',  ( 3.376099380956842921, -9.627698927086855818, 9.328225822815269908 ) ) ;
#1672=CARTESIAN_POINT ( 'NONE',  ( 4.962356264823608143, 0.000000000000000000, 0.000000000000000000 ) ) ;
#1675=ORIENTED_EDGE ( 'NONE', *, *, #39734, .T. ) ;
#1676=CARTESIAN_POINT ( 'NONE',  ( 0.8554163680231708922, -44.61245466728234987, 14.52357950615124160 ) ) ;
#1685=B_SPLINE_CURVE_WITH_KNOTS ( 'NONE', 3,
 ( #43605, #24155, #52346, #38592 ),
 .UNSPECIFIED., .F., .F.,
 ( 4, 4 ),
 ( 0.000000000000000000, 0.004447772540403801579 ),
 .UNSPECIFIED. ) ;
#1696=CARTESIAN_POINT ( 'NONE',  ( 0.5848930533535030563, 27.67115520191724443, 37.86264983039310295 ) ) ;
#1723=CARTESIAN_POINT ( 'NONE',  ( 0.9790850452238877288, 41.54146669795389357, 5.535690999864669060 ) ) ;
#1724=CARTESIAN_POINT ( 'NONE',  ( 0.5837800304671217910, 27.85439319122116686, -37.72757760747899169 ) ) ;
#1728=CARTESIAN_POINT ( 'NONE',  ( 1.231276596079881047, -31.65135013586901991, 27.48579279545509380 ) ) ;
#1730=CARTESIAN_POINT ( 'NONE',  ( 4.960386119450149955, -43.75174247978070952, -0.4706321868421235455 ) ) ;
#1733=B_SPLINE_CURVE_WITH_KNOTS ( 'NONE', 3,
 ( #46527, #3576, #60281, #51817, #22708, #12711 ),
 .UNSPECIFIED., .F., .F.,
 ( 4, 2, 4 ),
 ( 1.226145898665688582E-16, 0.0002448718616795922832, 0.0004897437233590619431 ),
 .UNSPECIFIED. ) ;
#1736=FACE_OUTER_BOUND ( 'NONE', #26676, .T. ) ;
#1738=B_SPLINE_CURVE_WITH_KNOTS ( 'NONE', 3,
 ( #27448, #51242, #55946, #37816, #3015, #3930, #12763, #3315, #4239, #3619, #51548, #23374, #36563, #47193, #60633, #13064, #13996, #37183, #61561 ),
 .UNSPECIFIED., .F., .F.,
 ( 4, 3, 3, 3, 3, 3, 4 ),
 ( 8.674294979774126656E-18, 0.0002732106629380585830, 0.0004098138914053739684, 0.0005464171197651428950, 0.0006830203481512547902, 0.0008196235766963618982, 0.001011968216111142028 ),
 .UNSPECIFIED. ) ;
#1741=CARTESIAN_POINT ( 'NONE',  ( 5.895596859100789899, 8.469463536102802337, 18.24270732712424348 ) ) ;
#1742=B_SPLINE_CURVE_WITH_KNOTS ( 'NONE', 3,
 ( #25440, #1621, #19845, #39266, #54236, #58953 ),
 .UNSPECIFIED., .F., .F.,
 ( 4, 2, 4 ),
 ( 0.000000000000000000, 0.0002291459268755689067, 0.0004582918537511378133 ),
 .UNSPECIFIED. ) ;
#1751=CARTESIAN_POINT ( 'NONE',  ( 0.7056759521544992975, 31.99426006192621230, 34.29454989071619764 ) ) ;
#1764=CARTESIAN_POINT ( 'NONE',  ( 0.9754292589017198312, -27.49953653147686694, -31.62440445999337157 ) ) ;
#1765=EDGE_CURVE ( 'NONE', #58463, #53012, #24756, .T. ) ;
#1774=CARTESIAN_POINT ( 'NONE',  ( 0.5837800304671211249, -19.78143393310113396, 42.51978602638839533 ) ) ;
#1777=EDGE_CURVE ( 'NONE', #18401, #35559, #18782, .T. ) ;
#1783=CARTESIAN_POINT ( 'NONE',  ( 0.5782707292762423457, 17.53027906811894709, 43.50201914281093707 ) ) ;
#1796=ORIENTED_EDGE ( 'NONE', *, *, #1228, .T. ) ;
#1808=CARTESIAN_POINT ( 'NONE',  ( 2.618530812446115519, -15.26631161697991601, -44.45971793445684028 ) ) ;
#1809=VERTEX_POINT ( 'NONE', #60827 ) ;
#1827=EDGE_CURVE ( 'NONE', #40810, #10512, #4408, .T. ) ;
#1832=CARTESIAN_POINT ( 'NONE',  ( 1.157643937452368821, 38.90537125510820715, 15.60046031682893286 ) ) ;
#1839=CARTESIAN_POINT ( 'NONE',  ( 5.894904586330512508, -13.98146465072135847, 14.45849432971053794 ) ) ;
#1840=CARTESIAN_POINT ( 'NONE',  ( 0.5326698147273788431, 0.000000000000000000, 0.000000000000000000 ) ) ;
#1841=ORIENTED_EDGE ( 'NONE', *, *, #58152, .F. ) ;
#1850=CARTESIAN_POINT ( 'NONE',  ( 1.000110580585052311, -26.55225625611131690, -32.42522429346786339 ) ) ;
#1851=ORIENTED_EDGE ( 'NONE', *, *, #6408, .T. ) ;
#1859=CARTESIAN_POINT ( 'NONE',  ( 5.896782393890504181, 16.58545041924856278, 11.37756218478545911 ) ) ;
#1862=B_SPLINE_CURVE_WITH_KNOTS ( 'NONE', 3,
 ( #11174, #53140, #835, #10247 ),
 .UNSPECIFIED., .F., .F.,
 ( 4, 4 ),
 ( 0.000000000000000000, 0.005004948556313794025 ),
 .UNSPECIFIED. ) ;
#1868=CARTESIAN_POINT ( 'NONE',  ( 0.5806925824938499181, -34.41156632303712826, -31.86010774524751454 ) ) ;
#1870=ORIENTED_EDGE ( 'NONE', *, *, #54295, .T. ) ;
#1881=CARTESIAN_POINT ( 'NONE',  ( 0.9790724872846777727, -12.37788730724380315, -40.03901991546029393 ) ) ;
#1882=CARTESIAN_POINT ( 'NONE',  ( 4.962356264823608143, -36.43094049105388166, 21.07183363638861096 ) ) ;
#1886=LINE ( 'NONE', #50135, #48953 ) ;
#1890=LINE ( 'NONE', #20401, #30786 ) ;
#1891=B_SPLINE_CURVE_WITH_KNOTS ( 'NONE', 3,
 ( #12129, #50311, #49694, #21502 ),
 .UNSPECIFIED., .F., .F.,
 ( 4, 4 ),
 ( 7.589415207398532001E-19, 0.004446298630425063285 ),
 .UNSPECIFIED. ) ;
#1893=CARTESIAN_POINT ( 'NONE',  ( 4.956445790443991584, 29.98832127573247774, 36.30755619981999871 ) ) ;
#1894=CARTESIAN_POINT ( 'NONE',  ( 4.956445790443998689, -16.41925925744477510, 44.13554095710679093 ) ) ;
#1900=CARTESIAN_POINT ( 'NONE',  ( 5.901463166500146684, -17.29756286482734495, 10.26217273670555130 ) ) ;
#1902=B_SPLINE_CURVE_WITH_KNOTS ( 'NONE', 3,
 ( #49260, #6014, #26387, #54557 ),
 .UNSPECIFIED., .F., .F.,
 ( 4, 4 ),
 ( 8.673617379884035472E-19, 0.004446298630425045070 ),
 .UNSPECIFIED. ) ;
#1906=CARTESIAN_POINT ( 'NONE',  ( 0.5326698147273788431, 0.000000000000000000, 0.000000000000000000 ) ) ;
#1908=VERTEX_POINT ( 'NONE', #50366 ) ;
#1911=CARTESIAN_POINT ( 'NONE',  ( 0.9762797500689124330, 20.58271139965489738, 36.50584578699993443 ) ) ;
#1918=( BOUNDED_SURFACE ( )  B_SPLINE_SURFACE ( 3, 1, ( 
 ( #47050, #32950 ),
 ( #13846, #23522 ),
 ( #5323, #42971 ),
 ( #61714, #23225 ) ),
 .UNSPECIFIED., .F., .F., .F. ) 
 B_SPLINE_SURFACE_WITH_KNOTS ( ( 4, 4 ),
 ( 2, 2 ),
 ( 0.000000000000000000, 1.000000000000000000 ),
 ( 0.000000000000000000, 1.000000000000000000 ),
 .UNSPECIFIED. ) 
 GEOMETRIC_REPRESENTATION_ITEM ( )  RATIONAL_B_SPLINE_SURFACE ( (
 ( 1.000000000000000000, 1.000000000000000000),
 ( 0.9729067724841187204, 0.9999501103223794596),
 ( 0.9729067724841187204, 0.9999501103223794596),
 ( 1.000000000000000000, 1.000000000000000000) ) ) 
 REPRESENTATION_ITEM ( '' )  SURFACE ( )  );
#1923=CARTESIAN_POINT ( 'NONE',  ( 1.231276596079887931, 41.42457922925077440, -6.425029704024191268 ) ) ;
#1927=ORIENTED_EDGE ( 'NONE', *, *, #21557, .T. ) ;
#1930=CARTESIAN_POINT ( 'NONE',  ( 3.782625744892855302, -38.26642674074366823, -17.40455941959752195 ) ) ;
#1932=CARTESIAN_POINT ( 'NONE',  ( 1.231276596079887264, -21.83837404314831332, 35.78214904347716185 ) ) ;
#1934=EDGE_CURVE ( 'NONE', #16409, #27021, #41097, .T. ) ;
#1941=CARTESIAN_POINT ( 'NONE',  ( 0.9769922540276061440, 35.83105161777989878, 21.73631282094816797 ) ) ;
#1943=ORIENTED_EDGE ( 'NONE', *, *, #27256, .F. ) ;
#1966=EDGE_CURVE ( 'NONE', #5597, #24375, #43297, .T. ) ;
#1976=FACE_OUTER_BOUND ( 'NONE', #25358, .T. ) ;
#1981=ADVANCED_FACE ( 'NONE', ( #3055 ), #20489, .F. ) ;
#1989=CARTESIAN_POINT ( 'NONE',  ( 1.000433927950261870, -23.10322705937726795, -34.96654940218871843 ) ) ;
#1994=CARTESIAN_POINT ( 'NONE',  ( 0.5804410086790514622, -44.48029469925801038, 14.86685021524586325 ) ) ;
#1995=CARTESIAN_POINT ( 'NONE',  ( 1.157643937452369931, 36.47889976118223387, 20.64684350714105321 ) ) ;
#1999=CARTESIAN_POINT ( 'NONE',  ( 0.5806925824938499181, -29.85799195566266917, -36.16244846134105018 ) ) ;
#2004=CARTESIAN_POINT ( 'NONE',  ( 0.5806925824938499181, 27.37593026015182218, 38.07598724570208049 ) ) ;
#2019=CARTESIAN_POINT ( 'NONE',  ( 4.956445790443996025, 14.46717203539371610, 44.81337951368942640 ) ) ;
#2028=DIRECTION ( 'NONE',  ( -1.000000000000000000, -0.000000000000000000, -0.000000000000000000 ) ) ;
#2041=CARTESIAN_POINT ( 'NONE',  ( 1.000110580585051867, -34.92014527540499813, 23.17328066365460870 ) ) ;
#2042=CARTESIAN_POINT ( 'NONE',  ( 4.962356264823608143, 0.000000000000000000, 0.000000000000000000 ) ) ;
#2044=CARTESIAN_POINT ( 'NONE',  ( 0.9790724872846771065, -31.10874810710284422, 28.08168444360627092 ) ) ;
#2049=CARTESIAN_POINT ( 'NONE',  ( 1.231276596079881047, 41.91134057782998212, 0.8463462572780127147 ) ) ;
#2058=CARTESIAN_POINT ( 'NONE',  ( 4.291220156522059348, -36.34793638197146493, 29.97026056072670741 ) ) ;
#2061=ORIENTED_EDGE ( 'NONE', *, *, #8099, .F. ) ;
#2065=ORIENTED_EDGE ( 'NONE', *, *, #35663, .F. ) ;
#2088=ORIENTED_EDGE ( 'NONE', *, *, #55043, .T. ) ;
#2090=ADVANCED_FACE ( 'NONE', ( #32828 ), #4079, .T. ) ;
#2092=CARTESIAN_POINT ( 'NONE',  ( 4.962356264823602814, 42.01891079680549979, 2.376285612557970772 ) ) ;
#2093=CARTESIAN_POINT ( 'NONE',  ( 0.9785694773339239649, 24.67983040667081340, 33.87095181438870384 ) ) ;
#2095=EDGE_LOOP ( 'NONE', ( #22526, #10405, #52719, #3876 ) ) ;
#2105=CARTESIAN_POINT ( 'NONE',  ( 0.5834584762367737154, -30.13807749983152817, -35.92954597023653918 ) ) ;
#2110=CARTESIAN_POINT ( 'NONE',  ( 4.956445790444004018, -45.55738122058073003, 11.91902120403828036 ) ) ;
#2115=CARTESIAN_POINT ( 'NONE',  ( 0.5824935313925952984, 45.32465144643322930, 12.03802925371000399 ) ) ;
#2116=B_SPLINE_CURVE_WITH_KNOTS ( 'NONE', 3,
 ( #48192, #38193, #37570, #47264, #18145, #4008, #23147, #33174, #56332, #52559, #52248, #9037, #9345, #9653, #32870, #4940, #33797, #9976, #32555 ),
 .UNSPECIFIED., .F., .F.,
 ( 4, 3, 3, 3, 3, 3, 4 ),
 ( 9.541595121948225732E-18, 0.0002732106629380623777, 0.0004098138914053767873, 0.0005464171197651445213, 0.0006830203481512576091, 0.0008196235766963660182, 0.001011968216111140077 ),
 .UNSPECIFIED. ) ;
#2120=FACE_OUTER_BOUND ( 'NONE', #57558, .T. ) ;
#2121=CONICAL_SURFACE ( 'NONE', #54163, 42.08604991992415023, 1.569615340895231137 ) ;
#2122=VECTOR ( 'NONE', #21712, 1000.000000000000000 ) ;
#2127=CARTESIAN_POINT ( 'NONE',  ( 0.9789889208857696090, 9.808795407786901066, 40.74460001878221505 ) ) ;
#2129=CARTESIAN_POINT ( 'NONE',  ( 3.782625744892851749, 13.48684605329171049, -39.81636708226672283 ) ) ;
#2131=EDGE_LOOP ( 'NONE', ( #49457, #40864, #51409, #49024 ) ) ;
#2143=VERTEX_POINT ( 'NONE', #827 ) ;
#2146=CARTESIAN_POINT ( 'NONE',  ( 5.895596859100789899, 20.06773179721813349, 1.346968346847024822 ) ) ;
#2149=ORIENTED_EDGE ( 'NONE', *, *, #43157, .T. ) ;
#2150=CARTESIAN_POINT ( 'NONE',  ( 1.231276596079887931, -35.03243822710496858, -23.02183839058345072 ) ) ;
#2152=ADVANCED_FACE ( 'NONE', ( #10864 ), #14113, .F. ) ;
#2161=B_SPLINE_CURVE_WITH_KNOTS ( 'NONE', 3,
 ( #10477, #34596, #53661, #10791 ),
 .UNSPECIFIED., .F., .F.,
 ( 4, 4 ),
 ( 1.440969542111313559E-17, 0.004042984057420977162 ),
 .UNSPECIFIED. ) ;
#2164=( BOUNDED_SURFACE ( )  B_SPLINE_SURFACE ( 3, 1, ( 
 ( #12359, #31446 ),
 ( #50542, #7621 ),
 ( #45881, #2929 ),
 ( #12984, #47399 ) ),
 .UNSPECIFIED., .F., .F., .F. ) 
 B_SPLINE_SURFACE_WITH_KNOTS ( ( 4, 4 ),
 ( 2, 2 ),
 ( 0.000000000000000000, 1.000000000000000000 ),
 ( 0.000000000000000000, 1.000000000000000000 ),
 .UNSPECIFIED. ) 
 GEOMETRIC_REPRESENTATION_ITEM ( )  RATIONAL_B_SPLINE_SURFACE ( (
 ( 1.000000000000000000, 1.000000000000000000),
 ( 0.7282232189291693025, 0.9929344683865674037),
 ( 0.7282232189291693025, 0.9929344683865674037),
 ( 1.000000000000000000, 1.000000000000000000) ) ) 
 REPRESENTATION_ITEM ( '' )  SURFACE ( )  );
#2166=CARTESIAN_POINT ( 'NONE',  ( 4.956445790443988031, 0.000000000000000000, 0.000000000000000000 ) ) ;
#2170=CARTESIAN_POINT ( 'NONE',  ( 0.5832655196449135770, 32.76499612651431192, -33.55130715490577131 ) ) ;
#2182=DIRECTION ( 'NONE',  ( -1.000000000000000000, -0.000000000000000000, -0.000000000000000000 ) ) ;
#2192=CARTESIAN_POINT ( 'NONE',  ( 0.7056759521545007408, 17.64077833824084607, -43.45747080466188805 ) ) ;
#2198=CARTESIAN_POINT ( 'NONE',  ( 5.895596859100789899, 19.71057157537860149, -4.002693016503341639 ) ) ;
#2204=CARTESIAN_POINT ( 'NONE',  ( 0.6064515330803585957, -7.098679639542389452, 46.35669405180046709 ) ) ;
#2234=ADVANCED_FACE ( 'NONE', ( #31183 ), #32945, .F. ) ;
#2236=CARTESIAN_POINT ( 'NONE',  ( 0.8554163680231720024, 46.36773742900852113, -7.158100224664473821 ) ) ;
#2238=ORIENTED_EDGE ( 'NONE', *, *, #32665, .T. ) ;
#2253=ORIENTED_EDGE ( 'NONE', *, *, #27298, .T. ) ;
#2255=CARTESIAN_POINT ( 'NONE',  ( 5.838029081930957709, 7.836690858011984950, -46.57951625498993309 ) ) ;
#2256=CARTESIAN_POINT ( 'NONE',  ( 1.000433927950264756, 41.44279064093520049, -6.238091177953354993 ) ) ;
#2265=VECTOR ( 'NONE', #24584, 1000.000000000000000 ) ;
#2267=CARTESIAN_POINT ( 'NONE',  ( 3.782625744892853525, 21.69837273921715948, 36.00581514929220361 ) ) ;
#2273=DIRECTION ( 'NONE',  ( 0.07906939808003035641, -0.3507354328807343324, -0.9331305837926573421 ) ) ;
#2275=B_SPLINE_CURVE_WITH_KNOTS ( 'NONE', 3,
 ( #21622, #11296, #59508, #45450 ),
 .UNSPECIFIED., .F., .F.,
 ( 4, 4 ),
 ( 1.409462824231155764E-18, 0.004446298630425050274 ),
 .UNSPECIFIED. ) ;
#2280=LINE ( 'NONE', #2906, #49470 ) ;
#2281=CARTESIAN_POINT ( 'NONE',  ( 4.962356264823608143, 0.000000000000000000, 0.000000000000000000 ) ) ;
#2305=B_SPLINE_CURVE_WITH_KNOTS ( 'NONE', 3,
 ( #38814, #5246, #550, #6160, #24377, #25297 ),
 .UNSPECIFIED., .F., .F.,
 ( 4, 2, 4 ),
 ( 0.000000000000000000, 0.0002291459268755701264, 0.0004582918537511402528 ),
 .UNSPECIFIED. ) ;
#2307=EDGE_CURVE ( 'NONE', #26672, #35006, #12672, .T. ) ;
#2311=ORIENTED_EDGE ( 'NONE', *, *, #38579, .F. ) ;
#2313=CARTESIAN_POINT ( 'NONE',  ( 0.8554163680231720024, -20.57434774096662977, -42.16517150618031451 ) ) ;
#2317=CARTESIAN_POINT ( 'NONE',  ( 2.282803330402968456, -12.65678521539727619, -45.23607736606130914 ) ) ;
#2319=CARTESIAN_POINT ( 'NONE',  ( 0.5804410086790514622, 27.37779091616948079, 38.07855586029891271 ) ) ;
#2334=ORIENTED_EDGE ( 'NONE', *, *, #1448, .T. ) ;
#2337=EDGE_CURVE ( 'NONE', #18623, #39044, #19433, .T. ) ;
#2348=CARTESIAN_POINT ( 'NONE',  ( 0.9762797500689124330, 14.58899758184639595, 39.28722355604407568 ) ) ;
#2353=CARTESIAN_POINT ( 'NONE',  ( 0.5832655196449136881, -34.62741248031726116, -31.62558280714044301 ) ) ;
#2361=CARTESIAN_POINT ( 'NONE',  ( 0.9787464366903563251, -7.145144750301928305, 41.29504691107269565 ) ) ;
#2363=CARTESIAN_POINT ( 'NONE',  ( 5.895596859100789899, 8.462961974658517406, 18.24572437114984780 ) ) ;
#2393=ORIENTED_EDGE ( 'NONE', *, *, #22307, .F. ) ;
#2394=CARTESIAN_POINT ( 'NONE',  ( 4.291220156522060236, 41.58924158504501634, 22.12970812474624438 ) ) ;
#2402=FACE_OUTER_BOUND ( 'NONE', #50002, .T. ) ;
#2407=CARTESIAN_POINT ( 'NONE',  ( 0.9787284016396627928, 4.381134602593736993, 41.67903140096688475 ) ) ;
#2415=CARTESIAN_POINT ( 'NONE',  ( 0.5804410086790514622, 17.36461428077124935, 43.56592731407690877 ) ) ;
#2418=CARTESIAN_POINT ( 'NONE',  ( 3.238018933889920792, -2.498552698661987925, 13.15920692061880537 ) ) ;
#2427=EDGE_LOOP ( 'NONE', ( #4011, #46448, #1469, #5991 ) ) ;
#2429=CARTESIAN_POINT ( 'NONE',  ( 0.5817216825391099411, 37.08439865257854962, 28.70509238417621845 ) ) ;
#2430=CARTESIAN_POINT ( 'NONE',  ( 0.5782707292762442330, 3.973746573563663009, 46.73270473529977664 ) ) ;
#2439=CARTESIAN_POINT ( 'NONE',  ( 2.618530812446111078, -18.50060774051875967, -43.21405214082170687 ) ) ;
#2443=LINE ( 'NONE', #46626, #14497 ) ;
#2462=VERTEX_POINT ( 'NONE', #44018 ) ;
#2472=ORIENTED_EDGE ( 'NONE', *, *, #49512, .F. ) ;
#2473=CARTESIAN_POINT ( 'NONE',  ( 1.231276596079881935, 35.62927148397020005, 22.08691432816306133 ) ) ;
#2475=ORIENTED_EDGE ( 'NONE', *, *, #49175, .F. ) ;
#2476=CARTESIAN_POINT ( 'NONE',  ( 4.291220156522059348, 20.72764654175944443, 42.30548033228772908 ) ) ;
#2480=AXIS2_PLACEMENT_3D ( 'NONE', #61725, #13854, #43598 ) ;
#2482=EDGE_LOOP ( 'NONE', ( #60136, #24303, #6387, #24058 ) ) ;
#2486=CONICAL_SURFACE ( 'NONE', #19503, 42.08604991992415023, 1.569615340895231137 ) ;
#2505=CARTESIAN_POINT ( 'NONE',  ( 3.238018933889920792, -13.34321331060666083, 1.168824587054079878 ) ) ;
#2508=CARTESIAN_POINT ( 'NONE',  ( 5.895881250540457863, 5.963300346357645942, 19.20850672455908992 ) ) ;
#2518=CARTESIAN_POINT ( 'NONE',  ( 0.6845945791218023269, 43.51705215793850812, 17.51207275559363907 ) ) ;
#2522=CARTESIAN_POINT ( 'NONE',  ( 4.962356264823608143, 34.44911810793244200, 24.17630781256866612 ) ) ;
#2523=B_SPLINE_CURVE_WITH_KNOTS ( 'NONE', 3,
 ( #18871, #42373, #23545, #47072 ),
 .UNSPECIFIED., .F., .F.,
 ( 4, 4 ),
 ( 2.168404344971008868E-19, 0.004041751736740997747 ),
 .UNSPECIFIED. ) ;
#2538=CARTESIAN_POINT ( 'NONE',  ( 0.5797568665920715958, -14.49376217790061183, -44.59995702388432193 ) ) ;
#2542=ADVANCED_FACE ( 'NONE', ( #49283 ), #52494, .F. ) ;
#2554=EDGE_CURVE ( 'NONE', #61929, #715, #58988, .T. ) ;
#2556=ORIENTED_EDGE ( 'NONE', *, *, #40784, .F. ) ;
#2559=CARTESIAN_POINT ( 'NONE',  ( 0.5824935313925951874, -44.41938431943384558, -15.03849971693567511 ) ) ;
#2560=CARTESIAN_POINT ( 'NONE',  ( 0.5830082357119561465, -30.48544060673254918, 35.63523461339518406 ) ) ;
#2561=ORIENTED_EDGE ( 'NONE', *, *, #37649, .F. ) ;
#2563=EDGE_CURVE ( 'NONE', #14707, #41543, #59604, .T. ) ;
#2564=VERTEX_POINT ( 'NONE', #2591 ) ;
#2568=ORIENTED_EDGE ( 'NONE', *, *, #11533, .F. ) ;
#2574=VERTEX_POINT ( 'NONE', #3205 ) ;
#2576=ORIENTED_EDGE ( 'NONE', *, *, #23148, .T. ) ;
#2577=CARTESIAN_POINT ( 'NONE',  ( 0.9762797500689124330, -39.42083772998312696, -14.22400568939859866 ) ) ;
#2583=CARTESIAN_POINT ( 'NONE',  ( 0.8554163680231708922, -30.98316862405949124, 35.23136010892730496 ) ) ;
#2586=CARTESIAN_POINT ( 'NONE',  ( -69.95594261585600293, 1.530808498934191521E-15, 12.50000000000000000 ) ) ;
#2587=CARTESIAN_POINT ( 'NONE',  ( 3.376099380956838925, -0.9076095657324720900, 13.37477583020582905 ) ) ;
#2589=EDGE_CURVE ( 'NONE', #19228, #15999, #14131, .T. ) ;
#2591=CARTESIAN_POINT ( 'NONE',  ( 1.231276596079887264, 3.353048872156665805, -41.78556968953512296 ) ) ;
#2592=CARTESIAN_POINT ( 'NONE',  ( 0.5824936645240075261, -13.54584401086361112, -44.89708552983879741 ) ) ;
#2598=CARTESIAN_POINT ( 'NONE',  ( 3.238018933889920792, 13.30865154331497280, -1.512377752505324358 ) ) ;
#2600=ADVANCED_FACE ( 'NONE', ( #32052 ), #9690, .F. ) ;
#2601=ORIENTED_EDGE ( 'NONE', *, *, #17120, .T. ) ;
#2603=LINE ( 'NONE', #59305, #48905 ) ;
#2608=ORIENTED_EDGE ( 'NONE', *, *, #42852, .T. ) ;
#2616=CONICAL_SURFACE ( 'NONE', #14638, 42.08604991992415023, 1.569615340895231137 ) ;
#2618=AXIS2_PLACEMENT_3D ( 'NONE', #47580, #3399, #13150 ) ;
#2623=EDGE_LOOP ( 'NONE', ( #54315, #25988, #22454, #19690 ) ) ;
#2628=EDGE_LOOP ( 'NONE', ( #18829, #12248, #48276, #60391 ) ) ;
#2633=EDGE_CURVE ( 'NONE', #49170, #14203, #6085, .T. ) ;
#2635=LINE ( 'NONE', #17074, #47894 ) ;
#2646=CARTESIAN_POINT ( 'NONE',  ( 1.000433927950264534, -13.04434877168812790, -39.82792541390282537 ) ) ;
#2650=( BOUNDED_SURFACE ( )  B_SPLINE_SURFACE ( 3, 1, ( 
 ( #55883, #50566 ),
 ( #51180, #3869 ),
 ( #32717, #22378 ),
 ( #27080, #22691 ) ),
 .UNSPECIFIED., .F., .F., .F. ) 
 B_SPLINE_SURFACE_WITH_KNOTS ( ( 4, 4 ),
 ( 2, 2 ),
 ( 0.000000000000000000, 1.000000000000000000 ),
 ( 0.000000000000000000, 1.000000000000000000 ),
 .UNSPECIFIED. ) 
 GEOMETRIC_REPRESENTATION_ITEM ( )  RATIONAL_B_SPLINE_SURFACE ( (
 ( 1.000000000000000000, 1.000000000000000000),
 ( 0.9952954269826590483, 0.8620686068821339365),
 ( 0.9952954269826590483, 0.8620686068821339365),
 ( 1.000000000000000000, 1.000000000000000000) ) ) 
 REPRESENTATION_ITEM ( '' )  SURFACE ( )  );
#2657=ORIENTED_EDGE ( 'NONE', *, *, #41689, .F. ) ;
#2662=CARTESIAN_POINT ( 'NONE',  ( 1.157644175074339588, -35.01838093932130391, 23.03725834095192937 ) ) ;
#2665=FACE_OUTER_BOUND ( 'NONE', #47818, .T. ) ;
#2678=CARTESIAN_POINT ( 'NONE',  ( 0.5837799406558227266, -7.710363279387344448, 46.25790578568249600 ) ) ;
#2688=CARTESIAN_POINT ( 'NONE',  ( 4.960386119450147291, 32.13287905145141821, -29.69704612477700678 ) ) ;
#2699=CARTESIAN_POINT ( 'NONE',  ( 4.956445790444027999, 24.88142650099568698, -39.98065363916886383 ) ) ;
#2702=VERTEX_POINT ( 'NONE', #57355 ) ;
#2705=CARTESIAN_POINT ( 'NONE',  ( 0.5806925824938499181, 46.89268439822727430, 0.5463627657667635695 ) ) ;
#2708=ORIENTED_EDGE ( 'NONE', *, *, #9982, .T. ) ;
#2709=CARTESIAN_POINT ( 'NONE',  ( 0.5782707292762423457, 36.35509350284772268, -29.63179930592838218 ) ) ;
#2722=ORIENTED_EDGE ( 'NONE', *, *, #60540, .F. ) ;
#2726=VERTEX_POINT ( 'NONE', #20113 ) ;
#2729=CARTESIAN_POINT ( 'NONE',  ( 0.9790724872846762183, 38.59896336290614727, -16.32345665876211527 ) ) ;
#2734=CARTESIAN_POINT ( 'NONE',  ( 4.291220156522060236, -46.81214323738926453, 5.292659334195587206 ) ) ;
#2742=CARTESIAN_POINT ( 'NONE',  ( 4.962356264823608143, 41.32726869310149453, -7.955655864260332777 ) ) ;
#2743=CARTESIAN_POINT ( 'NONE',  ( 2.618530812446115519, 3.301668998266477306, -46.89163860459650124 ) ) ;
#2754=CARTESIAN_POINT ( 'NONE',  ( 5.895596859100789899, 17.95274561709302930, 9.067916410093047830 ) ) ;
#2757=CARTESIAN_POINT ( 'NONE',  ( 0.9762797500689124330, -7.469026406145721886, -41.23758515880873432 ) ) ;
#2766=CARTESIAN_POINT ( 'NONE',  ( 4.960386119450146403, 38.83699438620099897, -20.15252668323582697 ) ) ;
#2767=ORIENTED_EDGE ( 'NONE', *, *, #56931, .F. ) ;
#2785=ORIENTED_EDGE ( 'NONE', *, *, #7532, .T. ) ;
#2786=CARTESIAN_POINT ( 'NONE',  ( 0.5782707292762423457, -38.25309408463888161, 27.13737545635878590 ) ) ;
#2787=EDGE_CURVE ( 'NONE', #58874, #34772, #33539, .T. ) ;
#2788=ORIENTED_EDGE ( 'NONE', *, *, #57317, .F. ) ;
#2789=ORIENTED_EDGE ( 'NONE', *, *, #10264, .F. ) ;
#2790=FACE_OUTER_BOUND ( 'NONE', #6094, .T. ) ;
#2793=VECTOR ( 'NONE', #3966, 1000.000000000000000 ) ;
#2797=CARTESIAN_POINT ( 'NONE',  ( 5.838029081930955932, -43.47829931555671834, -18.45812955799640420 ) ) ;
#2801=VERTEX_POINT ( 'NONE', #53586 ) ;
#2807=CARTESIAN_POINT ( 'NONE',  ( 0.5804410086790514622, 4.150428748651751043, 46.71502748642842562 ) ) ;
#2813=CARTESIAN_POINT ( 'NONE',  ( 5.896782393890504181, 5.965008392936887560, 19.20793486427431418 ) ) ;
#2819=CARTESIAN_POINT ( 'NONE',  ( 5.896782393890504181, 19.00205529748295774, -6.591508275759957236 ) ) ;
#2827=CARTESIAN_POINT ( 'NONE',  ( 0.5824935313925948543, 32.86262163222748711, 33.45573607785207315 ) ) ;
#2835=B_SPLINE_CURVE_WITH_KNOTS ( 'NONE', 3,
 ( #22043, #60850, #23886, #9466, #23570, #52068 ),
 .UNSPECIFIED., .F., .F.,
 ( 4, 2, 4 ),
 ( 1.233001025668604810E-16, 0.0002448718616795908195, 0.0004897437233590583652 ),
 .UNSPECIFIED. ) ;
#2846=CARTESIAN_POINT ( 'NONE',  ( 0.5806925824938502512, 40.06810415365508504, -24.36738377166110325 ) ) ;
#2848=DIRECTION ( 'NONE',  ( 0.000000000000000000, 0.000000000000000000, 1.000000000000000000 ) ) ;
#2850=CARTESIAN_POINT ( 'NONE',  ( 5.895596859100789899, -2.009647457887034694, 20.01223376606159121 ) ) ;
#2853=ORIENTED_EDGE ( 'NONE', *, *, #55652, .F. ) ;
#2857=B_SPLINE_CURVE_WITH_KNOTS ( 'NONE', 3,
 ( #31874, #50959, #7732, #60054, #36272, #40676 ),
 .UNSPECIFIED., .F., .F.,
 ( 4, 2, 4 ),
 ( 5.966068130930023556E-18, 0.0002291472222819933963, 0.0004582944445639808295 ),
 .UNSPECIFIED. ) ;
#2859=CARTESIAN_POINT ( 'NONE',  ( 2.618530812446115519, 18.20180174657032879, 43.34075682745686464 ) ) ;
#2864=FACE_OUTER_BOUND ( 'NONE', #2427, .T. ) ;
#2871=CARTESIAN_POINT ( 'NONE',  ( 0.7764139734771235979, -30.95828352313330711, 35.23670177823344574 ) ) ;
#2873=CARTESIAN_POINT ( 'NONE',  ( 0.7764146366350271888, -25.98546534488490778, -39.04863716544984698 ) ) ;
#2875=EDGE_LOOP ( 'NONE', ( #61577, #34846, #28820, #58367 ) ) ;
#2880=SURFACE_STYLE_FILL_AREA ( #45835 ) ;
#2881=AXIS2_PLACEMENT_3D ( 'NONE', #43874, #48844, #15347 ) ;
#2882=AXIS2_PLACEMENT_3D ( 'NONE', #4169, #27696, #46826 ) ;
#2883=ORIENTED_EDGE ( 'NONE', *, *, #21075, .T. ) ;
#2885=CARTESIAN_POINT ( 'NONE',  ( 0.9787464366903567692, -39.53137008141080599, -13.91419319892470341 ) ) ;
#2889=CARTESIAN_POINT ( 'NONE',  ( 0.5837799406558222826, 4.603457743365774846, -46.66960173798624822 ) ) ;
#2891=CARTESIAN_POINT ( 'NONE',  ( 5.895881250540457863, 12.98195518060028419, -15.36217827318725071 ) ) ;
#2894=CARTESIAN_POINT ( 'NONE',  ( 5.917102823773431552, -15.78915961314075034, 12.45761440896719385 ) ) ;
#2896=ADVANCED_FACE ( 'NONE', ( #59533 ), #30910, .F. ) ;
#2899=CARTESIAN_POINT ( 'NONE',  ( 5.896782393890504181, 14.92098591823879872, -13.48666994130618235 ) ) ;
#2904=B_SPLINE_CURVE_WITH_KNOTS ( 'NONE', 3,
 ( #43423, #47801, #52786, #23369 ),
 .UNSPECIFIED., .F., .F.,
 ( 4, 4 ),
 ( 9.309503074677274191E-17, 0.005004948556313900711 ),
 .UNSPECIFIED. ) ;
#2906=CARTESIAN_POINT ( 'NONE',  ( 3.376099380956838925, -13.22083125066029474, 2.217657474370499759 ) ) ;
#2910=CARTESIAN_POINT ( 'NONE',  ( 0.5804410086790514622, -41.60900809504509823, -21.63816760268458950 ) ) ;
#2912=ORIENTED_EDGE ( 'NONE', *, *, #61029, .T. ) ;
#2922=VECTOR ( 'NONE', #27208, 1000.000000000000114 ) ;
#2926=( BOUNDED_SURFACE ( )  B_SPLINE_SURFACE ( 3, 1, ( 
 ( #16153, #22383 ),
 ( #35579, #27086 ),
 ( #7647, #36196 ),
 ( #35267, #26775 ) ),
 .UNSPECIFIED., .F., .F., .F. ) 
 B_SPLINE_SURFACE_WITH_KNOTS ( ( 4, 4 ),
 ( 2, 2 ),
 ( 0.000000000000000000, 1.000000000000000000 ),
 ( 0.000000000000000000, 1.000000000000000000 ),
 .UNSPECIFIED. ) 
 GEOMETRIC_REPRESENTATION_ITEM ( )  RATIONAL_B_SPLINE_SURFACE ( (
 ( 1.000000000000000000, 1.000000000000000000),
 ( 0.7282232189291694135, 0.9929344683865672927),
 ( 0.7282232189291694135, 0.9929344683865672927),
 ( 1.000000000000000000, 1.000000000000000000) ) ) 
 REPRESENTATION_ITEM ( '' )  SURFACE ( )  );
#2929=CARTESIAN_POINT ( 'NONE',  ( 2.618530812446115519, 26.73752065161077951, -38.66305443964414224 ) ) ;
#2943=CARTESIAN_POINT ( 'NONE',  ( 5.895596859100789899, -2.016778947468235828, 20.01151633159107845 ) ) ;
#2946=ORIENTED_EDGE ( 'NONE', *, *, #1448, .F. ) ;
#2954=EDGE_CURVE ( 'NONE', #50432, #31086, #17901, .T. ) ;
#2956=CARTESIAN_POINT ( 'NONE',  ( 0.6064782688330891958, -41.53115349968965830, -21.78296892996878498 ) ) ;
#2958=EDGE_CURVE ( 'NONE', #14741, #10982, #9670, .T. ) ;
#2963=CARTESIAN_POINT ( 'NONE',  ( 1.092182651088184242, 40.62377872806010970, 10.31841975769022035 ) ) ;
#2965=CARTESIAN_POINT ( 'NONE',  ( 0.5832655196449142432, -46.80593288449814793, 2.905138513940911160 ) ) ;
#2966=EDGE_CURVE ( 'NONE', #53003, #59514, #17570, .T. ) ;
#2976=CARTESIAN_POINT ( 'NONE',  ( 0.9754292580325131246, -18.16743313816920491, 37.76601435251217964 ) ) ;
#2980=CARTESIAN_POINT ( 'NONE',  ( 5.896782393890504181, 19.70854070425246363, 4.012419492879101490 ) ) ;
#2983=CARTESIAN_POINT ( 'NONE',  ( 1.231276596079887264, -41.76121777166943616, 3.643825084340432952 ) ) ;
#2984=CARTESIAN_POINT ( 'NONE',  ( 1.231276596079881047, -13.22565419922034557, 39.77887431816932917 ) ) ;
#2989=CARTESIAN_POINT ( 'NONE',  ( 0.8560838555295158248, 46.89922841446242074, 0.9138972643637033322 ) ) ;
#3000=DIRECTION ( 'NONE',  ( 0.000000000000000000, 0.000000000000000000, 1.000000000000000000 ) ) ;
#3001=CARTESIAN_POINT ( 'NONE',  ( 0.9762797500689124330, 32.57381952463267538, -26.36799322592379369 ) ) ;
#3002=ORIENTED_EDGE ( 'NONE', *, *, #44980, .F. ) ;
#3011=CARTESIAN_POINT ( 'NONE',  ( 3.238018933889920792, 7.722174679335315872, 10.94419986063327777 ) ) ;
#3013=CARTESIAN_POINT ( 'NONE',  ( 3.782625744892855302, -32.30858446067052370, -26.89597505655302712 ) ) ;
#3015=CARTESIAN_POINT ( 'NONE',  ( 0.9787284016396604613, 4.008534792623077436, -41.71651528765511330 ) ) ;
#3018=EDGE_LOOP ( 'NONE', ( #58492, #39630, #26110, #795 ) ) ;
#3024=VERTEX_POINT ( 'NONE', #52287 ) ;
#3025=CARTESIAN_POINT ( 'NONE',  ( 0.9762797500689124330, -39.75277516423506086, -13.26806888463731227 ) ) ;
#3030=EDGE_CURVE ( 'NONE', #57391, #57208, #19421, .T. ) ;
#3033=ORIENTED_EDGE ( 'NONE', *, *, #21432, .T. ) ;
#3034=CARTESIAN_POINT ( 'NONE',  ( 4.962356264823596597, 37.75702904547799932, 18.59145920903680249 ) ) ;
#3035=EDGE_CURVE ( 'NONE', #40578, #41808, #39541, .T. ) ;
#3037=CARTESIAN_POINT ( 'NONE',  ( 5.895596859100789899, -18.51832497669317945, -7.848555489392246010 ) ) ;
#3038=ORIENTED_EDGE ( 'NONE', *, *, #31491, .T. ) ;
#3041=CARTESIAN_POINT ( 'NONE',  ( 1.231276596079887264, -26.41281459480383376, 32.55211200826430229 ) ) ;
#3044=CARTESIAN_POINT ( 'NONE',  ( 5.901463166500145796, -19.93509711719968891, 2.666415809369121259 ) ) ;
#3047=CARTESIAN_POINT ( 'NONE',  ( 2.618530812446115519, -46.78761446237187016, 4.543778396736469105 ) ) ;
#3052=CARTESIAN_POINT ( 'NONE',  ( 0.7056313189692721144, -42.23391001524242938, -20.39719315940220667 ) ) ;
#3055=FACE_OUTER_BOUND ( 'NONE', #18462, .T. ) ;
#3058=CARTESIAN_POINT ( 'NONE',  ( 0.5817217712918324457, 10.42802360358725267, 45.72189057477174146 ) ) ;
#3060=CARTESIAN_POINT ( 'NONE',  ( 4.962356264823609031, 31.50371261889155150, -27.90612278853226513 ) ) ;
#3061=CARTESIAN_POINT ( 'NONE',  ( 1.157644175074336479, 10.51841484064714471, -40.57542636521812796 ) ) ;
#3066=CARTESIAN_POINT ( 'NONE',  ( 1.157643937452369043, -7.784786284043311966, -41.18736914524311743 ) ) ;
#3067=DIRECTION ( 'NONE',  ( -1.000000000000000000, -0.000000000000000000, -0.000000000000000000 ) ) ;
#3078=CARTESIAN_POINT ( 'NONE',  ( 1.231276596079887931, -41.24008908601417289, -7.518764738684258653 ) ) ;
#3082=ORIENTED_EDGE ( 'NONE', *, *, #55762, .F. ) ;
#3086=CARTESIAN_POINT ( 'NONE',  ( 1.231276596079881047, -30.51591784428347154, -28.74118176309054107 ) ) ;
#3097=ORIENTED_EDGE ( 'NONE', *, *, #1827, .F. ) ;
#3102=CARTESIAN_POINT ( 'NONE',  ( 0.5806925824938499181, -44.47729014209976128, 14.86583411581871772 ) ) ;
#3104=CARTESIAN_POINT ( 'NONE',  ( 5.910764540655177868, 19.00446553125926030, -6.582668785556639257 ) ) ;
#3109=CARTESIAN_POINT ( 'NONE',  ( 0.9789233960466710016, -17.76001420651944684, 37.95943390274106832 ) ) ;
#3111=ORIENTED_EDGE ( 'NONE', *, *, #14511, .T. ) ;
#3113=ORIENTED_EDGE ( 'NONE', *, *, #24046, .T. ) ;
#3117=CARTESIAN_POINT ( 'NONE',  ( 0.5837800005270555870, -44.30119575061277004, 15.38308531172059723 ) ) ;
#3123=CARTESIAN_POINT ( 'NONE',  ( 2.347501380054781706, -0.2125736986915482685, -41.96959656111437198 ) ) ;
#3131=ORIENTED_EDGE ( 'NONE', *, *, #11533, .T. ) ;
#3133=CARTESIAN_POINT ( 'NONE',  ( 2.618530812446115519, -18.50060774051936363, 43.21405214082143686 ) ) ;
#3137=CARTESIAN_POINT ( 'NONE',  ( 0.5834584762367762689, 32.47060451932831171, 33.83630936084141183 ) ) ;
#3138=CARTESIAN_POINT ( 'NONE',  ( 0.6064782688330851990, -38.25720568296584645, -27.12417113480179509 ) ) ;
#3141=B_SPLINE_CURVE_WITH_KNOTS ( 'NONE', 3,
 ( #22316, #41446, #47066, #37055 ),
 .UNSPECIFIED., .F., .F.,
 ( 4, 4 ),
 ( 0.000000000000000000, 0.004447772540403798977 ),
 .UNSPECIFIED. ) ;
#3147=EDGE_CURVE ( 'NONE', #48016, #35743, #22417, .T. ) ;
#3149=CARTESIAN_POINT ( 'NONE',  ( 0.5804410086790514622, 10.33990028284823559, -45.74501408892724186 ) ) ;
#3153=CARTESIAN_POINT ( 'NONE',  ( 5.896782393890504181, 19.71107130340476132, -3.999969368645934775 ) ) ;
#3154=CARTESIAN_POINT ( 'NONE',  ( 0.9787284016396613495, -41.82716437040105717, -2.612339882228906340 ) ) ;
#3155=AXIS2_PLACEMENT_3D ( 'NONE', #36886, #13071, #23381 ) ;
#3175=CARTESIAN_POINT ( 'NONE',  ( 0.5806925824938502512, -29.85799195566318431, 36.16244846134061675 ) ) ;
#3177=EDGE_CURVE ( 'NONE', #9918, #36162, #12574, .T. ) ;
#3184=CARTESIAN_POINT ( 'NONE',  ( 0.5806925824938499181, -25.69265091980040339, 39.23149310256803801 ) ) ;
#3194=CARTESIAN_POINT ( 'NONE',  ( 5.896782393890504181, -20.11283288166117345, 0.006352352428115353410 ) ) ;
#3196=EDGE_CURVE ( 'NONE', #29061, #26516, #61143, .T. ) ;
#3202=CARTESIAN_POINT ( 'NONE',  ( 1.231276596079887264, 10.53918392497828727, 40.57341954055075917 ) ) ;
#3203=CARTESIAN_POINT ( 'NONE',  ( 0.9762797500689124330, -34.83496347773922963, -23.29914386174477059 ) ) ;
#3204=CARTESIAN_POINT ( 'NONE',  ( 0.9787464366903563251, 32.77986221879337592, 26.11158030084323300 ) ) ;
#3205=CARTESIAN_POINT ( 'NONE',  ( 4.956445790444041322, 46.03642002599030292, -9.908889005849065512 ) ) ;
#3226=CARTESIAN_POINT ( 'NONE',  ( 0.9762797500689124330, 19.69530149098714489, -36.99215976885945167 ) ) ;
#3227=ADVANCED_FACE ( 'NONE', ( #37786 ), #44129, .F. ) ;
#3233=CARTESIAN_POINT ( 'NONE',  ( 1.231276596079887264, 3.353048872156665805, -41.78556968953512296 ) ) ;
#3241=CARTESIAN_POINT ( 'NONE',  ( 0.8554163680231708922, -35.40260165760500399, 30.78735566729890749 ) ) ;
#3243=CARTESIAN_POINT ( 'NONE',  ( 0.8560838555295158248, -20.57050347530512724, 42.15717282805135113 ) ) ;
#3248=CARTESIAN_POINT ( 'NONE',  ( 4.962356264823608143, 41.15374796524913847, 8.809348799718396350 ) ) ;
#3252=ORIENTED_EDGE ( 'NONE', *, *, #29798, .T. ) ;
#3256=CARTESIAN_POINT ( 'NONE',  ( 0.9754292589017228288, -12.97161685674443454, -39.85052851615772340 ) ) ;
#3261=CARTESIAN_POINT ( 'NONE',  ( 2.282803330402972009, 33.58715474468253603, -32.83900034431218984 ) ) ;
#3266=( BOUNDED_SURFACE ( )  B_SPLINE_SURFACE ( 3, 1, ( 
 ( #52368, #60849 ),
 ( #12968, #18895 ),
 ( #9160, #32064 ),
 ( #61152, #28570 ) ),
 .UNSPECIFIED., .F., .F., .F. ) 
 B_SPLINE_SURFACE_WITH_KNOTS ( ( 4, 4 ),
 ( 2, 2 ),
 ( 0.000000000000000000, 1.000000000000000000 ),
 ( 0.000000000000000000, 1.000000000000000000 ),
 .UNSPECIFIED. ) 
 GEOMETRIC_REPRESENTATION_ITEM ( )  RATIONAL_B_SPLINE_SURFACE ( (
 ( 1.000000000000000000, 1.000000000000000000),
 ( 0.9952954269826590483, 0.8620686068821339365),
 ( 0.9952954269826590483, 0.8620686068821339365),
 ( 1.000000000000000000, 1.000000000000000000) ) ) 
 REPRESENTATION_ITEM ( '' )  SURFACE ( )  );
#3267=CARTESIAN_POINT ( 'NONE',  ( 0.5782707292762442330, 10.16715070324103287, 45.78608304152260189 ) ) ;
#3272=CARTESIAN_POINT ( 'NONE',  ( 0.5837157313716024865, -34.71940262318195636, -31.52459587483094694 ) ) ;
#3273=CARTESIAN_POINT ( 'NONE',  ( 4.960386119450149955, 23.93873278148768691, -36.62476672265461985 ) ) ;
#3277=CARTESIAN_POINT ( 'NONE',  ( 5.895596859100789899, 17.94951300836817865, -9.074313526372616678 ) ) ;
#3289=( BOUNDED_SURFACE ( )  B_SPLINE_SURFACE ( 3, 1, ( 
 ( #33651, #27390 ),
 ( #52729, #3566 ),
 ( #47744, #4480 ),
 ( #14243, #56505 ) ),
 .UNSPECIFIED., .F., .F., .F. ) 
 B_SPLINE_SURFACE_WITH_KNOTS ( ( 4, 4 ),
 ( 2, 2 ),
 ( 0.000000000000000000, 1.000000000000000000 ),
 ( 0.000000000000000000, 1.000000000000000000 ),
 .UNSPECIFIED. ) 
 GEOMETRIC_REPRESENTATION_ITEM ( )  RATIONAL_B_SPLINE_SURFACE ( (
 ( 1.000000000000000000, 1.000000000000000000),
 ( 0.7282232189291694135, 0.9929344683865672927),
 ( 0.7282232189291694135, 0.9929344683865672927),
 ( 1.000000000000000000, 1.000000000000000000) ) ) 
 REPRESENTATION_ITEM ( '' )  SURFACE ( )  );
#3291=CARTESIAN_POINT ( 'NONE',  ( 4.956445790443988031, 0.000000000000000000, -47.09074272231896430 ) ) ;
#3292=CIRCLE ( 'NONE', #37361, 47.09074272231896430 ) ;
#3298=CARTESIAN_POINT ( 'NONE',  ( 0.9780106845699481077, 25.11113889175388181, -33.55237622009033771 ) ) ;
#3299=EDGE_CURVE ( 'NONE', #5770, #31240, #24264, .T. ) ;
#3308=EDGE_CURVE ( 'NONE', #26439, #49329, #55142, .T. ) ;
#3315=CARTESIAN_POINT ( 'NONE',  ( 0.9790850452238870627, 4.144492514655467197, -41.70324342373339022 ) ) ;
#3319=ORIENTED_EDGE ( 'NONE', *, *, #397, .F. ) ;
#3321=CARTESIAN_POINT ( 'NONE',  ( 0.5806925824938502512, 45.37089516811273882, 11.86188155343358197 ) ) ;
#3323=EDGE_CURVE ( 'NONE', #19581, #36353, #53070, .T. ) ;
#3327=ORIENTED_EDGE ( 'NONE', *, *, #13810, .F. ) ;
#3332=CARTESIAN_POINT ( 'NONE',  ( 5.917102823773431552, 14.92182362673000284, -13.48439459910989946 ) ) ;
#3334=CARTESIAN_POINT ( 'NONE',  ( 0.9762797500689124330, 29.49606728235556830, -29.77090526101713763 ) ) ;
#3342=CARTESIAN_POINT ( 'NONE',  ( 4.956445790444029775, 25.79263028817611314, -39.39896284113449809 ) ) ;
#3349=CARTESIAN_POINT ( 'NONE',  ( 5.896278296736517710, -2.018661446113561908, -20.01129644926481532 ) ) ;
#3357=CARTESIAN_POINT ( 'NONE',  ( 1.231276596079881935, 10.53918392497884149, -40.57341954055061706 ) ) ;
#3362=ADVANCED_FACE ( 'NONE', ( #1358 ), #24885, .F. ) ;
#3365=CARTESIAN_POINT ( 'NONE',  ( 0.5817217712918324457, 46.41469452300511023, 6.701573423047251232 ) ) ;
#3371=EDGE_CURVE ( 'NONE', #37569, #18665, #37997, .T. ) ;
#3376=EDGE_CURVE ( 'NONE', #11571, #4545, #2603, .T. ) ;
#3378=CARTESIAN_POINT ( 'NONE',  ( 4.962356264823601926, -42.08379584346671720, 0.4355746408606013254 ) ) ;
#3380=CARTESIAN_POINT ( 'NONE',  ( 5.838029081930957709, -37.08173278831614539, -29.25765116288114243 ) ) ;
#3384=EDGE_LOOP ( 'NONE', ( #1943, #39526, #52066, #17337 ) ) ;
#3393=ORIENTED_EDGE ( 'NONE', *, *, #40427, .T. ) ;
#3395=VERTEX_POINT ( 'NONE', #49601 ) ;
#3399=DIRECTION ( 'NONE',  ( 1.000000000000000000, 0.000000000000000000, 0.000000000000000000 ) ) ;
#3404=ORIENTED_EDGE ( 'NONE', *, *, #867, .F. ) ;
#3405=CARTESIAN_POINT ( 'NONE',  ( 1.157643937452367933, -39.31880107603836905, 14.52701471527025845 ) ) ;
#3411=ORIENTED_EDGE ( 'NONE', *, *, #13810, .T. ) ;
#3414=EDGE_CURVE ( 'NONE', #57834, #51445, #50839, .T. ) ;
#3416=ORIENTED_EDGE ( 'NONE', *, *, #9264, .T. ) ;
#3426=CARTESIAN_POINT ( 'NONE',  ( 0.5806925824938499181, -41.60618895332673617, -21.63671424046719594 ) ) ;
#3434=CARTESIAN_POINT ( 'NONE',  ( 0.9787464366903554369, 29.00705047156419525, 30.24772744902649890 ) ) ;
#3437=CARTESIAN_POINT ( 'NONE',  ( 0.5782707292762442330, 17.53027906811957237, -43.50201914281066706 ) ) ;
#3443=EDGE_CURVE ( 'NONE', #47205, #54614, #46540, .T. ) ;
#3447=CARTESIAN_POINT ( 'NONE',  ( 0.8560838555295223751, -45.77741231505103059, 10.23725333375835689 ) ) ;
#3457=CARTESIAN_POINT ( 'NONE',  ( 2.282803330402976005, 41.06968832204452013, -22.79863172620468603 ) ) ;
#3461=VECTOR ( 'NONE', #126, 1000.000000000000114 ) ;
#3462=VERTEX_POINT ( 'NONE', #9465 ) ;
#3469=ORIENTED_EDGE ( 'NONE', *, *, #1827, .T. ) ;
#3476=CARTESIAN_POINT ( 'NONE',  ( 0.5835226383429280572, -30.13809304758011010, 35.92962318201194449 ) ) ;
#3480=CARTESIAN_POINT ( 'NONE',  ( 0.5806925824938499181, -30.69245420804209701, 35.45695442407318154 ) ) ;
#3484=( BOUNDED_SURFACE ( )  B_SPLINE_SURFACE ( 3, 1, ( 
 ( #52723, #42740 ),
 ( #19547, #38355 ),
 ( #33346, #23315 ),
 ( #56805, #43676 ) ),
 .UNSPECIFIED., .F., .F., .F. ) 
 B_SPLINE_SURFACE_WITH_KNOTS ( ( 4, 4 ),
 ( 2, 2 ),
 ( 0.000000000000000000, 1.000000000000000000 ),
 ( 0.000000000000000000, 1.000000000000000000 ),
 .UNSPECIFIED. ) 
 GEOMETRIC_REPRESENTATION_ITEM ( )  RATIONAL_B_SPLINE_SURFACE ( (
 ( 1.000000000000000000, 1.000000000000000000),
 ( 0.7282232189291694135, 0.9929344683865672927),
 ( 0.7282232189291694135, 0.9929344683865672927),
 ( 1.000000000000000000, 1.000000000000000000) ) ) 
 REPRESENTATION_ITEM ( '' )  SURFACE ( )  );
#3490=CARTESIAN_POINT ( 'NONE',  ( 4.962356264823599261, -28.94323483023637777, 30.55363735178087126 ) ) ;
#3504=CARTESIAN_POINT ( 'NONE',  ( 4.956445790444001354, -33.12351118015997997, 33.47194433010209025 ) ) ;
#3511=CARTESIAN_POINT ( 'NONE',  ( 0.9762797500689124330, -26.66896101499594707, 32.32787193067817810 ) ) ;
#3515=CARTESIAN_POINT ( 'NONE',  ( 4.962356264823608143, -9.332162870646227404, -41.03835198954849517 ) ) ;
#3521=CARTESIAN_POINT ( 'NONE',  ( 5.838029081930957709, 1.598329895848616067, 47.20710115752668656 ) ) ;
#3522=ADVANCED_FACE ( 'NONE', ( #18271 ), #3266, .F. ) ;
#3523=ORIENTED_EDGE ( 'NONE', *, *, #61931, .T. ) ;
#3530=CARTESIAN_POINT ( 'NONE',  ( 5.895881250540457863, -19.39704354167978906, -5.318118412604147416 ) ) ;
#3540=( BOUNDED_SURFACE ( )  B_SPLINE_SURFACE ( 3, 1, ( 
 ( #18008, #37749 ),
 ( #3563, #27085 ),
 ( #51802, #18617 ),
 ( #56499, #4176 ) ),
 .UNSPECIFIED., .F., .F., .F. ) 
 B_SPLINE_SURFACE_WITH_KNOTS ( ( 4, 4 ),
 ( 2, 2 ),
 ( 0.000000000000000000, 1.000000000000000000 ),
 ( 0.000000000000000000, 1.000000000000000000 ),
 .UNSPECIFIED. ) 
 GEOMETRIC_REPRESENTATION_ITEM ( )  RATIONAL_B_SPLINE_SURFACE ( (
 ( 1.000000000000000000, 1.000000000000000000),
 ( 0.9729067724841187204, 0.9999501103223794596),
 ( 0.9729067724841187204, 0.9999501103223794596),
 ( 1.000000000000000000, 1.000000000000000000) ) ) 
 REPRESENTATION_ITEM ( '' )  SURFACE ( )  );
#3551=CARTESIAN_POINT ( 'NONE',  ( 0.5832655196449124668, -38.79139163682725666, 26.35266813534483887 ) ) ;
#3554=ORIENTED_EDGE ( 'NONE', *, *, #22993, .F. ) ;
#3563=CARTESIAN_POINT ( 'NONE',  ( 5.894904586330512508, 3.346579165707559866, -19.83254446482585820 ) ) ;
#3566=CARTESIAN_POINT ( 'NONE',  ( 2.618530812446111078, 37.74802994993080318, -28.01451452546210774 ) ) ;
#3575=CARTESIAN_POINT ( 'NONE',  ( 0.9784957157296367836, -1.632997897510987118, -41.87679995963272717 ) ) ;
#3576=CARTESIAN_POINT ( 'NONE',  ( 0.7764139734771262624, 11.73874210050403555, -45.41191919314488956 ) ) ;
#3579=CARTESIAN_POINT ( 'NONE',  ( 0.6064782688330867533, -46.73948921451010108, -3.841170965404212101 ) ) ;
#3580=CARTESIAN_POINT ( 'NONE',  ( 0.6064782688330858651, -25.83066036557900702, 39.14219502655511462 ) ) ;
#3582=CARTESIAN_POINT ( 'NONE',  ( 0.5837800005270554760, -34.78054197040876971, -31.45710029367646143 ) ) ;
#3596=FACE_OUTER_BOUND ( 'NONE', #14812, .T. ) ;
#3619=CARTESIAN_POINT ( 'NONE',  ( 0.9790724872846768845, 4.235103416345695315, -41.69411360173413073 ) ) ;
#3626=CARTESIAN_POINT ( 'NONE',  ( 0.6064515330803583737, -2.277169567790236382, -46.84174243980059060 ) ) ;
#3628=LINE ( 'NONE', #31543, #21505 ) ;
#3636=ORIENTED_EDGE ( 'NONE', *, *, #34980, .T. ) ;
#3647=CARTESIAN_POINT ( 'NONE',  ( 4.956445790444027999, 24.88142650099568698, -39.98065363916886383 ) ) ;
#3652=CARTESIAN_POINT ( 'NONE',  ( 1.231276596079881047, -39.86997064245551314, 12.94844438485960580 ) ) ;
#3655=( BOUNDED_SURFACE ( )  B_SPLINE_SURFACE ( 3, 1, ( 
 ( #3332, #35969 ),
 ( #36896, #22463 ),
 ( #7731, #45367 ),
 ( #35658, #8345 ) ),
 .UNSPECIFIED., .F., .F., .F. ) 
 B_SPLINE_SURFACE_WITH_KNOTS ( ( 4, 4 ),
 ( 2, 2 ),
 ( 0.000000000000000000, 1.000000000000000000 ),
 ( 0.000000000000000000, 1.000000000000000000 ),
 .UNSPECIFIED. ) 
 GEOMETRIC_REPRESENTATION_ITEM ( )  RATIONAL_B_SPLINE_SURFACE ( (
 ( 1.000000000000000000, 1.000000000000000000),
 ( 0.7282232189291693025, 0.9929344683865674037),
 ( 0.7282232189291693025, 0.9929344683865674037),
 ( 1.000000000000000000, 1.000000000000000000) ) ) 
 REPRESENTATION_ITEM ( '' )  SURFACE ( )  );
#3661=CARTESIAN_POINT ( 'NONE',  ( 0.8560838555295223751, 23.34035564869547841, 40.68907263964295851 ) ) ;
#3682=ORIENTED_EDGE ( 'NONE', *, *, #32587, .F. ) ;
#3683=CARTESIAN_POINT ( 'NONE',  ( 5.917102823773431552, 0.6634426252560792214, 20.10098410363869093 ) ) ;
#3692=ORIENTED_EDGE ( 'NONE', *, *, #34905, .T. ) ;
#3697=LINE ( 'NONE', #27527, #19375 ) ;
#3706=PLANE ( 'NONE',  #2618 ) ;
#3712=CARTESIAN_POINT ( 'NONE',  ( 0.9762797500689124330, -39.42083772998332591, 14.22400568939802845 ) ) ;
#3713=EDGE_CURVE ( 'NONE', #48545, #58092, #6890, .T. ) ;
#3731=CARTESIAN_POINT ( 'NONE',  ( 0.9754292589017200532, -17.11069906115304562, 38.25639089791319947 ) ) ;
#3739=CARTESIAN_POINT ( 'NONE',  ( 1.231276596079887264, 41.65019306089983786, 4.747440258480190245 ) ) ;
#3740=CARTESIAN_POINT ( 'NONE',  ( 5.910764540655177868, 8.479982303153068557, -18.23708141692013740 ) ) ;
#3743=CARTESIAN_POINT ( 'NONE',  ( 5.894904586330512508, 19.70964338679887362, 4.007414331817764186 ) ) ;
#3746=AXIS2_PLACEMENT_3D ( 'NONE', #21161, #54650, #35895 ) ;
#3752=DIRECTION ( 'NONE',  ( -1.000000000000000000, -0.000000000000000000, -0.000000000000000000 ) ) ;
#3753=CARTESIAN_POINT ( 'NONE',  ( 0.7764139734771247081, -2.458099863852005740, 46.84013467066674252 ) ) ;
#3757=EDGE_CURVE ( 'NONE', #41399, #16218, #7218, .T. ) ;
#3759=CARTESIAN_POINT ( 'NONE',  ( 0.000000000000000000, 0.000000000000000000, 0.000000000000000000 ) ) ;
#3768=ORIENTED_EDGE ( 'NONE', *, *, #38628, .F. ) ;
#3774=CARTESIAN_POINT ( 'NONE',  ( 0.9762797500689124330, 24.45014227843030596, -34.03697001423921620 ) ) ;
#3781=CARTESIAN_POINT ( 'NONE',  ( 1.231276596079881047, -35.03243822710529543, 23.02183839058294623 ) ) ;
#3783=CARTESIAN_POINT ( 'NONE',  ( 5.895596859100789899, -9.669028665050335647, 17.63627137143570067 ) ) ;
#3785=CARTESIAN_POINT ( 'NONE',  ( 0.7056313189692711152, 46.89390071911098090, -0.8430416974981863598 ) ) ;
#3786=VERTEX_POINT ( 'NONE', #59856 ) ;
#3789=ORIENTED_EDGE ( 'NONE', *, *, #49175, .T. ) ;
#3792=B_SPLINE_CURVE_WITH_KNOTS ( 'NONE', 3,
 ( #58770, #35013, #12135, #25903 ),
 .UNSPECIFIED., .F., .F.,
 ( 4, 4 ),
 ( 0.000000000000000000, 0.005004948556313781882 ),
 .UNSPECIFIED. ) ;
#3793=EDGE_CURVE ( 'NONE', #59500, #9430, #56936, .T. ) ;
#3798=CARTESIAN_POINT ( 'NONE',  ( 0.5835226383429285013, 4.875290024808289324, 46.64197703485532998 ) ) ;
#3802=VECTOR ( 'NONE', #51739, 1000.000000000000114 ) ;
#3805=DIRECTION ( 'NONE',  ( -0.07500201931887527651, 0.9232442575324670830, 0.3768218916562764975 ) ) ;
#3806=EDGE_CURVE ( 'NONE', #21146, #36659, #10699, .T. ) ;
#3808=CARTESIAN_POINT ( 'NONE',  ( 0.8560838555295158248, 9.983184696770717181, 45.83349056521764453 ) ) ;
#3810=CARTESIAN_POINT ( 'NONE',  ( 0.8554163680231708922, -46.86440027434177580, 2.221139355847124186 ) ) ;
#3811=CARTESIAN_POINT ( 'NONE',  ( 0.5806925824938511393, 5.237374507879287044, 46.60249210726590263 ) ) ;
#3812=CARTESIAN_POINT ( 'NONE',  ( 0.5832655196449136881, 4.920529935022127432, -46.63714794165569799 ) ) ;
#3818=CARTESIAN_POINT ( 'NONE',  ( 0.9769922540276048117, -12.83782684460722123, 39.89388119742184102 ) ) ;
#3821=CARTESIAN_POINT ( 'NONE',  ( 0.5782707292762423457, 42.89195216551532042, -18.97410849391256349 ) ) ;
#3826=CARTESIAN_POINT ( 'NONE',  ( 0.8560838555295223751, -6.899551485032601406, 46.39794201672221163 ) ) ;
#3829=VERTEX_POINT ( 'NONE', #39867 ) ;
#3835=ORIENTED_EDGE ( 'NONE', *, *, #43345, .F. ) ;
#3838=VERTEX_POINT ( 'NONE', #35145 ) ;
#3840=EDGE_CURVE ( 'NONE', #33545, #27840, #19915, .T. ) ;
#3860=LINE ( 'NONE', #42131, #49255 ) ;
#3863=FACE_OUTER_BOUND ( 'NONE', #20398, .T. ) ;
#3869=CARTESIAN_POINT ( 'NONE',  ( 0.5782707292762442330, 42.89195216551504330, 18.97410849391315324 ) ) ;
#3876=ORIENTED_EDGE ( 'NONE', *, *, #49989, .F. ) ;
#3888=CARTESIAN_POINT ( 'NONE',  ( 0.9790724872846784388, -1.359965803035979137, -41.88658141930447698 ) ) ;
#3891=EDGE_LOOP ( 'NONE', ( #44011, #14653, #58884, #58223 ) ) ;
#3892=CARTESIAN_POINT ( 'NONE',  ( 0.5797568665920713737, -46.74494072455451033, 3.759763989900801295 ) ) ;
#3899=CARTESIAN_POINT ( 'NONE',  ( 0.5817216825391118284, -24.84894157072779919, 39.77141002054133168 ) ) ;
#3901=CARTESIAN_POINT ( 'NONE',  ( 5.896782393890504181, -4.668739246792323883, 19.56345983519973686 ) ) ;
#3906=CONICAL_SURFACE ( 'NONE', #27944, 42.08604991992415023, 1.569615340895231137 ) ;
#3909=CARTESIAN_POINT ( 'NONE',  ( 2.618530812446115519, -41.30116959783759256, 22.44861196263268255 ) ) ;
#3914=( BOUNDED_SURFACE ( )  B_SPLINE_SURFACE ( 3, 1, ( 
 ( #59417, #45979 ),
 ( #26532, #21527 ),
 ( #31233, #1783 ),
 ( #30604, #41275 ) ),
 .UNSPECIFIED., .F., .F., .F. ) 
 B_SPLINE_SURFACE_WITH_KNOTS ( ( 4, 4 ),
 ( 2, 2 ),
 ( 0.000000000000000000, 1.000000000000000000 ),
 ( 0.000000000000000000, 1.000000000000000000 ),
 .UNSPECIFIED. ) 
 GEOMETRIC_REPRESENTATION_ITEM ( )  RATIONAL_B_SPLINE_SURFACE ( (
 ( 1.000000000000000000, 1.000000000000000000),
 ( 0.9952954269826590483, 0.8620686068821307169),
 ( 0.9952954269826590483, 0.8620686068821307169),
 ( 1.000000000000000000, 1.000000000000000000) ) ) 
 REPRESENTATION_ITEM ( '' )  SURFACE ( )  );
#3915=VERTEX_POINT ( 'NONE', #37306 ) ;
#3924=ORIENTED_EDGE ( 'NONE', *, *, #24771, .F. ) ;
#3930=CARTESIAN_POINT ( 'NONE',  ( 0.9788927965476029724, 4.053859047820351336, -41.71214259004423752 ) ) ;
#3931=CARTESIAN_POINT ( 'NONE',  ( 1.231276596079887264, 32.36747132271594296, -26.63876069172940930 ) ) ;
#3936=CARTESIAN_POINT ( 'NONE',  ( 4.960386119450139297, -3.911092338299068327, 43.57912139308960064 ) ) ;
#3939=ORIENTED_EDGE ( 'NONE', *, *, #30256, .F. ) ;
#3940=CARTESIAN_POINT ( 'NONE',  ( 1.092182651088184242, -39.84386646767028850, -13.00874664788052115 ) ) ;
#3944=DIRECTION ( 'NONE',  ( -1.000000000000000000, -0.000000000000000000, -0.000000000000000000 ) ) ;
#3951=CARTESIAN_POINT ( 'NONE',  ( 0.5804410086790514622, 42.96136033320046010, 18.81067170986478487 ) ) ;
#3952=VERTEX_POINT ( 'NONE', #27893 ) ;
#3954=FACE_OUTER_BOUND ( 'NONE', #11802, .T. ) ;
#3957=B_SPLINE_CURVE_WITH_KNOTS ( 'NONE', 3,
 ( #34630, #57164, #28373, #154, #57467, #47494 ),
 .UNSPECIFIED., .F., .F.,
 ( 4, 2, 4 ),
 ( 7.023086426956682172E-18, 0.0002448709889506543377, 0.0004897419779013016282 ),
 .UNSPECIFIED. ) ;
#3965=CARTESIAN_POINT ( 'NONE',  ( 0.9762797500689124330, -26.66896101499594707, 32.32787193067817810 ) ) ;
#3966=DIRECTION ( 'NONE',  ( 0.07906939808003032866, 0.9752531043637134855, 0.2064689146486738125 ) ) ;
#3975=DIRECTION ( 'NONE',  ( 0.000000000000000000, 0.000000000000000000, 1.000000000000000000 ) ) ;
#3981=CARTESIAN_POINT ( 'NONE',  ( 0.5806925824938494740, 46.54710689580857519, 5.708695295225819422 ) ) ;
#3983=B_SPLINE_CURVE_WITH_KNOTS ( 'NONE', 3,
 ( #3243, #61186, #27376, #46499, #46197, #55876 ),
 .UNSPECIFIED., .F., .F.,
 ( 4, 2, 4 ),
 ( 1.202235021059306678E-16, 0.0002448718616795958068, 0.0004897437233590713757 ),
 .UNSPECIFIED. ) ;
#3996=CARTESIAN_POINT ( 'NONE',  ( 0.5806925824938499181, 37.13995815321135296, -28.63295078613577971 ) ) ;
#3997=VERTEX_POINT ( 'NONE', #31669 ) ;
#4001=ORIENTED_EDGE ( 'NONE', *, *, #31684, .T. ) ;
#4005=CARTESIAN_POINT ( 'NONE',  ( 0.5837800304671212359, -7.755313095589508876, -46.25032379312472131 ) ) ;
#4008=CARTESIAN_POINT ( 'NONE',  ( 0.9788927965476035276, -7.110334182851104856, -41.30108667383892396 ) ) ;
#4011=ORIENTED_EDGE ( 'NONE', *, *, #13738, .F. ) ;
#4023=EDGE_CURVE ( 'NONE', #41472, #56267, #57289, .T. ) ;
#4033=CARTESIAN_POINT ( 'NONE',  ( 0.9785694773339266295, -41.11263117936924516, 8.129388859184128791 ) ) ;
#4043=FACE_OUTER_BOUND ( 'NONE', #14161, .T. ) ;
#4045=CARTESIAN_POINT ( 'NONE',  ( 0.9785694773339244090, 28.97418037048111827, 30.27923839156954955 ) ) ;
#4049=CARTESIAN_POINT ( 'NONE',  ( 5.901463166500146684, -13.99254106127013841, -14.44737571288660760 ) ) ;
#4055=CARTESIAN_POINT ( 'NONE',  ( 3.782542959838395724, 40.05509967486248257, 12.76036219836252705 ) ) ;
#4058=ADVANCED_FACE ( 'NONE', ( #52605 ), #7283, .F. ) ;
#4068=ORIENTED_EDGE ( 'NONE', *, *, #24947, .F. ) ;
#4069=EDGE_CURVE ( 'NONE', #41171, #22554, #9879, .T. ) ;
#4070=CARTESIAN_POINT ( 'NONE',  ( 4.956445790444031552, 30.81386304088997719, -35.60960396630257208 ) ) ;
#4079=CONICAL_SURFACE ( 'NONE', #58103, 42.08604991992415023, 1.569615340895231137 ) ;
#4083=VERTEX_POINT ( 'NONE', #52293 ) ;
#4084=FACE_OUTER_BOUND ( 'NONE', #33964, .T. ) ;
#4099=VERTEX_POINT ( 'NONE', #20655 ) ;
#4102=CARTESIAN_POINT ( 'NONE',  ( 4.956445790444035104, 38.51510088324747016, -27.09474218539284252 ) ) ;
#4108=CARTESIAN_POINT ( 'NONE',  ( 5.896782393890504181, 10.81700609697900894, -16.95636948099241792 ) ) ;
#4116=CARTESIAN_POINT ( 'NONE',  ( 0.5806925824938502512, 40.06810415365508504, -24.36738377166110325 ) ) ;
#4139=EDGE_CURVE ( 'NONE', #2726, #15046, #12815, .T. ) ;
#4142=ORIENTED_EDGE ( 'NONE', *, *, #56953, .T. ) ;
#4158=CARTESIAN_POINT ( 'NONE',  ( 0.9791128995231619392, -39.58816053567403515, 13.75190821842056543 ) ) ;
#4165=CARTESIAN_POINT ( 'NONE',  ( 0.9762797500689124330, -0.8945891712305065191, 41.89897964629235361 ) ) ;
#4167=CARTESIAN_POINT ( 'NONE',  ( 5.895596859100789899, 16.57987064389762111, 11.38578379577399069 ) ) ;
#4168=ORIENTED_EDGE ( 'NONE', *, *, #35231, .T. ) ;
#4169=CARTESIAN_POINT ( 'NONE',  ( 4.962356264823608143, 0.000000000000000000, 0.000000000000000000 ) ) ;
#4175=CARTESIAN_POINT ( 'NONE',  ( 4.956445790443993360, 20.31112743693043399, 42.48524629068788983 ) ) ;
#4176=CARTESIAN_POINT ( 'NONE',  ( 0.5804410086790514622, -8.338934868871040962, 46.15172821366631695 ) ) ;
#4179=ORIENTED_EDGE ( 'NONE', *, *, #16249, .T. ) ;
#4181=CARTESIAN_POINT ( 'NONE',  ( 0.8554163680231708922, 21.74163052365331694, 41.57531689939074226 ) ) ;
#4188=CARTESIAN_POINT ( 'NONE',  ( 4.291220156522060236, 39.39367666905506127, -25.83654844981511189 ) ) ;
#4189=B_SPLINE_CURVE_WITH_KNOTS ( 'NONE', 3,
 ( #21793, #12403, #17101, #31490 ),
 .UNSPECIFIED., .F., .F.,
 ( 4, 4 ),
 ( 4.336808689942017736E-19, 0.004041751736740989073 ),
 .UNSPECIFIED. ) ;
#4201=CARTESIAN_POINT ( 'NONE',  ( 0.5837799406558226156, -25.15713538965591667, 39.57729258759022883 ) ) ;
#4202=CARTESIAN_POINT ( 'NONE',  ( -4.467300000000000715, 0.000000000000000000, 0.000000000000000000 ) ) ;
#4205=ORIENTED_EDGE ( 'NONE', *, *, #8467, .T. ) ;
#4206=ORIENTED_EDGE ( 'NONE', *, *, #42033, .T. ) ;
#4217=VECTOR ( 'NONE', #23916, 1000.000000000000000 ) ;
#4222=CARTESIAN_POINT ( 'NONE',  ( 0.9769922540276039236, 25.21368293196807286, -33.47539018581124282 ) ) ;
#4227=CARTESIAN_POINT ( 'NONE',  ( 4.958415959904823644, -45.08182420577205818, -5.552754280760447969 ) ) ;
#4228=B_SPLINE_CURVE_WITH_KNOTS ( 'NONE', 3,
 ( #9662, #18154, #9353, #24383 ),
 .UNSPECIFIED., .F., .F.,
 ( 4, 4 ),
 ( 4.336808689942017736E-19, 0.004446298630425045070 ),
 .UNSPECIFIED. ) ;
#4231=VERTEX_POINT ( 'NONE', #7657 ) ;
#4232=CARTESIAN_POINT ( 'NONE',  ( 4.956445790444005794, -33.12351118015950391, -33.47194433010255921 ) ) ;
#4239=CARTESIAN_POINT ( 'NONE',  ( 0.9791128995231609400, 4.189801958621016453, -41.69871693222346209 ) ) ;
#4241=EDGE_CURVE ( 'NONE', #9401, #20518, #21004, .T. ) ;
#4251=DIRECTION ( 'NONE',  ( 0.07906939808003035641, 0.04137963570464910784, -0.9960099176394842102 ) ) ;
#4253=CARTESIAN_POINT ( 'NONE',  ( 0.5804410086790514622, 40.62771722849995371, -23.42879520283626604 ) ) ;
#4263=ORIENTED_EDGE ( 'NONE', *, *, #3035, .F. ) ;
#4264=CARTESIAN_POINT ( 'NONE',  ( 0.9772918015221172539, 41.58800822122364593, 5.174401215804053322 ) ) ;
#4270=CARTESIAN_POINT ( 'NONE',  ( 0.5804410086790514622, 40.07081992599750464, -24.36902218624453909 ) ) ;
#4276=( BOUNDED_SURFACE ( )  B_SPLINE_SURFACE ( 3, 1, ( 
 ( #57495, #33126 ),
 ( #27792, #37843 ),
 ( #9928, #29026 ),
 ( #51897, #8990 ) ),
 .UNSPECIFIED., .F., .F., .F. ) 
 B_SPLINE_SURFACE_WITH_KNOTS ( ( 4, 4 ),
 ( 2, 2 ),
 ( 0.000000000000000000, 1.000000000000000000 ),
 ( 0.000000000000000000, 1.000000000000000000 ),
 .UNSPECIFIED. ) 
 GEOMETRIC_REPRESENTATION_ITEM ( )  RATIONAL_B_SPLINE_SURFACE ( (
 ( 1.000000000000000000, 1.000000000000000000),
 ( 0.9952954269826590483, 0.8620686068821307169),
 ( 0.9952954269826590483, 0.8620686068821307169),
 ( 1.000000000000000000, 1.000000000000000000) ) ) 
 REPRESENTATION_ITEM ( '' )  SURFACE ( )  );
#4279=CARTESIAN_POINT ( 'NONE',  ( 0.5817217712918331118, 32.27292434475872085, 34.02489247956344798 ) ) ;
#4282=CARTESIAN_POINT ( 'NONE',  ( 1.231276596079881047, -2.246340108600348717, 41.85965512441018888 ) ) ;
#4287=( BOUNDED_SURFACE ( )  B_SPLINE_SURFACE ( 3, 1, ( 
 ( #36763, #42690 ),
 ( #56754, #28565 ),
 ( #37073, #9456 ),
 ( #55836, #23562 ) ),
 .UNSPECIFIED., .F., .F., .F. ) 
 B_SPLINE_SURFACE_WITH_KNOTS ( ( 4, 4 ),
 ( 2, 2 ),
 ( 0.000000000000000000, 1.000000000000000000 ),
 ( 0.000000000000000000, 1.000000000000000000 ),
 .UNSPECIFIED. ) 
 GEOMETRIC_REPRESENTATION_ITEM ( )  RATIONAL_B_SPLINE_SURFACE ( (
 ( 1.000000000000000000, 1.000000000000000000),
 ( 0.9729067724841187204, 0.9999501103223794596),
 ( 0.9729067724841187204, 0.9999501103223794596),
 ( 1.000000000000000000, 1.000000000000000000) ) ) 
 REPRESENTATION_ITEM ( '' )  SURFACE ( )  );
#4291=CARTESIAN_POINT ( 'NONE',  ( 5.901463166500146684, -11.94204572599448966, -16.18349202795532094 ) ) ;
#4293=EDGE_LOOP ( 'NONE', ( #51650, #8712, #2785, #8608 ) ) ;
#4296=VECTOR ( 'NONE', #32147, 1000.000000000000227 ) ;
#4297=CARTESIAN_POINT ( 'NONE',  ( 0.8554163680231708922, 44.99993935735606243, 13.27444654010463942 ) ) ;
#4298=ORIENTED_EDGE ( 'NONE', *, *, #14781, .F. ) ;
#4314=CARTESIAN_POINT ( 'NONE',  ( 4.962356264823608143, 42.01891079680549268, -2.376285612557975213 ) ) ;
#4323=FACE_OUTER_BOUND ( 'NONE', #11629, .T. ) ;
#4333=CARTESIAN_POINT ( 'NONE',  ( 0.9780303403264770656, 38.70851733140969486, 16.06207643485240766 ) ) ;
#4338=B_SPLINE_CURVE_WITH_KNOTS ( 'NONE', 3,
 ( #1553, #54168, #20082, #44830 ),
 .UNSPECIFIED., .F., .F.,
 ( 4, 4 ),
 ( 2.168404344971008868E-19, 0.004446298630425069356 ),
 .UNSPECIFIED. ) ;
#4340=CARTESIAN_POINT ( 'NONE',  ( 1.231276596079881047, -35.03243822710529543, 23.02183839058294623 ) ) ;
#4341=CARTESIAN_POINT ( 'NONE',  ( 1.231276596079887264, -6.136529359146732254, 41.46829847537028257 ) ) ;
#4346=CARTESIAN_POINT ( 'NONE',  ( 5.895881250540457863, 20.06826253866635668, 1.338850360369496784 ) ) ;
#4348=CARTESIAN_POINT ( 'NONE',  ( 0.9790320750461911636, -34.59983469426835967, 23.64716836476394235 ) ) ;
#4350=CARTESIAN_POINT ( 'NONE',  ( 1.231276596079887264, -31.65135013586864332, -27.48579279545554144 ) ) ;
#4356=CARTESIAN_POINT ( 'NONE',  ( 0.9790724872846777727, 20.10506717481070282, 36.77120454755054624 ) ) ;
#4357=DIRECTION ( 'NONE',  ( 0.000000000000000000, 0.000000000000000000, 1.000000000000000000 ) ) ;
#4358=CARTESIAN_POINT ( 'NONE',  ( 4.960386119450145515, -16.16390115411087791, -40.65912891531831974 ) ) ;
#4362=CARTESIAN_POINT ( 'NONE',  ( 0.5848930533535030563, -44.24150702629557941, 15.55513222154659125 ) ) ;
#4363=EDGE_CURVE ( 'NONE', #32404, #54938, #32059, .T. ) ;
#4383=ORIENTED_EDGE ( 'NONE', *, *, #23262, .T. ) ;
#4384=CARTESIAN_POINT ( 'NONE',  ( 4.962356264823608143, 0.000000000000000000, 0.000000000000000000 ) ) ;
#4385=CARTESIAN_POINT ( 'NONE',  ( 0.8554163680231816613, -45.78608427674282666, 10.23913862172123146 ) ) ;
#4387=CARTESIAN_POINT ( 'NONE',  ( 0.5834584762367742705, 16.68472608544807301, 43.82757014102836024 ) ) ;
#4394=CARTESIAN_POINT ( 'NONE',  ( 3.376099380956838925, -5.222100608646857545, -12.34658045230489165 ) ) ;
#4395=CARTESIAN_POINT ( 'NONE',  ( 0.5806925824938499181, 11.40214825760356376, -45.48860711711441240 ) ) ;
#4396=VERTEX_POINT ( 'NONE', #54680 ) ;
#4397=CARTESIAN_POINT ( 'NONE',  ( 0.9789889208857696090, -34.60556929628447165, -23.63872821711065342 ) ) ;
#4399=CARTESIAN_POINT ( 'NONE',  ( 4.956445790444040433, 46.94638516972321440, -3.684422564748698115 ) ) ;
#4403=CARTESIAN_POINT ( 'NONE',  ( 0.8554163680231708922, 46.90810212776801791, 0.9140174411379320407 ) ) ;
#4407=APPLICATION_CONTEXT ( 'automotive_design' ) ;
#4408=B_SPLINE_CURVE_WITH_KNOTS ( 'NONE', 3,
 ( #44775, #59138, #58208, #6496 ),
 .UNSPECIFIED., .F., .F.,
 ( 4, 4 ),
 ( 0.000000000000000000, 0.004446298630425099714 ),
 .UNSPECIFIED. ) ;
#4410=CARTESIAN_POINT ( 'NONE',  ( 0.6845945791218034371, -46.85360930762398368, 2.268439014493165651 ) ) ;
#4415=CARTESIAN_POINT ( 'NONE',  ( 0.5837800304671217910, 40.37258561079670471, -23.85983368086184697 ) ) ;
#4418=CARTESIAN_POINT ( 'NONE',  ( 0.6064782688330851990, 33.10963464956490299, -33.21274664629680018 ) ) ;
#4419=CARTESIAN_POINT ( 'NONE',  ( 0.5804410086790514622, 46.55025363952972128, -5.709092568074903618 ) ) ;
#4429=CONICAL_SURFACE ( 'NONE', #34618, 42.08604991992415023, 1.569615340895231137 ) ;
#4441=CARTESIAN_POINT ( 'NONE',  ( 4.956445790444031552, 30.81386304088997719, -35.60960396630257208 ) ) ;
#4445=ORIENTED_EDGE ( 'NONE', *, *, #10402, .T. ) ;
#4457=CARTESIAN_POINT ( 'NONE',  ( 0.9772918015221170318, -39.45178799254951230, 14.13836199641267122 ) ) ;
#4470=CARTESIAN_POINT ( 'NONE',  ( 0.5797568599927143129, 46.55714417914590797, -5.626511757139216918 ) ) ;
#4471=CARTESIAN_POINT ( 'NONE',  ( 5.896782393890504181, 18.99788783847851548, 6.603510017755907846 ) ) ;
#4480=CARTESIAN_POINT ( 'NONE',  ( 4.291220156522059348, 38.26855966511131157, -27.47555892904659913 ) ) ;
#4483=CARTESIAN_POINT ( 'NONE',  ( 4.956445790444006683, -32.34643101787064978, -34.22347806032829709 ) ) ;
#4484=AXIS2_PLACEMENT_3D ( 'NONE', #7006, #16435, #29602 ) ;
#4493=CARTESIAN_POINT ( 'NONE',  ( 3.661933894777875675, -41.09997021044436138, -22.87845304325095697 ) ) ;
#4500=CARTESIAN_POINT ( 'NONE',  ( 0.7056313189692713372, -46.73287197163856632, 3.973326218673276511 ) ) ;
#4504=CARTESIAN_POINT ( 'NONE',  ( 4.962356264823608143, 23.01169039590672938, -35.23773124060741679 ) ) ;
#4505=DIRECTION ( 'NONE',  ( -1.000000000000000000, -0.000000000000000000, -0.000000000000000000 ) ) ;
#4508=ADVANCED_FACE ( 'NONE', ( #14279 ), #52865, .F. ) ;
#4509=CARTESIAN_POINT ( 'NONE',  ( 5.901463166500145796, -4.676581321914135003, 19.56137667650619960 ) ) ;
#4514=ORIENTED_EDGE ( 'NONE', *, *, #12981, .T. ) ;
#4520=CARTESIAN_POINT ( 'NONE',  ( 0.5830081025819944252, -45.90105815717110715, 9.608584413650092415 ) ) ;
#4524=VECTOR ( 'NONE', #80, 1000.000000000000000 ) ;
#4527=CIRCLE ( 'NONE', #34570, 47.09074272231896430 ) ;
#4530=CARTESIAN_POINT ( 'NONE',  ( 0.8560838555295223751, -41.44626783305086093, 21.96769712083507287 ) ) ;
#4539=ORIENTED_EDGE ( 'NONE', *, *, #20231, .F. ) ;
#4545=VERTEX_POINT ( 'NONE', #11114 ) ;
#4548=CARTESIAN_POINT ( 'NONE',  ( 4.956445790444027999, 19.33052208089617352, -42.94029536716791995 ) ) ;
#4558=DIRECTION ( 'NONE',  ( -1.000000000000000000, -0.000000000000000000, -0.000000000000000000 ) ) ;
#4559=EDGE_LOOP ( 'NONE', ( #44351, #11142, #17776, #29089, #19454, #53381, #6531, #16915, #53615, #20973, #20892, #60016, #50175, #35917, #51876, #8872, #49689, #37409, #53604, #11031, #21911, #14495, #33238, #45642, #43438, #49008, #10934, #32120, #46419, #33954, #61890, #47392, #31652, #55862, #27283, #19608, #18843, #55225, #20094, #16822, #26224, #18869, #21248, #59101, #39721, #53608, #34108, #41338, #38975, #21458, #11306, #16421, #48951, #49240, #20935, #30908, #28844, #4806, #43842, #22367, #32853, #19656, #32226, #51152, #8412, #22351, #8867, #24268, #30430, #14931, #45658, #28278, #56728, #32554, #31721, #45985, #45791, #59759, #6911, #30551, #46476, #20138, #56255, #21763, #52499, #25826, #2576, #25813, #48668, #1796, #45739, #8441, #16824, #15983, #60428, #55472, #11104, #6582, #50235, #58855, #13070, #29326, #15937, #46897, #13612, #41421, #53946, #6871, #46794, #8647, #61251, #19790, #2065, #1000, #55502, #123, #43400, #46573, #41332, #40104, #30671, #55262, #52006, #10450, #51658, #16627, #54691, #13938, #1870, #12790, #11163, #48695, #54140, #24458, #40030, #6609, #39447, #49996, #10914, #51947, #27983, #7070, #52997, #47604 ) ) ;
#4568=EDGE_CURVE ( 'NONE', #23055, #59500, #30926, .T. ) ;
#4571=CARTESIAN_POINT ( 'NONE',  ( 0.5848930533535030563, 36.69111421824766239, -29.20676667847815722 ) ) ;
#4575=CARTESIAN_POINT ( 'NONE',  ( 0.5797568665920713737, 16.26612276559258063, -43.98452635616917661 ) ) ;
#4577=CARTESIAN_POINT ( 'NONE',  ( 3.376099380956842921, 12.15487954915009716, -5.653962042472503668 ) ) ;
#4579=CARTESIAN_POINT ( 'NONE',  ( 0.9762797500689124330, -6.471194619075845367, 41.40589843715202534 ) ) ;
#4583=LINE ( 'NONE', #57831, #36410 ) ;
#4589=CARTESIAN_POINT ( 'NONE',  ( 1.231276596079881935, -41.24008908601427237, 7.518764738683684001 ) ) ;
#4591=ORIENTED_EDGE ( 'NONE', *, *, #29836, .F. ) ;
#4596=CARTESIAN_POINT ( 'NONE',  ( 0.9762797500689124330, -41.16654106227468901, -7.851158013551661874 ) ) ;
#4598=FACE_OUTER_BOUND ( 'NONE', #7332, .T. ) ;
#4606=VECTOR ( 'NONE', #56488, 1000.000000000000114 ) ;
#4609=CARTESIAN_POINT ( 'NONE',  ( 0.8560838555295158248, -46.85553835019179303, 2.220666565569249684 ) ) ;
#4619=CARTESIAN_POINT ( 'NONE',  ( -69.95594261585601714, 9.797174393178825657E-16, -8.000000000000000000 ) ) ;
#4624=ORIENTED_EDGE ( 'NONE', *, *, #39334, .T. ) ;
#4627=VERTEX_POINT ( 'NONE', #8864 ) ;
#4638=EDGE_CURVE ( 'NONE', #43273, #9908, #27664, .T. ) ;
#4640=EDGE_CURVE ( 'NONE', #47523, #47700, #46798, .T. ) ;
#4652=CARTESIAN_POINT ( 'NONE',  ( 0.8554163680231708922, -46.74230100997657900, -4.045092014350431420 ) ) ;
#4655=LINE ( 'NONE', #42931, #1183 ) ;
#4658=CARTESIAN_POINT ( 'NONE',  ( 0.5837800005270546988, 22.53733638163336650, -41.12546324921934371 ) ) ;
#4666=VERTEX_POINT ( 'NONE', #18578 ) ;
#4671=B_SPLINE_CURVE_WITH_KNOTS ( 'NONE', 3,
 ( #48222, #57579, #14714, #14106 ),
 .UNSPECIFIED., .F., .F.,
 ( 4, 4 ),
 ( 2.168404344971008868E-19, 0.004041751736740997747 ),
 .UNSPECIFIED. ) ;
#4680=VERTEX_POINT ( 'NONE', #37389 ) ;
#4683=CARTESIAN_POINT ( 'NONE',  ( 0.9762797500689124330, -6.471194619075235188, -41.40589843715211771 ) ) ;
#4685=EDGE_CURVE ( 'NONE', #28949, #9908, #9014, .T. ) ;
#4687=CARTESIAN_POINT ( 'NONE',  ( 5.895596859100789899, 5.955534046174526530, -19.21092911436986128 ) ) ;
#4688=ORIENTED_EDGE ( 'NONE', *, *, #19755, .F. ) ;
#4690=CARTESIAN_POINT ( 'NONE',  ( 0.5837800304671211249, 40.32620748771655883, 23.93813530409446599 ) ) ;
#4707=CARTESIAN_POINT ( 'NONE',  ( 0.5824936645240097466, 4.331538183493719885, 46.69556677036101888 ) ) ;
#4709=CARTESIAN_POINT ( 'NONE',  ( 4.956445790444026223, 13.43466403631445338, -45.13366650706537797 ) ) ;
#4710=CARTESIAN_POINT ( 'NONE',  ( 0.9790320750461890542, -22.47781024749384926, -35.37068247885321171 ) ) ;
#4717=CIRCLE ( 'NONE', #54725, 42.08604991992415023 ) ;
#4723=B_SPLINE_CURVE_WITH_KNOTS ( 'NONE', 3,
 ( #15611, #10912, #3940, #32171, #45984, #3025 ),
 .UNSPECIFIED., .F., .F.,
 ( 4, 2, 4 ),
 ( 6.523258043322125742E-18, 0.0002291472222819933150, 0.0004582944445639800706 ),
 .UNSPECIFIED. ) ;
#4724=CARTESIAN_POINT ( 'NONE',  ( 0.8560838555295223751, -34.16988317699956923, 32.13708010619405542 ) ) ;
#4733=CARTESIAN_POINT ( 'NONE',  ( 3.661921753702001237, -5.960919088269102772, 46.65938884573115786 ) ) ;
#4741=ORIENTED_EDGE ( 'NONE', *, *, #39916, .T. ) ;
#4746=ORIENTED_EDGE ( 'NONE', *, *, #5983, .T. ) ;
#4749=VERTEX_POINT ( 'NONE', #52374 ) ;
#4752=AXIS2_PLACEMENT_3D ( 'NONE', #12793, #7745, #61590 ) ;
#4763=ORIENTED_EDGE ( 'NONE', *, *, #47753, .F. ) ;
#4774=CARTESIAN_POINT ( 'NONE',  ( 3.376099380956838925, 1.798919266859539512, -13.28428669908131354 ) ) ;
#4778=ORIENTED_EDGE ( 'NONE', *, *, #28555, .T. ) ;
#4780=CARTESIAN_POINT ( 'NONE',  ( 1.157644175074336923, 41.42449707941300829, 6.404164051371970423 ) ) ;
#4781=CARTESIAN_POINT ( 'NONE',  ( 0.5806925824938502512, -30.69245420804159252, -35.45695442407362208 ) ) ;
#4789=ORIENTED_EDGE ( 'NONE', *, *, #13660, .F. ) ;
#4795=CARTESIAN_POINT ( 'NONE',  ( 0.6845945791218023269, 27.12315006394096883, -38.27193817045177582 ) ) ;
#4803=CARTESIAN_POINT ( 'NONE',  ( 0.5848930533535030563, -30.41648929863175255, -35.69468113226083972 ) ) ;
#4804=CARTESIAN_POINT ( 'NONE',  ( 0.9789233960466692253, 41.90846494442085657, 0.1315022227620240847 ) ) ;
#4805=DIRECTION ( 'NONE',  ( 0.000000000000000000, 0.000000000000000000, 1.000000000000000000 ) ) ;
#4806=ORIENTED_EDGE ( 'NONE', *, *, #40163, .T. ) ;
#4812=ADVANCED_FACE ( 'NONE', ( #43638 ), #61269, .F. ) ;
#4836=VECTOR ( 'NONE', #16035, 1000.000000000000114 ) ;
#4840=CARTESIAN_POINT ( 'NONE',  ( 0.5834584762367737154, 17.02460257627602402, -43.69666916520123578 ) ) ;
#4843=EDGE_CURVE ( 'NONE', #25596, #57756, #21350, .T. ) ;
#4846=ORIENTED_EDGE ( 'NONE', *, *, #1472, .T. ) ;
#4858=VERTEX_POINT ( 'NONE', #10722 ) ;
#4859=ORIENTED_EDGE ( 'NONE', *, *, #3030, .F. ) ;
#4861=CARTESIAN_POINT ( 'NONE',  ( 4.958415959904821868, 18.66009313388002155, -41.41261737752838457 ) ) ;
#4864=EDGE_CURVE ( 'NONE', #38640, #44157, #16337, .T. ) ;
#4869=FACE_OUTER_BOUND ( 'NONE', #49548, .T. ) ;
#4870=CARTESIAN_POINT ( 'NONE',  ( 0.5837800005270549208, 27.81778570091245584, 37.75455015411910153 ) ) ;
#4872=ORIENTED_EDGE ( 'NONE', *, *, #23185, .F. ) ;
#4878=CARTESIAN_POINT ( 'NONE',  ( 4.962356264823608143, 0.000000000000000000, 0.000000000000000000 ) ) ;
#4884=CARTESIAN_POINT ( 'NONE',  ( 0.7764139734771230428, -42.25777068362622657, 20.35488363407972656 ) ) ;
#4889=CARTESIAN_POINT ( 'NONE',  ( 1.092182651088185796, 32.40425343836902528, -26.58431010096432345 ) ) ;
#4892=B_SPLINE_CURVE_WITH_KNOTS ( 'NONE', 3,
 ( #45453, #13167, #31959, #31330, #36365, #41077 ),
 .UNSPECIFIED., .F., .F.,
 ( 4, 2, 4 ),
 ( 7.152448122690996019E-18, 0.0002291472222819938029, 0.0004582944445639804501 ),
 .UNSPECIFIED. ) ;
#4894=CARTESIAN_POINT ( 'NONE',  ( 4.956445790443988031, 47.01859095792194410, 2.605792484304518375 ) ) ;
#4907=CARTESIAN_POINT ( 'NONE',  ( 1.157644175074337145, -2.225587469958278941, 41.85748482521073299 ) ) ;
#4920=CARTESIAN_POINT ( 'NONE',  ( 5.838029081930955932, 7.836690858011332139, 46.57951625499005388 ) ) ;
#4921=CARTESIAN_POINT ( 'NONE',  ( 0.5837157313716021534, -25.15714033038016950, -39.57720750608339699 ) ) ;
#4922=ORIENTED_EDGE ( 'NONE', *, *, #10884, .T. ) ;
#4924=B_SPLINE_CURVE_WITH_KNOTS ( 'NONE', 3,
 ( #453, #24905, #33389, #1074, #18987, #29280 ),
 .UNSPECIFIED., .F., .F.,
 ( 4, 2, 4 ),
 ( 5.421010862427522170E-18, 0.0002291472222819961068, 0.0004582944445639867926 ),
 .UNSPECIFIED. ) ;
#4933=ORIENTED_EDGE ( 'NONE', *, *, #9400, .F. ) ;
#4935=CARTESIAN_POINT ( 'NONE',  ( 5.917102823773431552, -20.11192790512648543, 0.008601786823265991991 ) ) ;
#4940=CARTESIAN_POINT ( 'NONE',  ( 0.9780106845699476636, -6.661169069550109789, -41.37583924323842410 ) ) ;
#4941=ORIENTED_EDGE ( 'NONE', *, *, #32751, .T. ) ;
#4944=ORIENTED_EDGE ( 'NONE', *, *, #27298, .F. ) ;
#4950=ORIENTED_EDGE ( 'NONE', *, *, #14403, .F. ) ;
#4951=CARTESIAN_POINT ( 'NONE',  ( 5.896782393890504181, -4.656380635072583374, -19.56640504178867346 ) ) ;
#4952=CARTESIAN_POINT ( 'NONE',  ( 5.901463166500146684, 12.97422524546425926, -15.36838799681328105 ) ) ;
#4958=CARTESIAN_POINT ( 'NONE',  ( 4.962356264823608143, 30.91935898304044272, 28.55221248765537467 ) ) ;
#4962=VERTEX_POINT ( 'NONE', #27282 ) ;
#4965=FACE_OUTER_BOUND ( 'NONE', #39554, .T. ) ;
#4967=CARTESIAN_POINT ( 'NONE',  ( 0.5806925824938499181, 5.237374507879953178, -46.60249210726582447 ) ) ;
#4969=EDGE_CURVE ( 'NONE', #16055, #20290, #28420, .T. ) ;
#4970=VERTEX_POINT ( 'NONE', #32607 ) ;
#4971=CARTESIAN_POINT ( 'NONE',  ( 1.231276596079881047, -39.86997064245551314, 12.94844438485960580 ) ) ;
#4972=CARTESIAN_POINT ( 'NONE',  ( 1.231276596079881935, 10.53918392497884149, -40.57341954055061706 ) ) ;
#4983=CARTESIAN_POINT ( 'NONE',  ( 0.5804410086790514622, 40.07081992599749043, -24.36902218624454619 ) ) ;
#4995=ADVANCED_FACE ( 'NONE', ( #9091 ), #55778, .F. ) ;
#4999=EDGE_CURVE ( 'NONE', #28755, #18623, #30638, .T. ) ;
#5005=ORIENTED_EDGE ( 'NONE', *, *, #38708, .F. ) ;
#5006=CARTESIAN_POINT ( 'NONE',  ( 0.8560838555295223751, 11.76118766017263972, 45.40977096290989579 ) ) ;
#5007=( BOUNDED_SURFACE ( )  B_SPLINE_SURFACE ( 3, 1, ( 
 ( #12817, #12502 ),
 ( #12200, #21267 ),
 ( #60090, #17194 ),
 ( #7448, #11895 ) ),
 .UNSPECIFIED., .F., .F., .F. ) 
 B_SPLINE_SURFACE_WITH_KNOTS ( ( 4, 4 ),
 ( 2, 2 ),
 ( 0.000000000000000000, 1.000000000000000000 ),
 ( 0.000000000000000000, 1.000000000000000000 ),
 .UNSPECIFIED. ) 
 GEOMETRIC_REPRESENTATION_ITEM ( )  RATIONAL_B_SPLINE_SURFACE ( (
 ( 1.000000000000000000, 1.000000000000000000),
 ( 0.9952954269826590483, 0.8620686068821307169),
 ( 0.9952954269826590483, 0.8620686068821307169),
 ( 1.000000000000000000, 1.000000000000000000) ) ) 
 REPRESENTATION_ITEM ( '' )  SURFACE ( )  );
#5011=CARTESIAN_POINT ( 'NONE',  ( 4.962356264823601926, 34.44911810793277596, -24.17630781256817940 ) ) ;
#5012=ADVANCED_FACE ( 'NONE', ( #28817 ), #25788, .F. ) ;
#5015=CARTESIAN_POINT ( 'NONE',  ( 0.5837157313716019313, 16.76980906724618947, 43.79509752735039996 ) ) ;
#5017=FACE_OUTER_BOUND ( 'NONE', #18234, .T. ) ;
#5018=EDGE_CURVE ( 'NONE', #44940, #13226, #18822, .T. ) ;
#5021=CARTESIAN_POINT ( 'NONE',  ( 0.5817216825391120505, 42.99501409996830148, -18.72601705518253823 ) ) ;
#5025=CARTESIAN_POINT ( 'NONE',  ( 5.838029081930955932, -28.03445132514733729, 38.01492597718512911 ) ) ;
#5028=CARTESIAN_POINT ( 'NONE',  ( 0.9787464366903567692, -34.45072202728288602, -23.86381664129499924 ) ) ;
#5036=CARTESIAN_POINT ( 'NONE',  ( 5.895596859100789899, 10.81936814621394127, -16.95492424427719413 ) ) ;
#5038=CARTESIAN_POINT ( 'NONE',  ( 3.238018933889920792, 9.111992562714181787, -9.817284955867094709 ) ) ;
#5049=CARTESIAN_POINT ( 'NONE',  ( 0.9780106845699487739, 9.409895146977072855, 40.83852494616247242 ) ) ;
#5051=CARTESIAN_POINT ( 'NONE',  ( 0.5806925824938499181, -13.37132486740634540, -44.94919391528445374 ) ) ;
#5055=CARTESIAN_POINT ( 'NONE',  ( 0.9780303403264759554, -1.076676298148392830, 41.89487297443557878 ) ) ;
#5063=ORIENTED_EDGE ( 'NONE', *, *, #48003, .F. ) ;
#5070=VERTEX_POINT ( 'NONE', #38551 ) ;
#5083=ORIENTED_EDGE ( 'NONE', *, *, #52548, .T. ) ;
#5088=ADVANCED_FACE ( 'NONE', ( #42945 ), #17383, .F. ) ;
#5093=CARTESIAN_POINT ( 'NONE',  ( 0.5832655196449136881, 36.94460163995477586, -28.88479864285675447 ) ) ;
#5095=ORIENTED_EDGE ( 'NONE', *, *, #4023, .T. ) ;
#5098=CARTESIAN_POINT ( 'NONE',  ( 4.956445790443988031, 5.766952734435944596E-15, 47.09074272231896430 ) ) ;
#5102=CARTESIAN_POINT ( 'NONE',  ( 3.238018933889920792, 12.98832471626936247, -3.272753188433144445 ) ) ;
#5135=B_SPLINE_CURVE_WITH_KNOTS ( 'NONE', 3,
 ( #16235, #35358, #30621, #49739, #7420, #40373, #6795, #26234, #12468, #2729, #22168, #26550, #16540, #45677, #59749, #59433, #31254, #7738, #46000 ),
 .UNSPECIFIED., .F., .F.,
 ( 4, 3, 3, 3, 3, 3, 4 ),
 ( 1.551621725782133898E-17, 0.0002732106629380501805, 0.0004098138914053729926, 0.0005464171197651409434, 0.0006830203481512506702, 0.0008196235766963562604, 0.001011968216111135740 ),
 .UNSPECIFIED. ) ;
#5148=CARTESIAN_POINT ( 'NONE',  ( 0.5830081025819923157, 16.59954784437812947, -43.85985688239814095 ) ) ;
#5163=CARTESIAN_POINT ( 'NONE',  ( 0.7056759521544990754, 5.532722967652889068, -46.57400353931571857 ) ) ;
#5169=CARTESIAN_POINT ( 'NONE',  ( 0.5830082357119570347, 46.51316245118321291, -5.979778735720702620 ) ) ;
#5170=CARTESIAN_POINT ( 'NONE',  ( 0.5782707292762442330, -2.290569157858767912, 46.84538020595716290 ) ) ;
#5175=ORIENTED_EDGE ( 'NONE', *, *, #43157, .F. ) ;
#5176=CARTESIAN_POINT ( 'NONE',  ( 3.782542959838394836, 39.34345065763542237, -14.80981916657911235 ) ) ;
#5178=ORIENTED_EDGE ( 'NONE', *, *, #4363, .F. ) ;
#5179=CARTESIAN_POINT ( 'NONE',  ( 5.895881250540457863, -17.30282815192082779, 10.25377099185450902 ) ) ;
#5181=CARTESIAN_POINT ( 'NONE',  ( 0.5804410086790514622, -35.14691939471148885, -31.05179397260405949 ) ) ;
#5192=CARTESIAN_POINT ( 'NONE',  ( 0.9754292589017210524, 14.51724368765255768, -39.31382838911252975 ) ) ;
#5193=CARTESIAN_POINT ( 'NONE',  ( 0.5804410086790514622, 36.46521478791949988, -29.49250688439850876 ) ) ;
#5196=CARTESIAN_POINT ( 'NONE',  ( 0.5326698147273805084, 0.000000000000000000, 0.000000000000000000 ) ) ;
#5198=CARTESIAN_POINT ( 'NONE',  ( 4.958415959904820092, -45.41969080731320219, -0.5056093261671902317 ) ) ;
#5201=CARTESIAN_POINT ( 'NONE',  ( 0.8554163680231708922, 33.26717477998096228, -33.08323677136227303 ) ) ;
#5204=EDGE_CURVE ( 'NONE', #7531, #40743, #36623, .T. ) ;
#5208=AXIS2_PLACEMENT_3D ( 'NONE', #22202, #55079, #41330 ) ;
#5211=CARTESIAN_POINT ( 'NONE',  ( 1.157644175074336923, -11.62785181577198657, -40.27152018026674796 ) ) ;
#5218=CARTESIAN_POINT ( 'NONE',  ( 0.6064515330803637028, 23.15851657376443740, 40.78011091377467778 ) ) ;
#5220=CARTESIAN_POINT ( 'NONE',  ( 5.895596859100789899, -11.93344155749905866, 16.19015613903219730 ) ) ;
#5224=EDGE_CURVE ( 'NONE', #54810, #48392, #41035, .T. ) ;
#5232=VERTEX_POINT ( 'NONE', #3378 ) ;
#5238=CARTESIAN_POINT ( 'NONE',  ( 2.282803330402962683, -46.93788402311890451, 1.825363221177198403 ) ) ;
#5240=CARTESIAN_POINT ( 'NONE',  ( 0.9784957157296367836, 40.48045361714974177, 10.84739286382488999 ) ) ;
#5246=CARTESIAN_POINT ( 'NONE',  ( 0.9754292580325136797, 40.56950064046846904, -10.50919048676124667 ) ) ;
#5250=ORIENTED_EDGE ( 'NONE', *, *, #1934, .T. ) ;
#5251=CARTESIAN_POINT ( 'NONE',  ( 5.917102823773431552, 0.6806365918034013029, -20.10040924662083128 ) ) ;
#5262=CARTESIAN_POINT ( 'NONE',  ( 4.960386119450153508, 32.13287905145099899, 29.69704612477748640 ) ) ;
#5268=ADVANCED_FACE ( 'NONE', ( #55084 ), #57778, .F. ) ;
#5270=CARTESIAN_POINT ( 'NONE',  ( 5.895596859100789899, 0.6756533542673609505, 20.10153416427101192 ) ) ;
#5279=EDGE_CURVE ( 'NONE', #23457, #7531, #13463, .T. ) ;
#5285=CARTESIAN_POINT ( 'NONE',  ( 0.9788927965476029724, -34.47085361914916035, 23.83478263796355634 ) ) ;
#5288=ORIENTED_EDGE ( 'NONE', *, *, #44717, .F. ) ;
#5290=( BOUNDED_SURFACE ( )  B_SPLINE_SURFACE ( 3, 1, ( 
 ( #39768, #58823 ),
 ( #30957, #2430 ),
 ( #3349, #17788 ),
 ( #40693, #7430 ) ),
 .UNSPECIFIED., .F., .F., .F. ) 
 B_SPLINE_SURFACE_WITH_KNOTS ( ( 4, 4 ),
 ( 2, 2 ),
 ( 0.000000000000000000, 1.000000000000000000 ),
 ( 0.000000000000000000, 1.000000000000000000 ),
 .UNSPECIFIED. ) 
 GEOMETRIC_REPRESENTATION_ITEM ( )  RATIONAL_B_SPLINE_SURFACE ( (
 ( 1.000000000000000000, 1.000000000000000000),
 ( 0.9952954269826590483, 0.8620686068821339365),
 ( 0.9952954269826590483, 0.8620686068821339365),
 ( 1.000000000000000000, 1.000000000000000000) ) ) 
 REPRESENTATION_ITEM ( '' )  SURFACE ( )  );
#5323=CARTESIAN_POINT ( 'NONE',  ( 5.894904586330512508, 17.95060305802262590, -9.072224750024185269 ) ) ;
#5325=ORIENTED_EDGE ( 'NONE', *, *, #9816, .F. ) ;
#5328=VERTEX_POINT ( 'NONE', #56625 ) ;
#5339=CARTESIAN_POINT ( 'NONE',  ( 4.291220156522059348, 0.5803847665936985312, -47.10681639453468250 ) ) ;
#5350=DIRECTION ( 'NONE',  ( -1.000000000000000000, -0.000000000000000000, -0.000000000000000000 ) ) ;
#5355=CARTESIAN_POINT ( 'NONE',  ( 5.910764540655177868, -4.647344284406774939, -19.56791837603976703 ) ) ;
#5363=B_SPLINE_CURVE_WITH_KNOTS ( 'NONE', 3,
 ( #20532, #30523, #55881, #36494, #61490, #32406 ),
 .UNSPECIFIED., .F., .F.,
 ( 4, 2, 4 ),
 ( 3.471140604459641645E-18, 0.0002291459268755693403, 0.0004582918537511352112 ),
 .UNSPECIFIED. ) ;
#5364=CARTESIAN_POINT ( 'NONE',  ( 0.9787284016396597952, -1.213227321156433725, 41.89109784185695418 ) ) ;
#5366=ORIENTED_EDGE ( 'NONE', *, *, #6044, .F. ) ;
#5378=VERTEX_POINT ( 'NONE', #44958 ) ;
#5382=CARTESIAN_POINT ( 'NONE',  ( 4.962356264823608143, 0.000000000000000000, 0.000000000000000000 ) ) ;
#5383=CARTESIAN_POINT ( 'NONE',  ( 3.376099380956842921, 7.576724406378523291, -11.05900677736726223 ) ) ;
#5385=B_SPLINE_CURVE_WITH_KNOTS ( 'NONE', 3,
 ( #25630, #35365, #52972, #35984 ),
 .UNSPECIFIED., .F., .F.,
 ( 4, 4 ),
 ( 0.000000000000000000, 0.004447772540403805916 ),
 .UNSPECIFIED. ) ;
#5387=VERTEX_POINT ( 'NONE', #60239 ) ;
#5398=CARTESIAN_POINT ( 'NONE',  ( 2.528100132419516921, 28.30161947981979864, -31.00438861599369034 ) ) ;
#5400=VERTEX_POINT ( 'NONE', #11421 ) ;
#5403=CARTESIAN_POINT ( 'NONE',  ( 0.5837799406558226156, 36.74750401072321893, -29.13527927717670707 ) ) ;
#5410=ORIENTED_EDGE ( 'NONE', *, *, #3299, .F. ) ;
#5417=CARTESIAN_POINT ( 'NONE',  ( 4.962356264823608143, -9.332162870646227404, -41.03835198954849517 ) ) ;
#5421=EDGE_CURVE ( 'NONE', #24638, #4666, #15038, .T. ) ;
#5423=CARTESIAN_POINT ( 'NONE',  ( 0.9754292589017218296, 3.614901353133219253, -41.75236466479944397 ) ) ;
#5433=CARTESIAN_POINT ( 'NONE',  ( 4.962356264823608143, 12.05238263218917716, 40.32338863178108568 ) ) ;
#5438=CARTESIAN_POINT ( 'NONE',  ( 1.000433927950261870, -37.10347441663083856, 19.48719743491265888 ) ) ;
#5440=ORIENTED_EDGE ( 'NONE', *, *, #42526, .F. ) ;
#5441=ORIENTED_EDGE ( 'NONE', *, *, #40913, .T. ) ;
#5444=LINE ( 'NONE', #1666, #44521 ) ;
#5446=EDGE_CURVE ( 'NONE', #60852, #6434, #56173, .T. ) ;
#5453=FACE_OUTER_BOUND ( 'NONE', #50463, .T. ) ;
#5455=DIRECTION ( 'NONE',  ( -1.000000000000000000, -0.000000000000000000, -0.000000000000000000 ) ) ;
#5458=B_SPLINE_CURVE_WITH_KNOTS ( 'NONE', 3,
 ( #49038, #24621, #15536, #39353 ),
 .UNSPECIFIED., .F., .F.,
 ( 4, 4 ),
 ( 0.000000000000000000, 0.004447772540403795508 ),
 .UNSPECIFIED. ) ;
#5461=ADVANCED_FACE ( 'NONE', ( #31134 ), #2164, .F. ) ;
#5470=CARTESIAN_POINT ( 'NONE',  ( 0.9787284016396613495, -37.48834466450204417, -18.73392679723960086 ) ) ;
#5471=CARTESIAN_POINT ( 'NONE',  ( 0.5806925824938499181, 5.237374507879953178, -46.60249210726582447 ) ) ;
#5475=VERTEX_POINT ( 'NONE', #23584 ) ;
#5476=CARTESIAN_POINT ( 'NONE',  ( 0.5830082357119559244, -14.15480402886485400, 44.70876377001235369 ) ) ;
#5478=CARTESIAN_POINT ( 'NONE',  ( 4.962356264823609031, 37.75702904547822669, -18.59145920903629090 ) ) ;
#5500=VERTEX_POINT ( 'NONE', #8870 ) ;
#5509=FACE_OUTER_BOUND ( 'NONE', #6763, .T. ) ;
#5510=CARTESIAN_POINT ( 'NONE',  ( 0.9788927965476035276, -6.830870151262773859, 41.34822639011696310 ) ) ;
#5515=ORIENTED_EDGE ( 'NONE', *, *, #54374, .T. ) ;
#5518=VECTOR ( 'NONE', #57222, 1000.000000000000114 ) ;
#5540=CARTESIAN_POINT ( 'NONE',  ( -4.467300000000000715, 0.000000000000000000, 0.000000000000000000 ) ) ;
#5542=DIRECTION ( 'NONE',  ( -1.000000000000000000, -0.000000000000000000, -0.000000000000000000 ) ) ;
#5546=CARTESIAN_POINT ( 'NONE',  ( 4.291220156522060236, -36.34793638197106702, -29.97026056072721545 ) ) ;
#5549=ORIENTED_EDGE ( 'NONE', *, *, #43175, .T. ) ;
#5550=CARTESIAN_POINT ( 'NONE',  ( 4.962356264823608143, 0.000000000000000000, 0.000000000000000000 ) ) ;
#5553=EDGE_CURVE ( 'NONE', #2462, #53003, #51616, .T. ) ;
#5557=CARTESIAN_POINT ( 'NONE',  ( 3.238018933889920792, 9.507325605900359022, -9.434948446655354815 ) ) ;
#5572=AXIS2_PLACEMENT_3D ( 'NONE', #57813, #53719, #58124 ) ;
#5580=EDGE_CURVE ( 'NONE', #7415, #12199, #21799, .T. ) ;
#5582=CARTESIAN_POINT ( 'NONE',  ( 3.376099380956838925, -13.33697911751163012, -1.354020550481378704 ) ) ;
#5584=CARTESIAN_POINT ( 'NONE',  ( 1.231276596079887931, 5.037240371905710390, 41.61613846158375196 ) ) ;
#5588=CARTESIAN_POINT ( 'NONE',  ( 5.895596859100789899, 16.57987064389777743, -11.38578379577375088 ) ) ;
#5595=CARTESIAN_POINT ( 'NONE',  ( 5.917102823773431552, -15.78915961314057270, -12.45761440896741767 ) ) ;
#5597=VERTEX_POINT ( 'NONE', #57683 ) ;
#5615=CARTESIAN_POINT ( 'NONE',  ( 0.5806925824938511393, 40.62497527030930655, 23.42720099863236882 ) ) ;
#5616=EDGE_CURVE ( 'NONE', #60728, #13851, #13594, .T. ) ;
#5618=CARTESIAN_POINT ( 'NONE',  ( 0.5804410086790514622, -7.261380058784011382, -46.33348909263462190 ) ) ;
#5628=CARTESIAN_POINT ( 'NONE',  ( 0.5834584762367741595, 43.24557549772239895, -18.13990597781544878 ) ) ;
#5635=CARTESIAN_POINT ( 'NONE',  ( 0.5806925824938494740, -38.35106547415225009, 26.98922265165951018 ) ) ;
#5636=CARTESIAN_POINT ( 'NONE',  ( 0.5806925824938506953, -46.06186276235258958, -8.804950948515241294 ) ) ;
#5643=CARTESIAN_POINT ( 'NONE',  ( 0.9787284016396619046, 41.50936080613161039, -5.771391894094023201 ) ) ;
#5644=B_SPLINE_CURVE_WITH_KNOTS ( 'NONE', 3,
 ( #35319, #45343, #59400, #50020 ),
 .UNSPECIFIED., .F., .F.,
 ( 4, 4 ),
 ( 0.000000000000000000, 0.004447772540403806783 ),
 .UNSPECIFIED. ) ;
#5651=( BOUNDED_SURFACE ( )  B_SPLINE_SURFACE ( 3, 1, ( 
 ( #57482, #4253 ),
 ( #5179, #18081 ),
 ( #9913, #24308 ),
 ( #19314, #38133 ) ),
 .UNSPECIFIED., .F., .F., .F. ) 
 B_SPLINE_SURFACE_WITH_KNOTS ( ( 4, 4 ),
 ( 2, 2 ),
 ( 0.000000000000000000, 1.000000000000000000 ),
 ( 0.000000000000000000, 1.000000000000000000 ),
 .UNSPECIFIED. ) 
 GEOMETRIC_REPRESENTATION_ITEM ( )  RATIONAL_B_SPLINE_SURFACE ( (
 ( 1.000000000000000000, 1.000000000000000000),
 ( 0.9952954269826590483, 0.8620686068821339365),
 ( 0.9952954269826590483, 0.8620686068821339365),
 ( 1.000000000000000000, 1.000000000000000000) ) ) 
 REPRESENTATION_ITEM ( '' )  SURFACE ( )  );
#5652=CARTESIAN_POINT ( 'NONE',  ( 4.291220156522060236, 13.00516750528111132, 45.27973736082483924 ) ) ;
#5658=CARTESIAN_POINT ( 'NONE',  ( 0.5832655196449137991, -1.794523853054427409, 46.86165668341387658 ) ) ;
#5659=EDGE_CURVE ( 'NONE', #44157, #7098, #55389, .T. ) ;
#5661=CARTESIAN_POINT ( 'NONE',  ( 0.8560838555295214869, 21.73747136795201129, -41.56747734237908531 ) ) ;
#5662=EDGE_LOOP ( 'NONE', ( #16859, #52144, #6355, #16895 ) ) ;
#5664=CARTESIAN_POINT ( 'NONE',  ( 0.9783242366443547500, -1.668301681818695759, 41.87542548685285482 ) ) ;
#5668=CARTESIAN_POINT ( 'NONE',  ( 5.896278296736517710, -15.78795198421076940, -12.46064010228362484 ) ) ;
#5672=CIRCLE ( 'NONE', #40766, 47.09074272231896430 ) ;
#5674=CARTESIAN_POINT ( 'NONE',  ( 1.157644175074337367, -41.87004051356380785, 1.975343735077094376 ) ) ;
#5677=ORIENTED_EDGE ( 'NONE', *, *, #1042, .T. ) ;
#5679=VERTEX_POINT ( 'NONE', #999 ) ;
#5691=EDGE_CURVE ( 'NONE', #45083, #19517, #49236, .T. ) ;
#5692=CARTESIAN_POINT ( 'NONE',  ( 5.895596859100789899, -9.662743138698242973, -17.63971593444825103 ) ) ;
#5694=CARTESIAN_POINT ( 'NONE',  ( 0.8560838555295158248, -14.76796170096741534, 44.52280473286123907 ) ) ;
#5705=CARTESIAN_POINT ( 'NONE',  ( 1.231276596079881047, 32.36747132271556637, 26.63876069172986405 ) ) ;
#5709=ORIENTED_EDGE ( 'NONE', *, *, #8833, .T. ) ;
#5712=CARTESIAN_POINT ( 'NONE',  ( 0.9790724872846757743, 15.10001979691015528, -39.09379250104007042 ) ) ;
#5722=ORIENTED_EDGE ( 'NONE', *, *, #43935, .F. ) ;
#5723=AXIS2_PLACEMENT_3D ( 'NONE', #18932, #33950, #38055 ) ;
#5730=CARTESIAN_POINT ( 'NONE',  ( 0.5817217712918332229, -13.45862205245476773, -44.92327288229956395 ) ) ;
#5747=CARTESIAN_POINT ( 'NONE',  ( 4.962356264823608143, 0.000000000000000000, 0.000000000000000000 ) ) ;
#5749=CARTESIAN_POINT ( 'NONE',  ( 0.6845945791218034371, 45.46290160446757511, -11.55556569002327194 ) ) ;
#5752=VERTEX_POINT ( 'NONE', #16985 ) ;
#5758=CARTESIAN_POINT ( 'NONE',  ( 1.231276596079881935, 3.353048872156085825, 41.78556968953515849 ) ) ;
#5767=CARTESIAN_POINT ( 'NONE',  ( 1.157643937452369931, -30.52765900992394776, 28.72393270373265750 ) ) ;
#5770=VERTEX_POINT ( 'NONE', #1923 ) ;
#5772=CARTESIAN_POINT ( 'NONE',  ( 0.8560838555295158248, 5.603718208094640829, -46.57221463840858888 ) ) ;
#5777=CARTESIAN_POINT ( 'NONE',  ( 0.5834584762367771571, 46.50150427475632853, -6.070097956211762735 ) ) ;
#5791=B_SPLINE_CURVE_WITH_KNOTS ( 'NONE', 3,
 ( #24381, #556, #29385, #58184, #48489, #39744, #15311, #34413, #15920, #38819, #35037, #54095, #11217, #53484, #30306, #49415, #6469, #57873, #10598 ),
 .UNSPECIFIED., .F., .F.,
 ( 4, 3, 3, 3, 3, 3, 4 ),
 ( 1.250973872328959318E-17, 0.0002732106629380645461, 0.0004098138914053644816, 0.0005464171197651422444, 0.0006830203481512590186, 0.0008196235766963655845, 0.001011968216111138776 ),
 .UNSPECIFIED. ) ;
#5795=CARTESIAN_POINT ( 'NONE',  ( 2.282816707992307848, -18.57323074318924228, 43.14547561643301066 ) ) ;
#5796=CARTESIAN_POINT ( 'NONE',  ( 0.6064515330803569304, 45.41333491424882851, 11.70313411028668860 ) ) ;
#5800=FACE_OUTER_BOUND ( 'NONE', #1304, .T. ) ;
#5801=CARTESIAN_POINT ( 'NONE',  ( 0.9787284016396604613, 41.55927417454115869, 5.400252680583206732 ) ) ;
#5810=CARTESIAN_POINT ( 'NONE',  ( 5.917102823773431552, 20.06644099299509776, 1.351911212464782075 ) ) ;
#5811=EDGE_CURVE ( 'NONE', #57208, #58714, #27008, .T. ) ;
#5826=ORIENTED_EDGE ( 'NONE', *, *, #43405, .F. ) ;
#5833=CARTESIAN_POINT ( 'NONE',  ( 4.956445790443991584, 30.81386304088947625, 35.60960396630300551 ) ) ;
#5845=FACE_OUTER_BOUND ( 'NONE', #2095, .T. ) ;
#5846=ADVANCED_FACE ( 'NONE', ( #42338 ), #49385, .F. ) ;
#5847=CARTESIAN_POINT ( 'NONE',  ( 4.956445790443988031, 0.000000000000000000, 0.000000000000000000 ) ) ;
#5851=CARTESIAN_POINT ( 'NONE',  ( 4.291220156522059348, 14.90393520085114254, 44.69073408252013024 ) ) ;
#5857=CARTESIAN_POINT ( 'NONE',  ( 1.000433927950261870, -31.52035191441499862, -27.62039269895128868 ) ) ;
#5862=ORIENTED_EDGE ( 'NONE', *, *, #42667, .T. ) ;
#5869=CARTESIAN_POINT ( 'NONE',  ( 0.9762797500689124330, -31.41867615533366376, -27.73430319715951242 ) ) ;
#5870=LINE ( 'NONE', #55970, #28159 ) ;
#5876=CARTESIAN_POINT ( 'NONE',  ( 3.661921753701996352, 41.39923634030784427, 22.33236114416415319 ) ) ;
#5880=CARTESIAN_POINT ( 'NONE',  ( 2.788021980263895028, 5.971756191165462832E-15, 46.99417130740431503 ) ) ;
#5881=LINE ( 'NONE', #49135, #60985 ) ;
#5885=CARTESIAN_POINT ( 'NONE',  ( 4.958415959904820092, -11.02103540056541497, 44.06518730837441922 ) ) ;
#5886=CARTESIAN_POINT ( 'NONE',  ( 0.9754292580325134576, -39.77696751020019406, 13.19546598633348644 ) ) ;
#5887=CARTESIAN_POINT ( 'NONE',  ( 0.6845945791218023269, -41.46895371680806619, 21.92561055813899529 ) ) ;
#5893=ORIENTED_EDGE ( 'NONE', *, *, #54682, .F. ) ;
#5910=CARTESIAN_POINT ( 'NONE',  ( 4.956445790444026223, 13.43466403631445338, -45.13366650706537797 ) ) ;
#5914=AXIS2_PLACEMENT_3D ( 'NONE', #51156, #8238, #41179 ) ;
#5922=CARTESIAN_POINT ( 'NONE',  ( 0.8560838555295223751, -46.85553835019177882, -2.220666565569921591 ) ) ;
#5924=CARTESIAN_POINT ( 'NONE',  ( 0.9784957157296358954, 19.93608022797447532, -36.86306772551813538 ) ) ;
#5929=CARTESIAN_POINT ( 'NONE',  ( 5.894904586330512508, 16.58261916749243881, 11.38183436918475167 ) ) ;
#5938=CARTESIAN_POINT ( 'NONE',  ( 0.5806925824938502512, -46.82446035038566379, -2.586943222941716858 ) ) ;
#5946=CARTESIAN_POINT ( 'NONE',  ( 0.9762797500689124330, -22.97506929404158171, -35.04955029839458547 ) ) ;
#5947=CONICAL_SURFACE ( 'NONE', #26998, 47.09074272231896430, 0.04450589592586084303 ) ;
#5952=CARTESIAN_POINT ( 'NONE',  ( 5.901463166500146684, 17.94437285245843228, -9.083906278280815982 ) ) ;
#5968=VERTEX_POINT ( 'NONE', #57012 ) ;
#5969=CARTESIAN_POINT ( 'NONE',  ( 3.661933894777872567, -39.81515357561435309, 25.04764880586393971 ) ) ;
#5978=ORIENTED_EDGE ( 'NONE', *, *, #42470, .F. ) ;
#5983=EDGE_CURVE ( 'NONE', #32172, #32810, #59044, .T. ) ;
#5989=B_SPLINE_CURVE_WITH_KNOTS ( 'NONE', 3,
 ( #21368, #59249, #39260, #11352 ),
 .UNSPECIFIED., .F., .F.,
 ( 4, 4 ),
 ( 0.000000000000000000, 0.004447772540403784232 ),
 .UNSPECIFIED. ) ;
#5991=ORIENTED_EDGE ( 'NONE', *, *, #26883, .F. ) ;
#5998=ORIENTED_EDGE ( 'NONE', *, *, #46695, .T. ) ;
#6001=CARTESIAN_POINT ( 'NONE',  ( 0.8554163680231708922, 16.00619315955180610, 44.10223637924653417 ) ) ;
#6002=LINE ( 'NONE', #12300, #12269 ) ;
#6004=EDGE_CURVE ( 'NONE', #2143, #26111, #19467, .T. ) ;
#6006=ORIENTED_EDGE ( 'NONE', *, *, #53242, .T. ) ;
#6014=CARTESIAN_POINT ( 'NONE',  ( 2.282816707992305627, 45.63374358165494726, 11.13815124388837319 ) ) ;
#6016=CARTESIAN_POINT ( 'NONE',  ( 4.956445790443988031, 0.000000000000000000, 0.000000000000000000 ) ) ;
#6019=DIRECTION ( 'NONE',  ( 0.07906939808003035641, -0.9635513351855560238, 0.2555716235214582910 ) ) ;
#6028=CARTESIAN_POINT ( 'NONE',  ( 2.528100132419517365, 8.550405663958636993, -41.09920122841587187 ) ) ;
#6033=CARTESIAN_POINT ( 'NONE',  ( 5.896782393890504181, -13.97772289704270676, -14.46199673252280249 ) ) ;
#6043=B_SPLINE_CURVE_WITH_KNOTS ( 'NONE', 3,
 ( #1728, #34661, #49058, #54043 ),
 .UNSPECIFIED., .F., .F.,
 ( 4, 4 ),
 ( 0.000000000000000000, 0.004041751736740996012 ),
 .UNSPECIFIED. ) ;
#6044=EDGE_CURVE ( 'NONE', #16350, #16052, #44896, .T. ) ;
#6049=ORIENTED_EDGE ( 'NONE', *, *, #36538, .T. ) ;
#6060=EDGE_LOOP ( 'NONE', ( #18084, #18729, #4539, #27927 ) ) ;
#6067=CARTESIAN_POINT ( 'NONE',  ( 0.9769922540276041456, -40.97853790617248393, -8.780147274306424166 ) ) ;
#6068=B_SPLINE_CURVE_WITH_KNOTS ( 'NONE', 3,
 ( #34915, #7284, #25484, #11719 ),
 .UNSPECIFIED., .F., .F.,
 ( 4, 4 ),
 ( 0.000000000000000000, 0.005004948556313800964 ),
 .UNSPECIFIED. ) ;
#6078=CARTESIAN_POINT ( 'NONE',  ( 5.895881250540457863, 8.462078741123386649, -18.24612027219289700 ) ) ;
#6085=CIRCLE ( 'NONE', #37136, 42.08604991992415023 ) ;
#6094=EDGE_LOOP ( 'NONE', ( #55324, #38272, #54863, #25909 ) ) ;
#6101=( BOUNDED_SURFACE ( )  B_SPLINE_SURFACE ( 3, 1, ( 
 ( #45370, #2415 ),
 ( #16227, #50344 ),
 ( #44155, #44753 ),
 ( #20924, #35660 ) ),
 .UNSPECIFIED., .F., .F., .F. ) 
 B_SPLINE_SURFACE_WITH_KNOTS ( ( 4, 4 ),
 ( 2, 2 ),
 ( 0.000000000000000000, 1.000000000000000000 ),
 ( 0.000000000000000000, 1.000000000000000000 ),
 .UNSPECIFIED. ) 
 GEOMETRIC_REPRESENTATION_ITEM ( )  RATIONAL_B_SPLINE_SURFACE ( (
 ( 1.000000000000000000, 1.000000000000000000),
 ( 0.9729067724841187204, 0.9999501103223794596),
 ( 0.9729067724841187204, 0.9999501103223794596),
 ( 1.000000000000000000, 1.000000000000000000) ) ) 
 REPRESENTATION_ITEM ( '' )  SURFACE ( )  );
#6109=CARTESIAN_POINT ( 'NONE',  ( 0.5830081025819913165, 27.59732473080532245, -37.91595577174246046 ) ) ;
#6114=CARTESIAN_POINT ( 'NONE',  ( 0.8560838555295223751, -44.60403252362528548, -14.52078223489045072 ) ) ;
#6122=CARTESIAN_POINT ( 'NONE',  ( 0.5804410086790514622, -20.23572001627558947, -42.30881098870896295 ) ) ;
#6128=CARTESIAN_POINT ( 'NONE',  ( 0.8560838555295214869, 21.73747136795201129, -41.56747734237908531 ) ) ;
#6137=VERTEX_POINT ( 'NONE', #22824 ) ;
#6138=CARTESIAN_POINT ( 'NONE',  ( 0.6064515330803585957, -38.25723792261539558, 27.12412362767662799 ) ) ;
#6142=VERTEX_POINT ( 'NONE', #18133 ) ;
#6148=CARTESIAN_POINT ( 'NONE',  ( 4.962356264823608143, 17.31942680647409460, 38.35717733303029320 ) ) ;
#6150=EDGE_LOOP ( 'NONE', ( #35718, #16587, #20888, #785 ) ) ;
#6160=CARTESIAN_POINT ( 'NONE',  ( 1.091591847532193960, 40.62362772340473782, -10.31890796286426415 ) ) ;
#6162=VERTEX_POINT ( 'NONE', #27520 ) ;
#6163=CARTESIAN_POINT ( 'NONE',  ( 0.9787464366903556590, 4.018689650996690510, 41.71551421688862149 ) ) ;
#6172=ORIENTED_EDGE ( 'NONE', *, *, #25234, .F. ) ;
#6183=CARTESIAN_POINT ( 'NONE',  ( 4.960386119450144626, -40.46376651419608095, -16.64692356433961606 ) ) ;
#6185=CARTESIAN_POINT ( 'NONE',  ( 0.5806925824938502512, 37.13995815321093374, 28.63295078613632683 ) ) ;
#6186=CARTESIAN_POINT ( 'NONE',  ( 5.896278296736517710, 0.6775463355846830238, 20.10144051001120147 ) ) ;
#6194=CARTESIAN_POINT ( 'NONE',  ( 0.9754292580325141238, 10.28092798196799507, -40.62794588375828653 ) ) ;
#6195=CARTESIAN_POINT ( 'NONE',  ( 2.282816707992309624, -37.96808949008106282, 27.65720786487965910 ) ) ;
#6200=CARTESIAN_POINT ( 'NONE',  ( 0.8560838555295158248, -42.27062166135473120, 20.33635607586422012 ) ) ;
#6201=CARTESIAN_POINT ( 'NONE',  ( 0.8560838555295223751, -39.18289055412714106, -25.78902716088815694 ) ) ;
#6202=ORIENTED_EDGE ( 'NONE', *, *, #50208, .F. ) ;
#6207=CARTESIAN_POINT ( 'NONE',  ( 5.838029081930955932, -32.82243551873101950, -33.96693664096990517 ) ) ;
#6217=CARTESIAN_POINT ( 'NONE',  ( 5.895881250540457863, 12.98890680526542951, 15.35630103939195301 ) ) ;
#6220=CARTESIAN_POINT ( 'NONE',  ( 4.958415959904820092, -26.53498967168953371, 36.86595010230943359 ) ) ;
#6228=CARTESIAN_POINT ( 'NONE',  ( 0.9780106845699483298, 20.41499038561383017, -36.59999199468128239 ) ) ;
#6230=B_SPLINE_CURVE_WITH_KNOTS ( 'NONE', 3,
 ( #56521, #21792, #60912, #17100 ),
 .UNSPECIFIED., .F., .F.,
 ( 4, 4 ),
 ( 5.818439421673295599E-18, 0.004042984057420976295 ),
 .UNSPECIFIED. ) ;
#6233=FACE_OUTER_BOUND ( 'NONE', #24152, .T. ) ;
#6235=CARTESIAN_POINT ( 'NONE',  ( 0.5835226383429288344, 32.47062518953475774, -33.83638536171847733 ) ) ;
#6243=CARTESIAN_POINT ( 'NONE',  ( 0.8560838555295158248, 31.94705745926175311, 34.34761059777461867 ) ) ;
#6276=B_SPLINE_CURVE_WITH_KNOTS ( 'NONE', 3,
 ( #26521, #3013, #55626, #36876 ),
 .UNSPECIFIED., .F., .F.,
 ( 4, 4 ),
 ( 4.336808689942017736E-18, 0.004042984057420974560 ),
 .UNSPECIFIED. ) ;
#6279=CARTESIAN_POINT ( 'NONE',  ( 5.895596859100789899, -20.11288567981415909, -0.003583743010673907416 ) ) ;
#6284=CARTESIAN_POINT ( 'NONE',  ( 4.956445790443988031, 0.000000000000000000, 0.000000000000000000 ) ) ;
#6291=ORIENTED_EDGE ( 'NONE', *, *, #26434, .T. ) ;
#6292=EDGE_LOOP ( 'NONE', ( #56120, #17153, #23354, #43883 ) ) ;
#6297=B_SPLINE_CURVE_WITH_KNOTS ( 'NONE', 3,
 ( #53332, #38352, #61798, #18933, #5093, #57103, #52105, #33953, #57401, #9203, #5403, #10131, #38056, #24222, #43053, #15147 ),
 .UNSPECIFIED., .F., .F.,
 ( 4, 3, 3, 3, 3, 4 ),
 ( 9.813676791237319219E-18, 0.0002732102107931898912, 0.0004098135523333789319, 0.0005464168938824946970, 0.0008195847345945537436, 0.001092771384553115890 ),
 .UNSPECIFIED. ) ;
#6298=CARTESIAN_POINT ( 'NONE',  ( 4.962356264823608143, -38.57439820587617163, -16.83007429920747811 ) ) ;
#6302=ORIENTED_EDGE ( 'NONE', *, *, #9063, .F. ) ;
#6304=CARTESIAN_POINT ( 'NONE',  ( 5.896278296736517710, -7.233829247026186238, -18.76695750619295922 ) ) ;
#6305=CARTESIAN_POINT ( 'NONE',  ( 5.896782393890504181, -4.656380635072850716, 19.56640504178861306 ) ) ;
#6306=CARTESIAN_POINT ( 'NONE',  ( 0.9787464366903567692, 35.96771654815888297, 21.50947138359660116 ) ) ;
#6327=LINE ( 'NONE', #44608, #13607 ) ;
#6338=CARTESIAN_POINT ( 'NONE',  ( 5.896278296736517710, 14.92041660055668295, -13.48733287496887634 ) ) ;
#6341=CARTESIAN_POINT ( 'NONE',  ( 0.5806925824938494740, -19.24316026636509136, 42.76591101925167493 ) ) ;
#6346=DIRECTION ( 'NONE',  ( 0.000000000000000000, 0.000000000000000000, -1.000000000000000000 ) ) ;
#6352=CARTESIAN_POINT ( 'NONE',  ( 1.231276596079881047, 36.49189576017899839, -20.63051901543672884 ) ) ;
#6355=ORIENTED_EDGE ( 'NONE', *, *, #14726, .F. ) ;
#6357=ORIENTED_EDGE ( 'NONE', *, *, #37311, .T. ) ;
#6359=AXIS2_PLACEMENT_3D ( 'NONE', #20298, #5542, #24682 ) ;
#6366=CARTESIAN_POINT ( 'NONE',  ( 0.5830081025819940921, -38.81694609819070507, -26.31495259339077109 ) ) ;
#6373=EDGE_LOOP ( 'NONE', ( #10883, #4933, #41070, #51838 ) ) ;
#6377=CARTESIAN_POINT ( 'NONE',  ( 4.956445790443995136, 19.33052208089553758, 42.94029536716820417 ) ) ;
#6379=EDGE_CURVE ( 'NONE', #15970, #33742, #7446, .T. ) ;
#6386=FACE_OUTER_BOUND ( 'NONE', #22664, .T. ) ;
#6387=ORIENTED_EDGE ( 'NONE', *, *, #37375, .F. ) ;
#6389=CARTESIAN_POINT ( 'NONE',  ( 0.5806925824938511393, 5.237374507879287044, 46.60249210726590263 ) ) ;
#6403=EDGE_CURVE ( 'NONE', #59315, #30302, #39672, .T. ) ;
#6406=CARTESIAN_POINT ( 'NONE',  ( 0.9754292589017190540, 29.55040399309918087, 29.71701685465599141 ) ) ;
#6408=EDGE_CURVE ( 'NONE', #3997, #22756, #37458, .T. ) ;
#6410=CARTESIAN_POINT ( 'NONE',  ( 0.9784957157296353403, 15.27927399397425567, 39.02405467412931017 ) ) ;
#6411=ORIENTED_EDGE ( 'NONE', *, *, #40389, .T. ) ;
#6420=CARTESIAN_POINT ( 'NONE',  ( 5.901463166500145796, -9.653076390470529233, -17.64471554149788801 ) ) ;
#6432=CARTESIAN_POINT ( 'NONE',  ( 4.291220156522059348, -5.703517857940158642, -46.76386298574845313 ) ) ;
#6434=VERTEX_POINT ( 'NONE', #53763 ) ;
#6436=VERTEX_POINT ( 'NONE', #2699 ) ;
#6439=CONICAL_SURFACE ( 'NONE', #25470, 42.08604991992415023, 1.569615340895231137 ) ;
#6450=CARTESIAN_POINT ( 'NONE',  ( 4.956445790443995136, 19.33052208089553758, 42.94029536716820417 ) ) ;
#6453=DIRECTION ( 'NONE',  ( -0.07906939808003035641, -0.1578407582592981639, 0.9842938206244065125 ) ) ;
#6457=B_SPLINE_CURVE_WITH_KNOTS ( 'NONE', 3,
 ( #7594, #17327, #12643, #17954, #27335, #46157 ),
 .UNSPECIFIED., .F., .F.,
 ( 4, 2, 4 ),
 ( 8.344835848757739736E-18, 0.0002291472222819933150, 0.0004582944445639782816 ),
 .UNSPECIFIED. ) ;
#6458=ORIENTED_EDGE ( 'NONE', *, *, #59686, .T. ) ;
#6459=CARTESIAN_POINT ( 'NONE',  ( 0.5797568665920715958, -19.16764089848626185, 42.79984638977747124 ) ) ;
#6462=CARTESIAN_POINT ( 'NONE',  ( 3.376099380956842921, 12.80002687883565748, -3.983427611134879864 ) ) ;
#6466=CARTESIAN_POINT ( 'NONE',  ( 0.9790724872846784388, 4.154643925904573543, 41.70220790114591836 ) ) ;
#6469=CARTESIAN_POINT ( 'NONE',  ( 0.9775691876210979014, 36.24929767012833537, -21.03145566556006330 ) ) ;
#6475=CARTESIAN_POINT ( 'NONE',  ( 0.8560838555295223751, -44.60403252362528548, -14.52078223489045072 ) ) ;
#6479=CARTESIAN_POINT ( 'NONE',  ( 0.9762797500689124330, -30.73989051779308568, -28.48480149377557424 ) ) ;
#6482=DIRECTION ( 'NONE',  ( 0.07500201931887538753, 0.01982172072487804054, 0.9969863572213993885 ) ) ;
#6487=CARTESIAN_POINT ( 'NONE',  ( 4.956445790443991584, 41.78282513192503700, 21.71942849465911252 ) ) ;
#6496=CARTESIAN_POINT ( 'NONE',  ( 4.956445790444035104, 39.12691469764034480, -26.20348443209818967 ) ) ;
#6497=CARTESIAN_POINT ( 'NONE',  ( 0.5782707292762423457, 40.71812376972668801, 23.27596937574968905 ) ) ;
#6504=DIRECTION ( 'NONE',  ( 0.000000000000000000, 0.000000000000000000, 1.000000000000000000 ) ) ;
#6512=CARTESIAN_POINT ( 'NONE',  ( 5.895596859100789899, -13.98490190264574196, 14.45512718677573538 ) ) ;
#6518=CARTESIAN_POINT ( 'NONE',  ( 4.962356264823608143, 0.000000000000000000, 0.000000000000000000 ) ) ;
#6521=CIRCLE ( 'NONE', #8514, 42.08604991992415023 ) ;
#6529=CARTESIAN_POINT ( 'NONE',  ( 4.962356264823609031, -35.98698831890617100, -21.82137185415387037 ) ) ;
#6531=ORIENTED_EDGE ( 'NONE', *, *, #27579, .T. ) ;
#6550=B_SPLINE_CURVE_WITH_KNOTS ( 'NONE', 3,
 ( #19772, #15071, #38893, #42353 ),
 .UNSPECIFIED., .F., .F.,
 ( 4, 4 ),
 ( 1.734723475976807094E-18, 0.004042984057420972825 ),
 .UNSPECIFIED. ) ;
#6552=FACE_OUTER_BOUND ( 'NONE', #8235, .T. ) ;
#6565=EDGE_CURVE ( 'NONE', #3838, #3952, #2904, .T. ) ;
#6568=CARTESIAN_POINT ( 'NONE',  ( 0.5806925824938499181, 17.36345040154836994, -43.56297685531297503 ) ) ;
#6571=VECTOR ( 'NONE', #43666, 999.9999999999998863 ) ;
#6579=FACE_OUTER_BOUND ( 'NONE', #4559, .T. ) ;
#6582=ORIENTED_EDGE ( 'NONE', *, *, #61154, .T. ) ;
#6590=DIRECTION ( 'NONE',  ( 0.000000000000000000, 0.000000000000000000, 1.000000000000000000 ) ) ;
#6591=PRODUCT_DEFINITION_CONTEXT ( 'detailed design', #4407, 'design' ) ;
#6601=DIRECTION ( 'NONE',  ( -0.07500201931887529039, -0.1525301372901670394, 0.9854487578338784193 ) ) ;
#6607=EDGE_CURVE ( 'NONE', #38419, #33924, #43329, .T. ) ;
#6609=ORIENTED_EDGE ( 'NONE', *, *, #46006, .T. ) ;
#6611=VECTOR ( 'NONE', #40481, 999.9999999999998863 ) ;
#6612=FACE_OUTER_BOUND ( 'NONE', #26292, .T. ) ;
#6614=CIRCLE ( 'NONE', #60655, 47.09074272231896430 ) ;
#6624=CARTESIAN_POINT ( 'NONE',  ( 0.8554163680231738898, 5.604726001789477330, -46.58103175710779453 ) ) ;
#6627=ORIENTED_EDGE ( 'NONE', *, *, #33888, .T. ) ;
#6629=CARTESIAN_POINT ( 'NONE',  ( 0.9790850452238856194, -39.60641447000896420, -13.69924315767353740 ) ) ;
#6631=CARTESIAN_POINT ( 'NONE',  ( 3.661921753702025661, 2.831104162483613518, -46.95333825251623949 ) ) ;
#6639=CARTESIAN_POINT ( 'NONE',  ( 0.6064782688330875304, -24.63250656785344717, -39.90706787780114695 ) ) ;
#6644=CARTESIAN_POINT ( 'NONE',  ( 5.896278296736517710, 14.92041660055649821, 13.48733287496908062 ) ) ;
#6647=DIRECTION ( 'NONE',  ( -1.000000000000000000, -0.000000000000000000, -0.000000000000000000 ) ) ;
#6648=DIRECTION ( 'NONE',  ( 0.07906939808003035641, -0.4861426559824300053, 0.8702949777642121632 ) ) ;
#6667=CARTESIAN_POINT ( 'NONE',  ( 1.092182651088182910, -23.20727262041672745, -34.90248819158799876 ) ) ;
#6672=ORIENTED_EDGE ( 'NONE', *, *, #2563, .F. ) ;
#6674=EDGE_CURVE ( 'NONE', #29292, #28734, #59707, .T. ) ;
#6681=CARTESIAN_POINT ( 'NONE',  ( 0.9787284016396615716, -41.10577017155041091, -8.164046639535335714 ) ) ;
#6692=CARTESIAN_POINT ( 'NONE',  ( 5.895596859100789899, -11.92767122914683675, -16.19440774656085935 ) ) ;
#6699=ORIENTED_EDGE ( 'NONE', *, *, #23148, .F. ) ;
#6712=PRODUCT ( 'straight bevel gear(output)_iso_ISO - Straight bevel gear 2M 47GT 48PT 20PA 5FW ---47O25H120MD16.0N', 'straight bevel gear(output)_iso_ISO - Straight bevel gear 2M 47GT 48PT 20PA 5FW ---47O25H120MD16.0N', '', ( #45612 ) ) ;
#6715=CARTESIAN_POINT ( 'NONE',  ( 5.895596859100789899, -7.232071727010249695, 18.76766692340490295 ) ) ;
#6719=CARTESIAN_POINT ( 'NONE',  ( 4.956445790444040433, 44.65954324082233029, -14.93530206124928128 ) ) ;
#6726=CIRCLE ( 'NONE', #60762, 12.50000000000000000 ) ;
#6727=CARTESIAN_POINT ( 'NONE',  ( 0.9787284016396591291, -30.95573971909037425, 28.25027747426143421 ) ) ;
#6740=EDGE_CURVE ( 'NONE', #61467, #43662, #8128, .T. ) ;
#6746=EDGE_CURVE ( 'NONE', #49329, #33083, #41777, .T. ) ;
#6747=VERTEX_POINT ( 'NONE', #35560 ) ;
#6763=EDGE_LOOP ( 'NONE', ( #13672, #23227, #40995, #58881 ) ) ;
#6764=EDGE_CURVE ( 'NONE', #28331, #12754, #12703, .T. ) ;
#6770=DIRECTION ( 'NONE',  ( 0.07906939808003035641, 0.4269277467251280100, -0.9008222518141226764 ) ) ;
#6773=ORIENTED_EDGE ( 'NONE', *, *, #58185, .T. ) ;
#6774=CARTESIAN_POINT ( 'NONE',  ( 5.896782393890504181, -15.78847575145224447, 12.45994062280461634 ) ) ;
#6778=CARTESIAN_POINT ( 'NONE',  ( 4.962356264823608143, 0.000000000000000000, 0.000000000000000000 ) ) ;
#6779=ORIENTED_EDGE ( 'NONE', *, *, #48651, .F. ) ;
#6795=CARTESIAN_POINT ( 'NONE',  ( 0.9789889208857700531, 38.54554747982771801, -16.44918440296411077 ) ) ;
#6796=EDGE_CURVE ( 'NONE', #55475, #11923, #14926, .T. ) ;
#6798=CARTESIAN_POINT ( 'NONE',  ( 0.5837800005270544768, -30.27739104966287087, -35.81221648917557587 ) ) ;
#6801=CARTESIAN_POINT ( 'NONE',  ( 4.962356264823603702, -20.60668162140254722, -36.69605251817282010 ) ) ;
#6805=CONICAL_SURFACE ( 'NONE', #11873, 42.08604991992415023, 1.569615340895231137 ) ;
#6807=CARTESIAN_POINT ( 'NONE',  ( 0.5837800005270558090, 36.80397537723558798, 29.06376876927043895 ) ) ;
#6815=CARTESIAN_POINT ( 'NONE',  ( 2.528100132419517365, 19.10482268222866864, -37.37993484361196295 ) ) ;
#6816=CARTESIAN_POINT ( 'NONE',  ( 0.9754292589017219406, 4.774020992617491466, 41.63575615330319835 ) ) ;
#6817=VECTOR ( 'NONE', #52597, 1000.000000000000000 ) ;
#6819=CARTESIAN_POINT ( 'NONE',  ( 0.9783242366443560822, 9.454269318224707064, 40.82831470762658910 ) ) ;
#6821=CARTESIAN_POINT ( 'NONE',  ( 4.962356264823608143, 0.000000000000000000, 0.000000000000000000 ) ) ;
#6826=B_SPLINE_CURVE_WITH_KNOTS ( 'NONE', 3,
 ( #11390, #10465, #44928, #34586, #20791, #15790 ),
 .UNSPECIFIED., .F., .F.,
 ( 4, 2, 4 ),
 ( 0.000000000000000000, 0.0002291459268755689880, 0.0004582918537511379759 ),
 .UNSPECIFIED. ) ;
#6828=ADVANCED_FACE ( 'NONE', ( #12068 ), #41373, .F. ) ;
#6841=ORIENTED_EDGE ( 'NONE', *, *, #21236, .T. ) ;
#6844=ORIENTED_EDGE ( 'NONE', *, *, #45787, .T. ) ;
#6847=AXIS2_PLACEMENT_3D ( 'NONE', #61578, #33732, #14010 ) ;
#6855=CARTESIAN_POINT ( 'NONE',  ( 0.9787464366903548818, 20.29559929315806954, -36.66636936242839084 ) ) ;
#6859=ORIENTED_EDGE ( 'NONE', *, *, #15356, .T. ) ;
#6860=CARTESIAN_POINT ( 'NONE',  ( 2.618530812446115519, 37.74802994993038396, 28.01451452546264065 ) ) ;
#6861=CARTESIAN_POINT ( 'NONE',  ( 0.5848930533535030563, -7.979791871079970456, -46.21250917318604223 ) ) ;
#6865=CARTESIAN_POINT ( 'NONE',  ( 4.956445790444011124, -11.44166143951963122, -45.67960632101645757 ) ) ;
#6867=CARTESIAN_POINT ( 'NONE',  ( 3.238018933889920792, -8.855909537851408331, -10.04889837868039137 ) ) ;
#6870=CARTESIAN_POINT ( 'NONE',  ( 0.5835871038041854364, -46.78195124289987916, -3.268560969056623744 ) ) ;
#6871=ORIENTED_EDGE ( 'NONE', *, *, #31573, .T. ) ;
#6876=CARTESIAN_POINT ( 'NONE',  ( 0.5832655196449147983, -44.37535523958005257, 15.16782879433973541 ) ) ;
#6877=ORIENTED_EDGE ( 'NONE', *, *, #42124, .F. ) ;
#6890=B_SPLINE_CURVE_WITH_KNOTS ( 'NONE', 3,
 ( #43322, #5969, #14804, #43951 ),
 .UNSPECIFIED., .F., .F.,
 ( 4, 4 ),
 ( 0.000000000000000000, 0.004447772540403797242 ),
 .UNSPECIFIED. ) ;
#6891=VERTEX_POINT ( 'NONE', #56405 ) ;
#6892=CARTESIAN_POINT ( 'NONE',  ( 4.956445790443998689, -23.10347171912865250, 41.03373788314999615 ) ) ;
#6893=CARTESIAN_POINT ( 'NONE',  ( 0.7764139734771222656, 43.52296024007050335, -17.48692090815614364 ) ) ;
#6898=CARTESIAN_POINT ( 'NONE',  ( 5.894904586330512508, 5.960138742492302022, -19.20953300400311647 ) ) ;
#6911=ORIENTED_EDGE ( 'NONE', *, *, #19731, .T. ) ;
#6923=EDGE_LOOP ( 'NONE', ( #41248, #16299, #14838, #40828 ) ) ;
#6924=EDGE_LOOP ( 'NONE', ( #32609, #61839, #7403, #56997 ) ) ;
#6926=EDGE_CURVE ( 'NONE', #25242, #8101, #56710, .T. ) ;
#6929=CARTESIAN_POINT ( 'NONE',  ( 0.9762797500689124330, -17.18051571332090788, -38.22505284509149703 ) ) ;
#6930=ORIENTED_EDGE ( 'NONE', *, *, #12981, .F. ) ;
#6933=FACE_OUTER_BOUND ( 'NONE', #1255, .T. ) ;
#6939=CARTESIAN_POINT ( 'NONE',  ( 0.9789889208857709413, 36.10718377573707016, 21.27454295225910741 ) ) ;
#6941=ORIENTED_EDGE ( 'NONE', *, *, #28990, .T. ) ;
#6952=ORIENTED_EDGE ( 'NONE', *, *, #42667, .F. ) ;
#6953=ORIENTED_EDGE ( 'NONE', *, *, #35792, .F. ) ;
#6977=ORIENTED_EDGE ( 'NONE', *, *, #33888, .F. ) ;
#6991=CARTESIAN_POINT ( 'NONE',  ( 4.960386119450149955, -37.40422633003205988, -22.70154878690168587 ) ) ;
#7001=VERTEX_POINT ( 'NONE', #47958 ) ;
#7006=CARTESIAN_POINT ( 'NONE',  ( 4.962356264823608143, 0.000000000000000000, 0.000000000000000000 ) ) ;
#7007=CARTESIAN_POINT ( 'NONE',  ( 4.956445790443996913, 2.113652668516264654, 47.04328350079860854 ) ) ;
#7008=CARTESIAN_POINT ( 'NONE',  ( 0.5848930533535030563, 27.96442382265459514, 37.64656800632039335 ) ) ;
#7010=VERTEX_POINT ( 'NONE', #15066 ) ;
#7016=CARTESIAN_POINT ( 'NONE',  ( 0.8554163680231816613, 44.99993935735625428, -13.27444654010398573 ) ) ;
#7032=( BOUNDED_SURFACE ( )  B_SPLINE_SURFACE ( 3, 1, ( 
 ( #39574, #58627 ),
 ( #30137, #49249 ),
 ( #30441, #25136 ),
 ( #5692, #44278 ) ),
 .UNSPECIFIED., .F., .F., .F. ) 
 B_SPLINE_SURFACE_WITH_KNOTS ( ( 4, 4 ),
 ( 2, 2 ),
 ( 0.000000000000000000, 1.000000000000000000 ),
 ( 0.000000000000000000, 1.000000000000000000 ),
 .UNSPECIFIED. ) 
 GEOMETRIC_REPRESENTATION_ITEM ( )  RATIONAL_B_SPLINE_SURFACE ( (
 ( 1.000000000000000000, 1.000000000000000000),
 ( 0.9952954269826590483, 0.8620686068821307169),
 ( 0.9952954269826590483, 0.8620686068821307169),
 ( 1.000000000000000000, 1.000000000000000000) ) ) 
 REPRESENTATION_ITEM ( '' )  SURFACE ( )  );
#7040=ORIENTED_EDGE ( 'NONE', *, *, #38708, .T. ) ;
#7041=CARTESIAN_POINT ( 'NONE',  ( 0.8560838555295158248, -46.73345513967312570, -4.044379407262746362 ) ) ;
#7042=CARTESIAN_POINT ( 'NONE',  ( 0.5806925824938490299, 46.40146083665128174, 6.791670970260652140 ) ) ;
#7043=CARTESIAN_POINT ( 'NONE',  ( 1.231276596079881047, -35.03243822710529543, 23.02183839058294623 ) ) ;
#7047=CARTESIAN_POINT ( 'NONE',  ( 2.618530812446115519, -46.32565728282589390, -7.978738403554839209 ) ) ;
#7050=FACE_OUTER_BOUND ( 'NONE', #53319, .T. ) ;
#7070=ORIENTED_EDGE ( 'NONE', *, *, #44702, .T. ) ;
#7073=CARTESIAN_POINT ( 'NONE',  ( 4.962356264823608143, 0.9708976703217077064, 42.07484944210865052 ) ) ;
#7082=VERTEX_POINT ( 'NONE', #56306 ) ;
#7084=CARTESIAN_POINT ( 'NONE',  ( 0.5824935313925952984, -19.40916258553593821, 42.69101292757142119 ) ) ;
#7089=VERTEX_POINT ( 'NONE', #56617 ) ;
#7091=B_SPLINE_CURVE_WITH_KNOTS ( 'NONE', 3,
 ( #42490, #52163, #48099, #18994 ),
 .UNSPECIFIED., .F., .F.,
 ( 4, 4 ),
 ( 1.226634733346699156E-18, 0.004042984057420973693 ),
 .UNSPECIFIED. ) ;
#7092=EDGE_LOOP ( 'NONE', ( #8178, #2722, #52249, #42094 ) ) ;
#7094=EDGE_LOOP ( 'NONE', ( #11073, #38148, #13086, #24967 ) ) ;
#7095=CARTESIAN_POINT ( 'NONE',  ( 4.958415959904818315, -22.27126879049734143, -39.58780797523473893 ) ) ;
#7096=CARTESIAN_POINT ( 'NONE',  ( 0.9789889208857696090, 24.93672124877021901, 33.68226286049529250 ) ) ;
#7098=VERTEX_POINT ( 'NONE', #23734 ) ;
#7114=CARTESIAN_POINT ( 'NONE',  ( 0.5782707292762423457, 28.40044722094901886, 37.32493739254906728 ) ) ;
#7119=CARTESIAN_POINT ( 'NONE',  ( 5.917102823773431552, 16.57624106732485814, -11.38937882984295236 ) ) ;
#7146=CARTESIAN_POINT ( 'NONE',  ( 5.895596859100789899, -4.666058297670421240, -19.56415301451173150 ) ) ;
#7149=VERTEX_POINT ( 'NONE', #28740 ) ;
#7155=ORIENTED_EDGE ( 'NONE', *, *, #4843, .F. ) ;
#7158=CARTESIAN_POINT ( 'NONE',  ( 2.788021980277358036, 6.069845295522647588E-12, -46.99417130740492610 ) ) ;
#7161=CIRCLE ( 'NONE', #42237, 8.000000000000000000 ) ;
#7162=EDGE_LOOP ( 'NONE', ( #25861, #37858, #1239, #31853 ) ) ;
#7168=EDGE_LOOP ( 'NONE', ( #321, #1851, #40585, #12227 ) ) ;
#7171=CARTESIAN_POINT ( 'NONE',  ( 4.956445790443989807, 46.03642002599014660, 9.908889005849758291 ) ) ;
#7176=ADVANCED_FACE ( 'NONE', ( #29050 ), #28522, .F. ) ;
#7179=ADVANCED_FACE ( 'NONE', ( #48456 ), #21399, .F. ) ;
#7180=ORIENTED_EDGE ( 'NONE', *, *, #44702, .F. ) ;
#7183=CARTESIAN_POINT ( 'NONE',  ( 1.157643937452369709, 40.20129499413059904, -11.86836784859839788 ) ) ;
#7187=CARTESIAN_POINT ( 'NONE',  ( 0.9762797500689124330, -27.44172181261391330, -31.67454323498310842 ) ) ;
#7207=CARTESIAN_POINT ( 'NONE',  ( 0.8560838555295223751, -0.6537497281626496459, 46.90357604036880446 ) ) ;
#7208=CARTESIAN_POINT ( 'NONE',  ( 0.5830082357119554803, 32.40480661380604488, 33.89927054171182164 ) ) ;
#7216=LINE ( 'NONE', #60456, #16191 ) ;
#7218=LINE ( 'NONE', #12274, #4836 ) ;
#7230=ORIENTED_EDGE ( 'NONE', *, *, #44211, .F. ) ;
#7231=B_SPLINE_CURVE_WITH_KNOTS ( 'NONE', 3,
 ( #504, #5198, #1730, #34062 ),
 .UNSPECIFIED., .F., .F.,
 ( 4, 4 ),
 ( 4.164239746139790209E-17, 0.005004948556313859077 ),
 .UNSPECIFIED. ) ;
#7244=CARTESIAN_POINT ( 'NONE',  ( 2.282803330402968456, -6.514475874215432505, -46.51944229611155635 ) ) ;
#7262=ORIENTED_EDGE ( 'NONE', *, *, #10072, .T. ) ;
#7273=DIRECTION ( 'NONE',  ( -1.000000000000000000, -0.000000000000000000, -0.000000000000000000 ) ) ;
#7275=CARTESIAN_POINT ( 'NONE',  ( 0.5804410086790514622, -34.41390132670949242, -31.86225427258559151 ) ) ;
#7280=CARTESIAN_POINT ( 'NONE',  ( 0.9789233960466690032, -22.66104764199909027, 35.25356218312401779 ) ) ;
#7281=CARTESIAN_POINT ( 'NONE',  ( 4.956445790443988031, 0.000000000000000000, 0.000000000000000000 ) ) ;
#7283=( BOUNDED_SURFACE ( )  B_SPLINE_SURFACE ( 3, 1, ( 
 ( #5588, #595 ),
 ( #279, #15043 ),
 ( #34149, #14729 ),
 ( #24733, #29732 ) ),
 .UNSPECIFIED., .F., .F., .F. ) 
 B_SPLINE_SURFACE_WITH_KNOTS ( ( 4, 4 ),
 ( 2, 2 ),
 ( 0.000000000000000000, 1.000000000000000000 ),
 ( 0.000000000000000000, 1.000000000000000000 ),
 .UNSPECIFIED. ) 
 GEOMETRIC_REPRESENTATION_ITEM ( )  RATIONAL_B_SPLINE_SURFACE ( (
 ( 1.000000000000000000, 1.000000000000000000),
 ( 0.9952954269826590483, 0.8620686068821339365),
 ( 0.9952954269826590483, 0.8620686068821339365),
 ( 1.000000000000000000, 1.000000000000000000) ) ) 
 REPRESENTATION_ITEM ( '' )  SURFACE ( )  );
#7284=CARTESIAN_POINT ( 'NONE',  ( 4.960386119450141074, -20.61356833094631824, 38.59426466896017871 ) ) ;
#7295=B_SPLINE_CURVE_WITH_KNOTS ( 'NONE', 3,
 ( #16982, #54216, #9095, #41718 ),
 .UNSPECIFIED., .F., .F.,
 ( 4, 4 ),
 ( 0.000000000000000000, 0.004041751736741000349 ),
 .UNSPECIFIED. ) ;
#7303=CARTESIAN_POINT ( 'NONE',  ( 0.5817217712918331118, -38.40351169400030074, -26.91477742016745012 ) ) ;
#7308=CARTESIAN_POINT ( 'NONE',  ( 4.956445790444003130, -40.78973928653796577, 23.53157918788916803 ) ) ;
#7311=VERTEX_POINT ( 'NONE', #16589 ) ;
#7314=CARTESIAN_POINT ( 'NONE',  ( 4.956445790443987143, 47.01859095792193699, -2.605792484304513934 ) ) ;
#7315=ORIENTED_EDGE ( 'NONE', *, *, #26378, .F. ) ;
#7316=CARTESIAN_POINT ( 'NONE',  ( 0.5804410086790514622, -35.14691939471192939, 31.05179397260356211 ) ) ;
#7322=CARTESIAN_POINT ( 'NONE',  ( 0.5782707292762423457, -13.20261929688047076, 45.00474638756736567 ) ) ;
#7326=ORIENTED_EDGE ( 'NONE', *, *, #30256, .T. ) ;
#7332=EDGE_LOOP ( 'NONE', ( #7478, #31542, #47567, #58626 ) ) ;
#7333=CARTESIAN_POINT ( 'NONE',  ( 1.157643937452368821, -41.75974212862475810, 3.623011447058365864 ) ) ;
#7339=CARTESIAN_POINT ( 'NONE',  ( 4.956445790444031552, 34.56007374686835476, -31.98654955994249960 ) ) ;
#7343=CARTESIAN_POINT ( 'NONE',  ( 1.157643937452369043, 29.72797324181601653, 29.55080170703706699 ) ) ;
#7346=ADVANCED_FACE ( 'NONE', ( #30669 ), #54123, .F. ) ;
#7347=ORIENTED_EDGE ( 'NONE', *, *, #9134, .T. ) ;
#7355=CARTESIAN_POINT ( 'NONE',  ( 5.910764540655178756, -11.91768246006627763, 16.20092846876966775 ) ) ;
#7356=CARTESIAN_POINT ( 'NONE',  ( 5.910764540655177868, 19.70610972188033827, 4.021253299454832231 ) ) ;
#7359=LINE ( 'NONE', #41232, #23487 ) ;
#7365=CARTESIAN_POINT ( 'NONE',  ( 0.5837800304671212359, -7.845051310127922228, 46.23518683990537426 ) ) ;
#7368=DIRECTION ( 'NONE',  ( 0.07500201931887537365, 0.8296863770785113390, -0.5531683403706553204 ) ) ;
#7369=CARTESIAN_POINT ( 'NONE',  ( 0.7764139734771244861, 31.96094574548908440, 34.32984733378186348 ) ) ;
#7373=ADVANCED_FACE ( 'NONE', ( #21909 ), #58516, .F. ) ;
#7377=FACE_OUTER_BOUND ( 'NONE', #27359, .T. ) ;
#7382=CARTESIAN_POINT ( 'NONE',  ( 5.894904586330512508, -18.51743364446320328, 7.850736480391183214 ) ) ;
#7384=( BOUNDED_SURFACE ( )  B_SPLINE_SURFACE ( 3, 1, ( 
 ( #39616, #53976 ),
 ( #58363, #16405 ),
 ( #54276, #30482 ),
 ( #58671, #11717 ) ),
 .UNSPECIFIED., .F., .F., .F. ) 
 B_SPLINE_SURFACE_WITH_KNOTS ( ( 4, 4 ),
 ( 2, 2 ),
 ( 0.000000000000000000, 1.000000000000000000 ),
 ( 0.000000000000000000, 1.000000000000000000 ),
 .UNSPECIFIED. ) 
 GEOMETRIC_REPRESENTATION_ITEM ( )  RATIONAL_B_SPLINE_SURFACE ( (
 ( 1.000000000000000000, 1.000000000000000000),
 ( 0.9729067724841187204, 0.9999501103223794596),
 ( 0.9729067724841187204, 0.9999501103223794596),
 ( 1.000000000000000000, 1.000000000000000000) ) ) 
 REPRESENTATION_ITEM ( '' )  SURFACE ( )  );
#7391=CARTESIAN_POINT ( 'NONE',  ( 0.5797568599927133137, -46.82898596429171789, 2.504272794081084275 ) ) ;
#7394=CARTESIAN_POINT ( 'NONE',  ( 0.7056759521544994085, 46.89390201348435028, 0.8430795138737422478 ) ) ;
#7397=B_SPLINE_CURVE_WITH_KNOTS ( 'NONE', 3,
 ( #35735, #8124, #21308, #50719, #31947, #60126, #7811, #26935, #41362, #55111, #8420, #3109, #17232, #54802, #59820, #17536, #27544, #36656, #56038 ),
 .UNSPECIFIED., .F., .F.,
 ( 4, 3, 3, 3, 3, 3, 4 ),
 ( 9.813676791237320760E-18, 0.0002732106629380670940, 0.0004098138914053731010, 0.0005464171197651472318, 0.0006830203481512563081, 0.0008196235766963549593, 0.001011968216111140510 ),
 .UNSPECIFIED. ) ;
#7402=FACE_OUTER_BOUND ( 'NONE', #24816, .T. ) ;
#7403=ORIENTED_EDGE ( 'NONE', *, *, #53516, .T. ) ;
#7405=ADVANCED_FACE ( 'NONE', ( #17211 ), #52563, .T. ) ;
#7414=CARTESIAN_POINT ( 'NONE',  ( 1.000433927950262314, -41.85488811441339863, -2.141732612345590425 ) ) ;
#7415=VERTEX_POINT ( 'NONE', #43649 ) ;
#7419=CARTESIAN_POINT ( 'NONE',  ( 5.838029081930955932, -28.00222738077721729, -38.03866874468887715 ) ) ;
#7420=CARTESIAN_POINT ( 'NONE',  ( 0.9787284016396634589, 38.50972377290732140, -16.53291183860855895 ) ) ;
#7422=CARTESIAN_POINT ( 'NONE',  ( 5.895596859100789899, 12.98270243688433645, -15.36156309259591701 ) ) ;
#7429=CARTESIAN_POINT ( 'NONE',  ( 0.5824935313925939662, 37.02861770305457156, 28.77706809344680750 ) ) ;
#7430=CARTESIAN_POINT ( 'NONE',  ( 0.8554163680231708922, 3.785871848716424903, 46.76401017296224438 ) ) ;
#7435=CARTESIAN_POINT ( 'NONE',  ( 4.962356264823608143, 0.000000000000000000, 0.000000000000000000 ) ) ;
#7442=CARTESIAN_POINT ( 'NONE',  ( 0.5848930533535030563, -38.76613696830708733, 26.39052305169438029 ) ) ;
#7444=CARTESIAN_POINT ( 'NONE',  ( 1.092182651088188017, 38.88600182739025968, 15.64097331761952425 ) ) ;
#7445=B_SPLINE_CURVE_WITH_KNOTS ( 'NONE', 3,
 ( #11995, #24834, #43972, #48944, #58310, #25132 ),
 .UNSPECIFIED., .F., .F.,
 ( 4, 2, 4 ),
 ( 3.471140604459641645E-18, 0.0002291459268755755203, 0.0004582918537511475711 ),
 .UNSPECIFIED. ) ;
#7446=B_SPLINE_CURVE_WITH_KNOTS ( 'NONE', 3,
 ( #1459, #54696, #10580, #30591, #21207, #39413 ),
 .UNSPECIFIED., .F., .F.,
 ( 4, 2, 4 ),
 ( 8.673617379884034509E-19, 0.0002291459268755708311, 0.0004582918537511407949 ),
 .UNSPECIFIED. ) ;
#7448=CARTESIAN_POINT ( 'NONE',  ( 5.895596859100789899, -2.016778947468235828, 20.01151633159107845 ) ) ;
#7466=B_SPLINE_CURVE_WITH_KNOTS ( 'NONE', 3,
 ( #54486, #46368, #51036, #17543 ),
 .UNSPECIFIED., .F., .F.,
 ( 4, 4 ),
 ( 8.673617379884035472E-19, 0.004041751736740989941 ),
 .UNSPECIFIED. ) ;
#7478=ORIENTED_EDGE ( 'NONE', *, *, #34956, .F. ) ;
#7483=CARTESIAN_POINT ( 'NONE',  ( 1.157643937452369709, -37.77649500668685079, -18.16421480836746483 ) ) ;
#7485=CARTESIAN_POINT ( 'NONE',  ( 5.838029081930955932, -43.49392513872165011, 18.42127938499921314 ) ) ;
#7500=B_SPLINE_CURVE_WITH_KNOTS ( 'NONE', 3,
 ( #10704, #342, #48595, #24168, #1273, #24482 ),
 .UNSPECIFIED., .F., .F.,
 ( 4, 2, 4 ),
 ( 8.770652787438942800E-18, 0.0002448709889506568314, 0.0004897419779013048808 ),
 .UNSPECIFIED. ) ;
#7508=CARTESIAN_POINT ( 'NONE',  ( 0.9787464366903567692, 9.887393718638527673, -40.72558702269483177 ) ) ;
#7509=SHAPE_REPRESENTATION_RELATIONSHIP ( 'NONE' , 'NONE' ,  #42491, #32490 ) ;
#7511=( BOUNDED_SURFACE ( )  B_SPLINE_SURFACE ( 3, 1, ( 
 ( #50540, #26745 ),
 ( #36787, #59627 ),
 ( #3530, #17353 ),
 ( #41798, #7615 ) ),
 .UNSPECIFIED., .F., .F., .F. ) 
 B_SPLINE_SURFACE_WITH_KNOTS ( ( 4, 4 ),
 ( 2, 2 ),
 ( 0.000000000000000000, 1.000000000000000000 ),
 ( 0.000000000000000000, 1.000000000000000000 ),
 .UNSPECIFIED. ) 
 GEOMETRIC_REPRESENTATION_ITEM ( )  RATIONAL_B_SPLINE_SURFACE ( (
 ( 1.000000000000000000, 1.000000000000000000),
 ( 0.9952954269826590483, 0.8620686068821307169),
 ( 0.9952954269826590483, 0.8620686068821307169),
 ( 1.000000000000000000, 1.000000000000000000) ) ) 
 REPRESENTATION_ITEM ( '' )  SURFACE ( )  );
#7513=CARTESIAN_POINT ( 'NONE',  ( 1.000433927950264756, 10.35500712260046896, 40.61025123221650546 ) ) ;
#7518=CARTESIAN_POINT ( 'NONE',  ( 0.8560838555295223751, 31.94705745926225404, -34.34761059777416392 ) ) ;
#7526=EDGE_LOOP ( 'NONE', ( #18611, #43041, #56619, #35940 ) ) ;
#7527=CARTESIAN_POINT ( 'NONE',  ( 0.6064782688330876415, -46.09361631204276222, 8.643667144039953953 ) ) ;
#7531=VERTEX_POINT ( 'NONE', #8717 ) ;
#7532=EDGE_CURVE ( 'NONE', #3952, #55732, #6521, .T. ) ;
#7534=CIRCLE ( 'NONE', #33593, 42.08604991992415023 ) ;
#7548=CARTESIAN_POINT ( 'NONE',  ( 0.5797568599927126476, 21.98355117866222130, 41.42401219396963796 ) ) ;
#7560=CARTESIAN_POINT ( 'NONE',  ( 4.956445790444005794, -36.61936279692559992, -29.60676136437043127 ) ) ;
#7565=ORIENTED_EDGE ( 'NONE', *, *, #46023, .T. ) ;
#7577=ORIENTED_EDGE ( 'NONE', *, *, #57264, .F. ) ;
#7578=EDGE_LOOP ( 'NONE', ( #18913, #10567, #36025, #18361 ) ) ;
#7579=LINE ( 'NONE', #27946, #32967 ) ;
#7580=CARTESIAN_POINT ( 'NONE',  ( 4.956445790444010235, -22.15545010017738647, -41.55326799420456751 ) ) ;
#7591=CARTESIAN_POINT ( 'NONE',  ( 0.8554163680231816613, 36.24698750680841641, -29.78861141095861242 ) ) ;
#7593=CARTESIAN_POINT ( 'NONE',  ( 0.9784957157296348962, 33.03361919771707278, 25.78978595670369600 ) ) ;
#7594=CARTESIAN_POINT ( 'NONE',  ( 1.231276596079887264, 35.62927148397050559, -22.08691432816256395 ) ) ;
#7615=CARTESIAN_POINT ( 'NONE',  ( 0.5804410086790514622, 45.37396088368706870, 11.86269470150153005 ) ) ;
#7621=CARTESIAN_POINT ( 'NONE',  ( 4.291220156522060236, 26.18147253908353989, -39.16528428328985711 ) ) ;
#7629=EDGE_LOOP ( 'NONE', ( #39308, #58785, #53524, #20887 ) ) ;
#7632=EDGE_LOOP ( 'NONE', ( #29744, #25347, #28080, #48019 ) ) ;
#7636=CARTESIAN_POINT ( 'NONE',  ( 0.5830081025819929819, -38.50771568613562579, 26.76542297476333232 ) ) ;
#7645=CARTESIAN_POINT ( 'NONE',  ( 0.5782707292762423457, -29.72436028066441338, 36.27945368404655113 ) ) ;
#7646=CARTESIAN_POINT ( 'NONE',  ( 4.956445790443988031, 0.000000000000000000, 0.000000000000000000 ) ) ;
#7647=CARTESIAN_POINT ( 'NONE',  ( 5.910764540655178756, -19.93069368583282142, 2.696050383554946084 ) ) ;
#7652=LINE ( 'NONE', #11777, #21462 ) ;
#7657=CARTESIAN_POINT ( 'NONE',  ( 4.962356264823598373, -19.84272732133986139, 37.11471096901200895 ) ) ;
#7662=ORIENTED_EDGE ( 'NONE', *, *, #5553, .F. ) ;
#7676=CARTESIAN_POINT ( 'NONE',  ( 1.231276596079887931, -41.87427716283724521, -1.954912557623687652 ) ) ;
#7677=( BOUNDED_SURFACE ( )  B_SPLINE_SURFACE ( 3, 1, ( 
 ( #26180, #35915 ),
 ( #60296, #16482 ),
 ( #17722, #17409 ),
 ( #40319, #59374 ) ),
 .UNSPECIFIED., .F., .F., .F. ) 
 B_SPLINE_SURFACE_WITH_KNOTS ( ( 4, 4 ),
 ( 2, 2 ),
 ( 0.000000000000000000, 1.000000000000000000 ),
 ( 0.000000000000000000, 1.000000000000000000 ),
 .UNSPECIFIED. ) 
 GEOMETRIC_REPRESENTATION_ITEM ( )  RATIONAL_B_SPLINE_SURFACE ( (
 ( 1.000000000000000000, 1.000000000000000000),
 ( 0.7282232189291693025, 0.9929344683865674037),
 ( 0.7282232189291693025, 0.9929344683865674037),
 ( 1.000000000000000000, 1.000000000000000000) ) ) 
 REPRESENTATION_ITEM ( '' )  SURFACE ( )  );
#7681=DIRECTION ( 'NONE',  ( -1.000000000000000000, -0.000000000000000000, -0.000000000000000000 ) ) ;
#7682=CARTESIAN_POINT ( 'NONE',  ( 0.5835226383429290564, -7.620528918417245556, 46.27277832105536959 ) ) ;
#7683=CARTESIAN_POINT ( 'NONE',  ( 0.5848930533535030563, 22.69711449001842851, -41.03795896745540261 ) ) ;
#7688=DIRECTION ( 'NONE',  ( 1.000000000000000000, 0.000000000000000000, 0.000000000000000000 ) ) ;
#7689=VECTOR ( 'NONE', #46690, 999.9999999999998863 ) ;
#7694=EDGE_CURVE ( 'NONE', #7082, #38640, #58807, .T. ) ;
#7698=DIRECTION ( 'NONE',  ( -1.000000000000000000, -0.000000000000000000, -0.000000000000000000 ) ) ;
#7708=EDGE_CURVE ( 'NONE', #59248, #21575, #49065, .T. ) ;
#7711=AXIS2_PLACEMENT_3D ( 'NONE', #12927, #41744, #51405 ) ;
#7718=ORIENTED_EDGE ( 'NONE', *, *, #39459, .F. ) ;
#7723=DIRECTION ( 'NONE',  ( 1.000000000000000000, 0.000000000000000000, 0.000000000000000000 ) ) ;
#7731=CARTESIAN_POINT ( 'NONE',  ( 5.901463166500145796, 14.92627229327890426, -13.48051429907372878 ) ) ;
#7732=CARTESIAN_POINT ( 'NONE',  ( 1.092182651088186018, -0.6199217264839108621, 41.90915033134549361 ) ) ;
#7734=ORIENTED_EDGE ( 'NONE', *, *, #28591, .T. ) ;
#7738=CARTESIAN_POINT ( 'NONE',  ( 0.9769922540276056999, 38.75350856957730628, -15.95296613905461669 ) ) ;
#7742=VERTEX_POINT ( 'NONE', #31530 ) ;
#7744=CARTESIAN_POINT ( 'NONE',  ( 5.838029081930955932, -46.81536740852278200, 6.275861100912162982 ) ) ;
#7745=DIRECTION ( 'NONE',  ( -1.000000000000000000, -0.000000000000000000, -0.000000000000000000 ) ) ;
#7749=CARTESIAN_POINT ( 'NONE',  ( 0.9783242366443560822, -27.26157242999075692, 31.82987839830509103 ) ) ;
#7750=CARTESIAN_POINT ( 'NONE',  ( 0.5806925824938511393, -42.09901922557415332, -20.66143612114853312 ) ) ;
#7751=CARTESIAN_POINT ( 'NONE',  ( 0.5834584762367752697, 45.18130578213499859, 12.56525355233251062 ) ) ;
#7770=ORIENTED_EDGE ( 'NONE', *, *, #16211, .F. ) ;
#7778=EDGE_CURVE ( 'NONE', #11923, #58971, #36559, .T. ) ;
#7782=CARTESIAN_POINT ( 'NONE',  ( 5.901463166500146684, 16.58986915973321530, 11.37075686150967790 ) ) ;
#7785=CONICAL_SURFACE ( 'NONE', #40878, 42.08604991992415023, 1.569615340895231137 ) ;
#7792=CARTESIAN_POINT ( 'NONE',  ( 0.7056759521544989644, 42.84373637420357994, 19.08305747553924903 ) ) ;
#7793=CARTESIAN_POINT ( 'NONE',  ( 1.157644175074338477, 41.64460122042581958, -4.767542833671250868 ) ) ;
#7797=CARTESIAN_POINT ( 'NONE',  ( 1.231276596079881047, 40.64579686208666232, -10.25650859035628315 ) ) ;
#7811=CARTESIAN_POINT ( 'NONE',  ( 0.9789889208857684988, -17.55352473101461541, 38.05533691297488730 ) ) ;
#7812=CARTESIAN_POINT ( 'NONE',  ( 5.894904586330512508, 20.06791991542434772, -1.344619771443771983 ) ) ;
#7815=ORIENTED_EDGE ( 'NONE', *, *, #53010, .F. ) ;
#7826=ORIENTED_EDGE ( 'NONE', *, *, #52735, .T. ) ;
#7828=CARTESIAN_POINT ( 'NONE',  ( 5.896278296736517710, 5.964180709076651432, 19.20821511967891837 ) ) ;
#7829=CARTESIAN_POINT ( 'NONE',  ( 0.9775691876210987896, 10.08232880996395231, -40.67776241090162870 ) ) ;
#7833=EDGE_LOOP ( 'NONE', ( #14073, #3393, #29984, #58366, #31344, #59467, #12435, #29249, #35550, #32333, #30010, #15696, #17840, #23579, #5709, #51551, #17996, #5862, #17836, #23764, #17763, #34498, #25131, #55002, #3033, #57867, #56581, #19438, #38316, #11408, #33649, #46009, #18622, #13187, #32232, #55430, #40330, #52699, #58241, #33818, #61241, #58849, #2238, #25942, #56557, #23092, #24902, #29847, #47215, #15291, #55193, #4922, #42698, #51489, #59699, #26830, #46402, #38263, #51818, #49941, #9418, #313, #35848, #51086, #34632, #47506, #18156, #13586, #33803, #8020, #27351, #35456, #59441, #18783, #13432, #7262, #53469, #43453, #9019, #50251, #41601, #2149, #7347, #57293, #54393, #34696, #59934, #19940, #26605, #33156, #22820, #46949, #42229, #50781, #55488, #704, #17993, #15594, #3469, #21447, #41586, #12341, #41136, #20145, #576, #49132, #35249, #17044, #43338, #6627, #11589, #28134, #17301, #32961, #2253, #8661, #42806, #57371, #40129, #36725, #37397, #25930, #59935, #28797, #54526, #27542, #16921, #13589, #37305, #11872, #18383, #10975, #28401, #19761, #53100, #3111, #59940, #21748, #9366, #15371, #34240, #33885, #24520, #41757 ) ) ;
#7834=CARTESIAN_POINT ( 'NONE',  ( 0.5804410086790514622, -44.12183670707879202, 15.89916279082866701 ) ) ;
#7841=CARTESIAN_POINT ( 'NONE',  ( 0.5804410086790514622, -46.06497594411315788, 8.805557513506700573 ) ) ;
#7844=CARTESIAN_POINT ( 'NONE',  ( 0.5806925824938502512, -7.260877859417425029, 46.33035738103242096 ) ) ;
#7847=EDGE_CURVE ( 'NONE', #36392, #33340, #52048, .T. ) ;
#7851=ORIENTED_EDGE ( 'NONE', *, *, #59711, .T. ) ;
#7852=VECTOR ( 'NONE', #61954, 1000.000000000000114 ) ;
#7862=ORIENTED_EDGE ( 'NONE', *, *, #36238, .F. ) ;
#7869=ORIENTED_EDGE ( 'NONE', *, *, #24049, .F. ) ;
#7871=CARTESIAN_POINT ( 'NONE',  ( 0.6064782688330849769, 21.91200102226807189, 41.46322054084672004 ) ) ;
#7876=CARTESIAN_POINT ( 'NONE',  ( 5.896782393890504181, -7.222780579330470019, -18.77118876312469808 ) ) ;
#7886=B_SPLINE_CURVE_WITH_KNOTS ( 'NONE', 3,
 ( #46375, #36989, #3123, #46998 ),
 .UNSPECIFIED., .F., .F.,
 ( 4, 4 ),
 ( 0.000000000000000000, 0.001752131338475893668 ),
 .UNSPECIFIED. ) ;
#7887=ORIENTED_EDGE ( 'NONE', *, *, #37869, .T. ) ;
#7891=CARTESIAN_POINT ( 'NONE',  ( 1.231276596079881047, -26.41281459480337546, -32.55211200826465756 ) ) ;
#7903=CARTESIAN_POINT ( 'NONE',  ( 0.5804410086790514622, -1.020940616196076123, 46.88792522722238232 ) ) ;
#7905=EDGE_CURVE ( 'NONE', #7098, #5232, #10240, .T. ) ;
#7911=FACE_OUTER_BOUND ( 'NONE', #20005, .T. ) ;
#7914=VECTOR ( 'NONE', #33747, 1000.000000000000000 ) ;
#7915=B_SPLINE_CURVE_WITH_KNOTS ( 'NONE', 3,
 ( #15785, #38989, #20475, #48362 ),
 .UNSPECIFIED., .F., .F.,
 ( 4, 4 ),
 ( 1.301042606982605321E-18, 0.004041751736741002951 ),
 .UNSPECIFIED. ) ;
#7919=CARTESIAN_POINT ( 'NONE',  ( 5.896782393890504181, -18.51935720350340731, 7.845985957612901629 ) ) ;
#7922=CARTESIAN_POINT ( 'NONE',  ( 0.9769922540276052558, -22.92146824146746908, 35.08472386582974423 ) ) ;
#7929=VERTEX_POINT ( 'NONE', #54006 ) ;
#7944=CARTESIAN_POINT ( 'NONE',  ( 1.092182651088183354, 19.45474270483163082, -37.12511509384292197 ) ) ;
#7949=EDGE_CURVE ( 'NONE', #48449, #12657, #48543, .T. ) ;
#7958=ORIENTED_EDGE ( 'NONE', *, *, #39697, .F. ) ;
#7965=DIRECTION ( 'NONE',  ( -0.07500201931887527651, -0.2825166499419927146, 0.9563258020170973817 ) ) ;
#7969=ORIENTED_EDGE ( 'NONE', *, *, #17415, .T. ) ;
#7973=CARTESIAN_POINT ( 'NONE',  ( 0.5806925824938499181, -41.60618895332673617, -21.63671424046719594 ) ) ;
#7974=VERTEX_POINT ( 'NONE', #25830 ) ;
#7980=CARTESIAN_POINT ( 'NONE',  ( 0.9762797500689124330, -22.97506929404208975, 35.04955029839425151 ) ) ;
#7981=CARTESIAN_POINT ( 'NONE',  ( 0.5817216825391108292, -46.75865999591429301, 3.586456133001590718 ) ) ;
#7984=CARTESIAN_POINT ( 'NONE',  ( 4.956445790443996913, 2.113652668516264654, 47.04328350079860854 ) ) ;
#7993=CARTESIAN_POINT ( 'NONE',  ( 0.7056759521544982983, -46.73287073726609009, -3.973364037055558295 ) ) ;
#8003=CARTESIAN_POINT ( 'NONE',  ( 4.956445790443991584, 25.79263028817558023, 39.39896284113483915 ) ) ;
#8010=ORIENTED_EDGE ( 'NONE', *, *, #17850, .F. ) ;
#8020=ORIENTED_EDGE ( 'NONE', *, *, #65, .T. ) ;
#8022=B_SPLINE_CURVE_WITH_KNOTS ( 'NONE', 3,
 ( #21305, #24767, #30688, #20688, #2170, #15382, #35417, #58251, #29765, #10367, #49806, #6235, #53257, #59189, #29455, #949 ),
 .UNSPECIFIED., .F., .F.,
 ( 4, 3, 3, 3, 3, 4 ),
 ( 6.938893903907228378E-18, 0.0002732102107932006790, 0.0004098135523333823471, 0.0005464168938825062979, 0.0008195847345945526594, 0.001092771384553103313 ),
 .UNSPECIFIED. ) ;
#8027=ORIENTED_EDGE ( 'NONE', *, *, #4843, .T. ) ;
#8042=ORIENTED_EDGE ( 'NONE', *, *, #61931, .F. ) ;
#8044=EDGE_LOOP ( 'NONE', ( #25808, #4591, #29841, #12297 ) ) ;
#8052=CARTESIAN_POINT ( 'NONE',  ( 1.157643937452369265, -41.87004049989154453, -1.975343801011922640 ) ) ;
#8063=EDGE_CURVE ( 'NONE', #26937, #34397, #11682, .T. ) ;
#8069=CARTESIAN_POINT ( 'NONE',  ( 4.962356264823609031, -33.29728444345293781, 25.73958909062332268 ) ) ;
#8073=CARTESIAN_POINT ( 'NONE',  ( 0.8554163680231738898, -41.45413358837856066, -21.97180651536612572 ) ) ;
#8074=CARTESIAN_POINT ( 'NONE',  ( 3.661921753702003013, 6.578073271537795641, 46.57638968263120205 ) ) ;
#8076=CARTESIAN_POINT ( 'NONE',  ( 0.5830082357119563685, 10.60551434635580748, 45.68101466022376655 ) ) ;
#8087=CARTESIAN_POINT ( 'NONE',  ( 4.960386119450140185, -9.684723978932076704, 42.66898857629788466 ) ) ;
#8093=CARTESIAN_POINT ( 'NONE',  ( 5.896782393890504181, -11.93563916323470764, -16.18847134979303704 ) ) ;
#8097=CARTESIAN_POINT ( 'NONE',  ( 5.896782393890504181, -19.39988559968486115, -5.307591317834501332 ) ) ;
#8099=EDGE_CURVE ( 'NONE', #29343, #15708, #25871, .T. ) ;
#8101=VERTEX_POINT ( 'NONE', #56484 ) ;
#8104=VERTEX_POINT ( 'NONE', #26442 ) ;
#8107=ORIENTED_EDGE ( 'NONE', *, *, #51347, .F. ) ;
#8112=FACE_OUTER_BOUND ( 'NONE', #50632, .T. ) ;
#8117=CARTESIAN_POINT ( 'NONE',  ( 0.8554163680231816613, 37.37991192211390512, 28.35397075908109343 ) ) ;
#8124=CARTESIAN_POINT ( 'NONE',  ( 0.9772918015221172539, -17.26359481638464288, 38.18776178000455701 ) ) ;
#8126=ORIENTED_EDGE ( 'NONE', *, *, #7708, .F. ) ;
#8128=B_SPLINE_CURVE_WITH_KNOTS ( 'NONE', 3,
 ( #39969, #19925, #15517, #30213 ),
 .UNSPECIFIED., .F., .F.,
 ( 4, 4 ),
 ( 8.673617379884035472E-19, 0.004042984057420974560 ),
 .UNSPECIFIED. ) ;
#8129=ORIENTED_EDGE ( 'NONE', *, *, #5691, .F. ) ;
#8133=CARTESIAN_POINT ( 'NONE',  ( 0.5824935313925948543, -44.18041403804779321, 15.72670316628720144 ) ) ;
#8135=CARTESIAN_POINT ( 'NONE',  ( 3.376099380956842921, 10.22925587767808331, -8.664335394076998043 ) ) ;
#8136=CARTESIAN_POINT ( 'NONE',  ( 4.956445790444005794, -28.36659270909926533, -37.58822246682746737 ) ) ;
#8137=EDGE_CURVE ( 'NONE', #25214, #42400, #21752, .T. ) ;
#8138=ORIENTED_EDGE ( 'NONE', *, *, #53858, .F. ) ;
#8146=( BOUNDED_SURFACE ( )  B_SPLINE_SURFACE ( 3, 1, ( 
 ( #654, #31260 ),
 ( #41005, #19792 ),
 ( #45082, #1808 ),
 ( #11548, #30628 ) ),
 .UNSPECIFIED., .F., .F., .F. ) 
 B_SPLINE_SURFACE_WITH_KNOTS ( ( 4, 4 ),
 ( 2, 2 ),
 ( 0.000000000000000000, 1.000000000000000000 ),
 ( 0.000000000000000000, 1.000000000000000000 ),
 .UNSPECIFIED. ) 
 GEOMETRIC_REPRESENTATION_ITEM ( )  RATIONAL_B_SPLINE_SURFACE ( (
 ( 1.000000000000000000, 1.000000000000000000),
 ( 0.7282232189291693025, 0.9929344683865674037),
 ( 0.7282232189291693025, 0.9929344683865674037),
 ( 1.000000000000000000, 1.000000000000000000) ) ) 
 REPRESENTATION_ITEM ( '' )  SURFACE ( )  );
#8155=CARTESIAN_POINT ( 'NONE',  ( 4.962356264823593044, 18.10963840443015016, 37.99048031708913697 ) ) ;
#8163=CARTESIAN_POINT ( 'NONE',  ( 0.6064515330803602611, -45.81048872046274312, 10.03660596165072150 ) ) ;
#8171=CARTESIAN_POINT ( 'NONE',  ( 5.838029081930957709, 44.61407408311379186, -15.51288019225814985 ) ) ;
#8173=ORIENTED_EDGE ( 'NONE', *, *, #51612, .T. ) ;
#8178=ORIENTED_EDGE ( 'NONE', *, *, #34680, .F. ) ;
#8181=CARTESIAN_POINT ( 'NONE',  ( 0.8560838555295223751, -35.39593983670150124, -30.78149244527203621 ) ) ;
#8187=CARTESIAN_POINT ( 'NONE',  ( 0.5837157313716003770, -30.34684335673147260, 35.75340769582711431 ) ) ;
#8203=CARTESIAN_POINT ( 'NONE',  ( 0.7764139734771254853, 44.99430973300147230, 13.24962499686677653 ) ) ;
#8204=EDGE_CURVE ( 'NONE', #24845, #44371, #42424, .T. ) ;
#8209=LINE ( 'NONE', #8511, #3802 ) ;
#8210=CONICAL_SURFACE ( 'NONE', #22229, 42.08604991992415023, 1.569615340895231137 ) ;
#8213=CARTESIAN_POINT ( 'NONE',  ( 5.838029081930955932, 35.04472919977185086, -31.66910187339669491 ) ) ;
#8226=ORIENTED_EDGE ( 'NONE', *, *, #32665, .F. ) ;
#8229=CARTESIAN_POINT ( 'NONE',  ( 0.8554163680231708922, -8.703479761965583705, 46.10265624825618147 ) ) ;
#8231=ORIENTED_EDGE ( 'NONE', *, *, #23352, .F. ) ;
#8235=EDGE_LOOP ( 'NONE', ( #25664, #60476, #24579, #39128 ) ) ;
#8237=CARTESIAN_POINT ( 'NONE',  ( 1.157644175074336701, -37.77649504501447097, 18.16421475300208144 ) ) ;
#8238=DIRECTION ( 'NONE',  ( -1.000000000000000000, -0.000000000000000000, -0.000000000000000000 ) ) ;
#8244=ADVANCED_FACE ( 'NONE', ( #23912 ), #7032, .F. ) ;
#8246=VECTOR ( 'NONE', #43516, 1000.000000000000000 ) ;
#8253=EDGE_LOOP ( 'NONE', ( #53092, #54110, #50473, #48009 ) ) ;
#8271=CARTESIAN_POINT ( 'NONE',  ( 0.9754292589017210524, -41.77202903865140371, 3.380097171582762794 ) ) ;
#8275=CARTESIAN_POINT ( 'NONE',  ( 0.5834584762367753807, -46.80309860109110787, 2.950584747085512660 ) ) ;
#8279=CARTESIAN_POINT ( 'NONE',  ( 0.9790724872846768845, 41.90863365906401583, 0.04043280624974921605 ) ) ;
#8282=ORIENTED_EDGE ( 'NONE', *, *, #46260, .F. ) ;
#8286=CARTESIAN_POINT ( 'NONE',  ( 0.5835226383429282793, -34.90249509102868331, -31.32185037584284970 ) ) ;
#8288=CARTESIAN_POINT ( 'NONE',  ( 0.8560838555295158248, 21.73747136795142154, 41.56747734237938374 ) ) ;
#8298=CARTESIAN_POINT ( 'NONE',  ( 0.5804410086790514622, -24.77328595090334318, -39.82215658462223473 ) ) ;
#8302=CARTESIAN_POINT ( 'NONE',  ( 2.282803330402959130, 42.71620289003610793, 19.54028961183163204 ) ) ;
#8304=CARTESIAN_POINT ( 'NONE',  ( 0.5834584762367742705, -45.99222294191854132, 9.162500634327543025 ) ) ;
#8311=CARTESIAN_POINT ( 'NONE',  ( 0.9784957157296372277, 32.74509629232474595, -26.15514721424351308 ) ) ;
#8318=ORIENTED_EDGE ( 'NONE', *, *, #6403, .F. ) ;
#8332=ORIENTED_EDGE ( 'NONE', *, *, #48397, .T. ) ;
#8333=CARTESIAN_POINT ( 'NONE',  ( 1.000110580585052977, -31.51987383986781666, 27.62091663740936198 ) ) ;
#8336=ADVANCED_FACE ( 'NONE', ( #40505 ), #26265, .F. ) ;
#8345=CARTESIAN_POINT ( 'NONE',  ( 0.8554163680231816613, -34.17638377241251391, 32.14312158693671506 ) ) ;
#8352=CARTESIAN_POINT ( 'NONE',  ( 3.376099380956842921, -0.9076095657322794663, -13.37477583020583971 ) ) ;
#8353=DIRECTION ( 'NONE',  ( 0.000000000000000000, 0.000000000000000000, 1.000000000000000000 ) ) ;
#8367=CARTESIAN_POINT ( 'NONE',  ( 5.838029081930955932, 1.598329895849277538, -47.20710115752665104 ) ) ;
#8369=EDGE_CURVE ( 'NONE', #19302, #3395, #22884, .T. ) ;
#8374=CARTESIAN_POINT ( 'NONE',  ( 5.896278296736517710, 17.95357321928062433, 9.066211351734164481 ) ) ;
#8376=CARTESIAN_POINT ( 'NONE',  ( 5.895596859100789899, -17.30698493747174993, -10.24677781483592121 ) ) ;
#8382=ORIENTED_EDGE ( 'NONE', *, *, #8711, .F. ) ;
#8386=CARTESIAN_POINT ( 'NONE',  ( 1.231276596079881935, -41.76121777166937221, -3.643825084341031584 ) ) ;
#8396=B_SPLINE_CURVE_WITH_KNOTS ( 'NONE', 3,
 ( #14774, #9747, #4707, #56733, #9434, #42986, #13858, #33575, #33886, #52963, #10067, #3798, #22939, #42066, #48892, #25701 ),
 .UNSPECIFIED., .F., .F.,
 ( 4, 3, 3, 3, 3, 4 ),
 ( 1.040890552917501732E-17, 0.0002732102107931892406, 0.0004098135523333787692, 0.0005464168938824976243, 0.0008195847345945413837, 0.001092771384553106132 ),
 .UNSPECIFIED. ) ;
#8407=VERTEX_POINT ( 'NONE', #5011 ) ;
#8412=ORIENTED_EDGE ( 'NONE', *, *, #16776, .F. ) ;
#8413=CARTESIAN_POINT ( 'NONE',  ( 1.092182651088186018, 28.57178434915972787, -30.66617556115198440 ) ) ;
#8420=CARTESIAN_POINT ( 'NONE',  ( 0.9790320750461911636, -17.71876186423139643, 37.97871259720171366 ) ) ;
#8426=( BOUNDED_SURFACE ( )  B_SPLINE_SURFACE ( 3, 1, ( 
 ( #9570, #53399 ),
 ( #37815, #43744 ),
 ( #38414, #29603 ),
 ( #44061, #33098 ) ),
 .UNSPECIFIED., .F., .F., .F. ) 
 B_SPLINE_SURFACE_WITH_KNOTS ( ( 4, 4 ),
 ( 2, 2 ),
 ( 0.000000000000000000, 1.000000000000000000 ),
 ( 0.000000000000000000, 1.000000000000000000 ),
 .UNSPECIFIED. ) 
 GEOMETRIC_REPRESENTATION_ITEM ( )  RATIONAL_B_SPLINE_SURFACE ( (
 ( 1.000000000000000000, 1.000000000000000000),
 ( 0.9952954269826590483, 0.8620686068821307169),
 ( 0.9952954269826590483, 0.8620686068821307169),
 ( 1.000000000000000000, 1.000000000000000000) ) ) 
 REPRESENTATION_ITEM ( '' )  SURFACE ( )  );
#8428=CARTESIAN_POINT ( 'NONE',  ( 3.238018933889920792, -12.56031985276158913, 4.652510888109346432 ) ) ;
#8433=DIRECTION ( 'NONE',  ( -1.000000000000000000, 0.000000000000000000, 0.000000000000000000 ) ) ;
#8436=DIRECTION ( 'NONE',  ( 0.07500201931887538753, 0.9463514676414640503, -0.3143144870840953731 ) ) ;
#8438=( LENGTH_UNIT ( ) NAMED_UNIT ( * ) SI_UNIT ( .MILLI., .METRE. ) );
#8441=ORIENTED_EDGE ( 'NONE', *, *, #18404, .T. ) ;
#8449=LINE ( 'NONE', #41702, #40687 ) ;
#8452=ORIENTED_EDGE ( 'NONE', *, *, #44287, .T. ) ;
#8458=CARTESIAN_POINT ( 'NONE',  ( 4.956445790444005794, -33.12351118015950391, -33.47194433010255921 ) ) ;
#8459=CARTESIAN_POINT ( 'NONE',  ( 0.9780106845699503282, -41.79289930907007999, -3.112043347603926868 ) ) ;
#8460=B_SPLINE_CURVE_WITH_KNOTS ( 'NONE', 3,
 ( #29009, #19311, #5176, #482 ),
 .UNSPECIFIED., .F., .F.,
 ( 4, 4 ),
 ( 1.084202172485504241E-18, 0.004041751736740997747 ),
 .UNSPECIFIED. ) ;
#8461=ADVANCED_FACE ( 'NONE', ( #8808 ), #9070, .F. ) ;
#8467=EDGE_CURVE ( 'NONE', #61383, #48962, #9326, .T. ) ;
#8472=ADVANCED_FACE ( 'NONE', ( #28840 ), #51498, .F. ) ;
#8475=ORIENTED_EDGE ( 'NONE', *, *, #30680, .T. ) ;
#8476=CARTESIAN_POINT ( 'NONE',  ( 5.838029081930955932, 30.51096402024728249, -36.05753919373999139 ) ) ;
#8478=ORIENTED_EDGE ( 'NONE', *, *, #20625, .F. ) ;
#8482=ORIENTED_EDGE ( 'NONE', *, *, #43760, .F. ) ;
#8483=CARTESIAN_POINT ( 'NONE',  ( 5.901463166500146684, -19.39418503693773133, 5.327612701169004872 ) ) ;
#8484=ADVANCED_FACE ( 'NONE', ( #42050 ), #415, .T. ) ;
#8485=FACE_OUTER_BOUND ( 'NONE', #28209, .T. ) ;
#8493=DIRECTION ( 'NONE',  ( -1.000000000000000000, -0.000000000000000000, -0.000000000000000000 ) ) ;
#8494=( BOUNDED_SURFACE ( )  B_SPLINE_SURFACE ( 3, 1, ( 
 ( #24240, #52426 ),
 ( #43065, #19871 ),
 ( #57418, #48060 ),
 ( #42451, #43689 ) ),
 .UNSPECIFIED., .F., .F., .F. ) 
 B_SPLINE_SURFACE_WITH_KNOTS ( ( 4, 4 ),
 ( 2, 2 ),
 ( 0.000000000000000000, 1.000000000000000000 ),
 ( 0.000000000000000000, 1.000000000000000000 ),
 .UNSPECIFIED. ) 
 GEOMETRIC_REPRESENTATION_ITEM ( )  RATIONAL_B_SPLINE_SURFACE ( (
 ( 1.000000000000000000, 1.000000000000000000),
 ( 0.7282232189291694135, 0.9929344683865672927),
 ( 0.7282232189291694135, 0.9929344683865672927),
 ( 1.000000000000000000, 1.000000000000000000) ) ) 
 REPRESENTATION_ITEM ( '' )  SURFACE ( )  );
#8497=CONICAL_SURFACE ( 'NONE', #43550, 42.08604991992415023, 1.569615340895231137 ) ;
#8506=CARTESIAN_POINT ( 'NONE',  ( 5.895881250540457863, -20.11287301435476849, 0.004551564636878664520 ) ) ;
#8511=CARTESIAN_POINT ( 'NONE',  ( 3.238018933889920792, -12.56031985276152341, -4.652510888109532061 ) ) ;
#8514=AXIS2_PLACEMENT_3D ( 'NONE', #26914, #27834, #46963 ) ;
#8518=CARTESIAN_POINT ( 'NONE',  ( 0.9780303403264768436, -12.10685390290327490, 40.12186064938713770 ) ) ;
#8522=VECTOR ( 'NONE', #50729, 1000.000000000000000 ) ;
#8529=CARTESIAN_POINT ( 'NONE',  ( 0.5837800005270548098, 45.22974258645800916, -12.38973947282719301 ) ) ;
#8542=B_SPLINE_CURVE_WITH_KNOTS ( 'NONE', 3,
 ( #30436, #21056, #40196, #16054, #25433, #10428, #15750, #20437, #29517, #34857, #53924, #38955, #49869, #49547, #48625, #59247, #30130, #54228, #6929 ),
 .UNSPECIFIED., .F., .F.,
 ( 4, 3, 3, 3, 3, 3, 4 ),
 ( 6.938893903907228378E-18, 0.0002732106629380631367, 0.0004098138914053715831, 0.0005464171197651477739, 0.0006830203481512608617, 0.0008196235766963706803, 0.001011968216111143980 ),
 .UNSPECIFIED. ) ;
#8544=ORIENTED_EDGE ( 'NONE', *, *, #5580, .T. ) ;
#8551=VERTEX_POINT ( 'NONE', #10671 ) ;
#8559=VERTEX_POINT ( 'NONE', #34178 ) ;
#8567=CARTESIAN_POINT ( 'NONE',  ( 4.956445790443988031, 0.000000000000000000, 0.000000000000000000 ) ) ;
#8587=CARTESIAN_POINT ( 'NONE',  ( 0.5804410086790514622, 23.01644811389206424, 40.86273324284501740 ) ) ;
#8591=CARTESIAN_POINT ( 'NONE',  ( 0.9789889208857687208, -1.496490579766653672, -41.88192228142159479 ) ) ;
#8602=CARTESIAN_POINT ( 'NONE',  ( 0.5835226383429293895, -25.08023547371319140, 39.62605535665972667 ) ) ;
#8605=CARTESIAN_POINT ( 'NONE',  ( 4.962356264823608143, -42.08379584346670299, -0.4355746408611892995 ) ) ;
#8608=ORIENTED_EDGE ( 'NONE', *, *, #46410, .T. ) ;
#8610=CARTESIAN_POINT ( 'NONE',  ( 5.894904586330512508, 10.82344038793328345, 16.95236119926948248 ) ) ;
#8612=CIRCLE ( 'NONE', #20660, 42.08604991992415023 ) ;
#8614=VERTEX_POINT ( 'NONE', #7171 ) ;
#8616=CARTESIAN_POINT ( 'NONE',  ( 0.5806925824938499181, -46.06186276235273169, 8.804950948514585818 ) ) ;
#8623=EDGE_CURVE ( 'NONE', #48578, #14125, #54796, .T. ) ;
#8641=EDGE_CURVE ( 'NONE', #7311, #16730, #48941, .T. ) ;
#8647=ORIENTED_EDGE ( 'NONE', *, *, #30029, .T. ) ;
#8653=AXIS2_PLACEMENT_3D ( 'NONE', #6284, #44878, #6590 ) ;
#8659=CARTESIAN_POINT ( 'NONE',  ( 0.9762797500689124330, -41.84568905980455611, -2.294143041716810050 ) ) ;
#8661=ORIENTED_EDGE ( 'NONE', *, *, #47753, .T. ) ;
#8665=CARTESIAN_POINT ( 'NONE',  ( 0.5806925824938499181, 36.46274162637902094, 29.49052111156212774 ) ) ;
#8668=CARTESIAN_POINT ( 'NONE',  ( 4.956445790443996025, 14.46717203539371610, 44.81337951368942640 ) ) ;
#8675=CARTESIAN_POINT ( 'NONE',  ( 2.528100132419516477, 32.18157850662347386, -26.95551489870128492 ) ) ;
#8681=EDGE_CURVE ( 'NONE', #15676, #44940, #19909, .T. ) ;
#8685=CARTESIAN_POINT ( 'NONE',  ( 4.958415959904820092, 34.02476434053209431, -30.09184881980321435 ) ) ;
#8692=CARTESIAN_POINT ( 'NONE',  ( 0.5804410086790514622, 46.55025363952971418, -5.709092568074892071 ) ) ;
#8694=CARTESIAN_POINT ( 'NONE',  ( 0.5834584762367743815, 46.45295943560137175, 6.431061241161131647 ) ) ;
#8696=( BOUNDED_SURFACE ( )  B_SPLINE_SURFACE ( 3, 1, ( 
 ( #11312, #44546 ),
 ( #5952, #54822 ),
 ( #59212, #39224 ),
 ( #34507, #30399 ) ),
 .UNSPECIFIED., .F., .F., .F. ) 
 B_SPLINE_SURFACE_WITH_KNOTS ( ( 4, 4 ),
 ( 2, 2 ),
 ( 0.000000000000000000, 1.000000000000000000 ),
 ( 0.000000000000000000, 1.000000000000000000 ),
 .UNSPECIFIED. ) 
 GEOMETRIC_REPRESENTATION_ITEM ( )  RATIONAL_B_SPLINE_SURFACE ( (
 ( 1.000000000000000000, 1.000000000000000000),
 ( 0.7282232189291694135, 0.9929344683865672927),
 ( 0.7282232189291694135, 0.9929344683865672927),
 ( 1.000000000000000000, 1.000000000000000000) ) ) 
 REPRESENTATION_ITEM ( '' )  SURFACE ( )  );
#8706=EDGE_CURVE ( 'NONE', #43281, #4666, #59815, .T. ) ;
#8711=EDGE_CURVE ( 'NONE', #19581, #34712, #36325, .T. ) ;
#8712=ORIENTED_EDGE ( 'NONE', *, *, #6565, .T. ) ;
#8715=ORIENTED_EDGE ( 'NONE', *, *, #16920, .T. ) ;
#8717=CARTESIAN_POINT ( 'NONE',  ( 0.9762797500689124330, -41.16654106227468901, -7.851158013551661874 ) ) ;
#8722=DIRECTION ( 'NONE',  ( -0.07906939808003035641, -0.7338893160900470392, 0.6746513929550169708 ) ) ;
#8723=CARTESIAN_POINT ( 'NONE',  ( 0.8554163680231720024, -30.98316862405900096, -35.23136010892773839 ) ) ;
#8724=EDGE_CURVE ( 'NONE', #60706, #31862, #49446, .T. ) ;
#8727=ORIENTED_EDGE ( 'NONE', *, *, #13986, .F. ) ;
#8735=DIRECTION ( 'NONE',  ( 0.000000000000000000, 0.000000000000000000, 1.000000000000000000 ) ) ;
#8736=CARTESIAN_POINT ( 'NONE',  ( 4.962356264823608143, -41.76635909427997717, 5.177532797578748180 ) ) ;
#8740=CARTESIAN_POINT ( 'NONE',  ( 0.6064515330803571524, -46.09360457555626311, -8.643723345257249946 ) ) ;
#8744=CARTESIAN_POINT ( 'NONE',  ( 4.962356264823602814, 39.61238188121407688, -14.21600504921160812 ) ) ;
#8747=CARTESIAN_POINT ( 'NONE',  ( 4.962356264823608143, 0.000000000000000000, 0.000000000000000000 ) ) ;
#8754=EDGE_CURVE ( 'NONE', #33340, #13848, #14492, .T. ) ;
#8763=CARTESIAN_POINT ( 'NONE',  ( 0.9762797500689124330, -39.42083772998332591, 14.22400568939802845 ) ) ;
#8764=LINE ( 'NONE', #5582, #34623 ) ;
#8767=ADVANCED_FACE ( 'NONE', ( #48416 ), #19510, .F. ) ;
#8782=CARTESIAN_POINT ( 'NONE',  ( 0.5806925824938511393, -45.84420715090610798, 9.875780123533177246 ) ) ;
#8784=FACE_OUTER_BOUND ( 'NONE', #52546, .T. ) ;
#8785=CARTESIAN_POINT ( 'NONE',  ( 0.9787464366903556590, -41.80285375509220103, -2.975804230933245531 ) ) ;
#8790=CARTESIAN_POINT ( 'NONE',  ( 4.956445790444035104, 41.78282513192535674, -21.71942849465849079 ) ) ;
#8799=CARTESIAN_POINT ( 'NONE',  ( 5.895881250540457863, 5.954605924856151589, -19.21120375947246117 ) ) ;
#8802=CARTESIAN_POINT ( 'NONE',  ( 5.895596859100789899, -19.39731145114843613, -5.317188324634858354 ) ) ;
#8808=FACE_OUTER_BOUND ( 'NONE', #44624, .T. ) ;
#8810=CARTESIAN_POINT ( 'NONE',  ( 5.896782393890504181, 19.71107130340476132, -3.999969368645934775 ) ) ;
#8811=FACE_OUTER_BOUND ( 'NONE', #14221, .T. ) ;
#8812=CARTESIAN_POINT ( 'NONE',  ( 1.231276596079887264, -18.40965318903149495, -37.66113965983570466 ) ) ;
#8813=ORIENTED_EDGE ( 'NONE', *, *, #49722, .T. ) ;
#8821=CARTESIAN_POINT ( 'NONE',  ( 0.8560838555295158248, -20.57050347530512724, 42.15717282805135113 ) ) ;
#8822=CARTESIAN_POINT ( 'NONE',  ( 0.5837800304671224572, 10.91570225908018976, -45.60794641694153029 ) ) ;
#8823=VERTEX_POINT ( 'NONE', #47817 ) ;
#8833=EDGE_CURVE ( 'NONE', #54885, #48040, #13913, .T. ) ;
#8834=CARTESIAN_POINT ( 'NONE',  ( 4.962356264823600149, -40.47344704301802665, 11.53844366967928892 ) ) ;
#8836=B_SPLINE_CURVE_WITH_KNOTS ( 'NONE', 3,
 ( #19425, #58525, #43552, #11253 ),
 .UNSPECIFIED., .F., .F.,
 ( 4, 4 ),
 ( 4.336808689942017736E-19, 0.004041751736740990808 ),
 .UNSPECIFIED. ) ;
#8837=CARTESIAN_POINT ( 'NONE',  ( 0.8560838555295158248, -26.00596412780176081, 39.03924517540291106 ) ) ;
#8841=ADVANCED_FACE ( 'NONE', ( #6386 ), #39104, .F. ) ;
#8844=CARTESIAN_POINT ( 'NONE',  ( 0.5824935313925944103, 40.16257500733529895, -24.21168614190273161 ) ) ;
#8847=DIRECTION ( 'NONE',  ( -1.000000000000000000, -0.000000000000000000, -0.000000000000000000 ) ) ;
#8851=CARTESIAN_POINT ( 'NONE',  ( 1.231276596079881047, -7.805643096902013411, 41.18675402191647805 ) ) ;
#8859=CARTESIAN_POINT ( 'NONE',  ( 5.917102823773431552, -2.021675920616845090, -20.01006108245899640 ) ) ;
#8860=ORIENTED_EDGE ( 'NONE', *, *, #4969, .F. ) ;
#8864=CARTESIAN_POINT ( 'NONE',  ( 0.9762797500689124330, -12.89881610234976961, 39.87411852747928265 ) ) ;
#8866=EDGE_LOOP ( 'NONE', ( #32957, #24976, #25219, #52602 ) ) ;
#8867=ORIENTED_EDGE ( 'NONE', *, *, #40512, .T. ) ;
#8870=CARTESIAN_POINT ( 'NONE',  ( 1.231276596079881047, 8.892602616353681100, 40.96581977363184990 ) ) ;
#8872=ORIENTED_EDGE ( 'NONE', *, *, #28249, .T. ) ;
#8879=ORIENTED_EDGE ( 'NONE', *, *, #397, .T. ) ;
#8881=ADVANCED_FACE ( 'NONE', ( #30225 ), #45502, .F. ) ;
#8882=CARTESIAN_POINT ( 'NONE',  ( 4.956445790444004018, -45.55738122058057371, -11.91902120403893761 ) ) ;
#8885=ORIENTED_EDGE ( 'NONE', *, *, #3793, .F. ) ;
#8890=CARTESIAN_POINT ( 'NONE',  ( 2.347571140040969784, -0.2125464247640618254, 41.96959966789661678 ) ) ;
#8892=CARTESIAN_POINT ( 'NONE',  ( 0.5824935313925952984, -38.45572481770904716, 26.84018267073592057 ) ) ;
#8901=CARTESIAN_POINT ( 'NONE',  ( 4.956445790443991584, 34.56007374686787159, 31.98654955994301829 ) ) ;
#8908=CARTESIAN_POINT ( 'NONE',  ( 0.5782707292762442330, 21.90237606067556442, 41.47315127409978430 ) ) ;
#8910=B_SPLINE_CURVE_WITH_KNOTS ( 'NONE', 3,
 ( #37420, #33341, #42137, #61794 ),
 .UNSPECIFIED., .F., .F.,
 ( 4, 4 ),
 ( 3.736708725176134707E-17, 0.005004948556313845200 ),
 .UNSPECIFIED. ) ;
#8918=CARTESIAN_POINT ( 'NONE',  ( 0.9772918015221165877, 41.90661890918757138, -0.4149064362024745267 ) ) ;
#8922=CARTESIAN_POINT ( 'NONE',  ( 0.7764146366350254125, -46.73184010359712914, 4.021889381994030899 ) ) ;
#8930=CARTESIAN_POINT ( 'NONE',  ( 4.291220156522060236, -40.01826627095181266, -24.85814478139707617 ) ) ;
#8939=EDGE_CURVE ( 'NONE', #15929, #52958, #58686, .T. ) ;
#8946=CARTESIAN_POINT ( 'NONE',  ( 0.9789233960466690032, 24.96512103919651082, -33.66124564436990596 ) ) ;
#8949=DIRECTION ( 'NONE',  ( -1.000000000000000000, -0.000000000000000000, -0.000000000000000000 ) ) ;
#8950=CARTESIAN_POINT ( 'NONE',  ( 0.9780106845699481077, 33.08330293080910423, -25.72598518315200522 ) ) ;
#8951=CARTESIAN_POINT ( 'NONE',  ( 5.895596859100789899, 14.91436009500240445, 13.49407448360528861 ) ) ;
#8952=B_SPLINE_CURVE_WITH_KNOTS ( 'NONE', 3,
 ( #31803, #55578, #36204, #22090, #45920, #46523 ),
 .UNSPECIFIED., .F., .F.,
 ( 4, 2, 4 ),
 ( 1.266058488688919593E-17, 0.0002448709889506581867, 0.0004897419779013036881 ),
 .UNSPECIFIED. ) ;
#8961=CARTESIAN_POINT ( 'NONE',  ( 0.9787464366903563251, -37.32407051563441769, -19.05905960519595155 ) ) ;
#8963=CARTESIAN_POINT ( 'NONE',  ( 5.838029081930955932, 35.01788019483823433, 31.69878743442524538 ) ) ;
#8965=ORIENTED_EDGE ( 'NONE', *, *, #15871, .T. ) ;
#8970=CARTESIAN_POINT ( 'NONE',  ( 0.8560838555295223751, -2.480523550130904642, -46.84250032821665854 ) ) ;
#8976=CARTESIAN_POINT ( 'NONE',  ( 0.5817216825391123836, 28.18300595765020233, 37.48270437679907019 ) ) ;
#8977=VECTOR ( 'NONE', #58949, 1000.000000000000227 ) ;
#8980=CARTESIAN_POINT ( 'NONE',  ( 4.958415959904820092, -21.38448066593202768, -40.07378121005077531 ) ) ;
#8982=CARTESIAN_POINT ( 'NONE',  ( 5.894904586330512508, 14.91596325940019341, 13.49234790931016015 ) ) ;
#8985=CARTESIAN_POINT ( 'NONE',  ( 1.157643937452370153, -40.90424016976600541, 9.156713970025162297 ) ) ;
#8989=ADVANCED_FACE ( 'NONE', ( #17078 ), #2650, .F. ) ;
#8990=CARTESIAN_POINT ( 'NONE',  ( 0.5804410086790514622, -46.06497594411302288, -8.805557513507338285 ) ) ;
#8995=CARTESIAN_POINT ( 'NONE',  ( 0.9762797500689124330, 9.222352665238926051, -40.88120590813907285 ) ) ;
#9004=CARTESIAN_POINT ( 'NONE',  ( 5.896782393890504181, -18.51439742298330771, -7.857682542699298445 ) ) ;
#9012=CARTESIAN_POINT ( 'NONE',  ( 0.5837157313716021534, 46.46537190809685569, 6.340841980704805536 ) ) ;
#9014=B_SPLINE_CURVE_WITH_KNOTS ( 'NONE', 3,
 ( #31756, #56463, #13576, #56159, #36471, #22975 ),
 .UNSPECIFIED., .F., .F.,
 ( 4, 2, 4 ),
 ( 5.208685977958202256E-18, 0.0002291459268755725387, 0.0004582918537511398733 ),
 .UNSPECIFIED. ) ;
#9019=ORIENTED_EDGE ( 'NONE', *, *, #42404, .T. ) ;
#9037=CARTESIAN_POINT ( 'NONE',  ( 0.9789233960466703355, -6.840937495575606597, -41.34656335191559862 ) ) ;
#9039=LINE ( 'NONE', #42894, #20173 ) ;
#9045=B_SPLINE_CURVE_WITH_KNOTS ( 'NONE', 3,
 ( #955, #10997, #45143, #40147 ),
 .UNSPECIFIED., .F., .F.,
 ( 4, 4 ),
 ( 1.734723475976807094E-18, 0.004042984057420977162 ),
 .UNSPECIFIED. ) ;
#9046=CARTESIAN_POINT ( 'NONE',  ( 5.895881250540457863, 10.82621851909546606, -16.95053610317665616 ) ) ;
#9049=CARTESIAN_POINT ( 'NONE',  ( 0.6845945791218023269, 11.71498854670038803, 45.42208233959143371 ) ) ;
#9060=EDGE_CURVE ( 'NONE', #25214, #51700, #6297, .T. ) ;
#9061=B_SPLINE_CURVE_WITH_KNOTS ( 'NONE', 3,
 ( #46028, #3066, #36006, #12195, #50380, #2757 ),
 .UNSPECIFIED., .F., .F.,
 ( 4, 2, 4 ),
 ( 7.006328859705253345E-18, 0.0002291472222819953208, 0.0004582944445639836484 ),
 .UNSPECIFIED. ) ;
#9063=EDGE_CURVE ( 'NONE', #23007, #8551, #28748, .T. ) ;
#9068=ADVANCED_FACE ( 'NONE', ( #14539 ), #47502, .F. ) ;
#9070=( BOUNDED_SURFACE ( )  B_SPLINE_SURFACE ( 3, 1, ( 
 ( #9734, #43278 ),
 ( #33562, #57026 ),
 ( #61710, #23223 ),
 ( #32948, #14453 ) ),
 .UNSPECIFIED., .F., .F., .F. ) 
 B_SPLINE_SURFACE_WITH_KNOTS ( ( 4, 4 ),
 ( 2, 2 ),
 ( 0.000000000000000000, 1.000000000000000000 ),
 ( 0.000000000000000000, 1.000000000000000000 ),
 .UNSPECIFIED. ) 
 GEOMETRIC_REPRESENTATION_ITEM ( )  RATIONAL_B_SPLINE_SURFACE ( (
 ( 1.000000000000000000, 1.000000000000000000),
 ( 0.9952954269826590483, 0.8620686068821339365),
 ( 0.9952954269826590483, 0.8620686068821339365),
 ( 1.000000000000000000, 1.000000000000000000) ) ) 
 REPRESENTATION_ITEM ( '' )  SURFACE ( )  );
#9078=CARTESIAN_POINT ( 'NONE',  ( 0.9762797500689124330, 28.76866969767982951, 30.47438972336447804 ) ) ;
#9080=ADVANCED_FACE ( 'NONE', ( #14234 ), #25906, .F. ) ;
#9082=DIRECTION ( 'NONE',  ( -1.000000000000000000, -0.000000000000000000, -0.000000000000000000 ) ) ;
#9091=FACE_OUTER_BOUND ( 'NONE', #17758, .T. ) ;
#9093=B_SPLINE_CURVE_WITH_KNOTS ( 'NONE', 3,
 ( #50187, #45510, #46431, #2560, #55485, #21681, #40824, #8187, #12612, #31705, #60802, #3476, #46129, #50794, #17000, #3175 ),
 .UNSPECIFIED., .F., .F.,
 ( 4, 3, 3, 3, 3, 4 ),
 ( 1.250973872328959318E-17, 0.0002732102107931876143, 0.0004098135523333815882, 0.0005464168938824977327, 0.0008195847345945442026, 0.001092771384553106132 ),
 .UNSPECIFIED. ) ;
#9095=CARTESIAN_POINT ( 'NONE',  ( 3.782542959838397056, -5.285775259587299324, -41.70489699425842645 ) ) ;
#9096=CARTESIAN_POINT ( 'NONE',  ( 0.5824935313925956315, -46.02748767734610880, -8.983794029561840588 ) ) ;
#9108=ADVANCED_FACE ( 'NONE', ( #19854 ), #34217, .F. ) ;
#9109=DIRECTION ( 'NONE',  ( -1.000000000000000000, -0.000000000000000000, -0.000000000000000000 ) ) ;
#9113=ORIENTED_EDGE ( 'NONE', *, *, #15254, .F. ) ;
#9115=CARTESIAN_POINT ( 'NONE',  ( 5.895881250540457863, 20.06826253866637444, -1.338850360369210568 ) ) ;
#9124=CARTESIAN_POINT ( 'NONE',  ( 0.5824935313925970748, 43.03132588641753387, -18.64250974281010897 ) ) ;
#9134=EDGE_CURVE ( 'NONE', #2574, #17781, #17598, .T. ) ;
#9139=CARTESIAN_POINT ( 'NONE',  ( 0.8554163680231708922, -26.01084021241273092, 39.04666009476548538 ) ) ;
#9149=CARTESIAN_POINT ( 'NONE',  ( 4.962356264823608143, 0.000000000000000000, 0.000000000000000000 ) ) ;
#9150=CARTESIAN_POINT ( 'NONE',  ( 0.5804410086790514622, 46.40460073163232835, -6.792119168064279400 ) ) ;
#9154=ADVANCED_FACE ( 'NONE', ( #20766 ), #40639, .F. ) ;
#9158=CARTESIAN_POINT ( 'NONE',  ( 0.5806925824938502512, 43.38503874128546300, 17.80339225430713057 ) ) ;
#9160=CARTESIAN_POINT ( 'NONE',  ( 5.896278296736517710, -18.51475911848199374, 7.856887067978758132 ) ) ;
#9170=ORIENTED_EDGE ( 'NONE', *, *, #2966, .T. ) ;
#9184=CARTESIAN_POINT ( 'NONE',  ( 0.9785694773339257413, -39.66226175059299663, 13.53663172809687332 ) ) ;
#9191=ORIENTED_EDGE ( 'NONE', *, *, #54584, .F. ) ;
#9197=DIRECTION ( 'NONE',  ( 0.000000000000000000, 0.000000000000000000, 1.000000000000000000 ) ) ;
#9202=AXIS2_PLACEMENT_3D ( 'NONE', #32772, #8949, #3000 ) ;
#9203=CARTESIAN_POINT ( 'NONE',  ( 0.5837800005270550319, 36.80393597436502517, -29.06381866576765205 ) ) ;
#9205=CARTESIAN_POINT ( 'NONE',  ( 0.5806925824938499181, -42.09901922557445175, 20.66143612114793626 ) ) ;
#9206=CARTESIAN_POINT ( 'NONE',  ( -69.95594261585601714, 0.000000000000000000, 0.000000000000000000 ) ) ;
#9217=CARTESIAN_POINT ( 'NONE',  ( 3.238018933889920792, 13.39148516828231372, -0.2749861002446565839 ) ) ;
#9226=CARTESIAN_POINT ( 'NONE',  ( 3.238018933889920792, -9.747366695765240507, -9.186747785040122238 ) ) ;
#9227=CARTESIAN_POINT ( 'NONE',  ( 4.956445790444029775, 25.79263028817611314, -39.39896284113449809 ) ) ;
#9228=DIRECTION ( 'NONE',  ( 0.000000000000000000, 0.000000000000000000, 1.000000000000000000 ) ) ;
#9240=VERTEX_POINT ( 'NONE', #3184 ) ;
#9245=ORIENTED_EDGE ( 'NONE', *, *, #48043, .T. ) ;
#9247=LINE ( 'NONE', #47479, #4296 ) ;
#9250=EDGE_CURVE ( 'NONE', #56285, #10350, #54176, .T. ) ;
#9251=FACE_OUTER_BOUND ( 'NONE', #6060, .T. ) ;
#9252=B_SPLINE_CURVE_WITH_KNOTS ( 'NONE', 3,
 ( #25301, #15613, #44448, #5857, #20310, #30002 ),
 .UNSPECIFIED., .F., .F.,
 ( 4, 2, 4 ),
 ( 6.938893903907228378E-18, 0.0002291472222819913905, 0.0004582944445639758422 ),
 .UNSPECIFIED. ) ;
#9253=EDGE_CURVE ( 'NONE', #37333, #59587, #19057, .T. ) ;
#9255=B_SPLINE_CURVE_WITH_KNOTS ( 'NONE', 3,
 ( #3965, #50972, #18409, #13714, #12796, #61289, #36915, #23104, #18096, #37215, #41921, #37527, #55356, #51580, #7749, #60359, #32823, #12479, #55980 ),
 .UNSPECIFIED., .F., .F.,
 ( 4, 3, 3, 3, 3, 3, 4 ),
 ( 3.469446951953614189E-18, 0.0002732106629380679072, 0.0004098138914053798230, 0.0005464171197651472318, 0.0006830203481512555491, 0.0008196235766963701382, 0.001011968216111141161 ),
 .UNSPECIFIED. ) ;
#9259=CARTESIAN_POINT ( 'NONE',  ( 4.960386119450142850, -34.04466635746601355, 27.48448939458694795 ) ) ;
#9261=EDGE_LOOP ( 'NONE', ( #5893, #39349, #34028, #50319 ) ) ;
#9262=CARTESIAN_POINT ( 'NONE',  ( 0.9769922540276048117, -37.20286211167621104, -19.29452268872523391 ) ) ;
#9264=EDGE_CURVE ( 'NONE', #26111, #22599, #13837, .T. ) ;
#9274=EDGE_LOOP ( 'NONE', ( #932, #8885, #18791, #61113 ) ) ;
#9276=CARTESIAN_POINT ( 'NONE',  ( 4.962356264823608143, -41.65024625884313991, -6.040909239515997342 ) ) ;
#9278=EDGE_LOOP ( 'NONE', ( #13579, #17920, #7734, #56591 ) ) ;
#9281=CARTESIAN_POINT ( 'NONE',  ( 0.9762797500689124330, -30.73989051779308568, -28.48480149377557424 ) ) ;
#9288=CARTESIAN_POINT ( 'NONE',  ( 4.962356264823608143, 0.000000000000000000, 0.000000000000000000 ) ) ;
#9297=FACE_OUTER_BOUND ( 'NONE', #14210, .T. ) ;
#9298=CARTESIAN_POINT ( 'NONE',  ( 0.8554163680231738898, -34.17638377241206626, -32.14312158693720534 ) ) ;
#9310=CARTESIAN_POINT ( 'NONE',  ( 0.9790320750461911636, 29.19632847532770015, -30.06512158802884471 ) ) ;
#9312=ORIENTED_EDGE ( 'NONE', *, *, #34332, .F. ) ;
#9315=CARTESIAN_POINT ( 'NONE',  ( 0.9762797500689124330, -17.18051571332090788, -38.22505284509149703 ) ) ;
#9324=B_SPLINE_CURVE_WITH_KNOTS ( 'NONE', 3,
 ( #31028, #11950, #35751, #49510 ),
 .UNSPECIFIED., .F., .F.,
 ( 4, 4 ),
 ( 1.301042606982605128E-18, 0.004446298630425103184 ),
 .UNSPECIFIED. ) ;
#9326=B_SPLINE_CURVE_WITH_KNOTS ( 'NONE', 3,
 ( #52637, #56715, #18525, #19159 ),
 .UNSPECIFIED., .F., .F.,
 ( 4, 4 ),
 ( 0.000000000000000000, 0.005004948556313811373 ),
 .UNSPECIFIED. ) ;
#9337=CARTESIAN_POINT ( 'NONE',  ( 4.956445790444004018, -47.08764048036452721, 0.5405220916596411573 ) ) ;
#9340=DIRECTION ( 'NONE',  ( -0.07500201931887527651, -0.8296863770785034564, -0.5531683403706671998 ) ) ;
#9345=CARTESIAN_POINT ( 'NONE',  ( 0.9787464366903561030, -6.796004491807877024, -41.35393954435043895 ) ) ;
#9346=EDGE_CURVE ( 'NONE', #56041, #41141, #34520, .T. ) ;
#9347=ORIENTED_EDGE ( 'NONE', *, *, #16371, .F. ) ;
#9353=CARTESIAN_POINT ( 'NONE',  ( 3.661921753701995907, 46.83251652495474104, 4.398467889376776796 ) ) ;
#9357=CARTESIAN_POINT ( 'NONE',  ( 5.895596859100789899, -19.39731145114851074, 5.317188324634581242 ) ) ;
#9364=CARTESIAN_POINT ( 'NONE',  ( 4.962356264823603702, 17.31942680647464528, -38.35717733303005161 ) ) ;
#9366=ORIENTED_EDGE ( 'NONE', *, *, #1777, .T. ) ;
#9381=EDGE_CURVE ( 'NONE', #44630, #5475, #48223, .T. ) ;
#9384=DIRECTION ( 'NONE',  ( 0.000000000000000000, 0.000000000000000000, 1.000000000000000000 ) ) ;
#9385=EDGE_CURVE ( 'NONE', #58158, #789, #19783, .T. ) ;
#9386=ADVANCED_FACE ( 'NONE', ( #47973 ), #40758, .F. ) ;
#9396=ORIENTED_EDGE ( 'NONE', *, *, #58464, .F. ) ;
#9400=EDGE_CURVE ( 'NONE', #54025, #59710, #40038, .T. ) ;
#9401=VERTEX_POINT ( 'NONE', #57636 ) ;
#9402=CARTESIAN_POINT ( 'NONE',  ( 4.960386119450149955, -34.62801484853867606, 26.74578569273533901 ) ) ;
#9410=CARTESIAN_POINT ( 'NONE',  ( 0.5804410086790514622, -14.41595396256475325, 44.62846763227043567 ) ) ;
#9415=( BOUNDED_SURFACE ( )  B_SPLINE_SURFACE ( 3, 1, ( 
 ( #51436, #42391 ),
 ( #43010, #14493 ),
 ( #33602, #61146 ),
 ( #13564, #56757 ) ),
 .UNSPECIFIED., .F., .F., .F. ) 
 B_SPLINE_SURFACE_WITH_KNOTS ( ( 4, 4 ),
 ( 2, 2 ),
 ( 0.000000000000000000, 1.000000000000000000 ),
 ( 0.000000000000000000, 1.000000000000000000 ),
 .UNSPECIFIED. ) 
 GEOMETRIC_REPRESENTATION_ITEM ( )  RATIONAL_B_SPLINE_SURFACE ( (
 ( 1.000000000000000000, 1.000000000000000000),
 ( 0.9952954269826590483, 0.8620686068821339365),
 ( 0.9952954269826590483, 0.8620686068821339365),
 ( 1.000000000000000000, 1.000000000000000000) ) ) 
 REPRESENTATION_ITEM ( '' )  SURFACE ( )  );
#9418=ORIENTED_EDGE ( 'NONE', *, *, #24178, .T. ) ;
#9420=CARTESIAN_POINT ( 'NONE',  ( 5.896782393890504181, -9.671431223051156323, 17.63489452692596515 ) ) ;
#9422=CARTESIAN_POINT ( 'NONE',  ( 0.5835871038041854364, 16.72726757634624661, 43.81133383418971761 ) ) ;
#9427=CIRCLE ( 'NONE', #42464, 47.09074272231896430 ) ;
#9429=CARTESIAN_POINT ( 'NONE',  ( 0.5837800304671212359, 43.19256532450906860, -18.26580501558905922 ) ) ;
#9430=VERTEX_POINT ( 'NONE', #6243 ) ;
#9431=CARTESIAN_POINT ( 'NONE',  ( 0.9762797500689124330, 25.26481495167865532, 33.43671500974846822 ) ) ;
#9434=CARTESIAN_POINT ( 'NONE',  ( 0.5832655196449147983, 4.467535350384531867, 46.68271961728872554 ) ) ;
#9437=CARTESIAN_POINT ( 'NONE',  ( 0.9788927965476029724, -22.66962964973810202, -35.24804255806969877 ) ) ;
#9439=DIRECTION ( 'NONE',  ( 0.000000000000000000, 0.000000000000000000, 1.000000000000000000 ) ) ;
#9445=B_SPLINE_CURVE_WITH_KNOTS ( 'NONE', 3,
 ( #47028, #13201, #42633, #57009, #37953, #56695, #37634, #23503, #18206, #18826, #17904, #14135, #33236, #9096, #13825, #42032 ),
 .UNSPECIFIED., .F., .F.,
 ( 4, 3, 3, 3, 3, 4 ),
 ( 1.214354834101861570E-17, 0.0002732102107931916801, 0.0004098135523333818592, 0.0005464168938824978412, 0.0008195847345945461541, 0.001092771384553108084 ),
 .UNSPECIFIED. ) ;
#9449=CARTESIAN_POINT ( 'NONE',  ( 0.9789233960466712237, -12.54205289678194468, 39.98791862508804940 ) ) ;
#9453=CARTESIAN_POINT ( 'NONE',  ( 0.7056313189692727805, 33.20628302271070709, 33.12237026200259749 ) ) ;
#9456=CARTESIAN_POINT ( 'NONE',  ( 0.5848930533535030563, 17.02477461160273009, -43.69702657860927530 ) ) ;
#9460=EDGE_CURVE ( 'NONE', #7089, #4962, #16827, .T. ) ;
#9465=CARTESIAN_POINT ( 'NONE',  ( 4.956445790444006683, -32.34643101787064978, -34.22347806032829709 ) ) ;
#9466=CARTESIAN_POINT ( 'NONE',  ( 0.6064782688330861982, -19.09363116089746271, -42.83418839560724223 ) ) ;
#9479=CARTESIAN_POINT ( 'NONE',  ( 0.6064515330803581517, 28.38734125881933323, 37.32952172600688101 ) ) ;
#9483=ORIENTED_EDGE ( 'NONE', *, *, #60077, .T. ) ;
#9493=ORIENTED_EDGE ( 'NONE', *, *, #59196, .F. ) ;
#9495=ORIENTED_EDGE ( 'NONE', *, *, #44581, .F. ) ;
#9499=CARTESIAN_POINT ( 'NONE',  ( 0.8560838555295223751, 39.88643293834682879, -24.68694597426934223 ) ) ;
#9505=CARTESIAN_POINT ( 'NONE',  ( 0.6064515330803623705, -30.81728595274794813, -35.35009508535515721 ) ) ;
#9506=CIRCLE ( 'NONE', #12530, 42.08604991992415023 ) ;
#9523=CARTESIAN_POINT ( 'NONE',  ( 0.9784957157296361174, 41.90798102287331517, -0.2327736644509323383 ) ) ;
#9539=CARTESIAN_POINT ( 'NONE',  ( 1.157643937452367933, -37.03171704562910094, 19.63808053877000859 ) ) ;
#9540=EDGE_CURVE ( 'NONE', #25579, #7415, #36246, .T. ) ;
#9543=B_SPLINE_CURVE_WITH_KNOTS ( 'NONE', 3,
 ( #22942, #42069, #55813, #61123, #18241, #17618, #27627, #37353, #36745, #18540, #56426, #32030, #37668, #60817, #23541, #15087 ),
 .UNSPECIFIED., .F., .F.,
 ( 4, 3, 3, 3, 3, 4 ),
 ( 1.084256381238943740E-17, 0.0002732102107931889154, 0.0004098135523333797450, 0.0005464168938824980580, 0.0008195847345945433352, 0.001092771384553107867 ),
 .UNSPECIFIED. ) ;
#9550=CARTESIAN_POINT ( 'NONE',  ( 0.5835226383429280572, 22.69696281568404217, 41.03766993250741990 ) ) ;
#9560=CARTESIAN_POINT ( 'NONE',  ( 0.5837800304671192375, 46.89600475158708548, 0.04550295183057281867 ) ) ;
#9565=ORIENTED_EDGE ( 'NONE', *, *, #16783, .F. ) ;
#9569=CARTESIAN_POINT ( 'NONE',  ( 4.956445790443998689, -22.15545010017797622, 41.55326799420426198 ) ) ;
#9570=CARTESIAN_POINT ( 'NONE',  ( 5.896782393890504181, 0.6657210432555761281, 20.10181341000306077 ) ) ;
#9576=CARTESIAN_POINT ( 'NONE',  ( 0.5804410086790514622, -2.113107284889306658, 46.85141011173456604 ) ) ;
#9583=CARTESIAN_POINT ( 'NONE',  ( 4.958415959904820092, -44.94704195038531225, -6.554950322690599407 ) ) ;
#9585=CARTESIAN_POINT ( 'NONE',  ( 3.782542959838393504, 34.03285927320680315, -24.67797283179218226 ) ) ;
#9590=( BOUNDED_SURFACE ( )  B_SPLINE_SURFACE ( 3, 1, ( 
 ( #50403, #21597 ),
 ( #49793, #54155 ),
 ( #36034, #55096 ),
 ( #60398, #50103 ) ),
 .UNSPECIFIED., .F., .F., .F. ) 
 B_SPLINE_SURFACE_WITH_KNOTS ( ( 4, 4 ),
 ( 2, 2 ),
 ( 0.000000000000000000, 1.000000000000000000 ),
 ( 0.000000000000000000, 1.000000000000000000 ),
 .UNSPECIFIED. ) 
 GEOMETRIC_REPRESENTATION_ITEM ( )  RATIONAL_B_SPLINE_SURFACE ( (
 ( 1.000000000000000000, 1.000000000000000000),
 ( 0.7282232189291694135, 0.9929344683865672927),
 ( 0.7282232189291694135, 0.9929344683865672927),
 ( 1.000000000000000000, 1.000000000000000000) ) ) 
 REPRESENTATION_ITEM ( '' )  SURFACE ( )  );
#9591=CARTESIAN_POINT ( 'NONE',  ( 3.238018933889920792, 12.22151767825363500, 5.481058110236275205 ) ) ;
#9600=CIRCLE ( 'NONE', #47619, 47.09074272231896430 ) ;
#9601=CARTESIAN_POINT ( 'NONE',  ( 3.661921753702004789, -28.90718528634099371, 37.10802827765424894 ) ) ;
#9604=CIRCLE ( 'NONE', #48512, 47.09074272231896430 ) ;
#9607=CARTESIAN_POINT ( 'NONE',  ( 0.7764139734771253742, -6.921054633042174054, -46.39115727887494955 ) ) ;
#9616=B_SPLINE_CURVE_WITH_KNOTS ( 'NONE', 3,
 ( #23259, #32358, #18562, #51130 ),
 .UNSPECIFIED., .F., .F.,
 ( 4, 4 ),
 ( 4.336808689942017736E-19, 0.004041751736740987339 ),
 .UNSPECIFIED. ) ;
#9623=CARTESIAN_POINT ( 'NONE',  ( 1.000110580585052533, -2.057808565348302032, 41.85908392070087558 ) ) ;
#9636=B_SPLINE_CURVE_WITH_KNOTS ( 'NONE', 3,
 ( #4548, #17759, #61871, #55954 ),
 .UNSPECIFIED., .F., .F.,
 ( 4, 4 ),
 ( 0.000000000000000000, 0.004447772540403829335 ),
 .UNSPECIFIED. ) ;
#9637=LINE ( 'NONE', #29665, #5518 ) ;
#9638=CARTESIAN_POINT ( 'NONE',  ( 0.5824936645240094135, -24.92615255297814514, -39.72310534117351466 ) ) ;
#9649=CARTESIAN_POINT ( 'NONE',  ( 4.291220156522059348, 47.06111669607643933, 2.154133845417246729 ) ) ;
#9653=CARTESIAN_POINT ( 'NONE',  ( 0.9785694773339252972, -6.751071488010489396, -41.36131573679015361 ) ) ;
#9655=CARTESIAN_POINT ( 'NONE',  ( 0.5806925824938502512, -7.260877859417425029, 46.33035738103242096 ) ) ;
#9657=EDGE_LOOP ( 'NONE', ( #39247, #52628, #38757, #31554 ) ) ;
#9662=CARTESIAN_POINT ( 'NONE',  ( 0.8560838555295223751, 46.60258007729417784, 5.345312359546021241 ) ) ;
#9664=ORIENTED_EDGE ( 'NONE', *, *, #34726, .T. ) ;
#9665=CARTESIAN_POINT ( 'NONE',  ( 5.895596859100789899, -4.659086063545737844, -19.56581458219824299 ) ) ;
#9670=B_SPLINE_CURVE_WITH_KNOTS ( 'NONE', 3,
 ( #37007, #50752, #13489, #8155 ),
 .UNSPECIFIED., .F., .F.,
 ( 4, 4 ),
 ( 1.951563910473907981E-18, 0.004041751736740987339 ),
 .UNSPECIFIED. ) ;
#9679=DIRECTION ( 'NONE',  ( -1.000000000000000000, -0.000000000000000000, -0.000000000000000000 ) ) ;
#9690=( BOUNDED_SURFACE ( )  B_SPLINE_SURFACE ( 3, 1, ( 
 ( #7919, #41773 ),
 ( #17636, #56444 ),
 ( #27336, #3821 ),
 ( #13557, #47370 ) ),
 .UNSPECIFIED., .F., .F., .F. ) 
 B_SPLINE_SURFACE_WITH_KNOTS ( ( 4, 4 ),
 ( 2, 2 ),
 ( 0.000000000000000000, 1.000000000000000000 ),
 ( 0.000000000000000000, 1.000000000000000000 ),
 .UNSPECIFIED. ) 
 GEOMETRIC_REPRESENTATION_ITEM ( )  RATIONAL_B_SPLINE_SURFACE ( (
 ( 1.000000000000000000, 1.000000000000000000),
 ( 0.9952954269826590483, 0.8620686068821307169),
 ( 0.9952954269826590483, 0.8620686068821307169),
 ( 1.000000000000000000, 1.000000000000000000) ) ) 
 REPRESENTATION_ITEM ( '' )  SURFACE ( )  );
#9691=CARTESIAN_POINT ( 'NONE',  ( 5.896278296736517710, 3.350760724586565154, -19.83177708075985279 ) ) ;
#9696=EDGE_CURVE ( 'NONE', #5968, #46746, #45129, .T. ) ;
#9703=CARTESIAN_POINT ( 'NONE',  ( 4.962356264823608143, -29.56943756613123497, 29.94802096775367772 ) ) ;
#9721=ORIENTED_EDGE ( 'NONE', *, *, #4864, .T. ) ;
#9724=ORIENTED_EDGE ( 'NONE', *, *, #59905, .T. ) ;
#9731=VECTOR ( 'NONE', #57617, 1000.000000000000000 ) ;
#9734=CARTESIAN_POINT ( 'NONE',  ( 5.895596859100789899, -19.93390588528919949, -2.677233529022096992 ) ) ;
#9735=AXIS2_PLACEMENT_3D ( 'NONE', #42965, #9109, #57313 ) ;
#9736=CARTESIAN_POINT ( 'NONE',  ( 0.5824936645240106348, 16.51438908705373265, 43.89206229059765008 ) ) ;
#9741=CARTESIAN_POINT ( 'NONE',  ( 0.8560838555295223751, 46.35895890951135812, -7.156798369939577853 ) ) ;
#9742=EDGE_CURVE ( 'NONE', #21941, #5232, #9506, .T. ) ;
#9744=CARTESIAN_POINT ( 'NONE',  ( 1.000433927950265423, 25.38714267670817293, 33.34533946993654752 ) ) ;
#9747=CARTESIAN_POINT ( 'NONE',  ( 0.5817217712918344441, 4.240847850817598186, 46.70385598122052784 ) ) ;
#9749=EDGE_CURVE ( 'NONE', #26754, #37717, #25681, .T. ) ;
#9758=LINE ( 'NONE', #5038, #18868 ) ;
#9761=AXIS2_PLACEMENT_3D ( 'NONE', #41863, #60931, #18043 ) ;
#9763=CARTESIAN_POINT ( 'NONE',  ( 0.9790320750461907195, -12.49859903051836696, 40.00152690606341821 ) ) ;
#9774=CARTESIAN_POINT ( 'NONE',  ( 0.5837800304671210139, 45.24177268675465768, -12.34582262708807754 ) ) ;
#9775=CARTESIAN_POINT ( 'NONE',  ( 3.661933894777869014, 15.13536249802464262, 44.53708529983796183 ) ) ;
#9781=CONICAL_SURFACE ( 'NONE', #61622, 42.08604991992415023, 1.569615340895231137 ) ;
#9787=( BOUNDED_SURFACE ( )  B_SPLINE_SURFACE ( 3, 1, ( 
 ( #13622, #51809 ),
 ( #43369, #8908 ),
 ( #23322, #47138 ),
 ( #42749, #4181 ) ),
 .UNSPECIFIED., .F., .F., .F. ) 
 B_SPLINE_SURFACE_WITH_KNOTS ( ( 4, 4 ),
 ( 2, 2 ),
 ( 0.000000000000000000, 1.000000000000000000 ),
 ( 0.000000000000000000, 1.000000000000000000 ),
 .UNSPECIFIED. ) 
 GEOMETRIC_REPRESENTATION_ITEM ( )  RATIONAL_B_SPLINE_SURFACE ( (
 ( 1.000000000000000000, 1.000000000000000000),
 ( 0.9952954269826590483, 0.8620686068821339365),
 ( 0.9952954269826590483, 0.8620686068821339365),
 ( 1.000000000000000000, 1.000000000000000000) ) ) 
 REPRESENTATION_ITEM ( '' )  SURFACE ( )  );
#9793=CARTESIAN_POINT ( 'NONE',  ( 0.9762797500689124330, -41.84568905980458453, 2.294143041716202092 ) ) ;
#9794=ORIENTED_EDGE ( 'NONE', *, *, #16249, .F. ) ;
#9795=EDGE_LOOP ( 'NONE', ( #30879, #24084, #1625, #110 ) ) ;
#9803=CARTESIAN_POINT ( 'NONE',  ( 4.962356264823608143, 0.000000000000000000, 0.000000000000000000 ) ) ;
#9804=B_SPLINE_CURVE_WITH_KNOTS ( 'NONE', 3,
 ( #8605, #27734, #13645, #7676 ),
 .UNSPECIFIED., .F., .F.,
 ( 4, 4 ),
 ( 3.954366397011470641E-18, 0.004042984057420973693 ),
 .UNSPECIFIED. ) ;
#9805=CARTESIAN_POINT ( 'NONE',  ( 0.9780303403264770656, -39.48244899217856840, 14.05260954325215472 ) ) ;
#9808=VERTEX_POINT ( 'NONE', #21856 ) ;
#9809=EDGE_CURVE ( 'NONE', #50058, #26084, #40680, .T. ) ;
#9816=EDGE_CURVE ( 'NONE', #23687, #10199, #35665, .T. ) ;
#9821=CARTESIAN_POINT ( 'NONE',  ( 5.910764540655178756, 10.83508461757070229, 16.94408981914477863 ) ) ;
#9833=CARTESIAN_POINT ( 'NONE',  ( 3.661921753702002569, -31.78300939732352859, -34.67666993071396320 ) ) ;
#9855=B_SPLINE_CURVE_WITH_KNOTS ( 'NONE', 3,
 ( #36017, #11577, #16267, #41034 ),
 .UNSPECIFIED., .F., .F.,
 ( 4, 4 ),
 ( 3.469446951953614189E-18, 0.004042984057420975427 ),
 .UNSPECIFIED. ) ;
#9866=CARTESIAN_POINT ( 'NONE',  ( 5.896782393890504181, 19.70854070425251692, -4.012419492878830596 ) ) ;
#9867=CARTESIAN_POINT ( 'NONE',  ( 0.5824935313925952984, -7.440769710676105042, 46.30197752976132364 ) ) ;
#9872=CARTESIAN_POINT ( 'NONE',  ( 0.5837800005270550319, 22.53739213693909704, 41.12543269447289163 ) ) ;
#9875=ORIENTED_EDGE ( 'NONE', *, *, #55439, .F. ) ;
#9879=CIRCLE ( 'NONE', #2881, 47.09074272231896430 ) ;
#9881=CARTESIAN_POINT ( 'NONE',  ( 0.5837157313716013762, 16.93971847026775279, -43.72965814787597338 ) ) ;
#9882=CARTESIAN_POINT ( 'NONE',  ( 0.6845945791218023269, -35.36481895536415720, -30.81778870990359209 ) ) ;
#9895=CARTESIAN_POINT ( 'NONE',  ( 4.962356264823597485, -9.332162870646813602, 41.03835198954837438 ) ) ;
#9898=ORIENTED_EDGE ( 'NONE', *, *, #30008, .T. ) ;
#9908=VERTEX_POINT ( 'NONE', #55969 ) ;
#9909=CARTESIAN_POINT ( 'NONE',  ( 0.8560838555295158248, -44.00447048317951726, -16.24744323198929052 ) ) ;
#9913=CARTESIAN_POINT ( 'NONE',  ( 5.896278296736517710, -17.30234040492943492, 10.25455977242953409 ) ) ;
#9915=CARTESIAN_POINT ( 'NONE',  ( 0.6845945791218034371, 27.12315006394041816, 38.27193817045215241 ) ) ;
#9918=VERTEX_POINT ( 'NONE', #31252 ) ;
#9919=DIRECTION ( 'NONE',  ( 0.07906939808003035641, -0.9145849808368756717, -0.3965883799544224764 ) ) ;
#9920=CARTESIAN_POINT ( 'NONE',  ( 5.838029081930957709, 19.86434078294020011, -42.85408992630853220 ) ) ;
#9923=DIRECTION ( 'NONE',  ( -0.07906939808003035641, 0.7873210066865946599, 0.6114520935586604811 ) ) ;
#9925=CARTESIAN_POINT ( 'NONE',  ( 0.8560838555295223751, -24.46533024579953164, 40.02274915651970133 ) ) ;
#9928=CARTESIAN_POINT ( 'NONE',  ( 5.895881250540457863, 19.70893872444546702, 4.010662783674901810 ) ) ;
#9931=AXIS2_PLACEMENT_3D ( 'NONE', #46411, #56088, #42336 ) ;
#9945=VERTEX_POINT ( 'NONE', #33428 ) ;
#9947=CARTESIAN_POINT ( 'NONE',  ( 1.231276596079887264, 28.52807286890788419, -30.71523773966838888 ) ) ;
#9952=CARTESIAN_POINT ( 'NONE',  ( 0.5804410086790514622, 27.37779091617001370, -38.07855586029853612 ) ) ;
#9956=CARTESIAN_POINT ( 'NONE',  ( 4.956445790443988919, 44.65954324082213134, 14.93530206124989945 ) ) ;
#9960=CARTESIAN_POINT ( 'NONE',  ( 0.8554163680231816613, 5.604726001788831624, 46.58103175710786559 ) ) ;
#9967=CIRCLE ( 'NONE', #19997, 42.08604991992415023 ) ;
#9976=CARTESIAN_POINT ( 'NONE',  ( 0.9769922540276037015, -6.534541844522391507, -41.39603021991737819 ) ) ;
#9978=( BOUNDED_SURFACE ( )  B_SPLINE_SURFACE ( 3, 1, ( 
 ( #27228, #35411 ),
 ( #40428, #41053 ),
 ( #16601, #2786 ),
 ( #60115, #22228 ) ),
 .UNSPECIFIED., .F., .F., .F. ) 
 B_SPLINE_SURFACE_WITH_KNOTS ( ( 4, 4 ),
 ( 2, 2 ),
 ( 0.000000000000000000, 1.000000000000000000 ),
 ( 0.000000000000000000, 1.000000000000000000 ),
 .UNSPECIFIED. ) 
 GEOMETRIC_REPRESENTATION_ITEM ( )  RATIONAL_B_SPLINE_SURFACE ( (
 ( 1.000000000000000000, 1.000000000000000000),
 ( 0.9952954269826590483, 0.8620686068821307169),
 ( 0.9952954269826590483, 0.8620686068821307169),
 ( 1.000000000000000000, 1.000000000000000000) ) ) 
 REPRESENTATION_ITEM ( '' )  SURFACE ( )  );
#9980=FACE_OUTER_BOUND ( 'NONE', #60697, .T. ) ;
#9982=EDGE_CURVE ( 'NONE', #7415, #29994, #46918, .T. ) ;
#9992=ADVANCED_FACE ( 'NONE', ( #3954 ), #56495, .T. ) ;
#9993=CARTESIAN_POINT ( 'NONE',  ( 5.917102823773431552, 12.97825203069059974, -15.36407147469762613 ) ) ;
#10007=CARTESIAN_POINT ( 'NONE',  ( 0.9762797500689124330, -40.96497924994823592, 8.842808390834631993 ) ) ;
#10011=CARTESIAN_POINT ( 'NONE',  ( 4.962356264823608143, 1.841560470688809792, -42.04574000888963781 ) ) ;
#10014=CARTESIAN_POINT ( 'NONE',  ( 1.000110580585050979, -39.80167790415918461, 13.12417307053917170 ) ) ;
#10016=CARTESIAN_POINT ( 'NONE',  ( 0.5804410086790514622, -46.75463715370012352, -3.677466040800478453 ) ) ;
#10031=CARTESIAN_POINT ( 'NONE',  ( 5.894904586330512508, 19.00045333391160085, -6.596376669618728705 ) ) ;
#10039=LINE ( 'NONE', #29138, #45624 ) ;
#10045=VERTEX_POINT ( 'NONE', #14018 ) ;
#10052=EDGE_LOOP ( 'NONE', ( #14699, #12061, #30892, #46964 ) ) ;
#10058=CARTESIAN_POINT ( 'NONE',  ( 5.894904586330512508, 0.6732998044288336370, -20.10164369983208488 ) ) ;
#10061=CARTESIAN_POINT ( 'NONE',  ( 4.962356264823608143, 26.83784316460287300, 32.41860225448540689 ) ) ;
#10065=CARTESIAN_POINT ( 'NONE',  ( 0.9784957157296378938, 40.35745815350055921, -11.29639891207905578 ) ) ;
#10067=CARTESIAN_POINT ( 'NONE',  ( 0.5837799406558246140, 4.784718297332236858, 46.65136675803160671 ) ) ;
#10072=EDGE_CURVE ( 'NONE', #15708, #48962, #27830, .T. ) ;
#10074=CARTESIAN_POINT ( 'NONE',  ( 5.901463166500146684, 0.6865185226677115171, 20.10090949829561424 ) ) ;
#10075=EDGE_CURVE ( 'NONE', #60616, #47712, #45903, .T. ) ;
#10084=( BOUNDED_SURFACE ( )  B_SPLINE_SURFACE ( 3, 1, ( 
 ( #44674, #35269 ),
 ( #54327, #15539 ),
 ( #49041, #10218 ),
 ( #11450, #29314 ) ),
 .UNSPECIFIED., .F., .F., .F. ) 
 B_SPLINE_SURFACE_WITH_KNOTS ( ( 4, 4 ),
 ( 2, 2 ),
 ( 0.000000000000000000, 1.000000000000000000 ),
 ( 0.000000000000000000, 1.000000000000000000 ),
 .UNSPECIFIED. ) 
 GEOMETRIC_REPRESENTATION_ITEM ( )  RATIONAL_B_SPLINE_SURFACE ( (
 ( 1.000000000000000000, 1.000000000000000000),
 ( 0.9729067724841187204, 0.9999501103223794596),
 ( 0.9729067724841187204, 0.9999501103223794596),
 ( 1.000000000000000000, 1.000000000000000000) ) ) 
 REPRESENTATION_ITEM ( '' )  SURFACE ( )  );
#10088=CARTESIAN_POINT ( 'NONE',  ( 0.5837800304671232343, -1.612506461858141060, 46.86829584153834816 ) ) ;
#10090=EDGE_CURVE ( 'NONE', #22979, #56285, #25238, .T. ) ;
#10092=CARTESIAN_POINT ( 'NONE',  ( 3.376099380956838925, -9.001307264898121829, 9.934024922203457564 ) ) ;
#10096=CARTESIAN_POINT ( 'NONE',  ( 0.5848930533535030563, 46.89605428954452293, 0.1821385726608843458 ) ) ;
#10101=ORIENTED_EDGE ( 'NONE', *, *, #29151, .T. ) ;
#10104=VERTEX_POINT ( 'NONE', #15543 ) ;
#10108=LINE ( 'NONE', #35166, #36766 ) ;
#10116=B_SPLINE_CURVE_WITH_KNOTS ( 'NONE', 3,
 ( #39101, #38178, #48780, #33467, #28432, #18749, #58159, #42559, #37877, #14057, #52543, #33155, #52232, #24053, #38795, #47559 ),
 .UNSPECIFIED., .F., .F.,
 ( 4, 3, 3, 3, 3, 4 ),
 ( 1.551621725782133898E-17, 0.0002732102107931851749, 0.0004098135523333776308, 0.0005464168938824964317, 0.0008195847345945365047, 0.001092771384553102880 ),
 .UNSPECIFIED. ) ;
#10117=CARTESIAN_POINT ( 'NONE',  ( 5.838029081930957709, 25.39899213859872518, -39.82406629785964469 ) ) ;
#10121=EDGE_LOOP ( 'NONE', ( #20530, #10196, #50993, #52557, #32679, #57552, #32238, #18922, #31162, #5515, #28779, #7040, #16061, #39516, #12381, #892, #8475, #57619, #40887, #17367, #45366, #17162, #14829, #44888, #29046, #21353, #46871, #33117, #56025, #60786, #39179, #27041, #32875, #8452, #9724, #22997, #20294, #57475, #34657, #22056, #26990, #40291, #23243, #49799, #52378, #33926, #50535, #61573, #43964, #15493, #50774, #2334, #45456, #3113, #58921, #22687, #48529, #25775, #53297, #16349, #22174, #23505, #29927, #6844, #3789, #25384, #52643, #388, #30696, #39945, #11914, #29752, #1675, #48051, #34599, #23050, #6, #40947, #25187, #17279, #46661, #44059, #31070, #26808, #4514, #5250, #29197, #25192, #290, #17293, #8332, #24817, #4142, #48113, #24779, #56533, #12315, #41899, #59418, #40482, #10269, #38616, #12888, #32500, #52773, #45873, #47513, #60475, #38019, #3252, #18936, #151, #54369, #27591, #8813, #10101, #40568, #52176, #12012, #1555, #36797, #23452, #14601, #48080, #50479, #58177, #28215, #46354, #3523, #8965, #8715, #32894, #24230, #7851, #6773, #29698, #49850, #59079, #43816, #43458, #34760, #57446, #58192, #34465, #11652, #9898 ) ) ;
#10125=CARTESIAN_POINT ( 'NONE',  ( 0.7056313189692698939, 39.91795815694759142, -24.62326665042111529 ) ) ;
#10127=ORIENTED_EDGE ( 'NONE', *, *, #38525, .T. ) ;
#10130=ADVANCED_FACE ( 'NONE', ( #20547 ), #53875, .F. ) ;
#10131=CARTESIAN_POINT ( 'NONE',  ( 0.5835226383429302777, 36.69085443737677110, -29.20656904193287673 ) ) ;
#10133=ORIENTED_EDGE ( 'NONE', *, *, #14726, .T. ) ;
#10137=CARTESIAN_POINT ( 'NONE',  ( 1.231276596079881047, 33.41651732065586344, -25.31033664684003170 ) ) ;
#10144=CARTESIAN_POINT ( 'NONE',  ( 0.5804410086790514622, 27.37779091617000304, -38.07855586029853612 ) ) ;
#10145=CARTESIAN_POINT ( 'NONE',  ( 0.5848930533535030563, -44.24150702629536624, -15.55513222154723429 ) ) ;
#10154=ORIENTED_EDGE ( 'NONE', *, *, #31991, .F. ) ;
#10158=LINE ( 'NONE', #9226, #43090 ) ;
#10173=CARTESIAN_POINT ( 'NONE',  ( 5.838029081930957709, -46.81003243000947123, 6.315530227493348470 ) ) ;
#10174=CARTESIAN_POINT ( 'NONE',  ( 0.5782707292762423457, 32.08118243870044495, -34.21306895094969036 ) ) ;
#10176=EDGE_CURVE ( 'NONE', #3786, #18314, #15274, .T. ) ;
#10179=CARTESIAN_POINT ( 'NONE',  ( 3.376099380956838925, -2.682194557846333094, 13.13446671874906002 ) ) ;
#10184=CARTESIAN_POINT ( 'NONE',  ( 2.618530812446111078, 26.73752065161024305, 38.66305443964451172 ) ) ;
#10196=ORIENTED_EDGE ( 'NONE', *, *, #20453, .F. ) ;
#10199=VERTEX_POINT ( 'NONE', #3811 ) ;
#10206=CARTESIAN_POINT ( 'NONE',  ( 0.5832655196449147983, 46.50736770247006291, -6.024942519275434449 ) ) ;
#10207=FACE_OUTER_BOUND ( 'NONE', #6923, .T. ) ;
#10209=CARTESIAN_POINT ( 'NONE',  ( 4.960386119450149955, 41.48529788082174719, -13.90706742673764396 ) ) ;
#10211=B_SPLINE_CURVE_WITH_KNOTS ( 'NONE', 3,
 ( #47763, #23950, #43075, #33667, #52749, #28952 ),
 .UNSPECIFIED., .F., .F.,
 ( 4, 2, 4 ),
 ( 1.216356941739949889E-16, 0.0002448718616795908195, 0.0004897437233590599915 ),
 .UNSPECIFIED. ) ;
#10212=ORIENTED_EDGE ( 'NONE', *, *, #33422, .T. ) ;
#10218=CARTESIAN_POINT ( 'NONE',  ( 0.5848930533535030563, -1.384993715959497163, -46.87595198813897923 ) ) ;
#10222=EDGE_CURVE ( 'NONE', #8104, #28949, #8209, .T. ) ;
#10229=CARTESIAN_POINT ( 'NONE',  ( 4.291220156522060236, 47.06111669607644643, -2.154133845417245396 ) ) ;
#10236=CARTESIAN_POINT ( 'NONE',  ( 5.896278296736517710, 19.71091930359935773, 4.000829891582261766 ) ) ;
#10240=B_SPLINE_CURVE_WITH_KNOTS ( 'NONE', 3,
 ( #43741, #150, #15215, #34321 ),
 .UNSPECIFIED., .F., .F.,
 ( 4, 4 ),
 ( 2.168404344971008627E-19, 0.004041751736740995145 ),
 .UNSPECIFIED. ) ;
#10242=CARTESIAN_POINT ( 'NONE',  ( 5.896782393890504181, 20.06749419425502978, 1.349727247095894089 ) ) ;
#10244=B_SPLINE_CURVE_WITH_KNOTS ( 'NONE', 3,
 ( #59164, #25979, #11580, #35395 ),
 .UNSPECIFIED., .F., .F.,
 ( 4, 4 ),
 ( 0.000000000000000000, 0.005004948556313804434 ),
 .UNSPECIFIED. ) ;
#10245=CARTESIAN_POINT ( 'NONE',  ( 0.9762797500689124330, -6.471194619075845367, 41.40589843715202534 ) ) ;
#10247=CARTESIAN_POINT ( 'NONE',  ( 4.956445790444004906, -37.28933980949924631, -28.75835855384189443 ) ) ;
#10251=CARTESIAN_POINT ( 'NONE',  ( 4.956445790443998689, -23.10347171912865250, 41.03373788314999615 ) ) ;
#10257=ADVANCED_FACE ( 'NONE', ( #21469 ), #7785, .T. ) ;
#10262=B_SPLINE_CURVE_WITH_KNOTS ( 'NONE', 3,
 ( #7750, #26873, #46013, #3052, #22177, #41304 ),
 .UNSPECIFIED., .F., .F.,
 ( 4, 2, 4 ),
 ( 9.913782460405889843E-18, 0.0002448709889506571025, 0.0004897419779013042302 ),
 .UNSPECIFIED. ) ;
#10263=CARTESIAN_POINT ( 'NONE',  ( 3.238018933889920792, 12.98832471626931628, 3.272753188433335847 ) ) ;
#10264=EDGE_CURVE ( 'NONE', #45332, #37468, #13550, .T. ) ;
#10269=ORIENTED_EDGE ( 'NONE', *, *, #52661, .T. ) ;
#10282=VERTEX_POINT ( 'NONE', #16787 ) ;
#10296=EDGE_CURVE ( 'NONE', #36573, #23457, #1039, .T. ) ;
#10299=CARTESIAN_POINT ( 'NONE',  ( 0.9780106845699478857, -30.87035316765414450, -28.34347441228304021 ) ) ;
#10302=CARTESIAN_POINT ( 'NONE',  ( 4.958415959904820980, 33.34645430971423963, 30.84182126257750056 ) ) ;
#10303=AXIS2_PLACEMENT_3D ( 'NONE', #49928, #45874, #12051 ) ;
#10311=B_SPLINE_CURVE_WITH_KNOTS ( 'NONE', 3,
 ( #9281, #19019, #13388, #57181, #43135, #47510 ),
 .UNSPECIFIED., .F., .F.,
 ( 4, 2, 4 ),
 ( 4.911328137975851075E-18, 0.0002291459268755708853, 0.0004582918537511368917 ),
 .UNSPECIFIED. ) ;
#10319=CARTESIAN_POINT ( 'NONE',  ( 0.8560838555295223751, -38.14845555156087187, 27.29593693413575295 ) ) ;
#10323=CIRCLE ( 'NONE', #26328, 47.09074272231896430 ) ;
#10327=LINE ( 'NONE', #29423, #30251 ) ;
#10333=CARTESIAN_POINT ( 'NONE',  ( 2.528100132419516033, -30.30928330167931861, 29.04481234869007977 ) ) ;
#10338=CARTESIAN_POINT ( 'NONE',  ( 0.5848930533535030563, 10.69427347779456916, 45.66076649783376951 ) ) ;
#10341=CARTESIAN_POINT ( 'NONE',  ( 0.8554163680231816613, -24.47000373826210051, 40.03029340588521734 ) ) ;
#10343=VERTEX_POINT ( 'NONE', #52662 ) ;
#10350=VERTEX_POINT ( 'NONE', #37 ) ;
#10353=ORIENTED_EDGE ( 'NONE', *, *, #37586, .F. ) ;
#10354=CARTESIAN_POINT ( 'NONE',  ( 0.5804410086790514622, -19.24447200597979801, 42.76879877979338573 ) ) ;
#10356=B_SPLINE_CURVE_WITH_KNOTS ( 'NONE', 3,
 ( #17145, #27149, #31860, #17445 ),
 .UNSPECIFIED., .F., .F.,
 ( 4, 4 ),
 ( 1.734723475976807094E-18, 0.004042984057420977162 ),
 .UNSPECIFIED. ) ;
#10357=ORIENTED_EDGE ( 'NONE', *, *, #10418, .F. ) ;
#10358=CARTESIAN_POINT ( 'NONE',  ( 0.9762797500689124330, 19.69530149098714489, -36.99215976885945167 ) ) ;
#10362=B_SPLINE_CURVE_WITH_KNOTS ( 'NONE', 3,
 ( #29191, #25111, #58924, #16036 ),
 .UNSPECIFIED., .F., .F.,
 ( 4, 4 ),
 ( 1.843143693225357538E-18, 0.004446298630425066754 ),
 .UNSPECIFIED. ) ;
#10367=CARTESIAN_POINT ( 'NONE',  ( 0.5837800005270546988, 32.60172451818726103, -33.70998097124964232 ) ) ;
#10370=CARTESIAN_POINT ( 'NONE',  ( 1.231276596079881935, 3.353048872156085825, 41.78556968953515849 ) ) ;
#10379=CARTESIAN_POINT ( 'NONE',  ( 0.9790850452238872847, 40.40622100481030543, -11.12090978174100542 ) ) ;
#10381=CARTESIAN_POINT ( 'NONE',  ( 0.9775691876210976794, -12.05521307728244373, -40.13733357675007341 ) ) ;
#10400=CARTESIAN_POINT ( 'NONE',  ( 4.956445790444026223, 2.113652668516905031, -47.04328350079857302 ) ) ;
#10402=EDGE_CURVE ( 'NONE', #2702, #45432, #9758, .T. ) ;
#10405=ORIENTED_EDGE ( 'NONE', *, *, #19682, .F. ) ;
#10407=CARTESIAN_POINT ( 'NONE',  ( 0.9789233960466696693, -1.531799179696195834, 41.88066759383647053 ) ) ;
#10415=ORIENTED_EDGE ( 'NONE', *, *, #33199, .F. ) ;
#10418=EDGE_CURVE ( 'NONE', #45083, #58239, #47317, .T. ) ;
#10423=EDGE_CURVE ( 'NONE', #24845, #45260, #37572, .T. ) ;
#10424=ORIENTED_EDGE ( 'NONE', *, *, #38991, .F. ) ;
#10428=CARTESIAN_POINT ( 'NONE',  ( 0.9788927965476030835, -17.76925533521107425, -37.95510739628922892 ) ) ;
#10433=VERTEX_POINT ( 'NONE', #26027 ) ;
#10437=CARTESIAN_POINT ( 'NONE',  ( 0.9785694773339259633, 35.94433939501183772, 21.54854684592147862 ) ) ;
#10438=CARTESIAN_POINT ( 'NONE',  ( 0.6064782688330866423, -0.8565416045440378268, -46.88923952143449725 ) ) ;
#10441=CARTESIAN_POINT ( 'NONE',  ( 1.000110580585050979, 41.44288208944681884, 6.237387826014257897 ) ) ;
#10443=EDGE_CURVE ( 'NONE', #23055, #53844, #30107, .T. ) ;
#10449=CARTESIAN_POINT ( 'NONE',  ( 0.9754292589017203863, 41.90451262005537103, -0.5824851679641472879 ) ) ;
#10450=ORIENTED_EDGE ( 'NONE', *, *, #2958, .T. ) ;
#10454=CARTESIAN_POINT ( 'NONE',  ( 0.9790850452238869517, 15.01504043229814833, -39.12653691651804166 ) ) ;
#10457=CARTESIAN_POINT ( 'NONE',  ( 0.8560838555295223751, -20.57050347530454104, -42.15717282805163535 ) ) ;
#10465=CARTESIAN_POINT ( 'NONE',  ( 0.9754292580325125694, 15.60437149020586034, -38.89512896622989047 ) ) ;
#10476=ADVANCED_FACE ( 'NONE', ( #54191 ), #8696, .F. ) ;
#10477=CARTESIAN_POINT ( 'NONE',  ( 4.962356264823608143, -25.31392337492896161, 33.62202970123266965 ) ) ;
#10479=DIRECTION ( 'NONE',  ( 0.000000000000000000, 0.000000000000000000, 1.000000000000000000 ) ) ;
#10481=ORIENTED_EDGE ( 'NONE', *, *, #61075, .F. ) ;
#10482=CARTESIAN_POINT ( 'NONE',  ( 0.7056313189692711152, -24.52218711664568218, 39.98013235312978253 ) ) ;
#10484=CARTESIAN_POINT ( 'NONE',  ( 4.962356264823609031, -24.61258717641066696, -34.13877780978592824 ) ) ;
#10486=ORIENTED_EDGE ( 'NONE', *, *, #39334, .F. ) ;
#10487=DIRECTION ( 'NONE',  ( -1.000000000000000000, -0.000000000000000000, -0.000000000000000000 ) ) ;
#10489=CARTESIAN_POINT ( 'NONE',  ( 5.895596859100789899, -19.39731145114851074, 5.317188324634581242 ) ) ;
#10493=DIRECTION ( 'NONE',  ( 0.000000000000000000, 0.000000000000000000, 1.000000000000000000 ) ) ;
#10502=ORIENTED_EDGE ( 'NONE', *, *, #30529, .T. ) ;
#10509=CARTESIAN_POINT ( 'NONE',  ( 0.8554163680231816613, 33.26717477998048622, 33.08323677136276331 ) ) ;
#10512=VERTEX_POINT ( 'NONE', #50142 ) ;
#10520=CARTESIAN_POINT ( 'NONE',  ( 0.5804410086790514622, 23.01644811389265399, -40.86273324284467634 ) ) ;
#10521=B_SPLINE_CURVE_WITH_KNOTS ( 'NONE', 3,
 ( #30872, #27109, #11793, #50290, #6727, #40930, #25869, #60289, #16798, #2044, #12407, #31494, #22102, #54975, #55282, #36843, #50590, #35909, #41229 ),
 .UNSPECIFIED., .F., .F.,
 ( 4, 3, 3, 3, 3, 3, 4 ),
 ( 7.758676801208396025E-18, 0.0002732106629380558725, 0.0004098138914053752694, 0.0005464171197651503760, 0.0006830203481512575007, 0.0008196235766963642835, 0.001011968216111138559 ),
 .UNSPECIFIED. ) ;
#10522=ORIENTED_EDGE ( 'NONE', *, *, #41062, .F. ) ;
#10524=CARTESIAN_POINT ( 'NONE',  ( 5.896782393890504181, -11.93563916323470764, -16.18847134979303704 ) ) ;
#10527=DIRECTION ( 'NONE',  ( -0.07500201931887529039, 0.9899952385360571983, 0.1195162113440108032 ) ) ;
#10529=CARTESIAN_POINT ( 'NONE',  ( 5.910764540655178756, -7.214026563325572461, 18.77389302230083601 ) ) ;
#10536=CARTESIAN_POINT ( 'NONE',  ( 1.092182651088186018, 14.33286397384261690, -39.38692923737020379 ) ) ;
#10539=CARTESIAN_POINT ( 'NONE',  ( 4.962356264823608143, 41.96072444189411499, 3.245489512196318316 ) ) ;
#10544=B_SPLINE_CURVE_WITH_KNOTS ( 'NONE', 3,
 ( #12466, #12166, #60349, #3647 ),
 .UNSPECIFIED., .F., .F.,
 ( 4, 4 ),
 ( 0.000000000000000000, 0.005004948556313811373 ),
 .UNSPECIFIED. ) ;
#10547=CARTESIAN_POINT ( 'NONE',  ( 2.618530812446115519, 23.81615347600926214, 40.52798567416559194 ) ) ;
#10551=CARTESIAN_POINT ( 'NONE',  ( 0.9784957157296381158, 28.96678784324410927, -30.28627179163612126 ) ) ;
#10558=CARTESIAN_POINT ( 'NONE',  ( 4.962356264823608143, -38.57439820587617163, -16.83007429920747811 ) ) ;
#10567=ORIENTED_EDGE ( 'NONE', *, *, #28129, .F. ) ;
#10575=CARTESIAN_POINT ( 'NONE',  ( 4.962356264823596597, -3.779019546647577776, 41.91604238389407300 ) ) ;
#10579=ORIENTED_EDGE ( 'NONE', *, *, #41949, .T. ) ;
#10580=CARTESIAN_POINT ( 'NONE',  ( 1.000110580585050091, 4.849091690273542810, -41.62816105175947001 ) ) ;
#10584=FACE_OUTER_BOUND ( 'NONE', #28680, .T. ) ;
#10589=CARTESIAN_POINT ( 'NONE',  ( 0.8560838555295223751, -46.14148336882287538, -8.446084690930739214 ) ) ;
#10598=CARTESIAN_POINT ( 'NONE',  ( 0.9762797500689124330, 36.31338395866826829, -20.92039508843077300 ) ) ;
#10610=ORIENTED_EDGE ( 'NONE', *, *, #35583, .F. ) ;
#10614=CARTESIAN_POINT ( 'NONE',  ( 5.896782393890504181, -7.234636363571574691, 18.76662259344765715 ) ) ;
#10620=ORIENTED_EDGE ( 'NONE', *, *, #20508, .F. ) ;
#10627=CARTESIAN_POINT ( 'NONE',  ( 0.6845945791218034371, 31.98229355120833262, 34.31529425661801724 ) ) ;
#10631=CARTESIAN_POINT ( 'NONE',  ( 5.896782393890504181, 17.95394716461052909, -9.065421561537322148 ) ) ;
#10639=VERTEX_POINT ( 'NONE', #10011 ) ;
#10645=CARTESIAN_POINT ( 'NONE',  ( 0.6845945791218023269, 46.59746449482849329, 5.392849280959315372 ) ) ;
#10650=EDGE_CURVE ( 'NONE', #46003, #27817, #61669, .T. ) ;
#10653=CARTESIAN_POINT ( 'NONE',  ( 0.6064515330803530446, -35.25402489989757271, -30.92714122570154345 ) ) ;
#10655=CARTESIAN_POINT ( 'NONE',  ( 0.9762797500689124330, 25.26481495167912783, -33.43671500974812716 ) ) ;
#10667=DIRECTION ( 'NONE',  ( -1.000000000000000000, -0.000000000000000000, -0.000000000000000000 ) ) ;
#10671=CARTESIAN_POINT ( 'NONE',  ( 0.8560838555295223751, -30.97734773434455491, -35.22466126774295248 ) ) ;
#10679=CARTESIAN_POINT ( 'NONE',  ( 0.5837799406558241699, -46.79736417433153406, -3.041423336563346957 ) ) ;
#10685=CARTESIAN_POINT ( 'NONE',  ( 0.9788927965476027504, -12.55178823826572376, -39.98486244384882582 ) ) ;
#10691=EDGE_CURVE ( 'NONE', #26843, #47897, #4671, .T. ) ;
#10695=AXIS2_PLACEMENT_3D ( 'NONE', #9803, #37723, #57385 ) ;
#10698=CARTESIAN_POINT ( 'NONE',  ( 0.5797568599927137578, 17.44034498461612159, -43.53228314123417420 ) ) ;
#10699=B_SPLINE_CURVE_WITH_KNOTS ( 'NONE', 3,
 ( #20728, #31361, #50460, #7527, #26656, #45792 ),
 .UNSPECIFIED., .F., .F.,
 ( 4, 2, 4 ),
 ( 1.188253925084572214E-16, 0.0002448718616795905485, 0.0004897437233590622684 ),
 .UNSPECIFIED. ) ;
#10704=CARTESIAN_POINT ( 'NONE',  ( 0.5806925824938494740, 46.54710689580857519, 5.708695295225819422 ) ) ;
#10705=CARTESIAN_POINT ( 'NONE',  ( 3.238018933889920792, -11.82813123897603269, -6.285125596295774386 ) ) ;
#10708=CARTESIAN_POINT ( 'NONE',  ( 5.910764540655178756, -13.97071922697946533, 14.46790388238978231 ) ) ;
#10715=CARTESIAN_POINT ( 'NONE',  ( 4.960386119450144626, -43.75174247978073083, 0.4706321868415035969 ) ) ;
#10719=CARTESIAN_POINT ( 'NONE',  ( 1.231276596079887931, 5.037240371905710390, 41.61613846158375196 ) ) ;
#10722=CARTESIAN_POINT ( 'NONE',  ( 0.9762797500689124330, 33.20096159360316790, 25.57383300261796677 ) ) ;
#10728=AXIS2_PLACEMENT_3D ( 'NONE', #5847, #58472, #15601 ) ;
#10729=VERTEX_POINT ( 'NONE', #4341 ) ;
#10737=CARTESIAN_POINT ( 'NONE',  ( 0.8560838555295158248, 27.08392101972004440, 38.29926965725714894 ) ) ;
#10740=CARTESIAN_POINT ( 'NONE',  ( 0.5806925824938499181, 45.08220210717423271, 12.91578164539256335 ) ) ;
#10743=AXIS2_PLACEMENT_3D ( 'NONE', #1840, #30350, #40111 ) ;
#10746=B_SPLINE_CURVE_WITH_KNOTS ( 'NONE', 3,
 ( #3739, #27262, #17875, #51357, #41089, #54824 ),
 .UNSPECIFIED., .F., .F.,
 ( 4, 2, 4 ),
 ( 7.006328859705253345E-18, 0.0002291472222819939113, 0.0004582944445639808295 ),
 .UNSPECIFIED. ) ;
#10749=CARTESIAN_POINT ( 'NONE',  ( 0.9780106845699492180, 35.89738679733209636, 21.62657780551894859 ) ) ;
#10765=ORIENTED_EDGE ( 'NONE', *, *, #4640, .F. ) ;
#10768=EDGE_CURVE ( 'NONE', #3462, #29292, #42879, .T. ) ;
#10776=CARTESIAN_POINT ( 'NONE',  ( 0.5848930533535030563, -30.13830825645479550, -35.92986860296690566 ) ) ;
#10782=CARTESIAN_POINT ( 'NONE',  ( 5.838029081930957709, 38.95312035650108839, 26.71552867986823188 ) ) ;
#10785=CARTESIAN_POINT ( 'NONE',  ( 1.231276596079881047, -11.60895935156387537, -40.28037777618035875 ) ) ;
#10791=CARTESIAN_POINT ( 'NONE',  ( 1.231276596079887264, -26.41281459480383376, 32.55211200826430229 ) ) ;
#10795=EDGE_LOOP ( 'NONE', ( #36952, #48411, #50322, #54102 ) ) ;
#10796=CARTESIAN_POINT ( 'NONE',  ( 0.9754292580325135686, 36.35155301108883208, -20.85406580468192672 ) ) ;
#10814=CARTESIAN_POINT ( 'NONE',  ( 0.9789889208857707192, -41.08791942546226750, -8.253349340061184591 ) ) ;
#10819=CARTESIAN_POINT ( 'NONE',  ( 2.528190830796655852, 36.72068932201717928, -20.34318342514028899 ) ) ;
#10825=FACE_OUTER_BOUND ( 'NONE', #40119, .T. ) ;
#10826=CARTESIAN_POINT ( 'NONE',  ( 0.8554163680231720024, -8.703479761964910466, -46.10265624825630937 ) ) ;
#10835=ADVANCED_FACE ( 'NONE', ( #2120 ), #47143, .F. ) ;
#10838=CARTESIAN_POINT ( 'NONE',  ( 0.6845945791218034371, 23.29905063694718592, -40.71315217630433381 ) ) ;
#10843=ADVANCED_FACE ( 'NONE', ( #15949 ), #36721, .F. ) ;
#10844=CARTESIAN_POINT ( 'NONE',  ( 0.5804410086790514622, 27.37779091616946658, 38.07855586029891271 ) ) ;
#10852=VERTEX_POINT ( 'NONE', #54118 ) ;
#10856=CARTESIAN_POINT ( 'NONE',  ( 0.5824935313925935221, 27.52368752571334554, -37.96952464860119392 ) ) ;
#10857=ORIENTED_EDGE ( 'NONE', *, *, #45093, .F. ) ;
#10864=FACE_OUTER_BOUND ( 'NONE', #48406, .T. ) ;
#10866=CARTESIAN_POINT ( 'NONE',  ( 2.282816707992315841, -15.16645052872554977, -44.45757241199396503 ) ) ;
#10867=CARTESIAN_POINT ( 'NONE',  ( 4.960386119450137521, 36.33710775634285284, 24.37316279386549667 ) ) ;
#10871=CARTESIAN_POINT ( 'NONE',  ( 0.5806925824938502512, -29.85799195566318431, 36.16244846134061675 ) ) ;
#10877=CARTESIAN_POINT ( 'NONE',  ( 0.5848930533535030563, 22.37766167358117286, -41.21302391732853465 ) ) ;
#10879=CARTESIAN_POINT ( 'NONE',  ( 0.8560838555295158248, -46.14148336882297485, 8.446084690930096173 ) ) ;
#10880=CARTESIAN_POINT ( 'NONE',  ( 5.917102823773431552, 14.91028373222408732, -13.49715366572951858 ) ) ;
#10881=CARTESIAN_POINT ( 'NONE',  ( 5.894904586330512508, -11.92958617826559653, 16.19303509775042471 ) ) ;
#10883=ORIENTED_EDGE ( 'NONE', *, *, #35781, .F. ) ;
#10884=EDGE_CURVE ( 'NONE', #47641, #32860, #30726, .T. ) ;
#10885=FACE_OUTER_BOUND ( 'NONE', #26475, .T. ) ;
#10891=CARTESIAN_POINT ( 'NONE',  ( 0.9762797500689124330, -27.44172181261391330, -31.67454323498310842 ) ) ;
#10897=CARTESIAN_POINT ( 'NONE',  ( 0.5806925824938499181, -35.14454992382352572, 31.04968555388990836 ) ) ;
#10902=CARTESIAN_POINT ( 'NONE',  ( 0.9762797500689124330, 40.28286501695569655, 11.55922018180428168 ) ) ;
#10906=CARTESIAN_POINT ( 'NONE',  ( 4.956445790444004018, -46.59545590650535019, -6.811867512257778756 ) ) ;
#10912=CARTESIAN_POINT ( 'NONE',  ( 1.157643937452370153, -39.86048667108141075, -12.96703038244662842 ) ) ;
#10914=ORIENTED_EDGE ( 'NONE', *, *, #49430, .T. ) ;
#10934=ORIENTED_EDGE ( 'NONE', *, *, #36805, .T. ) ;
#10940=CARTESIAN_POINT ( 'NONE',  ( 0.5782707292762442330, -0.8434722838399307809, -46.89376193284147831 ) ) ;
#10942=CARTESIAN_POINT ( 'NONE',  ( 0.5835226383429302777, -41.93746949518194356, -20.98788047628082509 ) ) ;
#10950=CARTESIAN_POINT ( 'NONE',  ( 0.7056759521544945235, 40.77723470137082273, -23.17252595696689355 ) ) ;
#10951=CARTESIAN_POINT ( 'NONE',  ( 1.000110580585050979, 3.539822106476956609, 41.75987478700575650 ) ) ;
#10963=EDGE_CURVE ( 'NONE', #34397, #5387, #54726, .T. ) ;
#10971=CARTESIAN_POINT ( 'NONE',  ( 0.9762797500689124330, 15.53330887509081215, 38.92352888134283262 ) ) ;
#10975=ORIENTED_EDGE ( 'NONE', *, *, #27473, .T. ) ;
#10976=DIRECTION ( 'NONE',  ( -1.000000000000000000, -0.000000000000000000, -0.000000000000000000 ) ) ;
#10982=VERTEX_POINT ( 'NONE', #23112 ) ;
#10983=CARTESIAN_POINT ( 'NONE',  ( 0.9790724872846768845, 20.17598226788706128, -36.73234200956102313 ) ) ;
#10988=CARTESIAN_POINT ( 'NONE',  ( 0.5782707292762423457, -39.07253195953412472, -25.94366203871003762 ) ) ;
#10997=CARTESIAN_POINT ( 'NONE',  ( 3.782625744892852637, -21.14745495448669388, 36.33212425723217365 ) ) ;
#11000=CARTESIAN_POINT ( 'NONE',  ( 3.782625744892853525, -3.127219394304327160, -41.92205389714212771 ) ) ;
#11013=EDGE_CURVE ( 'NONE', #40686, #42210, #37678, .T. ) ;
#11023=CARTESIAN_POINT ( 'NONE',  ( 5.896782393890504181, -13.97772289704291460, 14.46199673252260354 ) ) ;
#11024=DIRECTION ( 'NONE',  ( 0.000000000000000000, 0.000000000000000000, 1.000000000000000000 ) ) ;
#11030=DIRECTION ( 'NONE',  ( 0.000000000000000000, 0.000000000000000000, 1.000000000000000000 ) ) ;
#11031=ORIENTED_EDGE ( 'NONE', *, *, #26734, .T. ) ;
#11037=VERTEX_POINT ( 'NONE', #32513 ) ;
#11042=EDGE_CURVE ( 'NONE', #44269, #15676, #44458, .T. ) ;
#11043=B_SPLINE_CURVE_WITH_KNOTS ( 'NONE', 3,
 ( #10007, #56666, #23790, #38222, #33822, #57269, #14402, #42918, #27872, #43224, #42301, #61970, #28171, #4033, #33511, #28792, #46683, #260, #19407 ),
 .UNSPECIFIED., .F., .F.,
 ( 4, 3, 3, 3, 3, 3, 4 ),
 ( 1.040890552917501732E-17, 0.0002732106629380587457, 0.0004098138914053709326, 0.0005464171197651407266, 0.0006830203481512488271, 0.0008196235766963528993, 0.001011968216111136607 ),
 .UNSPECIFIED. ) ;
#11049=EDGE_LOOP ( 'NONE', ( #29683, #26496, #15309, #10415 ) ) ;
#11053=CARTESIAN_POINT ( 'NONE',  ( 0.8560838555295158248, -2.480523550131575661, 46.84250032821661591 ) ) ;
#11061=CARTESIAN_POINT ( 'NONE',  ( 4.960386119450151732, -3.911092338298454152, -43.57912139308966459 ) ) ;
#11064=EDGE_LOOP ( 'NONE', ( #60636, #49572, #52885, #32244 ) ) ;
#11065=CARTESIAN_POINT ( 'NONE',  ( 3.661933894777873455, -46.77018561706699273, -5.018057621904368659 ) ) ;
#11070=FACE_OUTER_BOUND ( 'NONE', #34164, .T. ) ;
#11072=B_SPLINE_CURVE_WITH_KNOTS ( 'NONE', 3,
 ( #52529, #14043, #9623, #33143, #4907, #4282 ),
 .UNSPECIFIED., .F., .F.,
 ( 4, 2, 4 ),
 ( 4.336808689942017736E-19, 0.0002291459268755708040, 0.0004582918537511411743 ),
 .UNSPECIFIED. ) ;
#11073=ORIENTED_EDGE ( 'NONE', *, *, #31768, .T. ) ;
#11075=LINE ( 'NONE', #5102, #51937 ) ;
#11079=ADVANCED_FACE ( 'NONE', ( #24649 ), #60276, .F. ) ;
#11095=LINE ( 'NONE', #1655, #29647 ) ;
#11104=ORIENTED_EDGE ( 'NONE', *, *, #22563, .T. ) ;
#11114=CARTESIAN_POINT ( 'NONE',  ( 0.5806925824938502512, -29.85799195566318431, 36.16244846134061675 ) ) ;
#11115=ADVANCED_FACE ( 'NONE', ( #57826 ), #49873, .F. ) ;
#11117=ORIENTED_EDGE ( 'NONE', *, *, #42375, .F. ) ;
#11119=ADVANCED_FACE ( 'NONE', ( #1736 ), #53512, .F. ) ;
#11121=CARTESIAN_POINT ( 'NONE',  ( 0.5834584762367756028, -38.55966758064684541, -26.69059806529635637 ) ) ;
#11122=CARTESIAN_POINT ( 'NONE',  ( 2.528190830796655852, 2.996102205408210928, 41.87215671216083734 ) ) ;
#11137=CARTESIAN_POINT ( 'NONE',  ( 0.5817216825391139379, 46.41469338179018678, -6.701581192663303987 ) ) ;
#11141=CARTESIAN_POINT ( 'NONE',  ( 5.910764540655177868, -19.40170003828502487, 5.298610581423578658 ) ) ;
#11142=ORIENTED_EDGE ( 'NONE', *, *, #13232, .T. ) ;
#11144=CARTESIAN_POINT ( 'NONE',  ( 2.618530812446111078, -26.46994001813007813, 38.84673814665519131 ) ) ;
#11154=CARTESIAN_POINT ( 'NONE',  ( 2.282803330402966235, -37.96809118126141414, -27.65720447746669919 ) ) ;
#11157=ADVANCED_FACE ( 'NONE', ( #5509 ), #13481, .F. ) ;
#11162=CARTESIAN_POINT ( 'NONE',  ( 0.9772918015221170318, 15.44874721096192260, 38.95732364219180255 ) ) ;
#11163=ORIENTED_EDGE ( 'NONE', *, *, #7949, .F. ) ;
#11171=CARTESIAN_POINT ( 'NONE',  ( 0.8554163680231816613, -46.86440027434175448, -2.221139355847804531 ) ) ;
#11174=CARTESIAN_POINT ( 'NONE',  ( 4.962356264823602814, -33.29728444345256122, -25.73958909062380229 ) ) ;
#11181=CARTESIAN_POINT ( 'NONE',  ( 0.5326698147273822848, 0.000000000000000000, 0.000000000000000000 ) ) ;
#11182=CIRCLE ( 'NONE', #50204, 42.08604991992415023 ) ;
#11184=CIRCLE ( 'NONE', #56141, 42.08604991992415023 ) ;
#11185=ORIENTED_EDGE ( 'NONE', *, *, #41468, .F. ) ;
#11194=CARTESIAN_POINT ( 'NONE',  ( 5.894904586330512508, 10.82344038793352503, -16.95236119926932972 ) ) ;
#11196=( BOUNDED_SURFACE ( )  B_SPLINE_SURFACE ( 3, 1, ( 
 ( #59751, #12169 ),
 ( #32419, #45378 ),
 ( #11539, #30623 ),
 ( #7422, #49741 ) ),
 .UNSPECIFIED., .F., .F., .F. ) 
 B_SPLINE_SURFACE_WITH_KNOTS ( ( 4, 4 ),
 ( 2, 2 ),
 ( 0.000000000000000000, 1.000000000000000000 ),
 ( 0.000000000000000000, 1.000000000000000000 ),
 .UNSPECIFIED. ) 
 GEOMETRIC_REPRESENTATION_ITEM ( )  RATIONAL_B_SPLINE_SURFACE ( (
 ( 1.000000000000000000, 1.000000000000000000),
 ( 0.9729067724841187204, 0.9999501103223794596),
 ( 0.9729067724841187204, 0.9999501103223794596),
 ( 1.000000000000000000, 1.000000000000000000) ) ) 
 REPRESENTATION_ITEM ( '' )  SURFACE ( )  );
#11209=CARTESIAN_POINT ( 'NONE',  ( 0.8554163680231816613, -35.40260165760457056, -30.78735566729940487 ) ) ;
#11216=FACE_OUTER_BOUND ( 'NONE', #6373, .T. ) ;
#11217=CARTESIAN_POINT ( 'NONE',  ( 0.9787464366903551038, 36.14815773438009217, -21.20482693399881668 ) ) ;
#11231=CARTESIAN_POINT ( 'NONE',  ( 0.9780106845699474416, -26.81709666672181669, -32.20519481113468885 ) ) ;
#11234=CARTESIAN_POINT ( 'NONE',  ( 2.528190830796659405, -21.55884404307488822, -36.02041615083565773 ) ) ;
#11237=CARTESIAN_POINT ( 'NONE',  ( 0.5837157313716030416, 45.20563255473990694, 12.47749369496385441 ) ) ;
#11248=DIRECTION ( 'NONE',  ( 0.07500201931887537365, -0.9580968512853003105, -0.2764509371575435970 ) ) ;
#11249=CARTESIAN_POINT ( 'NONE',  ( 2.528100132419518253, 13.95210196817038018, -39.59283558046644913 ) ) ;
#11250=CARTESIAN_POINT ( 'NONE',  ( 0.5806925824938502512, -20.23436166722406426, -42.30594485723652554 ) ) ;
#11253=CARTESIAN_POINT ( 'NONE',  ( 4.962356264823601926, -38.91448554252674796, -16.02805081171206680 ) ) ;
#11264=( BOUNDED_SURFACE ( )  B_SPLINE_SURFACE ( 3, 1, ( 
 ( #50294, #45614 ),
 ( #61225, #28646 ),
 ( #4509, #33068 ),
 ( #3901, #51514 ) ),
 .UNSPECIFIED., .F., .F., .F. ) 
 B_SPLINE_SURFACE_WITH_KNOTS ( ( 4, 4 ),
 ( 2, 2 ),
 ( 0.000000000000000000, 1.000000000000000000 ),
 ( 0.000000000000000000, 1.000000000000000000 ),
 .UNSPECIFIED. ) 
 GEOMETRIC_REPRESENTATION_ITEM ( )  RATIONAL_B_SPLINE_SURFACE ( (
 ( 1.000000000000000000, 1.000000000000000000),
 ( 0.7282232189291693025, 0.9929344683865674037),
 ( 0.7282232189291693025, 0.9929344683865674037),
 ( 1.000000000000000000, 1.000000000000000000) ) ) 
 REPRESENTATION_ITEM ( '' )  SURFACE ( )  );
#11271=B_SPLINE_CURVE_WITH_KNOTS ( 'NONE', 3,
 ( #37660, #47654, #18859, #33265, #57033, #5628, #42360, #61414, #9429, #38277, #18532, #13852, #32956, #9124, #5021, #24146 ),
 .UNSPECIFIED., .F., .F.,
 ( 4, 3, 3, 3, 3, 4 ),
 ( 6.939740885162003740E-18, 0.0002732102107931890238, 0.0004098135523333774140, 0.0005464168938824980580, 0.0008195847345945439857, 0.001092771384553105915 ),
 .UNSPECIFIED. ) ;
#11280=ORIENTED_EDGE ( 'NONE', *, *, #15254, .T. ) ;
#11288=CARTESIAN_POINT ( 'NONE',  ( 1.000433927950260538, -18.23650333253261024, -37.73391874501472643 ) ) ;
#11289=EDGE_LOOP ( 'NONE', ( #41003, #21347, #35177, #1631 ) ) ;
#11295=CARTESIAN_POINT ( 'NONE',  ( 0.8560838555295223751, -46.73345513967318965, 4.044379407262076676 ) ) ;
#11296=CARTESIAN_POINT ( 'NONE',  ( 2.282816707992306515, 28.91046591422454881, 37.02272176691533190 ) ) ;
#11298=CARTESIAN_POINT ( 'NONE',  ( 0.8560838555295158248, -30.97734773434503808, 35.22466126774251194 ) ) ;
#11306=ORIENTED_EDGE ( 'NONE', *, *, #3308, .T. ) ;
#11309=CARTESIAN_POINT ( 'NONE',  ( 0.9787464366903565471, 41.55793433844984008, -5.410368417358930593 ) ) ;
#11312=CARTESIAN_POINT ( 'NONE',  ( 5.896782393890504181, 17.94821721415871352, -9.076760749925545824 ) ) ;
#11317=CARTESIAN_POINT ( 'NONE',  ( 4.956445790444006683, -23.10347171912805564, -41.03373788315033721 ) ) ;
#11322=CARTESIAN_POINT ( 'NONE',  ( 0.5797568665920715958, -7.179076188124985158, 46.34313513010278740 ) ) ;
#11327=CARTESIAN_POINT ( 'NONE',  ( -69.95594261585600293, 0.000000000000000000, 0.000000000000000000 ) ) ;
#11341=ORIENTED_EDGE ( 'NONE', *, *, #44443, .F. ) ;
#11352=CARTESIAN_POINT ( 'NONE',  ( 0.8560838555295158248, 36.24009790160309308, 29.78301761346479282 ) ) ;
#11353=CARTESIAN_POINT ( 'NONE',  ( 0.9762797500689124330, 41.59901070109194876, 5.084003725032276932 ) ) ;
#11357=CARTESIAN_POINT ( 'NONE',  ( 4.962356264823609031, -3.779019546646985361, -41.91604238389410853 ) ) ;
#11363=ORIENTED_EDGE ( 'NONE', *, *, #22362, .F. ) ;
#11367=ORIENTED_EDGE ( 'NONE', *, *, #173, .T. ) ;
#11372=EDGE_CURVE ( 'NONE', #9240, #37569, #25661, .T. ) ;
#11378=CARTESIAN_POINT ( 'NONE',  ( 0.9789889208857693870, 14.97250939922353297, -39.14280087490587334 ) ) ;
#11379=CARTESIAN_POINT ( 'NONE',  ( 0.8560838555295158248, 44.99141268455571208, 13.27198623905747432 ) ) ;
#11390=CARTESIAN_POINT ( 'NONE',  ( 0.9762797500689124330, 15.53330887509137703, -38.92352888134260525 ) ) ;
#11397=CARTESIAN_POINT ( 'NONE',  ( 0.9780303403264752893, -22.27669849432558991, 35.49772270988660239 ) ) ;
#11408=ORIENTED_EDGE ( 'NONE', *, *, #6796, .T. ) ;
#11414=B_SPLINE_CURVE_WITH_KNOTS ( 'NONE', 3,
 ( #20554, #26474, #40306, #6719 ),
 .UNSPECIFIED., .F., .F.,
 ( 4, 4 ),
 ( 1.084202172485504434E-19, 0.004446298630425104051 ),
 .UNSPECIFIED. ) ;
#11421=CARTESIAN_POINT ( 'NONE',  ( 1.231276596079881935, 41.65019306089989470, -4.747440258479600494 ) ) ;
#11430=CARTESIAN_POINT ( 'NONE',  ( 0.7056759521544992975, 27.13777475669688144, 38.25297387618083178 ) ) ;
#11432=ORIENTED_EDGE ( 'NONE', *, *, #32084, .F. ) ;
#11442=CARTESIAN_POINT ( 'NONE',  ( 3.661921753701998128, 12.72740550795439418, 45.28403993539147621 ) ) ;
#11444=ORIENTED_EDGE ( 'NONE', *, *, #22963, .F. ) ;
#11447=FACE_OUTER_BOUND ( 'NONE', #41785, .T. ) ;
#11450=CARTESIAN_POINT ( 'NONE',  ( 5.895596859100789899, 0.6756533542673609505, 20.10153416427101192 ) ) ;
#11458=( BOUNDED_SURFACE ( )  B_SPLINE_SURFACE ( 3, 1, ( 
 ( #40708, #51293 ),
 ( #32216, #22805 ),
 ( #41936, #60373 ),
 ( #8376, #59780 ) ),
 .UNSPECIFIED., .F., .F., .F. ) 
 B_SPLINE_SURFACE_WITH_KNOTS ( ( 4, 4 ),
 ( 2, 2 ),
 ( 0.000000000000000000, 1.000000000000000000 ),
 ( 0.000000000000000000, 1.000000000000000000 ),
 .UNSPECIFIED. ) 
 GEOMETRIC_REPRESENTATION_ITEM ( )  RATIONAL_B_SPLINE_SURFACE ( (
 ( 1.000000000000000000, 1.000000000000000000),
 ( 0.9729067724841187204, 0.9999501103223794596),
 ( 0.9729067724841187204, 0.9999501103223794596),
 ( 1.000000000000000000, 1.000000000000000000) ) ) 
 REPRESENTATION_ITEM ( '' )  SURFACE ( )  );
#11467=ORIENTED_EDGE ( 'NONE', *, *, #8204, .F. ) ;
#11473=CARTESIAN_POINT ( 'NONE',  ( 5.838029081930957709, 30.48039787783066146, -36.08338126287580394 ) ) ;
#11475=CARTESIAN_POINT ( 'NONE',  ( 0.8554163680231816613, 23.34472558242442375, 40.69679668712412735 ) ) ;
#11478=CARTESIAN_POINT ( 'NONE',  ( 0.5804410086790514622, -19.24447200597920826, -42.76879877979365574 ) ) ;
#11480=EDGE_LOOP ( 'NONE', ( #41869, #15061, #56804, #28213 ) ) ;
#11487=CARTESIAN_POINT ( 'NONE',  ( 5.901463166500146684, 3.359582080288941341, 19.83005493150329457 ) ) ;
#11493=CARTESIAN_POINT ( 'NONE',  ( 4.962356264823603702, 30.91935898304086550, -28.55221248765493414 ) ) ;
#11502=ORIENTED_EDGE ( 'NONE', *, *, #5224, .T. ) ;
#11507=CARTESIAN_POINT ( 'NONE',  ( 0.8560838555295158248, -46.85553835019179303, 2.220666565569249684 ) ) ;
#11512=CARTESIAN_POINT ( 'NONE',  ( 1.231276596079881047, 5.037240371906286818, -41.61613846158368091 ) ) ;
#11519=B_SPLINE_CURVE_WITH_KNOTS ( 'NONE', 3,
 ( #55512, #2267, #21397, #50818 ),
 .UNSPECIFIED., .F., .F.,
 ( 4, 4 ),
 ( 3.469446951953614189E-18, 0.004042984057420973693 ),
 .UNSPECIFIED. ) ;
#11526=CARTESIAN_POINT ( 'NONE',  ( 4.291220156522059348, -45.68901888636781905, -11.48488356522702247 ) ) ;
#11533=EDGE_CURVE ( 'NONE', #53953, #40503, #58591, .T. ) ;
#11535=CARTESIAN_POINT ( 'NONE',  ( 0.9789889208857693870, -31.14606658136087347, -28.04028235506562083 ) ) ;
#11537=CARTESIAN_POINT ( 'NONE',  ( 0.8560838555295223751, 27.08392101972057731, -38.29926965725677235 ) ) ;
#11539=CARTESIAN_POINT ( 'NONE',  ( 5.894904586330512508, 12.98452142685981769, -15.36006560458193704 ) ) ;
#11541=CARTESIAN_POINT ( 'NONE',  ( 0.9780106845699474416, 38.45963264927223690, 16.64896101678635532 ) ) ;
#11548=CARTESIAN_POINT ( 'NONE',  ( 5.896782393890504181, 5.952874097602427916, 19.21169895808557371 ) ) ;
#11559=CARTESIAN_POINT ( 'NONE',  ( 5.895596859100789899, -13.98490190264553412, -14.45512718677593611 ) ) ;
#11566=CARTESIAN_POINT ( 'NONE',  ( 0.9780303403264780648, 10.03001170075172510, 40.69076650393633088 ) ) ;
#11570=( BOUNDED_SURFACE ( )  B_SPLINE_SURFACE ( 3, 1, ( 
 ( #39174, #19434 ),
 ( #24427, #15049 ),
 ( #48853, #34156 ),
 ( #58227, #10341 ) ),
 .UNSPECIFIED., .F., .F., .F. ) 
 B_SPLINE_SURFACE_WITH_KNOTS ( ( 4, 4 ),
 ( 2, 2 ),
 ( 0.000000000000000000, 1.000000000000000000 ),
 ( 0.000000000000000000, 1.000000000000000000 ),
 .UNSPECIFIED. ) 
 GEOMETRIC_REPRESENTATION_ITEM ( )  RATIONAL_B_SPLINE_SURFACE ( (
 ( 1.000000000000000000, 1.000000000000000000),
 ( 0.7282232189291693025, 0.9929344683865674037),
 ( 0.7282232189291693025, 0.9929344683865674037),
 ( 1.000000000000000000, 1.000000000000000000) ) ) 
 REPRESENTATION_ITEM ( '' )  SURFACE ( )  );
#11571=VERTEX_POINT ( 'NONE', #3511 ) ;
#11577=CARTESIAN_POINT ( 'NONE',  ( 3.782625744892851749, -33.65307366127398581, 25.19342646889998250 ) ) ;
#11580=CARTESIAN_POINT ( 'NONE',  ( 4.958415959904823644, -15.85236509608435540, 42.56649474273264389 ) ) ;
#11589=ORIENTED_EDGE ( 'NONE', *, *, #5811, .T. ) ;
#11592=CARTESIAN_POINT ( 'NONE',  ( 2.528100132419515589, -35.27989545911430724, -22.75044516105213077 ) ) ;
#11609=ORIENTED_EDGE ( 'NONE', *, *, #49722, .F. ) ;
#11614=CARTESIAN_POINT ( 'NONE',  ( 0.9762797500689124330, 40.28286501695585997, -11.55922018180369548 ) ) ;
#11623=ORIENTED_EDGE ( 'NONE', *, *, #21432, .F. ) ;
#11624=EDGE_CURVE ( 'NONE', #14061, #36392, #41776, .T. ) ;
#11627=( BOUNDED_SURFACE ( )  B_SPLINE_SURFACE ( 3, 1, ( 
 ( #6692, #40895 ),
 ( #50257, #7008 ),
 ( #26141, #1696 ),
 ( #49635, #2319 ) ),
 .UNSPECIFIED., .F., .F., .F. ) 
 B_SPLINE_SURFACE_WITH_KNOTS ( ( 4, 4 ),
 ( 2, 2 ),
 ( 0.000000000000000000, 1.000000000000000000 ),
 ( 0.000000000000000000, 1.000000000000000000 ),
 .UNSPECIFIED. ) 
 GEOMETRIC_REPRESENTATION_ITEM ( )  RATIONAL_B_SPLINE_SURFACE ( (
 ( 1.000000000000000000, 1.000000000000000000),
 ( 0.9729067724841187204, 0.9999501103223794596),
 ( 0.9729067724841187204, 0.9999501103223794596),
 ( 1.000000000000000000, 1.000000000000000000) ) ) 
 REPRESENTATION_ITEM ( '' )  SURFACE ( )  );
#11628=CARTESIAN_POINT ( 'NONE',  ( 0.6064782688330866423, 17.51648129858323344, -43.50295770789789174 ) ) ;
#11629=EDGE_LOOP ( 'NONE', ( #21298, #12778, #57965, #54687 ) ) ;
#11634=CARTESIAN_POINT ( 'NONE',  ( 2.282803330402970232, -24.15824283434179520, -40.28493776356066292 ) ) ;
#11642=CARTESIAN_POINT ( 'NONE',  ( 4.956445790444027999, 20.31112743693101663, -42.48524629068760561 ) ) ;
#11652=ORIENTED_EDGE ( 'NONE', *, *, #60687, .T. ) ;
#11654=ADVANCED_FACE ( 'NONE', ( #52363 ), #4287, .F. ) ;
#11668=CARTESIAN_POINT ( 'NONE',  ( 0.6845945791218023269, 46.36658412396726447, -7.109598961194147471 ) ) ;
#11671=ORIENTED_EDGE ( 'NONE', *, *, #5421, .F. ) ;
#11676=AXIS2_PLACEMENT_3D ( 'NONE', #34718, #29384, #52880 ) ;
#11679=B_SPLINE_CURVE_WITH_KNOTS ( 'NONE', 3,
 ( #58648, #25458, #25152, #44299, #1328, #29237, #54564, #6629, #50506, #27022, #45840, #17316, #2885, #46147, #16698, #16381, #11694, #12316, #2577 ),
 .UNSPECIFIED., .F., .F.,
 ( 4, 3, 3, 3, 3, 3, 4 ),
 ( 1.250973872328959318E-17, 0.0002732106629380634077, 0.0004098138914053705531, 0.0005464171197651426781, 0.0006830203481512567417, 0.0008196235766963629824, 0.001011968216111134656 ),
 .UNSPECIFIED. ) ;
#11682=B_SPLINE_CURVE_WITH_KNOTS ( 'NONE', 3,
 ( #55242, #41810, #17994, #41188, #27372, #60251 ),
 .UNSPECIFIED., .F., .F.,
 ( 4, 2, 4 ),
 ( 1.193162889884620877E-16, 0.0002448718616795923374, 0.0004897437233590653041 ),
 .UNSPECIFIED. ) ;
#11687=CARTESIAN_POINT ( 'NONE',  ( 2.282816707992318062, -2.882087820334355843, -46.88486468151364761 ) ) ;
#11694=CARTESIAN_POINT ( 'NONE',  ( 0.9775691876210972353, -39.46427349087333170, -14.10336225258165399 ) ) ;
#11705=CARTESIAN_POINT ( 'NONE',  ( 0.5804410086790514622, -30.69452151258743555, 35.45935984995644930 ) ) ;
#11711=CARTESIAN_POINT ( 'NONE',  ( 5.895881250540457863, 14.91980774178292712, -13.48803241976142075 ) ) ;
#11716=VECTOR ( 'NONE', #8722, 1000.000000000000000 ) ;
#11717=CARTESIAN_POINT ( 'NONE',  ( 0.5804410086790514622, 46.40460073163221466, 6.792119168064940204 ) ) ;
#11719=CARTESIAN_POINT ( 'NONE',  ( 4.956445790443998689, -22.15545010017797622, 41.55326799420426198 ) ) ;
#11722=ORIENTED_EDGE ( 'NONE', *, *, #17980, .T. ) ;
#11728=ORIENTED_EDGE ( 'NONE', *, *, #31621, .F. ) ;
#11734=ORIENTED_EDGE ( 'NONE', *, *, #53116, .F. ) ;
#11736=( BOUNDED_SURFACE ( )  B_SPLINE_SURFACE ( 3, 1, ( 
 ( #36135, #12319 ),
 ( #54891, #18247 ),
 ( #12942, #51419 ),
 ( #31413, #22323 ) ),
 .UNSPECIFIED., .F., .F., .F. ) 
 B_SPLINE_SURFACE_WITH_KNOTS ( ( 4, 4 ),
 ( 2, 2 ),
 ( 0.000000000000000000, 1.000000000000000000 ),
 ( 0.000000000000000000, 1.000000000000000000 ),
 .UNSPECIFIED. ) 
 GEOMETRIC_REPRESENTATION_ITEM ( )  RATIONAL_B_SPLINE_SURFACE ( (
 ( 1.000000000000000000, 1.000000000000000000),
 ( 0.9952954269826590483, 0.8620686068821307169),
 ( 0.9952954269826590483, 0.8620686068821307169),
 ( 1.000000000000000000, 1.000000000000000000) ) ) 
 REPRESENTATION_ITEM ( '' )  SURFACE ( )  );
#11738=CARTESIAN_POINT ( 'NONE',  ( 0.8560838555295223751, 17.70877843982779609, 43.43698884880053157 ) ) ;
#11744=CARTESIAN_POINT ( 'NONE',  ( 5.917102823773431552, 18.99629506471996265, -6.605338134103194925 ) ) ;
#11747=EDGE_CURVE ( 'NONE', #18385, #15656, #39116, .T. ) ;
#11748=VECTOR ( 'NONE', #33293, 1000.000000000000114 ) ;
#11749=ORIENTED_EDGE ( 'NONE', *, *, #7847, .F. ) ;
#11758=ORIENTED_EDGE ( 'NONE', *, *, #47885, .F. ) ;
#11761=CARTESIAN_POINT ( 'NONE',  ( 0.8554163680231720024, -42.27859581856498750, -20.34025095032602337 ) ) ;
#11762=ORIENTED_EDGE ( 'NONE', *, *, #46606, .T. ) ;
#11763=CARTESIAN_POINT ( 'NONE',  ( 4.956445790443996913, 8.365049606151725214, 46.34181691762049127 ) ) ;
#11774=DIRECTION ( 'NONE',  ( -1.000000000000000000, -0.000000000000000000, -0.000000000000000000 ) ) ;
#11777=CARTESIAN_POINT ( 'NONE',  ( 3.238018933889920792, -6.973938193058373258, -11.43554451904476110 ) ) ;
#11782=CARTESIAN_POINT ( 'NONE',  ( 3.376099380956838925, 4.385778397990253374, 12.66780689289938522 ) ) ;
#11784=CARTESIAN_POINT ( 'NONE',  ( 0.9783242366443547500, 14.81179524866698749, 39.20389281331754461 ) ) ;
#11787=CARTESIAN_POINT ( 'NONE',  ( 4.962356264823608143, -28.94323483023595145, -30.55363735178127271 ) ) ;
#11789=CARTESIAN_POINT ( 'NONE',  ( 0.5806925824938499181, -34.41156632303712826, -31.86010774524751454 ) ) ;
#11793=CARTESIAN_POINT ( 'NONE',  ( 0.9780303403264750672, -30.86352413661125382, 28.35105802723950319 ) ) ;
#11795=CARTESIAN_POINT ( 'NONE',  ( 5.896278296736517710, 17.94863123379898440, -9.075991210191821423 ) ) ;
#11799=CARTESIAN_POINT ( 'NONE',  ( 0.9780106845699465534, 29.35917852947671847, -29.90601749698134881 ) ) ;
#11800=CARTESIAN_POINT ( 'NONE',  ( 4.958415959904816539, 44.40884735405912664, -9.542443633918582080 ) ) ;
#11802=EDGE_LOOP ( 'NONE', ( #11806, #39738, #31212, #11722 ) ) ;
#11806=ORIENTED_EDGE ( 'NONE', *, *, #16032, .F. ) ;
#11808=CARTESIAN_POINT ( 'NONE',  ( 5.838029081930957709, -4.747847248974175649, -46.99492530745558128 ) ) ;
#11812=B_SPLINE_CURVE_WITH_KNOTS ( 'NONE', 3,
 ( #17657, #21738, #55856, #45263, #8237, #12980 ),
 .UNSPECIFIED., .F., .F.,
 ( 4, 2, 4 ),
 ( 0.000000000000000000, 0.0002291459268755709124, 0.0004582918537511418249 ),
 .UNSPECIFIED. ) ;
#11820=ADVANCED_FACE ( 'NONE', ( #31905 ), #11458, .F. ) ;
#11822=ADVANCED_FACE ( 'NONE', ( #41619 ), #17873, .F. ) ;
#11833=CARTESIAN_POINT ( 'NONE',  ( 0.5830082357119554803, -34.96314582746199306, 31.25396724875045251 ) ) ;
#11838=ADVANCED_FACE ( 'NONE', ( #37234 ), #56260, .F. ) ;
#11839=CARTESIAN_POINT ( 'NONE',  ( 0.5830082357119558134, -19.98760262368099561, 42.42319856276937173 ) ) ;
#11840=CARTESIAN_POINT ( 'NONE',  ( 0.7764146366350263007, 44.99430970888712267, -13.24962518299705216 ) ) ;
#11849=ORIENTED_EDGE ( 'NONE', *, *, #33447, .F. ) ;
#11850=CARTESIAN_POINT ( 'NONE',  ( 0.9789233960466698914, 4.064014989232912711, 41.71115569005051071 ) ) ;
#11858=CARTESIAN_POINT ( 'NONE',  ( 4.962356264823608143, -41.65024625884313991, -6.040909239515997342 ) ) ;
#11866=CARTESIAN_POINT ( 'NONE',  ( 0.5824935313925948543, -30.55463868283966633, -35.57600640902456490 ) ) ;
#11868=ORIENTED_EDGE ( 'NONE', *, *, #25203, .F. ) ;
#11872=ORIENTED_EDGE ( 'NONE', *, *, #28437, .T. ) ;
#11873=AXIS2_PLACEMENT_3D ( 'NONE', #23417, #28733, #3975 ) ;
#11877=CARTESIAN_POINT ( 'NONE',  ( 0.5817216825391123836, 45.34790762631963901, 11.94998854067397787 ) ) ;
#11889=CARTESIAN_POINT ( 'NONE',  ( 3.376099380956838925, 13.33943071323252916, -1.329651036526449115 ) ) ;
#11895=CARTESIAN_POINT ( 'NONE',  ( 0.5804410086790514622, 4.150428748652395861, -46.71502748642834746 ) ) ;
#11910=VECTOR ( 'NONE', #44031, 1000.000000000000114 ) ;
#11914=ORIENTED_EDGE ( 'NONE', *, *, #29335, .T. ) ;
#11923=VERTEX_POINT ( 'NONE', #23421 ) ;
#11930=CARTESIAN_POINT ( 'NONE',  ( 3.661933894777864573, 39.48007685360700947, 25.57253793789223550 ) ) ;
#11931=EDGE_CURVE ( 'NONE', #10343, #60737, #15129, .T. ) ;
#11940=EDGE_LOOP ( 'NONE', ( #49796, #19700, #57676, #13283 ) ) ;
#11944=CARTESIAN_POINT ( 'NONE',  ( 0.7764146366350244133, 36.25149456319285690, -29.76356187696567801 ) ) ;
#11945=EDGE_LOOP ( 'NONE', ( #22727, #28585, #17992, #13372 ) ) ;
#11947=CARTESIAN_POINT ( 'NONE',  ( 1.231276596079887264, -37.02495017545888345, 19.65781868679367150 ) ) ;
#11950=CARTESIAN_POINT ( 'NONE',  ( 2.282816707992323835, 42.71620190746931911, -19.54029326822607260 ) ) ;
#11962=CARTESIAN_POINT ( 'NONE',  ( 4.962356264823608143, 22.27740539909265394, 35.70648129607319277 ) ) ;
#11964=FACE_OUTER_BOUND ( 'NONE', #58808, .T. ) ;
#11968=CARTESIAN_POINT ( 'NONE',  ( 5.917102823773431552, -19.39506196288385098, -5.321775033542660793 ) ) ;
#11969=CARTESIAN_POINT ( 'NONE',  ( 0.5806925824938499181, -13.37132486740634540, -44.94919391528445374 ) ) ;
#11975=ORIENTED_EDGE ( 'NONE', *, *, #27473, .F. ) ;
#11976=CARTESIAN_POINT ( 'NONE',  ( 0.5806925824938502512, -44.11884900496080775, 15.89809815106926116 ) ) ;
#11980=VERTEX_POINT ( 'NONE', #53448 ) ;
#11982=B_SPLINE_CURVE_WITH_KNOTS ( 'NONE', 3,
 ( #7207, #41094, #50748, #12568 ),
 .UNSPECIFIED., .F., .F.,
 ( 4, 4 ),
 ( 4.470280076681872512E-19, 0.002042055671079073039 ),
 .UNSPECIFIED. ) ;
#11995=CARTESIAN_POINT ( 'NONE',  ( 0.9762797500689124330, -34.26226594605912368, -24.13341909939868657 ) ) ;
#11998=ORIENTED_EDGE ( 'NONE', *, *, #38232, .F. ) ;
#12009=( BOUNDED_SURFACE ( )  B_SPLINE_SURFACE ( 3, 1, ( 
 ( #30903, #21202 ),
 ( #11194, #34695 ),
 ( #40337, #16506 ),
 ( #40960, #35317 ) ),
 .UNSPECIFIED., .F., .F., .F. ) 
 B_SPLINE_SURFACE_WITH_KNOTS ( ( 4, 4 ),
 ( 2, 2 ),
 ( 0.000000000000000000, 1.000000000000000000 ),
 ( 0.000000000000000000, 1.000000000000000000 ),
 .UNSPECIFIED. ) 
 GEOMETRIC_REPRESENTATION_ITEM ( )  RATIONAL_B_SPLINE_SURFACE ( (
 ( 1.000000000000000000, 1.000000000000000000),
 ( 0.9729067724841187204, 0.9999501103223794596),
 ( 0.9729067724841187204, 0.9999501103223794596),
 ( 1.000000000000000000, 1.000000000000000000) ) ) 
 REPRESENTATION_ITEM ( '' )  SURFACE ( )  );
#12012=ORIENTED_EDGE ( 'NONE', *, *, #33136, .T. ) ;
#12014=CARTESIAN_POINT ( 'NONE',  ( 2.618530812446111078, 6.104648047582966974, -46.60965631082621030 ) ) ;
#12015=CARTESIAN_POINT ( 'NONE',  ( 0.9762797500689124330, -17.18051571332090788, -38.22505284509149703 ) ) ;
#12020=CARTESIAN_POINT ( 'NONE',  ( 4.958415959904820980, 12.97383654754940530, 43.53025980924199700 ) ) ;
#12041=DIRECTION ( 'NONE',  ( -1.000000000000000000, -0.000000000000000000, -0.000000000000000000 ) ) ;
#12042=CARTESIAN_POINT ( 'NONE',  ( 0.9762797500689124330, -27.44172181261435739, 31.67454323498272117 ) ) ;
#12051=DIRECTION ( 'NONE',  ( 0.000000000000000000, 0.000000000000000000, 1.000000000000000000 ) ) ;
#12053=ORIENTED_EDGE ( 'NONE', *, *, #22087, .F. ) ;
#12056=ADVANCED_FACE ( 'NONE', ( #20276 ), #32683, .F. ) ;
#12059=CARTESIAN_POINT ( 'NONE',  ( 0.5806925824938506953, -38.96949031362410665, -26.08833430941730924 ) ) ;
#12061=ORIENTED_EDGE ( 'NONE', *, *, #35203, .F. ) ;
#12064=EDGE_CURVE ( 'NONE', #28734, #12846, #22730, .T. ) ;
#12066=ORIENTED_EDGE ( 'NONE', *, *, #59468, .T. ) ;
#12067=ORIENTED_EDGE ( 'NONE', *, *, #29256, .T. ) ;
#12068=FACE_OUTER_BOUND ( 'NONE', #13214, .T. ) ;
#12069=CARTESIAN_POINT ( 'NONE',  ( 4.962356264823608143, 0.000000000000000000, 0.000000000000000000 ) ) ;
#12070=B_SPLINE_CURVE_WITH_KNOTS ( 'NONE', 3,
 ( #44221, #30381, #1251, #20388 ),
 .UNSPECIFIED., .F., .F.,
 ( 4, 4 ),
 ( 2.787728152484798234E-17, 0.005004948556313835659 ),
 .UNSPECIFIED. ) ;
#12071=ORIENTED_EDGE ( 'NONE', *, *, #9742, .T. ) ;
#12073=CARTESIAN_POINT ( 'NONE',  ( 4.956445790444027111, 14.46717203539434671, -44.81337951368921324 ) ) ;
#12078=CARTESIAN_POINT ( 'NONE',  ( 3.661933894777890330, 12.72741214118793529, -45.28403852506967553 ) ) ;
#12088=ORIENTED_EDGE ( 'NONE', *, *, #31753, .F. ) ;
#12090=CARTESIAN_POINT ( 'NONE',  ( 1.231276596079881047, 20.88402890667877898, -36.34740854095476692 ) ) ;
#12092=CARTESIAN_POINT ( 'NONE',  ( 4.962356264823608143, 0.000000000000000000, 0.000000000000000000 ) ) ;
#12093=CARTESIAN_POINT ( 'NONE',  ( 0.5804410086790514622, 22.05813747677438741, 41.38790189066267544 ) ) ;
#12099=( BOUNDED_SURFACE ( )  B_SPLINE_SURFACE ( 3, 1, ( 
 ( #61513, #17392 ),
 ( #28028, #4188 ),
 ( #22705, #56821 ),
 ( #13950, #33051 ) ),
 .UNSPECIFIED., .F., .F., .F. ) 
 B_SPLINE_SURFACE_WITH_KNOTS ( ( 4, 4 ),
 ( 2, 2 ),
 ( 0.000000000000000000, 1.000000000000000000 ),
 ( 0.000000000000000000, 1.000000000000000000 ),
 .UNSPECIFIED. ) 
 GEOMETRIC_REPRESENTATION_ITEM ( )  RATIONAL_B_SPLINE_SURFACE ( (
 ( 1.000000000000000000, 1.000000000000000000),
 ( 0.7282232189291693025, 0.9929344683865674037),
 ( 0.7282232189291693025, 0.9929344683865674037),
 ( 1.000000000000000000, 1.000000000000000000) ) ) 
 REPRESENTATION_ITEM ( '' )  SURFACE ( )  );
#12100=CARTESIAN_POINT ( 'NONE',  ( 0.5834584762367746036, 27.96416347290652382, -37.64626874304744319 ) ) ;
#12108=CARTESIAN_POINT ( 'NONE',  ( 4.291220156522060236, -11.88564107118090973, 45.58640733412488544 ) ) ;
#12120=ORIENTED_EDGE ( 'NONE', *, *, #55504, .F. ) ;
#12129=CARTESIAN_POINT ( 'NONE',  ( 0.8560838555295223751, -42.27062166135446120, -20.33635607586480631 ) ) ;
#12131=B_SPLINE_CURVE_WITH_KNOTS ( 'NONE', 3,
 ( #33392, #142, #38406, #57452 ),
 .UNSPECIFIED., .F., .F.,
 ( 4, 4 ),
 ( 2.501853776554200607E-17, 0.005004948556313833924 ),
 .UNSPECIFIED. ) ;
#12135=CARTESIAN_POINT ( 'NONE',  ( 4.958415959904818315, 24.86570830293410594, 38.01184689561967645 ) ) ;
#12137=VECTOR ( 'NONE', #2273, 1000.000000000000000 ) ;
#12143=B_SPLINE_CURVE_WITH_KNOTS ( 'NONE', 3,
 ( #58908, #6893, #20407, #19799, #15097, #16023 ),
 .UNSPECIFIED., .F., .F.,
 ( 4, 2, 4 ),
 ( 1.167014589833948395E-16, 0.0002448718616795945600, 0.0004897437233590723514 ),
 .UNSPECIFIED. ) ;
#12146=CARTESIAN_POINT ( 'NONE',  ( 0.5830081025819928708, -19.49199439610001150, 42.65318497890458360 ) ) ;
#12152=ORIENTED_EDGE ( 'NONE', *, *, #13665, .T. ) ;
#12154=CARTESIAN_POINT ( 'NONE',  ( 0.9784957157296387820, 4.426412977119490222, 41.67421175197387129 ) ) ;
#12162=FACE_OUTER_BOUND ( 'NONE', #37238, .T. ) ;
#12166=CARTESIAN_POINT ( 'NONE',  ( 4.960386119450145515, 23.14534831554981764, -37.13124447179514931 ) ) ;
#12169=CARTESIAN_POINT ( 'NONE',  ( 0.5804410086790514622, -29.86002002114410558, 36.16488706179337953 ) ) ;
#12172=CARTESIAN_POINT ( 'NONE',  ( 2.528190830796657629, -40.03694634880724124, 12.62129403887486134 ) ) ;
#12173=FACE_OUTER_BOUND ( 'NONE', #56944, .T. ) ;
#12175=EDGE_CURVE ( 'NONE', #48936, #41808, #22112, .T. ) ;
#12183=CARTESIAN_POINT ( 'NONE',  ( 5.917102823773431552, -2.021675920617120870, 20.01006108245896442 ) ) ;
#12184=ADVANCED_FACE ( 'NONE', ( #3596 ), #27791, .T. ) ;
#12193=CARTESIAN_POINT ( 'NONE',  ( 5.917102823773431552, 3.336722021764624291, -19.83320458728778135 ) ) ;
#12195=CARTESIAN_POINT ( 'NONE',  ( 1.000433927950262092, -7.619417497986461285, -41.21120181023874096 ) ) ;
#12199=VERTEX_POINT ( 'NONE', #40945 ) ;
#12200=CARTESIAN_POINT ( 'NONE',  ( 5.896278296736517710, -2.018661446113838132, 20.01129644926478335 ) ) ;
#12208=B_SPLINE_CURVE_WITH_KNOTS ( 'NONE', 3,
 ( #32119, #13323, #60590, #36833 ),
 .UNSPECIFIED., .F., .F.,
 ( 4, 4 ),
 ( 0.000000000000000000, 0.004446298630425082367 ),
 .UNSPECIFIED. ) ;
#12219=CARTESIAN_POINT ( 'NONE',  ( 0.6064782688330849769, 42.89335125862529452, 18.96034979168258516 ) ) ;
#12220=CARTESIAN_POINT ( 'NONE',  ( 1.000110580585051201, 41.61827148400551835, -4.933250597274972726 ) ) ;
#12227=ORIENTED_EDGE ( 'NONE', *, *, #55119, .T. ) ;
#12234=ORIENTED_EDGE ( 'NONE', *, *, #21236, .F. ) ;
#12242=CARTESIAN_POINT ( 'NONE',  ( 0.5806925824938499181, -44.47729014209976128, 14.86583411581871772 ) ) ;
#12244=CARTESIAN_POINT ( 'NONE',  ( 4.962356264823608143, 0.000000000000000000, 0.000000000000000000 ) ) ;
#12248=ORIENTED_EDGE ( 'NONE', *, *, #18718, .F. ) ;
#12255=CARTESIAN_POINT ( 'NONE',  ( 1.157643937452368821, 10.51841477362188471, 40.57542637169456157 ) ) ;
#12256=CARTESIAN_POINT ( 'NONE',  ( 3.782625744892851749, -10.79728826547640530, 40.62827427060136642 ) ) ;
#12269=VECTOR ( 'NONE', #36730, 1000.000000000000000 ) ;
#12271=CARTESIAN_POINT ( 'NONE',  ( 0.9762797500689124330, 19.69530149098714489, -36.99215976885945167 ) ) ;
#12274=CARTESIAN_POINT ( 'NONE',  ( 3.238018933889920792, 12.84302458974300443, 3.803184422942107901 ) ) ;
#12275=DIRECTION ( 'NONE',  ( -0.07500201931887527651, -0.01982172072489229997, 0.9969863572213991665 ) ) ;
#12284=CARTESIAN_POINT ( 'NONE',  ( 5.901463166500146684, -18.51103891486777542, 7.865068889265228513 ) ) ;
#12285=CARTESIAN_POINT ( 'NONE',  ( 3.376099380956838925, 13.21675742563009770, 2.241808819707602041 ) ) ;
#12290=CARTESIAN_POINT ( 'NONE',  ( 0.8560838555295158248, 21.73747136795142154, 41.56747734237938374 ) ) ;
#12293=ORIENTED_EDGE ( 'NONE', *, *, #19755, .T. ) ;
#12295=ADVANCED_FACE ( 'NONE', ( #37161 ), #43493, .F. ) ;
#12297=ORIENTED_EDGE ( 'NONE', *, *, #19731, .F. ) ;
#12300=CARTESIAN_POINT ( 'NONE',  ( 3.376099380956842921, -4.408915724532880276, -12.65977273753497379 ) ) ;
#12303=CARTESIAN_POINT ( 'NONE',  ( 0.7056313189692702270, 43.50197882008412620, 17.53072966805745381 ) ) ;
#12304=ORIENTED_EDGE ( 'NONE', *, *, #24690, .F. ) ;
#12315=ORIENTED_EDGE ( 'NONE', *, *, #47815, .T. ) ;
#12316=CARTESIAN_POINT ( 'NONE',  ( 0.9769922540276048117, -39.44262731837918068, -14.16371085943138297 ) ) ;
#12319=CARTESIAN_POINT ( 'NONE',  ( 0.8554163680231720024, 44.99993935735625428, -13.27444654010398928 ) ) ;
#12327=CARTESIAN_POINT ( 'NONE',  ( 5.896782393890504181, -15.78847575145224447, 12.45994062280461634 ) ) ;
#12334=CARTESIAN_POINT ( 'NONE',  ( 4.962356264823608143, 0.000000000000000000, 0.000000000000000000 ) ) ;
#12336=CARTESIAN_POINT ( 'NONE',  ( 0.9788927965476029724, -22.43074396039533269, 35.40054149324505062 ) ) ;
#12340=CARTESIAN_POINT ( 'NONE',  ( 5.894904586330512508, 17.95171060118299522, 9.070032996247425316 ) ) ;
#12341=ORIENTED_EDGE ( 'NONE', *, *, #45144, .T. ) ;
#12344=DIRECTION ( 'NONE',  ( -0.07500201931887527651, -0.4319596767211244526, -0.8987688995426313943 ) ) ;
#12350=CARTESIAN_POINT ( 'NONE',  ( 4.956445790443998689, -10.39006634428300835, 45.93021414603936847 ) ) ;
#12352=CARTESIAN_POINT ( 'NONE',  ( 4.956445790443988031, 0.000000000000000000, 0.000000000000000000 ) ) ;
#12359=CARTESIAN_POINT ( 'NONE',  ( 5.917102823773431552, -11.93691330175311194, 16.18640846136571199 ) ) ;
#12360=EDGE_LOOP ( 'NONE', ( #41549, #17525, #27601, #25517 ) ) ;
#12364=( BOUNDED_SURFACE ( )  B_SPLINE_SURFACE ( 3, 1, ( 
 ( #20910, #36263 ),
 ( #40663, #12451 ),
 ( #31541, #60335 ),
 ( #57171, #38125 ) ),
 .UNSPECIFIED., .F., .F., .F. ) 
 B_SPLINE_SURFACE_WITH_KNOTS ( ( 4, 4 ),
 ( 2, 2 ),
 ( 0.000000000000000000, 1.000000000000000000 ),
 ( 0.000000000000000000, 1.000000000000000000 ),
 .UNSPECIFIED. ) 
 GEOMETRIC_REPRESENTATION_ITEM ( )  RATIONAL_B_SPLINE_SURFACE ( (
 ( 1.000000000000000000, 1.000000000000000000),
 ( 0.9952954269826590483, 0.8620686068821339365),
 ( 0.9952954269826590483, 0.8620686068821339365),
 ( 1.000000000000000000, 1.000000000000000000) ) ) 
 REPRESENTATION_ITEM ( '' )  SURFACE ( )  );
#12366=DIRECTION ( 'NONE',  ( 0.000000000000000000, 0.000000000000000000, 1.000000000000000000 ) ) ;
#12368=ORIENTED_EDGE ( 'NONE', *, *, #34617, .F. ) ;
#12374=CARTESIAN_POINT ( 'NONE',  ( 4.956445790443998689, -23.10347171912865250, 41.03373788314999615 ) ) ;
#12381=ORIENTED_EDGE ( 'NONE', *, *, #54682, .T. ) ;
#12383=CARTESIAN_POINT ( 'NONE',  ( 0.8554163680231720024, -29.58718577084438905, 36.41159034254562954 ) ) ;
#12388=CARTESIAN_POINT ( 'NONE',  ( 0.8554163680231708922, 37.37991192211431724, -28.35397075908055697 ) ) ;
#12392=CARTESIAN_POINT ( 'NONE',  ( 0.5824936645240089694, -46.81422852104944354, 2.768788005476148673 ) ) ;
#12394=CARTESIAN_POINT ( 'NONE',  ( 3.782625744892853525, -24.05484086317139614, -34.47611833055603370 ) ) ;
#12396=EDGE_CURVE ( 'NONE', #35884, #40578, #21777, .T. ) ;
#12398=CARTESIAN_POINT ( 'NONE',  ( 0.5804410086790514622, 10.33990028284759966, 45.74501408892737686 ) ) ;
#12403=CARTESIAN_POINT ( 'NONE',  ( 2.528190830796654964, 41.42606007575643901, 6.792325283202126585 ) ) ;
#12407=CARTESIAN_POINT ( 'NONE',  ( 0.9790320750461900534, -31.13925818481557073, 28.04788284775852603 ) ) ;
#12410=CARTESIAN_POINT ( 'NONE',  ( 0.9785694773339252972, -7.190011144658855713, 41.28727582990130429 ) ) ;
#12416=CARTESIAN_POINT ( 'NONE',  ( 0.5835871038041858805, -7.934817416658265010, 46.21983476242418476 ) ) ;
#12418=EDGE_CURVE ( 'NONE', #30761, #45872, #33000, .T. ) ;
#12422=ORIENTED_EDGE ( 'NONE', *, *, #36799, .T. ) ;
#12430=CARTESIAN_POINT ( 'NONE',  ( 4.960386119450136633, 28.60674280242237799, 33.10726099979272874 ) ) ;
#12435=ORIENTED_EDGE ( 'NONE', *, *, #55490, .T. ) ;
#12451=CARTESIAN_POINT ( 'NONE',  ( 0.5782707292762442330, -19.08336439318344802, -42.84345407579313303 ) ) ;
#12453=DIRECTION ( 'NONE',  ( -0.07500201931887529039, 0.08636880102339446197, -0.9934360207420870337 ) ) ;
#12461=CARTESIAN_POINT ( 'NONE',  ( 4.962356264823608143, 0.000000000000000000, 0.000000000000000000 ) ) ;
#12466=CARTESIAN_POINT ( 'NONE',  ( 4.962356264823602814, 22.27740539909316198, -35.70648129607287302 ) ) ;
#12468=CARTESIAN_POINT ( 'NONE',  ( 0.9791128995231602739, 38.58122919918244520, -16.36539604550769411 ) ) ;
#12469=AXIS2_PLACEMENT_3D ( 'NONE', #6821, #45098, #49147 ) ;
#12476=ORIENTED_EDGE ( 'NONE', *, *, #42809, .T. ) ;
#12479=CARTESIAN_POINT ( 'NONE',  ( 0.9769922540276050338, -27.39328719377936494, 31.71654728694862158 ) ) ;
#12500=CARTESIAN_POINT ( 'NONE',  ( 0.9762797500689124330, 38.77779312671030709, 15.89363222827819300 ) ) ;
#12501=ORIENTED_EDGE ( 'NONE', *, *, #9381, .F. ) ;
#12502=CARTESIAN_POINT ( 'NONE',  ( 0.8554163680231720024, 3.785871848717075494, -46.76401017296218043 ) ) ;
#12510=CARTESIAN_POINT ( 'NONE',  ( 5.917102823773431552, 16.58597737984205622, 11.37519548874259279 ) ) ;
#12513=B_SPLINE_CURVE_WITH_KNOTS ( 'NONE', 3,
 ( #8834, #53716, #30237, #16162 ),
 .UNSPECIFIED., .F., .F.,
 ( 4, 4 ),
 ( 0.000000000000000000, 0.005004948556313809638 ),
 .UNSPECIFIED. ) ;
#12515=ORIENTED_EDGE ( 'NONE', *, *, #40707, .F. ) ;
#12522=DIRECTION ( 'NONE',  ( -1.000000000000000000, -0.000000000000000000, -0.000000000000000000 ) ) ;
#12523=CARTESIAN_POINT ( 'NONE',  ( 1.091591847532195070, 41.63653874899925711, -4.812237728845413898 ) ) ;
#12525=ORIENTED_EDGE ( 'NONE', *, *, #1966, .T. ) ;
#12528=ORIENTED_EDGE ( 'NONE', *, *, #48528, .F. ) ;
#12530=AXIS2_PLACEMENT_3D ( 'NONE', #569, #59122, #48501 ) ;
#12531=VERTEX_POINT ( 'NONE', #17043 ) ;
#12541=CARTESIAN_POINT ( 'NONE',  ( 0.8554163680231816613, -42.27859581856498750, -20.34025095032602692 ) ) ;
#12542=CARTESIAN_POINT ( 'NONE',  ( 0.5797568665920712627, -34.35528743026003440, 31.92083229156293811 ) ) ;
#12548=CARTESIAN_POINT ( 'NONE',  ( 1.000433927950263868, 40.24156067008907200, -11.70621512224969329 ) ) ;
#12568=CARTESIAN_POINT ( 'NONE',  ( 2.788021980263895028, 5.971756191165462832E-15, 46.99417130740431503 ) ) ;
#12569=CARTESIAN_POINT ( 'NONE',  ( 0.5804410086790514622, -45.84731009780866628, 9.876437042312842252 ) ) ;
#12574=B_SPLINE_CURVE_WITH_KNOTS ( 'NONE', 3,
 ( #27118, #34756, #10951, #46242, #20647, #50600 ),
 .UNSPECIFIED., .F., .F.,
 ( 4, 2, 4 ),
 ( 4.336808689942017736E-19, 0.0002291459268755700993, 0.0004582918537511397649 ),
 .UNSPECIFIED. ) ;
#12576=VECTOR ( 'NONE', #32464, 1000.000000000000114 ) ;
#12577=CARTESIAN_POINT ( 'NONE',  ( 0.8554163680231816613, 45.48289776771366633, 11.51136324522541443 ) ) ;
#12580=CARTESIAN_POINT ( 'NONE',  ( 2.282803330402961794, 31.69834785191134330, 34.66571290073540723 ) ) ;
#12582=CARTESIAN_POINT ( 'NONE',  ( 5.896278296736517710, -4.667894692254015432, 19.56368418157506994 ) ) ;
#12584=VERTEX_POINT ( 'NONE', #14499 ) ;
#12585=CARTESIAN_POINT ( 'NONE',  ( 3.782625744892854414, -40.24479482953532283, -12.14885151870784874 ) ) ;
#12588=B_SPLINE_CURVE_WITH_KNOTS ( 'NONE', 3,
 ( #46912, #38432, #27778, #13697 ),
 .UNSPECIFIED., .F., .F.,
 ( 4, 4 ),
 ( 4.336808689942017736E-19, 0.004446298630425048540 ),
 .UNSPECIFIED. ) ;
#12589=CARTESIAN_POINT ( 'NONE',  ( 0.6064515330803578186, -14.57163282274000871, -44.57579895993265495 ) ) ;
#12595=CARTESIAN_POINT ( 'NONE',  ( 0.8554163680231708922, 5.604726001789484435, -46.58103175710778743 ) ) ;
#12598=ADVANCED_FACE ( 'NONE', ( #52370 ), #17499, .F. ) ;
#12610=CARTESIAN_POINT ( 'NONE',  ( 5.917102823773431552, 20.06759006498877795, 1.334746056486321164 ) ) ;
#12612=CARTESIAN_POINT ( 'NONE',  ( 0.5837800304671211249, -30.31211522357351384, 35.78285906481343659 ) ) ;
#12615=CARTESIAN_POINT ( 'NONE',  ( 0.5797568665920711517, 43.41643168312820222, 17.72678110955651931 ) ) ;
#12620=ADVANCED_FACE ( 'NONE', ( #32678 ), #50695, .T. ) ;
#12631=CARTESIAN_POINT ( 'NONE',  ( 0.9780106845699476636, -41.83479645273218495, 2.486172201176787500 ) ) ;
#12642=CARTESIAN_POINT ( 'NONE',  ( 0.9762797500689124330, 33.20096159360316790, 25.57383300261796677 ) ) ;
#12643=CARTESIAN_POINT ( 'NONE',  ( 1.092182651088183354, 35.65846785729959123, -22.02804699723095183 ) ) ;
#12644=DIRECTION ( 'NONE',  ( -1.000000000000000000, -0.000000000000000000, -0.000000000000000000 ) ) ;
#12655=CARTESIAN_POINT ( 'NONE',  ( 0.5782707292762442330, -8.514009628394607176, 46.12209875705161721 ) ) ;
#12657=VERTEX_POINT ( 'NONE', #47695 ) ;
#12664=DIRECTION ( 'NONE',  ( 0.07906939808003035641, -0.3658060745126776592, 0.9273262350094960693 ) ) ;
#12672=B_SPLINE_CURVE_WITH_KNOTS ( 'NONE', 3,
 ( #46535, #42166, #52439, #8288 ),
 .UNSPECIFIED., .F., .F.,
 ( 4, 4 ),
 ( 0.000000000000000000, 0.004447772540403789436 ),
 .UNSPECIFIED. ) ;
#12673=CARTESIAN_POINT ( 'NONE',  ( 0.8560838555295223751, -41.44626783305086093, 21.96769712083507287 ) ) ;
#12685=CARTESIAN_POINT ( 'NONE',  ( 3.238018933889920792, 6.676852487596914187, 11.61150865419837963 ) ) ;
#12702=CARTESIAN_POINT ( 'NONE',  ( 0.9754292589017241610, 40.56950062075481611, 10.50919056244812566 ) ) ;
#12703=B_SPLINE_CURVE_WITH_KNOTS ( 'NONE', 3,
 ( #39649, #5767, #24920, #30510, #1085, #49630 ),
 .UNSPECIFIED., .F., .F.,
 ( 4, 2, 4 ),
 ( 8.542522420166516410E-18, 0.0002291472222819935318, 0.0004582944445639785527 ),
 .UNSPECIFIED. ) ;
#12704=CARTESIAN_POINT ( 'NONE',  ( 0.5848930533535030563, 32.73270734968657791, 33.58337314724851552 ) ) ;
#12707=DIRECTION ( 'NONE',  ( 0.000000000000000000, 0.000000000000000000, 1.000000000000000000 ) ) ;
#12710=CARTESIAN_POINT ( 'NONE',  ( 5.901463166500145796, -18.52233187494223188, 7.838436850235891207 ) ) ;
#12711=CARTESIAN_POINT ( 'NONE',  ( 0.5806925824938499181, 11.40214825760356376, -45.48860711711441240 ) ) ;
#12725=CARTESIAN_POINT ( 'NONE',  ( 0.9775691876210976794, -7.342838859687320863, 41.26034932560141044 ) ) ;
#12731=B_SPLINE_CURVE_WITH_KNOTS ( 'NONE', 3,
 ( #52422, #52118, #47436, #48056, #38366, #24235 ),
 .UNSPECIFIED., .F., .F.,
 ( 4, 2, 4 ),
 ( 7.007167689862070887E-18, 0.0002448709889506557472, 0.0004897419779013045555 ),
 .UNSPECIFIED. ) ;
#12734=DIRECTION ( 'NONE',  ( 0.07906939808003035641, 0.8264033190538777607, -0.5574994031781526083 ) ) ;
#12740=( BOUNDED_SURFACE ( )  B_SPLINE_SURFACE ( 3, 1, ( 
 ( #50357, #7744 ),
 ( #26556, #2734 ),
 ( #26866, #3047 ),
 ( #22172, #22783 ) ),
 .UNSPECIFIED., .F., .F., .F. ) 
 B_SPLINE_SURFACE_WITH_KNOTS ( ( 4, 4 ),
 ( 2, 2 ),
 ( 0.000000000000000000, 1.000000000000000000 ),
 ( 0.000000000000000000, 1.000000000000000000 ),
 .UNSPECIFIED. ) 
 GEOMETRIC_REPRESENTATION_ITEM ( )  RATIONAL_B_SPLINE_SURFACE ( (
 ( 1.000000000000000000, 1.000000000000000000),
 ( 0.7282232189291693025, 0.9929344683865674037),
 ( 0.7282232189291693025, 0.9929344683865674037),
 ( 1.000000000000000000, 1.000000000000000000) ) ) 
 REPRESENTATION_ITEM ( '' )  SURFACE ( )  );
#12742=ORIENTED_EDGE ( 'NONE', *, *, #25464, .F. ) ;
#12743=CARTESIAN_POINT ( 'NONE',  ( 0.9784957157296357844, 24.67156637886485626, -33.87693713141196383 ) ) ;
#12745=CARTESIAN_POINT ( 'NONE',  ( 0.9790320750461900534, 32.94311240808050201, -25.90537545396250607 ) ) ;
#12752=EDGE_CURVE ( 'NONE', #5070, #10104, #59148, .T. ) ;
#12754=VERTEX_POINT ( 'NONE', #19818 ) ;
#12755=B_SPLINE_CURVE_WITH_KNOTS ( 'NONE', 3,
 ( #41014, #41309, #45694, #16556 ),
 .UNSPECIFIED., .F., .F.,
 ( 4, 4 ),
 ( 0.000000000000000000, 0.004447772540403837141 ),
 .UNSPECIFIED. ) ;
#12760=VECTOR ( 'NONE', #36340, 1000.000000000000000 ) ;
#12762=EDGE_CURVE ( 'NONE', #37909, #3915, #52375, .T. ) ;
#12763=CARTESIAN_POINT ( 'NONE',  ( 0.9789889208857696090, 4.099175781249488004, -41.70769300688767345 ) ) ;
#12767=CARTESIAN_POINT ( 'NONE',  ( 5.896278296736517710, -15.78795198421094170, 12.46064010228340280 ) ) ;
#12778=ORIENTED_EDGE ( 'NONE', *, *, #37191, .F. ) ;
#12781=EDGE_CURVE ( 'NONE', #58714, #2462, #46757, .T. ) ;
#12782=CARTESIAN_POINT ( 'NONE',  ( 0.5837800304671199036, -41.87608985909586323, 21.10996045217588701 ) ) ;
#12786=DIRECTION ( 'NONE',  ( -0.07906939808003035641, 0.1078133555909867869, 0.9910218517487257017 ) ) ;
#12787=CARTESIAN_POINT ( 'NONE',  ( 1.092182651088184242, -26.45970545413510777, 32.50607899643846110 ) ) ;
#12788=CARTESIAN_POINT ( 'NONE',  ( 5.917102823773431552, -19.93362549613927115, 2.672132599892532046 ) ) ;
#12790=ORIENTED_EDGE ( 'NONE', *, *, #36628, .T. ) ;
#12793=CARTESIAN_POINT ( 'NONE',  ( 4.962356264823608143, 0.000000000000000000, 0.000000000000000000 ) ) ;
#12796=CARTESIAN_POINT ( 'NONE',  ( 0.9787284016396617936, -26.91414329176047815, 32.12421033736727338 ) ) ;
#12802=CARTESIAN_POINT ( 'NONE',  ( 0.5834584762367747146, 10.69421303378797994, 45.66037446847265358 ) ) ;
#12803=ADVANCED_FACE ( 'NONE', ( #30115 ), #55158, .F. ) ;
#12805=CARTESIAN_POINT ( 'NONE',  ( 0.9754292580325140127, 19.62773382990652138, 37.02809111480564042 ) ) ;
#12814=CARTESIAN_POINT ( 'NONE',  ( 4.956445790444005794, -27.49627641100061837, -38.22947597953034204 ) ) ;
#12815=B_SPLINE_CURVE_WITH_KNOTS ( 'NONE', 3,
 ( #21894, #34762, #21578, #15966, #40108, #35386, #40715, #53829, #54762, #49152, #54445, #59787, #54136, #16897, #36012, #55077 ),
 .UNSPECIFIED., .F., .F.,
 ( 4, 3, 3, 3, 3, 4 ),
 ( 1.868385820337156008E-17, 0.0002732102107931905959, 0.0004098135523333825640, 0.0005464168938825052137, 0.0008195847345945452868, 0.001092771384553100928 ),
 .UNSPECIFIED. ) ;
#12817=CARTESIAN_POINT ( 'NONE',  ( 5.896782393890504181, -2.019528367549592307, 20.01118667272569951 ) ) ;
#12819=CARTESIAN_POINT ( 'NONE',  ( 5.838029081930957709, 25.43272996496265748, 39.80252887295241493 ) ) ;
#12837=ORIENTED_EDGE ( 'NONE', *, *, #47536, .F. ) ;
#12839=LINE ( 'NONE', #31929, #59324 ) ;
#12846=VERTEX_POINT ( 'NONE', #54841 ) ;
#12848=CARTESIAN_POINT ( 'NONE',  ( 0.5806925824938494740, 36.46274162637944016, -29.49052111156159128 ) ) ;
#12855=CARTESIAN_POINT ( 'NONE',  ( 1.092182651088184020, -39.33161120148861301, 14.48397544658308078 ) ) ;
#12856=CARTESIAN_POINT ( 'NONE',  ( 5.917102823773431552, 17.94639498788064813, 9.078360258918703352 ) ) ;
#12858=CARTESIAN_POINT ( 'NONE',  ( 0.8560838555295223751, -34.16988317699956923, 32.13708010619405542 ) ) ;
#12860=ORIENTED_EDGE ( 'NONE', *, *, #61435, .T. ) ;
#12870=CARTESIAN_POINT ( 'NONE',  ( 4.962356264823608143, 12.05238263218917716, 40.32338863178108568 ) ) ;
#12871=CARTESIAN_POINT ( 'NONE',  ( 0.9789889208857700531, 9.621692253337958078, -40.78918896257224702 ) ) ;
#12875=AXIS2_PLACEMENT_3D ( 'NONE', #58827, #48831, #43858 ) ;
#12878=CARTESIAN_POINT ( 'NONE',  ( 5.895596859100789899, 19.70914391261467102, 4.009716878325924050 ) ) ;
#12882=CARTESIAN_POINT ( 'NONE',  ( 0.5817217712918323347, 22.93558036730663829, -40.90469541780249330 ) ) ;
#12885=CARTESIAN_POINT ( 'NONE',  ( 5.901463166500145796, -19.39418503693765317, -5.327612701169281983 ) ) ;
#12888=ORIENTED_EDGE ( 'NONE', *, *, #31410, .T. ) ;
#12891=CARTESIAN_POINT ( 'NONE',  ( 0.9788927965476025284, 20.26469601834873657, 36.68349367107364145 ) ) ;
#12900=CARTESIAN_POINT ( 'NONE',  ( 5.910764540655178756, -18.51025558288811013, 7.865855117234400673 ) ) ;
#12904=CARTESIAN_POINT ( 'NONE',  ( 3.661921753702030102, 31.32117497468681933, -35.09437450702161954 ) ) ;
#12911=CARTESIAN_POINT ( 'NONE',  ( 4.962356264823608143, 0.000000000000000000, 0.000000000000000000 ) ) ;
#12920=CARTESIAN_POINT ( 'NONE',  ( 5.896782393890504181, 20.06834277495332941, 1.337050913387667350 ) ) ;
#12927=CARTESIAN_POINT ( 'NONE',  ( 4.962356264823608143, 0.000000000000000000, 0.000000000000000000 ) ) ;
#12931=CARTESIAN_POINT ( 'NONE',  ( 0.9762797500689124330, 41.46413394121043439, -6.086902470967093137 ) ) ;
#12942=CARTESIAN_POINT ( 'NONE',  ( 5.895881250540457863, -19.39944854657663242, 5.309338725022799466 ) ) ;
#12946=CARTESIAN_POINT ( 'NONE',  ( 0.5837800304671207918, 4.739362457610067025, -46.65592969467970619 ) ) ;
#12948=CARTESIAN_POINT ( 'NONE',  ( 0.9754292580325126805, -12.97161693114786019, 39.85052849204841863 ) ) ;
#12954=CARTESIAN_POINT ( 'NONE',  ( 2.528190830796658517, -36.90586700523726194, -20.00527722239178985 ) ) ;
#12956=CARTESIAN_POINT ( 'NONE',  ( 5.894904586330512508, -19.93362243062210482, 2.679572513488333474 ) ) ;
#12959=EDGE_CURVE ( 'NONE', #29761, #18772, #48612, .T. ) ;
#12965=DIRECTION ( 'NONE',  ( 0.07906939808003035641, 0.7447223275783754204, -0.6626738904570698141 ) ) ;
#12967=ORIENTED_EDGE ( 'NONE', *, *, #61957, .F. ) ;
#12968=CARTESIAN_POINT ( 'NONE',  ( 5.895881250540457863, -18.51513737938377346, 7.856040314996277196 ) ) ;
#12969=CARTESIAN_POINT ( 'NONE',  ( 5.895596859100789899, 3.341829471547073549, -19.83331437242869910 ) ) ;
#12978=ORIENTED_EDGE ( 'NONE', *, *, #38375, .T. ) ;
#12980=CARTESIAN_POINT ( 'NONE',  ( 1.231276596079881047, -37.78837162824498819, 18.14705873423338289 ) ) ;
#12981=EDGE_CURVE ( 'NONE', #42702, #16409, #794, .T. ) ;
#12984=CARTESIAN_POINT ( 'NONE',  ( 5.896782393890504181, -11.93563916323493146, 16.18847134979287361 ) ) ;
#12988=B_SPLINE_CURVE_WITH_KNOTS ( 'NONE', 3,
 ( #53428, #57816, #24326, #38760, #52199, #43457 ),
 .UNSPECIFIED., .F., .F.,
 ( 4, 2, 4 ),
 ( 1.196130537910465800E-16, 0.0002448718616795930421, 0.0004897437233590655210 ),
 .UNSPECIFIED. ) ;
#12990=B_SPLINE_CURVE_WITH_KNOTS ( 'NONE', 3,
 ( #12374, #32402, #17371, #55556 ),
 .UNSPECIFIED., .F., .F.,
 ( 4, 4 ),
 ( 5.594315114139762021E-17, 0.005004948556313858210 ),
 .UNSPECIFIED. ) ;
#13006=EDGE_CURVE ( 'NONE', #41352, #4083, #53043, .T. ) ;
#13018=FACE_OUTER_BOUND ( 'NONE', #23658, .T. ) ;
#13030=CARTESIAN_POINT ( 'NONE',  ( 0.5830081025819920937, -34.96316152485596973, -31.25394967950578007 ) ) ;
#13036=CARTESIAN_POINT ( 'NONE',  ( 3.661933894777873455, -45.01796196593215171, 13.63870468136689240 ) ) ;
#13038=EDGE_CURVE ( 'NONE', #31868, #47280, #34436, .T. ) ;
#13064=CARTESIAN_POINT ( 'NONE',  ( 0.9780106845699481077, 4.506814239222374674, -41.66557178137100692 ) ) ;
#13070=ORIENTED_EDGE ( 'NONE', *, *, #39777, .F. ) ;
#13071=DIRECTION ( 'NONE',  ( -1.000000000000000000, -0.000000000000000000, -0.000000000000000000 ) ) ;
#13074=ORIENTED_EDGE ( 'NONE', *, *, #35820, .T. ) ;
#13085=CARTESIAN_POINT ( 'NONE',  ( 0.5837799406558212834, -41.81448599028684754, 21.23187017069644611 ) ) ;
#13086=ORIENTED_EDGE ( 'NONE', *, *, #51253, .T. ) ;
#13087=CARTESIAN_POINT ( 'NONE',  ( 0.9769922540276050338, -22.17659144084161582, -35.56023547661229145 ) ) ;
#13089=DIRECTION ( 'NONE',  ( 0.07500201931887538753, 0.6334382584228924751, 0.7701497710603204538 ) ) ;
#13107=( BOUNDED_SURFACE ( )  B_SPLINE_SURFACE ( 3, 1, ( 
 ( #22849, #32885 ),
 ( #18779, #51959 ),
 ( #42287, #37587 ),
 ( #9357, #56655 ) ),
 .UNSPECIFIED., .F., .F., .F. ) 
 B_SPLINE_SURFACE_WITH_KNOTS ( ( 4, 4 ),
 ( 2, 2 ),
 ( 0.000000000000000000, 1.000000000000000000 ),
 ( 0.000000000000000000, 1.000000000000000000 ),
 .UNSPECIFIED. ) 
 GEOMETRIC_REPRESENTATION_ITEM ( )  RATIONAL_B_SPLINE_SURFACE ( (
 ( 1.000000000000000000, 1.000000000000000000),
 ( 0.9729067724841187204, 0.9999501103223794596),
 ( 0.9729067724841187204, 0.9999501103223794596),
 ( 1.000000000000000000, 1.000000000000000000) ) ) 
 REPRESENTATION_ITEM ( '' )  SURFACE ( )  );
#13110=ADVANCED_FACE ( 'NONE', ( #39475 ), #36746, .T. ) ;
#13118=CARTESIAN_POINT ( 'NONE',  ( 0.5817216825391118284, 46.53606797270585815, 5.799080086286046765 ) ) ;
#13126=CARTESIAN_POINT ( 'NONE',  ( 0.8554163680231720024, -26.01084021241217314, -39.04666009476586908 ) ) ;
#13127=ORIENTED_EDGE ( 'NONE', *, *, #57754, .F. ) ;
#13131=ORIENTED_EDGE ( 'NONE', *, *, #14610, .F. ) ;
#13141=DIRECTION ( 'NONE',  ( -0.07500201931887527651, 0.4673421949333779746, -0.8808893062882211522 ) ) ;
#13145=EDGE_LOOP ( 'NONE', ( #57183, #58309, #12234, #47416 ) ) ;
#13148=VERTEX_POINT ( 'NONE', #19740 ) ;
#13149=VERTEX_POINT ( 'NONE', #49155 ) ;
#13150=DIRECTION ( 'NONE',  ( 0.000000000000000000, 0.000000000000000000, -1.000000000000000000 ) ) ;
#13152=CARTESIAN_POINT ( 'NONE',  ( 0.7056759521545000746, -44.57577085471505285, 14.58593438299126177 ) ) ;
#13158=CARTESIAN_POINT ( 'NONE',  ( 0.5804410086790514622, -46.82762660194602944, 2.587129429331442854 ) ) ;
#13165=DIRECTION ( 'NONE',  ( -0.07906939808003035641, -0.9390317839750951245, 0.3346152103115038190 ) ) ;
#13167=CARTESIAN_POINT ( 'NONE',  ( 1.157643937452369487, 8.912044576298065124, -40.95824381079869880 ) ) ;
#13178=CARTESIAN_POINT ( 'NONE',  ( 4.962356264823608143, 0.000000000000000000, 0.000000000000000000 ) ) ;
#13179=ADVANCED_FACE ( 'NONE', ( #44491 ), #16387, .F. ) ;
#13182=CARTESIAN_POINT ( 'NONE',  ( 0.9790850452238875068, 29.17097364564380868, 30.08972626708911946 ) ) ;
#13187=ORIENTED_EDGE ( 'NONE', *, *, #4568, .T. ) ;
#13195=CARTESIAN_POINT ( 'NONE',  ( 0.9783242366443573035, -41.79629446811009075, -3.066636421480622765 ) ) ;
#13198=CIRCLE ( 'NONE', #46205, 42.08604991992415023 ) ;
#13200=CARTESIAN_POINT ( 'NONE',  ( 1.231276596079887264, 19.39962232756291272, -37.16088568059149111 ) ) ;
#13201=CARTESIAN_POINT ( 'NONE',  ( 0.5817217712918333339, -45.86342913730425863, -9.786767687844841745 ) ) ;
#13205=VERTEX_POINT ( 'NONE', #52609 ) ;
#13206=ORIENTED_EDGE ( 'NONE', *, *, #23040, .F. ) ;
#13210=ORIENTED_EDGE ( 'NONE', *, *, #21424, .F. ) ;
#13211=CARTESIAN_POINT ( 'NONE',  ( 0.8554163680231816613, 17.71207986799935696, 43.44522643353848679 ) ) ;
#13214=EDGE_LOOP ( 'NONE', ( #33408, #16109, #4688, #32339 ) ) ;
#13220=ADVANCED_FACE ( 'NONE', ( #919 ), #35623, .F. ) ;
#13226=VERTEX_POINT ( 'NONE', #44801 ) ;
#13228=CARTESIAN_POINT ( 'NONE',  ( 0.5832655196449132440, 11.09274990485192269, -45.56518498285437602 ) ) ;
#13231=CARTESIAN_POINT ( 'NONE',  ( 4.956445790444004906, -46.59545590650544966, 6.811867512257108181 ) ) ;
#13232=EDGE_CURVE ( 'NONE', #37323, #32724, #13754, .T. ) ;
#13237=CARTESIAN_POINT ( 'NONE',  ( 0.9787284016396609054, -41.80215183015796043, 2.985984142163401689 ) ) ;
#13241=CARTESIAN_POINT ( 'NONE',  ( 120.0000507999999968, 0.000000000000000000, 0.000000000000000000 ) ) ;
#13249=CARTESIAN_POINT ( 'NONE',  ( 0.5834584762367753807, 40.44190349954094899, -23.74212354333551644 ) ) ;
#13251=CARTESIAN_POINT ( 'NONE',  ( 0.9790724872846768845, 32.86481170631836335, 26.00460269817044434 ) ) ;
#13276=CARTESIAN_POINT ( 'NONE',  ( 1.000433927950261870, -2.058517538525916457, -41.85906333395944756 ) ) ;
#13277=ORIENTED_EDGE ( 'NONE', *, *, #48499, .T. ) ;
#13278=EDGE_LOOP ( 'NONE', ( #43888, #12067, #33557, #15498 ) ) ;
#13280=B_SPLINE_CURVE_WITH_KNOTS ( 'NONE', 3,
 ( #29331, #15253, #53433, #53729, #14957, #6114 ),
 .UNSPECIFIED., .F., .F.,
 ( 4, 2, 4 ),
 ( 5.294859796737922701E-18, 0.0002448709889506563977, 0.0004897419779013074828 ),
 .UNSPECIFIED. ) ;
#13283=ORIENTED_EDGE ( 'NONE', *, *, #15908, .F. ) ;
#13286=ORIENTED_EDGE ( 'NONE', *, *, #37430, .F. ) ;
#13287=ORIENTED_EDGE ( 'NONE', *, *, #47782, .F. ) ;
#13300=ADVANCED_FACE ( 'NONE', ( #43774 ), #43680, .T. ) ;
#13302=CONICAL_SURFACE ( 'NONE', #10303, 42.08604991992415023, 1.569615340895231137 ) ;
#13303=ORIENTED_EDGE ( 'NONE', *, *, #10443, .T. ) ;
#13304=CARTESIAN_POINT ( 'NONE',  ( 1.231276596079881047, -21.83837404314779462, -35.78214904347746739 ) ) ;
#13305=CARTESIAN_POINT ( 'NONE',  ( 5.895881250540457863, 12.98890680526564267, -15.35630103939177360 ) ) ;
#13306=ADVANCED_FACE ( 'NONE', ( #5800 ), #52781, .F. ) ;
#13310=ORIENTED_EDGE ( 'NONE', *, *, #16811, .F. ) ;
#13315=CARTESIAN_POINT ( 'NONE',  ( 0.5824936645240094135, -29.99832043048538210, -36.04634448026914839 ) ) ;
#13317=CARTESIAN_POINT ( 'NONE',  ( 5.894904586330512508, -9.664823957841305102, -17.63861077085095630 ) ) ;
#13320=FACE_OUTER_BOUND ( 'NONE', #9657, .T. ) ;
#13321=EDGE_CURVE ( 'NONE', #59308, #2462, #44877, .T. ) ;
#13322=CARTESIAN_POINT ( 'NONE',  ( 0.9783242366443558602, 41.90778699278978792, 0.2681036618207567890 ) ) ;
#13323=CARTESIAN_POINT ( 'NONE',  ( 2.282816707992316729, -9.105513224129030192, -46.08238921033910174 ) ) ;
#13326=CARTESIAN_POINT ( 'NONE',  ( 1.231276596079881047, -18.40965318903201364, 37.66113965983544887 ) ) ;
#13334=CARTESIAN_POINT ( 'NONE',  ( 0.5824936645240085253, -25.54018381715007990, 39.33112240486524769 ) ) ;
#13340=B_SPLINE_CURVE_WITH_KNOTS ( 'NONE', 3,
 ( #35654, #45665, #55642, #35966, #25927, #27159, #7096, #40985, #32174, #46285, #22460, #41584, #45062, #2093, #21224, #50042, #59422, #59736, #16852 ),
 .UNSPECIFIED., .F., .F.,
 ( 4, 3, 3, 3, 3, 3, 4 ),
 ( 1.250973872328959318E-17, 0.0002732106629380675819, 0.0004098138914053775462, 0.0005464171197651557970, 0.0006830203481512715953, 0.0008196235766963839075, 0.001011968216111141594 ),
 .UNSPECIFIED. ) ;
#13352=ORIENTED_EDGE ( 'NONE', *, *, #59905, .F. ) ;
#13355=CARTESIAN_POINT ( 'NONE',  ( 0.5806925824938499181, 46.89268439822727430, 0.5463627657667635695 ) ) ;
#13358=CARTESIAN_POINT ( 'NONE',  ( 0.5804410086790514622, 43.38796872094628299, -17.80460676694616851 ) ) ;
#13371=ORIENTED_EDGE ( 'NONE', *, *, #54120, .T. ) ;
#13372=ORIENTED_EDGE ( 'NONE', *, *, #50640, .T. ) ;
#13379=EDGE_CURVE ( 'NONE', #19517, #53916, #41877, .T. ) ;
#13387=EDGE_CURVE ( 'NONE', #33079, #33083, #16649, .T. ) ;
#13388=CARTESIAN_POINT ( 'NONE',  ( 1.000110580585052533, -30.63720285853708347, -28.59684045094404325 ) ) ;
#13389=CARTESIAN_POINT ( 'NONE',  ( 5.894904586330512508, -18.51743364446310025, -7.850736480391433680 ) ) ;
#13390=CIRCLE ( 'NONE', #60387, 8.000000000000000000 ) ;
#13394=CARTESIAN_POINT ( 'NONE',  ( 0.8554163680231816613, -26.01084021241216604, -39.04666009476586908 ) ) ;
#13397=CARTESIAN_POINT ( 'NONE',  ( 0.6064782688330846439, 36.36007787089019416, 29.61889909570526669 ) ) ;
#13414=CARTESIAN_POINT ( 'NONE',  ( 5.895881250540457863, 17.95317081027896577, 9.067046898811559785 ) ) ;
#13418=CARTESIAN_POINT ( 'NONE',  ( 4.958415959904821868, 1.012370948441741358, -45.41122172861453521 ) ) ;
#13421=ORIENTED_EDGE ( 'NONE', *, *, #3840, .F. ) ;
#13430=ORIENTED_EDGE ( 'NONE', *, *, #6796, .F. ) ;
#13432=ORIENTED_EDGE ( 'NONE', *, *, #8099, .T. ) ;
#13439=CARTESIAN_POINT ( 'NONE',  ( 0.5824936645240087474, -7.440785221794779858, -46.30197505855910123 ) ) ;
#13440=FACE_OUTER_BOUND ( 'NONE', #44457, .T. ) ;
#13441=ORIENTED_EDGE ( 'NONE', *, *, #561, .F. ) ;
#13448=ORIENTED_EDGE ( 'NONE', *, *, #22786, .F. ) ;
#13450=CARTESIAN_POINT ( 'NONE',  ( 0.9790850452238877288, -37.38141985983193649, 18.94641864643972085 ) ) ;
#13457=EDGE_CURVE ( 'NONE', #42659, #22425, #51598, .T. ) ;
#13459=CARTESIAN_POINT ( 'NONE',  ( 0.7056313189692728916, -34.21346071282268042, 32.08095618914278191 ) ) ;
#13462=( BOUNDED_SURFACE ( )  B_SPLINE_SURFACE ( 3, 1, ( 
 ( #2363, #6122 ),
 ( #35293, #21482 ),
 ( #44404, #25565 ),
 ( #1741, #11478 ) ),
 .UNSPECIFIED., .F., .F., .F. ) 
 B_SPLINE_SURFACE_WITH_KNOTS ( ( 4, 4 ),
 ( 2, 2 ),
 ( 0.000000000000000000, 1.000000000000000000 ),
 ( 0.000000000000000000, 1.000000000000000000 ),
 .UNSPECIFIED. ) 
 GEOMETRIC_REPRESENTATION_ITEM ( )  RATIONAL_B_SPLINE_SURFACE ( (
 ( 1.000000000000000000, 1.000000000000000000),
 ( 0.9729067724841187204, 0.9999501103223794596),
 ( 0.9729067724841187204, 0.9999501103223794596),
 ( 1.000000000000000000, 1.000000000000000000) ) ) 
 REPRESENTATION_ITEM ( '' )  SURFACE ( )  );
#13463=B_SPLINE_CURVE_WITH_KNOTS ( 'NONE', 3,
 ( #3078, #41334, #24911, #42557, #44344, #4596 ),
 .UNSPECIFIED., .F., .F.,
 ( 4, 2, 4 ),
 ( 6.106282077343214115E-18, 0.0002291472222819936945, 0.0004582944445639813174 ),
 .UNSPECIFIED. ) ;
#13466=DIRECTION ( 'NONE',  ( 0.07500201931887537365, -0.6834640454944218568, -0.7261209235481992375 ) ) ;
#13467=CARTESIAN_POINT ( 'NONE',  ( 0.9762797500689124330, 40.28286501695569655, 11.55922018180428168 ) ) ;
#13475=CARTESIAN_POINT ( 'NONE',  ( 1.231276596079887264, -16.87422718933211030, 38.37365278131431268 ) ) ;
#13478=LINE ( 'NONE', #14103, #975 ) ;
#13481=( BOUNDED_SURFACE ( )  B_SPLINE_SURFACE ( 3, 1, ( 
 ( #3277, #41231 ),
 ( #54977, #46236 ),
 ( #11795, #35910 ),
 ( #22104, #27111 ) ),
 .UNSPECIFIED., .F., .F., .F. ) 
 B_SPLINE_SURFACE_WITH_KNOTS ( ( 4, 4 ),
 ( 2, 2 ),
 ( 0.000000000000000000, 1.000000000000000000 ),
 ( 0.000000000000000000, 1.000000000000000000 ),
 .UNSPECIFIED. ) 
 GEOMETRIC_REPRESENTATION_ITEM ( )  RATIONAL_B_SPLINE_SURFACE ( (
 ( 1.000000000000000000, 1.000000000000000000),
 ( 0.9952954269826590483, 0.8620686068821339365),
 ( 0.9952954269826590483, 0.8620686068821339365),
 ( 1.000000000000000000, 1.000000000000000000) ) ) 
 REPRESENTATION_ITEM ( '' )  SURFACE ( )  );
#13489=CARTESIAN_POINT ( 'NONE',  ( 3.782542959838397945, 18.67355142067374985, 37.66346148106973146 ) ) ;
#13493=CARTESIAN_POINT ( 'NONE',  ( 5.896782393890504181, -13.98685533979004347, -14.45316451791091161 ) ) ;
#13494=EDGE_LOOP ( 'NONE', ( #28921, #57633, #48781, #525 ) ) ;
#13498=CARTESIAN_POINT ( 'NONE',  ( 4.962356264823596597, 39.89814050050772920, 13.39305724859313429 ) ) ;
#13499=CARTESIAN_POINT ( 'NONE',  ( 0.7056759521544998526, -2.409567365275814943, 46.83954327519839467 ) ) ;
#13502=CARTESIAN_POINT ( 'NONE',  ( 0.9762797500689124330, -41.77809974471938403, -3.303810967047359881 ) ) ;
#13511=ORIENTED_EDGE ( 'NONE', *, *, #11624, .F. ) ;
#13515=ORIENTED_EDGE ( 'NONE', *, *, #45769, .F. ) ;
#13516=CIRCLE ( 'NONE', #48515, 47.09074272231896430 ) ;
#13518=VERTEX_POINT ( 'NONE', #49209 ) ;
#13522=B_SPLINE_CURVE_WITH_KNOTS ( 'NONE', 3,
 ( #27955, #61134, #8518, #42083, #28253, #56748, #13554, #56440, #37367, #47078, #9763, #9449, #51742, #37684, #27641, #56134, #14483, #3818, #22954 ),
 .UNSPECIFIED., .F., .F.,
 ( 4, 3, 3, 3, 3, 3, 4 ),
 ( 6.939740885162003740E-18, 0.0002732106629380601551, 0.0004098138914053745105, 0.0005464171197651472318, 0.0006830203481512577175, 0.0008196235766963646087, 0.001011968216111144847 ),
 .UNSPECIFIED. ) ;
#13524=VERTEX_POINT ( 'NONE', #1894 ) ;
#13526=CARTESIAN_POINT ( 'NONE',  ( 0.5782707292762423457, 21.90237606067615772, -41.47315127409947166 ) ) ;
#13527=CARTESIAN_POINT ( 'NONE',  ( 0.5835226383429292785, -44.36069261528489704, -15.21089823903163030 ) ) ;
#13528=CARTESIAN_POINT ( 'NONE',  ( 0.5817216825391130497, 17.27888236047640547, 43.59673355402070882 ) ) ;
#13530=EDGE_CURVE ( 'NONE', #38058, #47205, #43312, .T. ) ;
#13537=CARTESIAN_POINT ( 'NONE',  ( 0.5837799406558237258, 10.78283246128463091, -45.63961079686228572 ) ) ;
#13545=CARTESIAN_POINT ( 'NONE',  ( 0.5804410086790514622, 46.89585601637878653, 0.5463884574786440629 ) ) ;
#13550=LINE ( 'NONE', #11782, #15816 ) ;
#13554=CARTESIAN_POINT ( 'NONE',  ( 0.9789889208857702751, -12.32462320582296478, 40.05544358607027533 ) ) ;
#13557=CARTESIAN_POINT ( 'NONE',  ( 5.895596859100789899, -18.51832497669328959, 7.848555489391991991 ) ) ;
#13564=CARTESIAN_POINT ( 'NONE',  ( 5.896782393890504181, -4.656380635072850716, 19.56640504178861306 ) ) ;
#13568=ORIENTED_EDGE ( 'NONE', *, *, #5616, .F. ) ;
#13573=ORIENTED_EDGE ( 'NONE', *, *, #9696, .F. ) ;
#13574=VERTEX_POINT ( 'NONE', #6892 ) ;
#13576=CARTESIAN_POINT ( 'NONE',  ( 1.000110580585053865, -39.37003715540507187, -14.36724250348427212 ) ) ;
#13579=ORIENTED_EDGE ( 'NONE', *, *, #44242, .F. ) ;
#13586=ORIENTED_EDGE ( 'NONE', *, *, #29836, .T. ) ;
#13589=ORIENTED_EDGE ( 'NONE', *, *, #29204, .T. ) ;
#13594=B_SPLINE_CURVE_WITH_KNOTS ( 'NONE', 3,
 ( #57374, #33927, #9479, #15428, #25123, #24503 ),
 .UNSPECIFIED., .F., .F.,
 ( 4, 2, 4 ),
 ( 9.929776742050823831E-18, 0.0002448709889506589456, 0.0004897419779013080249 ),
 .UNSPECIFIED. ) ;
#13602=CARTESIAN_POINT ( 'NONE',  ( 0.5797568599927133137, -8.419849506244490911, 46.13384270753087435 ) ) ;
#13605=CARTESIAN_POINT ( 'NONE',  ( 0.5837800304671219020, -38.68876759456514236, 26.50314310026687181 ) ) ;
#13607=VECTOR ( 'NONE', #34577, 999.9999999999998863 ) ;
#13610=EDGE_CURVE ( 'NONE', #44371, #55732, #28304, .T. ) ;
#13612=ORIENTED_EDGE ( 'NONE', *, *, #46563, .T. ) ;
#13622=CARTESIAN_POINT ( 'NONE',  ( 5.895596859100789899, -9.669028665050088733, -17.63627137143583568 ) ) ;
#13623=EDGE_CURVE ( 'NONE', #53003, #51245, #49271, .T. ) ;
#13625=CARTESIAN_POINT ( 'NONE',  ( 0.5837157313716013762, -30.20780093847265846, -35.87096076276234413 ) ) ;
#13629=DIRECTION ( 'NONE',  ( 0.000000000000000000, 0.000000000000000000, 1.000000000000000000 ) ) ;
#13632=CARTESIAN_POINT ( 'NONE',  ( 5.896278296736517710, -4.667894692253747202, -19.56368418157513034 ) ) ;
#13638=CARTESIAN_POINT ( 'NONE',  ( 0.5837799406558230597, -34.84162086156078431, -31.38956841558125532 ) ) ;
#13641=B_SPLINE_CURVE_WITH_KNOTS ( 'NONE', 3,
 ( #51899, #27479, #41300, #46007, #23402, #55663 ),
 .UNSPECIFIED., .F., .F.,
 ( 4, 2, 4 ),
 ( 1.184703104989684002E-16, 0.0002448718616795916327, 0.0004897437233590648704 ),
 .UNSPECIFIED. ) ;
#13644=FACE_OUTER_BOUND ( 'NONE', #54767, .T. ) ;
#13645=CARTESIAN_POINT ( 'NONE',  ( 2.528100132419515589, -41.94888324960150072, -1.595297070572732956 ) ) ;
#13648=VERTEX_POINT ( 'NONE', #27879 ) ;
#13660=EDGE_CURVE ( 'NONE', #19096, #29761, #43629, .T. ) ;
#13665=EDGE_CURVE ( 'NONE', #4970, #40810, #18482, .T. ) ;
#13666=AXIS2_PLACEMENT_3D ( 'NONE', #33218, #9082, #9384 ) ;
#13672=ORIENTED_EDGE ( 'NONE', *, *, #57741, .F. ) ;
#13677=CARTESIAN_POINT ( 'NONE',  ( 0.9790724872846782167, -37.38600932109895325, -18.93730490392327681 ) ) ;
#13679=CARTESIAN_POINT ( 'NONE',  ( 4.956445790444004906, -37.28933980949924631, -28.75835855384189443 ) ) ;
#13684=CARTESIAN_POINT ( 'NONE',  ( 0.9762797500689124330, 33.20096159360354449, -25.57383300261748360 ) ) ;
#13693=CARTESIAN_POINT ( 'NONE',  ( 0.5835226383429280572, 27.96423497704858363, 37.64630176649998816 ) ) ;
#13695=CARTESIAN_POINT ( 'NONE',  ( 4.956445790443988031, 46.25174887658550915, 8.849507104743643993 ) ) ;
#13697=CARTESIAN_POINT ( 'NONE',  ( 4.956445790443991584, 38.51510088324707226, 27.09474218539341450 ) ) ;
#13700=CARTESIAN_POINT ( 'NONE',  ( 0.5830082357119558134, -41.97803085087377895, 20.90638564700811841 ) ) ;
#13705=CARTESIAN_POINT ( 'NONE',  ( 4.962356264823602814, -36.43094049105359744, -21.07183363638911189 ) ) ;
#13713=CARTESIAN_POINT ( 'NONE',  ( 4.956445790444001354, -28.36659270909979114, 37.58822246682706947 ) ) ;
#13714=CARTESIAN_POINT ( 'NONE',  ( 0.9784957157296376717, -26.87920163080859837, 32.15340692185988303 ) ) ;
#13717=CARTESIAN_POINT ( 'NONE',  ( 1.157643937452368599, -6.156433921344971694, 41.46203801029162861 ) ) ;
#13725=CARTESIAN_POINT ( 'NONE',  ( 0.5837157313716039297, 32.53625919676243683, 33.77319796914579797 ) ) ;
#13730=ADVANCED_FACE ( 'NONE', ( #51669 ), #1547, .F. ) ;
#13738=EDGE_CURVE ( 'NONE', #34780, #16119, #8764, .T. ) ;
#13743=B_SPLINE_CURVE_WITH_KNOTS ( 'NONE', 3,
 ( #61103, #36414, #22607, #51089 ),
 .UNSPECIFIED., .F., .F.,
 ( 4, 4 ),
 ( 4.336808689942017736E-19, 0.004041751736740985604 ),
 .UNSPECIFIED. ) ;
#13746=VERTEX_POINT ( 'NONE', #53213 ) ;
#13750=ADVANCED_FACE ( 'NONE', ( #38533 ), #42635, .T. ) ;
#13754=CIRCLE ( 'NONE', #10743, 41.88877248453276536 ) ;
#13762=CARTESIAN_POINT ( 'NONE',  ( 0.5834584762367742705, -7.620554889515525510, -46.27270396453046430 ) ) ;
#13765=VERTEX_POINT ( 'NONE', #57902 ) ;
#13766=CARTESIAN_POINT ( 'NONE',  ( 5.838029081930955932, -37.08173278831655750, 29.25765116288059176 ) ) ;
#13785=CARTESIAN_POINT ( 'NONE',  ( 0.9754292580325131246, 40.26172079307664831, 11.63276861647064742 ) ) ;
#13787=CARTESIAN_POINT ( 'NONE',  ( 0.9762797500689124330, 10.20671408565980975, 40.64662068068264489 ) ) ;
#13789=ORIENTED_EDGE ( 'NONE', *, *, #18197, .T. ) ;
#13798=VERTEX_POINT ( 'NONE', #33519 ) ;
#13800=CARTESIAN_POINT ( 'NONE',  ( 0.7764139734771248191, 28.53559780214793662, -37.22579923898098286 ) ) ;
#13801=CARTESIAN_POINT ( 'NONE',  ( 5.896782393890504181, 3.351618377817360273, -19.83160964539916549 ) ) ;
#13803=CARTESIAN_POINT ( 'NONE',  ( 0.9775691876210981235, 28.86184834324568627, 30.38630315127980808 ) ) ;
#13807=CARTESIAN_POINT ( 'NONE',  ( 0.5817216825391133828, 22.13701364508538916, -41.34232188792448426 ) ) ;
#13810=EDGE_CURVE ( 'NONE', #7010, #37701, #58915, .T. ) ;
#13815=CARTESIAN_POINT ( 'NONE',  ( 0.9787464366903561030, 19.98509552998146788, 36.83653009646780419 ) ) ;
#13822=DIRECTION ( 'NONE',  ( 1.000000000000000000, 0.000000000000000000, 0.000000000000000000 ) ) ;
#13825=CARTESIAN_POINT ( 'NONE',  ( 0.5817216825391129387, -46.04481145225960859, -8.894396580618670001 ) ) ;
#13828=CARTESIAN_POINT ( 'NONE',  ( 0.8560838555295223751, 31.94705745926225404, -34.34761059777416392 ) ) ;
#13836=CARTESIAN_POINT ( 'NONE',  ( 0.7056313189692701160, 11.69102722649127202, 45.42101414925695479 ) ) ;
#13837=B_SPLINE_CURVE_WITH_KNOTS ( 'NONE', 3,
 ( #7891, #17931, #27010, #18235 ),
 .UNSPECIFIED., .F., .F.,
 ( 4, 4 ),
 ( 0.000000000000000000, 0.004041751736740996012 ),
 .UNSPECIFIED. ) ;
#13844=VECTOR ( 'NONE', #20852, 1000.000000000000114 ) ;
#13846=CARTESIAN_POINT ( 'NONE',  ( 5.894904586330512508, 17.95171060118311246, -9.070032996247173074 ) ) ;
#13848=VERTEX_POINT ( 'NONE', #38848 ) ;
#13851=VERTEX_POINT ( 'NONE', #15029 ) ;
#13852=CARTESIAN_POINT ( 'NONE',  ( 0.5835226383429308328, 43.10343935657192560, -18.47528051695807960 ) ) ;
#13854=DIRECTION ( 'NONE',  ( -1.000000000000000000, -0.000000000000000000, -0.000000000000000000 ) ) ;
#13858=CARTESIAN_POINT ( 'NONE',  ( 0.5835871038041867687, 4.558181011431630125, 46.67394818063417716 ) ) ;
#13863=EDGE_LOOP ( 'NONE', ( #24391, #48821, #20693, #51800 ) ) ;
#13864=CARTESIAN_POINT ( 'NONE',  ( 4.962356264823608143, 0.000000000000000000, 0.000000000000000000 ) ) ;
#13865=CARTESIAN_POINT ( 'NONE',  ( 0.9788927965476027504, -41.80537879722813699, 2.940563934357716125 ) ) ;
#13873=CARTESIAN_POINT ( 'NONE',  ( 0.5835871038041865466, 40.41881746160861866, -23.78137186763330746 ) ) ;
#13878=CARTESIAN_POINT ( 'NONE',  ( 4.960386119450149955, -42.32154583640194545, 11.10509895001706226 ) ) ;
#13880=ADVANCED_FACE ( 'NONE', ( #20950 ), #61553, .F. ) ;
#13883=CARTESIAN_POINT ( 'NONE',  ( 0.5824935313925952984, 45.13218173562562896, -12.74065731570774318 ) ) ;
#13888=CIRCLE ( 'NONE', #22860, 47.09074272231896430 ) ;
#13903=CARTESIAN_POINT ( 'NONE',  ( 0.8560838555295158248, 28.55542365806940452, -37.21505896528851309 ) ) ;
#13913=B_SPLINE_CURVE_WITH_KNOTS ( 'NONE', 3,
 ( #23997, #26453, #11442, #15840 ),
 .UNSPECIFIED., .F., .F.,
 ( 4, 4 ),
 ( 4.336808689942017736E-19, 0.004446298630425052009 ),
 .UNSPECIFIED. ) ;
#13918=ORIENTED_EDGE ( 'NONE', *, *, #15588, .F. ) ;
#13931=CARTESIAN_POINT ( 'NONE',  ( 5.901463166500145796, 18.99503018386004527, 6.611104193316173827 ) ) ;
#13934=CARTESIAN_POINT ( 'NONE',  ( 4.958415959904823644, 19.57736038521000665, 40.98696029434541543 ) ) ;
#13938=ORIENTED_EDGE ( 'NONE', *, *, #27382, .T. ) ;
#13946=CARTESIAN_POINT ( 'NONE',  ( 4.291220156522059348, 35.59851124210522499, 30.85668476442996777 ) ) ;
#13950=CARTESIAN_POINT ( 'NONE',  ( 5.896782393890504181, -17.30835043929363692, 10.24436879210309925 ) ) ;
#13951=CARTESIAN_POINT ( 'NONE',  ( 0.9780106845699465534, -1.086875070857868941, -41.89450977199504678 ) ) ;
#13961=VECTOR ( 'NONE', #17506, 1000.000000000000114 ) ;
#13964=DIRECTION ( 'NONE',  ( -1.000000000000000000, -0.000000000000000000, -0.000000000000000000 ) ) ;
#13973=CARTESIAN_POINT ( 'NONE',  ( 5.910764540655178756, 5.943959005785093730, -19.21381247453792440 ) ) ;
#13982=ORIENTED_EDGE ( 'NONE', *, *, #59954, .F. ) ;
#13986=EDGE_CURVE ( 'NONE', #36980, #26618, #22324, .T. ) ;
#13992=CARTESIAN_POINT ( 'NONE',  ( 2.282816707992310512, -44.78789143672629791, -14.16127632171569317 ) ) ;
#13996=CARTESIAN_POINT ( 'NONE',  ( 0.9775691876210976794, 4.570554008562618620, -41.65865750411074231 ) ) ;
#14009=ORIENTED_EDGE ( 'NONE', *, *, #14088, .F. ) ;
#14010=DIRECTION ( 'NONE',  ( 0.000000000000000000, 0.000000000000000000, 1.000000000000000000 ) ) ;
#14016=( BOUNDED_SURFACE ( )  B_SPLINE_SURFACE ( 3, 1, ( 
 ( #39192, #20373 ),
 ( #35101, #39500 ),
 ( #30067, #25680 ),
 ( #1859, #35410 ) ),
 .UNSPECIFIED., .F., .F., .F. ) 
 B_SPLINE_SURFACE_WITH_KNOTS ( ( 4, 4 ),
 ( 2, 2 ),
 ( 0.000000000000000000, 1.000000000000000000 ),
 ( 0.000000000000000000, 1.000000000000000000 ),
 .UNSPECIFIED. ) 
 GEOMETRIC_REPRESENTATION_ITEM ( )  RATIONAL_B_SPLINE_SURFACE ( (
 ( 1.000000000000000000, 1.000000000000000000),
 ( 0.9952954269826590483, 0.8620686068821339365),
 ( 0.9952954269826590483, 0.8620686068821339365),
 ( 1.000000000000000000, 1.000000000000000000) ) ) 
 REPRESENTATION_ITEM ( '' )  SURFACE ( )  );
#14018=CARTESIAN_POINT ( 'NONE',  ( 0.9762797500689124330, -22.12212327108586152, -35.59405072711710716 ) ) ;
#14020=CARTESIAN_POINT ( 'NONE',  ( 1.231276596079887931, -41.24008908601417289, -7.518764738684258653 ) ) ;
#14025=CARTESIAN_POINT ( 'NONE',  ( 5.895596859100789899, -15.78235929336536536, 12.46777118604649814 ) ) ;
#14029=CARTESIAN_POINT ( 'NONE',  ( 1.000433927950262980, 32.47840743411710918, -26.48719932715300018 ) ) ;
#14036=CARTESIAN_POINT ( 'NONE',  ( 0.5837157313716024865, 10.78286503748334546, 45.63953204367286531 ) ) ;
#14043=CARTESIAN_POINT ( 'NONE',  ( 0.9754292580325131246, -1.982398290965677656, 41.86164788825186633 ) ) ;
#14044=CARTESIAN_POINT ( 'NONE',  ( 0.5782707292762442330, 46.57382484760238839, -5.533099743586197050 ) ) ;
#14057=CARTESIAN_POINT ( 'NONE',  ( 0.5837800005270550319, 43.17481384069556327, 18.30766802361970136 ) ) ;
#14061=VERTEX_POINT ( 'NONE', #22189 ) ;
#14068=LINE ( 'NONE', #31928, #57679 ) ;
#14072=LINE ( 'NONE', #14374, #40770 ) ;
#14073=ORIENTED_EDGE ( 'NONE', *, *, #60382, .F. ) ;
#14077=CARTESIAN_POINT ( 'NONE',  ( 1.231276596079887264, 28.52807286890788419, -30.71523773966838888 ) ) ;
#14078=B_SPLINE_CURVE_WITH_KNOTS ( 'NONE', 3,
 ( #52765, #38095, #24265, #52451 ),
 .UNSPECIFIED., .F., .F.,
 ( 4, 4 ),
 ( 9.757819552369539906E-19, 0.004446298630425057213 ),
 .UNSPECIFIED. ) ;
#14079=CARTESIAN_POINT ( 'NONE',  ( 0.9787464366903551038, -37.48376074964096460, 18.74304332156709663 ) ) ;
#14088=EDGE_CURVE ( 'NONE', #48392, #14741, #19334, .T. ) ;
#14096=VECTOR ( 'NONE', #46176, 1000.000000000000227 ) ;
#14103=CARTESIAN_POINT ( 'NONE',  ( 3.376099380956838925, -12.80728341440187457, 3.960034744197806766 ) ) ;
#14106=CARTESIAN_POINT ( 'NONE',  ( 4.962356264823602814, 22.27740539909316198, -35.70648129607287302 ) ) ;
#14108=EDGE_CURVE ( 'NONE', #17781, #35390, #30504, .T. ) ;
#14113=( BOUNDED_SURFACE ( )  B_SPLINE_SURFACE ( 3, 1, ( 
 ( #34362, #29954 ),
 ( #53434, #48751 ),
 ( #57823, #19337 ),
 ( #39382, #5201 ) ),
 .UNSPECIFIED., .F., .F., .F. ) 
 B_SPLINE_SURFACE_WITH_KNOTS ( ( 4, 4 ),
 ( 2, 2 ),
 ( 0.000000000000000000, 1.000000000000000000 ),
 ( 0.000000000000000000, 1.000000000000000000 ),
 .UNSPECIFIED. ) 
 GEOMETRIC_REPRESENTATION_ITEM ( )  RATIONAL_B_SPLINE_SURFACE ( (
 ( 1.000000000000000000, 1.000000000000000000),
 ( 0.9952954269826590483, 0.8620686068821339365),
 ( 0.9952954269826590483, 0.8620686068821339365),
 ( 1.000000000000000000, 1.000000000000000000) ) ) 
 REPRESENTATION_ITEM ( '' )  SURFACE ( )  );
#14117=CARTESIAN_POINT ( 'NONE',  ( 0.5797568665920715958, 37.19047599010775684, 28.56735556944480336 ) ) ;
#14122=CARTESIAN_POINT ( 'NONE',  ( 0.9780303403264780648, 20.42395051976790654, 36.59510703032791668 ) ) ;
#14125=VERTEX_POINT ( 'NONE', #6341 ) ;
#14131=B_SPLINE_CURVE_WITH_KNOTS ( 'NONE', 3,
 ( #42086, #51745, #37371, #4418, #18884, #55518 ),
 .UNSPECIFIED., .F., .F.,
 ( 4, 2, 4 ),
 ( 1.189851992356654836E-16, 0.0002448718616795952647, 0.0004897437233590714841 ),
 .UNSPECIFIED. ) ;
#14135=CARTESIAN_POINT ( 'NONE',  ( 0.5835226383429293895, -45.99229812474374768, -9.162477162354004889 ) ) ;
#14141=FACE_OUTER_BOUND ( 'NONE', #26321, .T. ) ;
#14144=ORIENTED_EDGE ( 'NONE', *, *, #53130, .F. ) ;
#14153=CARTESIAN_POINT ( 'NONE',  ( 3.238018933889920792, 8.164940828001933326, 10.61796749113878313 ) ) ;
#14156=CARTESIAN_POINT ( 'NONE',  ( 5.894904586330512508, 0.6708454810754242992, -20.10172575681410123 ) ) ;
#14161=EDGE_LOOP ( 'NONE', ( #49637, #13131, #8138, #57851 ) ) ;
#14165=CARTESIAN_POINT ( 'NONE',  ( 5.896278296736517710, -17.30792457686169428, -10.24513184180911018 ) ) ;
#14170=ADVANCED_FACE ( 'NONE', ( #53362 ), #51640, .T. ) ;
#14173=EDGE_CURVE ( 'NONE', #48449, #27747, #61129, .T. ) ;
#14176=CARTESIAN_POINT ( 'NONE',  ( 0.5806925824938499181, 4.150136846022649095, 46.71186922510005957 ) ) ;
#14179=CARTESIAN_POINT ( 'NONE',  ( 4.956445790443998689, -27.49627641100115838, 38.22947597952995835 ) ) ;
#14182=CARTESIAN_POINT ( 'NONE',  ( 4.956445790444018229, -5.251077430595369577, -46.79705371022334504 ) ) ;
#14191=CARTESIAN_POINT ( 'NONE',  ( 4.956445790443998689, -5.251077430596073903, 46.79705371022326688 ) ) ;
#14194=ORIENTED_EDGE ( 'NONE', *, *, #23262, .F. ) ;
#14202=UNCERTAINTY_MEASURE_WITH_UNIT (LENGTH_MEASURE( 1.000000000000000082E-05 ), #17870, 'distance_accuracy_value', 'NONE');
#14203=VERTEX_POINT ( 'NONE', #58990 ) ;
#14210=EDGE_LOOP ( 'NONE', ( #30565, #16759, #7815, #8107 ) ) ;
#14211=ORIENTED_EDGE ( 'NONE', *, *, #3840, .T. ) ;
#14215=CARTESIAN_POINT ( 'NONE',  ( 4.960386119450151732, 38.83699438620071476, 20.15252668323636698 ) ) ;
#14219=CARTESIAN_POINT ( 'NONE',  ( 0.9762797500689124330, -39.75277516423524560, 13.26806888463673673 ) ) ;
#14221=EDGE_LOOP ( 'NONE', ( #7969, #58699, #1296, #54657 ) ) ;
#14223=ORIENTED_EDGE ( 'NONE', *, *, #8706, .F. ) ;
#14232=EDGE_CURVE ( 'NONE', #3395, #48545, #51363, .T. ) ;
#14234=FACE_OUTER_BOUND ( 'NONE', #34167, .T. ) ;
#14237=EDGE_CURVE ( 'NONE', #35972, #6137, #11095, .T. ) ;
#14242=ORIENTED_EDGE ( 'NONE', *, *, #33422, .F. ) ;
#14243=CARTESIAN_POINT ( 'NONE',  ( 5.917102823773431552, -15.77849770028359444, 12.47111576298958546 ) ) ;
#14248=CARTESIAN_POINT ( 'NONE',  ( 0.5797568665920715958, -20.30903389470142173, -42.27018394643840082 ) ) ;
#14254=CARTESIAN_POINT ( 'NONE',  ( 0.9762797500689124330, 41.90547441298052433, -0.5059638413352701702 ) ) ;
#14262=LINE ( 'NONE', #19882, #41041 ) ;
#14268=CARTESIAN_POINT ( 'NONE',  ( 5.896782393890504181, 16.57826022845085134, 11.38803647148080778 ) ) ;
#14277=CARTESIAN_POINT ( 'NONE',  ( 0.5830081025819919827, 22.77654563688193079, 40.99342634171097188 ) ) ;
#14279=FACE_OUTER_BOUND ( 'NONE', #57246, .T. ) ;
#14282=ORIENTED_EDGE ( 'NONE', *, *, #57749, .F. ) ;
#14287=CARTESIAN_POINT ( 'NONE',  ( 0.5835871038041848813, 16.98216052327276770, -43.71316365653826352 ) ) ;
#14289=CARTESIAN_POINT ( 'NONE',  ( 5.896782393890504181, -2.006887468070122527, -20.01245835894519587 ) ) ;
#14293=CARTESIAN_POINT ( 'NONE',  ( 4.956445790444002242, -36.61936279692601204, 29.60676136436992678 ) ) ;
#14295=ORIENTED_EDGE ( 'NONE', *, *, #47110, .T. ) ;
#14296=CARTESIAN_POINT ( 'NONE',  ( 0.9775691876210991227, -37.23235882800789653, -19.23759769546218834 ) ) ;
#14301=B_SPLINE_CURVE_WITH_KNOTS ( 'NONE', 3,
 ( #44957, #1995, #58384, #34309, #21121, #43729 ),
 .UNSPECIFIED., .F., .F.,
 ( 4, 2, 4 ),
 ( 5.637851296924623827E-18, 0.0002291472222819946974, 0.0004582944445639837569 ),
 .UNSPECIFIED. ) ;
#14311=CARTESIAN_POINT ( 'NONE',  ( 0.5837800304671210139, 27.78112706352523631, 37.78156046618196484 ) ) ;
#14312=VERTEX_POINT ( 'NONE', #17331 ) ;
#14320=DIRECTION ( 'NONE',  ( 0.000000000000000000, 0.000000000000000000, 1.000000000000000000 ) ) ;
#14321=CARTESIAN_POINT ( 'NONE',  ( 5.917102823773431552, -19.39960706793701917, -5.305182717059805597 ) ) ;
#14330=CARTESIAN_POINT ( 'NONE',  ( 5.901463166500145796, -19.93124146756672133, -2.695085138207230280 ) ) ;
#14334=VECTOR ( 'NONE', #12965, 999.9999999999998863 ) ;
#14335=B_SPLINE_CURVE_WITH_KNOTS ( 'NONE', 3,
 ( #52678, #9775, #61753, #27963 ),
 .UNSPECIFIED., .F., .F.,
 ( 4, 4 ),
 ( 0.000000000000000000, 0.004447772540403791171 ),
 .UNSPECIFIED. ) ;
#14336=CARTESIAN_POINT ( 'NONE',  ( 0.8560838555295158248, -6.899551485031924614, -46.39794201672231111 ) ) ;
#14346=CARTESIAN_POINT ( 'NONE',  ( 4.956445790444004018, -43.14021684453488348, -18.88014143872194950 ) ) ;
#14353=DIRECTION ( 'NONE',  ( -0.07906939808003035641, 0.9635513351855523601, 0.2555716235214721688 ) ) ;
#14360=CARTESIAN_POINT ( 'NONE',  ( 3.782542959838393504, -19.24495247062706227, 37.37471950128691134 ) ) ;
#14364=ORIENTED_EDGE ( 'NONE', *, *, #10075, .F. ) ;
#14368=CARTESIAN_POINT ( 'NONE',  ( 4.960386119450151732, 28.60674280242284695, -33.10726099979230241 ) ) ;
#14369=CARTESIAN_POINT ( 'NONE',  ( 5.895596859100789899, -4.666058297670689470, 19.56415301451167466 ) ) ;
#14374=CARTESIAN_POINT ( 'NONE',  ( 0.5326698147273788431, 5.129895114339477383E-15, 41.88877248453276536 ) ) ;
#14375=( BOUNDED_SURFACE ( )  B_SPLINE_SURFACE ( 3, 1, ( 
 ( #56644, #13766 ),
 ( #51946, #44138 ),
 ( #48480, #24684 ),
 ( #29376, #30296 ) ),
 .UNSPECIFIED., .F., .F., .F. ) 
 B_SPLINE_SURFACE_WITH_KNOTS ( ( 4, 4 ),
 ( 2, 2 ),
 ( 0.000000000000000000, 1.000000000000000000 ),
 ( 0.000000000000000000, 1.000000000000000000 ),
 .UNSPECIFIED. ) 
 GEOMETRIC_REPRESENTATION_ITEM ( )  RATIONAL_B_SPLINE_SURFACE ( (
 ( 1.000000000000000000, 1.000000000000000000),
 ( 0.7282232189291693025, 0.9929344683865674037),
 ( 0.7282232189291693025, 0.9929344683865674037),
 ( 1.000000000000000000, 1.000000000000000000) ) ) 
 REPRESENTATION_ITEM ( '' )  SURFACE ( )  );
#14376=ORIENTED_EDGE ( 'NONE', *, *, #16934, .F. ) ;
#14377=CARTESIAN_POINT ( 'NONE',  ( 0.7056313189692680066, -39.13839767847387208, -25.84442824129003569 ) ) ;
#14381=CARTESIAN_POINT ( 'NONE',  ( 4.962356264823603702, -4.645793755590432283, -41.82884409403234116 ) ) ;
#14382=CARTESIAN_POINT ( 'NONE',  ( 0.9790320750461896093, -37.44297633391666835, 18.82446960208836728 ) ) ;
#14393=( BOUNDED_SURFACE ( )  B_SPLINE_SURFACE ( 3, 1, ( 
 ( #39169, #6207 ),
 ( #29734, #44188 ),
 ( #43249, #20658 ),
 ( #1218, #20353 ) ),
 .UNSPECIFIED., .F., .F., .F. ) 
 B_SPLINE_SURFACE_WITH_KNOTS ( ( 4, 4 ),
 ( 2, 2 ),
 ( 0.000000000000000000, 1.000000000000000000 ),
 ( 0.000000000000000000, 1.000000000000000000 ),
 .UNSPECIFIED. ) 
 GEOMETRIC_REPRESENTATION_ITEM ( )  RATIONAL_B_SPLINE_SURFACE ( (
 ( 1.000000000000000000, 1.000000000000000000),
 ( 0.7282232189291693025, 0.9929344683865674037),
 ( 0.7282232189291693025, 0.9929344683865674037),
 ( 1.000000000000000000, 1.000000000000000000) ) ) 
 REPRESENTATION_ITEM ( '' )  SURFACE ( )  );
#14399=ORIENTED_EDGE ( 'NONE', *, *, #28496, .F. ) ;
#14402=CARTESIAN_POINT ( 'NONE',  ( 0.9789889208857702751, -41.04960742935966067, 8.441837947854031299 ) ) ;
#14403=EDGE_CURVE ( 'NONE', #27021, #60419, #48385, .T. ) ;
#14406=CARTESIAN_POINT ( 'NONE',  ( 1.231276596079887264, 41.65019306089983786, 4.747440258480190245 ) ) ;
#14412=CARTESIAN_POINT ( 'NONE',  ( 0.9762797500689124330, -39.75277516423524560, 13.26806888463673673 ) ) ;
#14413=CARTESIAN_POINT ( 'NONE',  ( 0.8554163680231720024, -6.900908941297191568, 46.40671211038057464 ) ) ;
#14414=CARTESIAN_POINT ( 'NONE',  ( 5.896278296736517710, 20.06830682785022191, 1.337924017888904471 ) ) ;
#14415=CARTESIAN_POINT ( 'NONE',  ( 0.9754292580325137907, -41.77202903244706533, -3.380097249548380756 ) ) ;
#14416=CARTESIAN_POINT ( 'NONE',  ( 0.9790724872846782167, -34.57410215488273764, 23.68473496083889529 ) ) ;
#14427=ORIENTED_EDGE ( 'NONE', *, *, #58145, .F. ) ;
#14430=CARTESIAN_POINT ( 'NONE',  ( 0.5848930533535030563, 11.04862722691790999, 45.57631971526624426 ) ) ;
#14435=EDGE_CURVE ( 'NONE', #42430, #16350, #40994, .T. ) ;
#14436=CARTESIAN_POINT ( 'NONE',  ( 1.091591847532195070, 25.48625600094100818, -33.27476139674539013 ) ) ;
#14438=CARTESIAN_POINT ( 'NONE',  ( 4.956445790444002242, -37.28933980949966553, 28.75835855384135087 ) ) ;
#14444=VERTEX_POINT ( 'NONE', #56753 ) ;
#14446=AXIS2_PLACEMENT_3D ( 'NONE', #17335, #51138, #37378 ) ;
#14451=EDGE_CURVE ( 'NONE', #58203, #44946, #59575, .T. ) ;
#14452=ORIENTED_EDGE ( 'NONE', *, *, #38922, .F. ) ;
#14453=CARTESIAN_POINT ( 'NONE',  ( 0.8554163680231708922, 46.36773742900841455, 7.158100224665131073 ) ) ;
#14457=EDGE_CURVE ( 'NONE', #34231, #10639, #34202, .T. ) ;
#14467=ORIENTED_EDGE ( 'NONE', *, *, #9540, .T. ) ;
#14468=CARTESIAN_POINT ( 'NONE',  ( 5.895881250540457863, -17.30746725809826358, -10.24593864505140317 ) ) ;
#14471=CARTESIAN_POINT ( 'NONE',  ( 0.9783242366443549720, -22.32385813646210693, -35.46801161764835086 ) ) ;
#14479=EDGE_CURVE ( 'NONE', #4083, #25777, #57344, .T. ) ;
#14480=CONICAL_SURFACE ( 'NONE', #12469, 42.08604991992415023, 1.569615340895231137 ) ;
#14483=CARTESIAN_POINT ( 'NONE',  ( 0.9775691876210985676, -12.77678863225218286, 39.91349873459780895 ) ) ;
#14489=CARTESIAN_POINT ( 'NONE',  ( 4.958415959904820092, 2.023024899603357074, -45.37743188059707222 ) ) ;
#14492=CIRCLE ( 'NONE', #46468, 47.09074272231896430 ) ;
#14493=CARTESIAN_POINT ( 'NONE',  ( 0.5782707292762442330, 11.57561326132714363, -45.45042938556033363 ) ) ;
#14495=ORIENTED_EDGE ( 'NONE', *, *, #13610, .T. ) ;
#14497=VECTOR ( 'NONE', #37231, 1000.000000000000114 ) ;
#14499=CARTESIAN_POINT ( 'NONE',  ( 4.956445790444011124, -11.44166143951963122, -45.67960632101645757 ) ) ;
#14511=EDGE_CURVE ( 'NONE', #5679, #26211, #32661, .T. ) ;
#14514=ORIENTED_EDGE ( 'NONE', *, *, #26883, .T. ) ;
#14530=ORIENTED_EDGE ( 'NONE', *, *, #50030, .F. ) ;
#14533=LINE ( 'NONE', #18927, #6571 ) ;
#14539=FACE_OUTER_BOUND ( 'NONE', #29948, .T. ) ;
#14552=CARTESIAN_POINT ( 'NONE',  ( 5.895881250540457863, -11.93421320881311232, 16.18957185026495793 ) ) ;
#14554=CARTESIAN_POINT ( 'NONE',  ( 0.5848930533535030563, -44.36099898510374118, -15.21101086158259541 ) ) ;
#14576=LINE ( 'NONE', #34290, #33339 ) ;
#14582=EDGE_LOOP ( 'NONE', ( #32288, #20119, #47971, #6699 ) ) ;
#14584=CARTESIAN_POINT ( 'NONE',  ( 4.962356264823608143, 0.9708976703217077064, 42.07484944210865052 ) ) ;
#14589=EDGE_CURVE ( 'NONE', #1466, #61467, #49943, .T. ) ;
#14601=ORIENTED_EDGE ( 'NONE', *, *, #38831, .T. ) ;
#14603=EDGE_CURVE ( 'NONE', #9240, #40503, #44861, .T. ) ;
#14605=ORIENTED_EDGE ( 'NONE', *, *, #31122, .T. ) ;
#14609=CARTESIAN_POINT ( 'NONE',  ( 0.5782707292762423457, -8.514009628393930385, -46.12209875705174511 ) ) ;
#14610=EDGE_CURVE ( 'NONE', #35234, #25288, #24527, .T. ) ;
#14612=EDGE_LOOP ( 'NONE', ( #25533, #50736, #47325, #17283 ) ) ;
#14616=DIRECTION ( 'NONE',  ( 0.000000000000000000, 0.000000000000000000, -1.000000000000000000 ) ) ;
#14621=CARTESIAN_POINT ( 'NONE',  ( 5.896278296736517710, -9.661066686814107740, 17.64060004895849332 ) ) ;
#14638=AXIS2_PLACEMENT_3D ( 'NONE', #61790, #28301, #23917 ) ;
#14640=CARTESIAN_POINT ( 'NONE',  ( 2.618530812446115519, 46.75512741918793580, 4.866708252371440224 ) ) ;
#14648=CARTESIAN_POINT ( 'NONE',  ( 0.5830081025819929819, 11.13700143456257052, 45.55435471421800742 ) ) ;
#14650=AXIS2_PLACEMENT_3D ( 'NONE', #19183, #34205, #15406 ) ;
#14653=ORIENTED_EDGE ( 'NONE', *, *, #26651, .F. ) ;
#14669=CARTESIAN_POINT ( 'NONE',  ( 5.901463166500145796, -1.998795974254174102, -20.01306285889149450 ) ) ;
#14670=CARTESIAN_POINT ( 'NONE',  ( 0.5835226383429282793, -25.38729180038570377, -39.43003791005067171 ) ) ;
#14677=AXIS2_PLACEMENT_3D ( 'NONE', #3759, #61387, #13822 ) ;
#14679=CARTESIAN_POINT ( 'NONE',  ( 4.291220156522059348, -43.75057291092625178, -17.47215977695438127 ) ) ;
#14680=CARTESIAN_POINT ( 'NONE',  ( 0.5848930533535030563, 11.04862722691854060, -45.57631971526609505 ) ) ;
#14681=CARTESIAN_POINT ( 'NONE',  ( 0.5806925824938511393, -42.09901922557415332, -20.66143612114853312 ) ) ;
#14684=B_SPLINE_CURVE_WITH_KNOTS ( 'NONE', 3,
 ( #1403, #40295, #36504, #2646, #3256, #31796 ),
 .UNSPECIFIED., .F., .F.,
 ( 4, 2, 4 ),
 ( 6.106282077343213345E-18, 0.0002291472222819920411, 0.0004582944445639780106 ),
 .UNSPECIFIED. ) ;
#14686=CARTESIAN_POINT ( 'NONE',  ( 0.5806925824938499181, -46.75147433417400578, -3.677228565731735621 ) ) ;
#14689=EDGE_LOOP ( 'NONE', ( #38186, #16989, #49619, #11117 ) ) ;
#14691=FACE_OUTER_BOUND ( 'NONE', #36367, .T. ) ;
#14697=CARTESIAN_POINT ( 'NONE',  ( 0.8554163680231816613, -20.57434774096662622, -42.16517150618031451 ) ) ;
#14699=ORIENTED_EDGE ( 'NONE', *, *, #38715, .T. ) ;
#14703=CARTESIAN_POINT ( 'NONE',  ( 1.231276596079881935, 38.91607545535268997, -15.58254928345689017 ) ) ;
#14704=EDGE_CURVE ( 'NONE', #18146, #47447, #60451, .T. ) ;
#14707=VERTEX_POINT ( 'NONE', #4350 ) ;
#14714=CARTESIAN_POINT ( 'NONE',  ( 3.782542959838390395, 21.69833210684487668, -36.00583615440189789 ) ) ;
#14718=AXIS2_PLACEMENT_3D ( 'NONE', #55264, #40296, #21774 ) ;
#14720=CARTESIAN_POINT ( 'NONE',  ( 1.231276596079881047, 36.49189576017899839, -20.63051901543672884 ) ) ;
#14722=CARTESIAN_POINT ( 'NONE',  ( 1.091591847532195070, -41.76074381686517256, -3.577606297232447385 ) ) ;
#14723=CARTESIAN_POINT ( 'NONE',  ( 0.9787284016396595732, -34.44493023777801000, 23.87221774036584776 ) ) ;
#14726=EDGE_CURVE ( 'NONE', #27747, #54885, #8449, .T. ) ;
#14729=CARTESIAN_POINT ( 'NONE',  ( 0.6845945791218034371, -39.15688516782669382, 25.82914757919002469 ) ) ;
#14734=EDGE_CURVE ( 'NONE', #35972, #9945, #22207, .T. ) ;
#14736=CARTESIAN_POINT ( 'NONE',  ( 5.894904586330512508, -4.663773726906127237, -19.56472914931006457 ) ) ;
#14741=VERTEX_POINT ( 'NONE', #37933 ) ;
#14752=CARTESIAN_POINT ( 'NONE',  ( 5.895596859100789899, 8.469463536103054579, -18.24270732712412624 ) ) ;
#14758=CARTESIAN_POINT ( 'NONE',  ( 0.5830081025819935370, 40.48790813666568056, 23.66350204638288091 ) ) ;
#14771=CARTESIAN_POINT ( 'NONE',  ( 4.291220156522060236, -28.73895862173628757, 37.32909394351577959 ) ) ;
#14774=CARTESIAN_POINT ( 'NONE',  ( 0.5806925824938499181, 4.150136846022649095, 46.71186922510005957 ) ) ;
#14777=CARTESIAN_POINT ( 'NONE',  ( 0.9785694773339241870, -22.36238727067532039, -35.44374474108247597 ) ) ;
#14778=B_SPLINE_CURVE_WITH_KNOTS ( 'NONE', 3,
 ( #53950, #53035, #57406, #48049, #43995, #10137 ),
 .UNSPECIFIED., .F., .F.,
 ( 4, 2, 4 ),
 ( 9.822656275951702151E-18, 0.0002291459268755758727, 0.0004582918537511419333 ),
 .UNSPECIFIED. ) ;
#14781=EDGE_CURVE ( 'NONE', #42220, #19259, #49827, .T. ) ;
#14784=CONICAL_SURFACE ( 'NONE', #61778, 42.08604991992415023, 1.569615340895231137 ) ;
#14786=LINE ( 'NONE', #29791, #23930 ) ;
#14789=EDGE_CURVE ( 'NONE', #22756, #10982, #55661, .T. ) ;
#14792=CARTESIAN_POINT ( 'NONE',  ( 0.8554163680231816613, 11.76336166872287947, 45.41837508500981357 ) ) ;
#14794=CARTESIAN_POINT ( 'NONE',  ( 0.8560838555295223751, 31.94705745926225404, -34.34761059777416392 ) ) ;
#14796=CARTESIAN_POINT ( 'NONE',  ( 0.9790724872846782167, 9.675934389771114752, 40.77635961763012773 ) ) ;
#14799=ADVANCED_FACE ( 'NONE', ( #47615 ), #42389, .F. ) ;
#14804=CARTESIAN_POINT ( 'NONE',  ( 2.282803330402965347, -39.45519406433361098, 25.49087226445491794 ) ) ;
#14810=EDGE_CURVE ( 'NONE', #47700, #5679, #50588, .T. ) ;
#14812=EDGE_LOOP ( 'NONE', ( #58799, #46657, #31843, #36270 ) ) ;
#14818=VERTEX_POINT ( 'NONE', #48233 ) ;
#14829=ORIENTED_EDGE ( 'NONE', *, *, #57991, .T. ) ;
#14836=CARTESIAN_POINT ( 'NONE',  ( 1.231276596079887264, 28.52807286890788419, -30.71523773966838888 ) ) ;
#14838=ORIENTED_EDGE ( 'NONE', *, *, #29715, .T. ) ;
#14840=CARTESIAN_POINT ( 'NONE',  ( 1.231276596079881047, 41.42457922925067493, 6.425029704024775690 ) ) ;
#14878=DIRECTION ( 'NONE',  ( -1.000000000000000000, -0.000000000000000000, -0.000000000000000000 ) ) ;
#14882=DIRECTION ( 'NONE',  ( -1.000000000000000000, 0.000000000000000000, 0.000000000000000000 ) ) ;
#14885=ADVANCED_FACE ( 'NONE', ( #40962 ), #59551, .F. ) ;
#14895=CARTESIAN_POINT ( 'NONE',  ( 3.782625744892853525, 40.05508866136273127, -12.76040659326237048 ) ) ;
#14901=CARTESIAN_POINT ( 'NONE',  ( 4.962356264823603702, 30.91935898304086550, -28.55221248765493414 ) ) ;
#14905=FACE_OUTER_BOUND ( 'NONE', #52082, .T. ) ;
#14907=CARTESIAN_POINT ( 'NONE',  ( 5.896278296736517710, -2.007758883826515017, -20.01239325714941941 ) ) ;
#14909=CARTESIAN_POINT ( 'NONE',  ( 0.8554163680231738898, -44.61245466728234987, 14.52357950615125048 ) ) ;
#14917=EDGE_LOOP ( 'NONE', ( #38933, #39816, #55879, #57330 ) ) ;
#14924=CARTESIAN_POINT ( 'NONE',  ( 0.5837157313716002660, -13.98107098236325641, 44.76345292499393480 ) ) ;
#14926=B_SPLINE_CURVE_WITH_KNOTS ( 'NONE', 3,
 ( #44652, #16135, #11430, #25829, #44966, #2004 ),
 .UNSPECIFIED., .F., .F.,
 ( 4, 2, 4 ),
 ( 1.206508049868409138E-16, 0.0002448718616795903316, 0.0004897437233590599915 ),
 .UNSPECIFIED. ) ;
#14931=ORIENTED_EDGE ( 'NONE', *, *, #40438, .T. ) ;
#14941=DIRECTION ( 'NONE',  ( -0.07906939808003037029, -0.5431863341251643718, -0.8358807550763009964 ) ) ;
#14942=CARTESIAN_POINT ( 'NONE',  ( 4.956445790443988031, 46.25174887658550915, 8.849507104743643993 ) ) ;
#14945=ORIENTED_EDGE ( 'NONE', *, *, #57312, .F. ) ;
#14946=CARTESIAN_POINT ( 'NONE',  ( 5.917102823773431552, -20.11192790512648543, -0.008601786823262999593 ) ) ;
#14953=EDGE_CURVE ( 'NONE', #10282, #17462, #20646, .T. ) ;
#14954=DIRECTION ( 'NONE',  ( -1.000000000000000000, 0.000000000000000000, -0.000000000000000000 ) ) ;
#14955=CARTESIAN_POINT ( 'NONE',  ( 4.291220156522060236, 46.92833126662970500, 4.137719400244832535 ) ) ;
#14957=CARTESIAN_POINT ( 'NONE',  ( 0.7764146366350266337, -44.59376577618206028, -14.54085718134173000 ) ) ;
#14964=EDGE_LOOP ( 'NONE', ( #13448, #27617 ) ) ;
#14965=VERTEX_POINT ( 'NONE', #6201 ) ;
#14967=DIRECTION ( 'NONE',  ( 0.000000000000000000, 0.000000000000000000, 1.000000000000000000 ) ) ;
#14974=CARTESIAN_POINT ( 'NONE',  ( 5.895596859100789899, 5.962379729971948983, 19.20880556328547684 ) ) ;
#14978=ORIENTED_EDGE ( 'NONE', *, *, #1260, .F. ) ;
#14980=CARTESIAN_POINT ( 'NONE',  ( 0.5806925824938499181, -24.77160101449041463, -39.81946942793766198 ) ) ;
#14989=ORIENTED_EDGE ( 'NONE', *, *, #23698, .F. ) ;
#14992=CARTESIAN_POINT ( 'NONE',  ( 0.9788927965476027504, 40.45682727923838939, 10.93534357620513298 ) ) ;
#14996=ORIENTED_EDGE ( 'NONE', *, *, #49449, .F. ) ;
#15000=CARTESIAN_POINT ( 'NONE',  ( 0.5797568665920715958, -46.82898593237341345, -2.504273377137976819 ) ) ;
#15002=CONICAL_SURFACE ( 'NONE', #40019, 42.08604991992415023, 1.569615340895231137 ) ;
#15003=DIRECTION ( 'NONE',  ( 0.07906939808003034253, -0.6987975377710964331, 0.7109360248941636318 ) ) ;
#15009=B_SPLINE_CURVE_WITH_KNOTS ( 'NONE', 3,
 ( #22394, #37139, #50893, #7984 ),
 .UNSPECIFIED., .F., .F.,
 ( 4, 4 ),
 ( 0.000000000000000000, 0.005004948556313786219 ),
 .UNSPECIFIED. ) ;
#15014=CARTESIAN_POINT ( 'NONE',  ( 1.091591847532196624, 38.88578709869444339, -15.64143703982636247 ) ) ;
#15016=CARTESIAN_POINT ( 'NONE',  ( 0.9790850452238858415, 38.60296000837998065, 16.31406782058402527 ) ) ;
#15024=CARTESIAN_POINT ( 'NONE',  ( 0.9762797500689124330, -37.17323042682959766, -19.35137526946170183 ) ) ;
#15029=CARTESIAN_POINT ( 'NONE',  ( 0.8560838555295223751, 28.55542365806889293, 37.21505896528891810 ) ) ;
#15038=B_SPLINE_CURVE_WITH_KNOTS ( 'NONE', 3,
 ( #16123, #55232, #21740, #40880, #16425, #11738 ),
 .UNSPECIFIED., .F., .F.,
 ( 4, 2, 4 ),
 ( 7.007167689862070887E-18, 0.0002448709889506568856, 0.0004897419779013068323 ),
 .UNSPECIFIED. ) ;
#15040=ORIENTED_EDGE ( 'NONE', *, *, #19673, .F. ) ;
#15043=CARTESIAN_POINT ( 'NONE',  ( 0.5782707292762442330, -39.07253195953447999, 25.94366203870946563 ) ) ;
#15045=CARTESIAN_POINT ( 'NONE',  ( 0.8554163680231720024, 39.89400665120465561, -24.69157156653778884 ) ) ;
#15046=VERTEX_POINT ( 'NONE', #11250 ) ;
#15049=CARTESIAN_POINT ( 'NONE',  ( 4.291220156522060236, -23.50705364442154988, 40.82655295593768585 ) ) ;
#15056=ORIENTED_EDGE ( 'NONE', *, *, #17695, .F. ) ;
#15058=ORIENTED_EDGE ( 'NONE', *, *, #26723, .F. ) ;
#15061=ORIENTED_EDGE ( 'NONE', *, *, #55972, .F. ) ;
#15062=CARTESIAN_POINT ( 'NONE',  ( 2.282816707992309180, -46.93788479523038859, -1.825359514628755342 ) ) ;
#15066=CARTESIAN_POINT ( 'NONE',  ( 0.9762797500689124330, -39.75277516423524560, 13.26806888463673673 ) ) ;
#15071=CARTESIAN_POINT ( 'NONE',  ( 3.782625744892852637, 16.70566327442924504, 38.57666287610150846 ) ) ;
#15083=CARTESIAN_POINT ( 'NONE',  ( 0.9789889208857693870, -12.50833032322637095, -39.99845710233616103 ) ) ;
#15086=CARTESIAN_POINT ( 'NONE',  ( 4.960386119450146403, 12.51307094103760065, -41.92683532413223446 ) ) ;
#15087=CARTESIAN_POINT ( 'NONE',  ( 0.5806925824938502512, -2.112975627976310111, -46.84824112321764744 ) ) ;
#15097=CARTESIAN_POINT ( 'NONE',  ( 0.5797568599927149791, 43.41643190453758194, -17.72678056923071210 ) ) ;
#15104=CARTESIAN_POINT ( 'NONE',  ( 0.5835871038041858805, -1.703517860905799264, 46.86504539418556448 ) ) ;
#15116=VECTOR ( 'NONE', #38537, 1000.000000000000000 ) ;
#15124=EDGE_LOOP ( 'NONE', ( #49606, #3097, #21845, #49542 ) ) ;
#15126=ORIENTED_EDGE ( 'NONE', *, *, #1116, .T. ) ;
#15128=CARTESIAN_POINT ( 'NONE',  ( 3.661933894777864573, 26.36408373158522878, 38.95595274082788961 ) ) ;
#15129=B_SPLINE_CURVE_WITH_KNOTS ( 'NONE', 3,
 ( #14346, #39706, #53743, #10558 ),
 .UNSPECIFIED., .F., .F.,
 ( 4, 4 ),
 ( 4.654751537338637096E-17, 0.005004948556313857343 ),
 .UNSPECIFIED. ) ;
#15135=EDGE_LOOP ( 'NONE', ( #28785, #14605, #13371, #53596 ) ) ;
#15142=CARTESIAN_POINT ( 'NONE',  ( 0.8560838555295158248, -0.6537497281619772949, -46.90357604036880446 ) ) ;
#15145=CARTESIAN_POINT ( 'NONE',  ( 1.231276596079887264, -26.41281459480383376, 32.55211200826430229 ) ) ;
#15146=B_SPLINE_CURVE_WITH_KNOTS ( 'NONE', 3,
 ( #57106, #49567, #31094, #2256, #1634, #44295 ),
 .UNSPECIFIED., .F., .F.,
 ( 4, 2, 4 ),
 ( 6.314488766312913488E-18, 0.0002291472222819943992, 0.0004582944445639824558 ),
 .UNSPECIFIED. ) ;
#15147=CARTESIAN_POINT ( 'NONE',  ( 0.5806925824938494740, 36.46274162637944016, -29.49052111156159128 ) ) ;
#15149=CARTESIAN_POINT ( 'NONE',  ( 2.528190830796658961, -41.36197007608242870, 7.172277712015144857 ) ) ;
#15154=CARTESIAN_POINT ( 'NONE',  ( 0.7056759521544979652, -35.34448603454957549, 30.83044171059700389 ) ) ;
#15155=EDGE_CURVE ( 'NONE', #25145, #60457, #39421, .T. ) ;
#15160=EDGE_CURVE ( 'NONE', #51214, #21652, #46855, .T. ) ;
#15164=EDGE_CURVE ( 'NONE', #33009, #27817, #37876, .T. ) ;
#15169=CARTESIAN_POINT ( 'NONE',  ( 5.895596859100789899, 12.98817590332804883, 15.35693556399505155 ) ) ;
#15172=VERTEX_POINT ( 'NONE', #51295 ) ;
#15175=CARTESIAN_POINT ( 'NONE',  ( 0.6845945791218023269, 33.22744374803170331, 33.11107824709630165 ) ) ;
#15178=EDGE_CURVE ( 'NONE', #10350, #30761, #52812, .T. ) ;
#15190=CARTESIAN_POINT ( 'NONE',  ( 0.5806925824938502512, -24.77160101449099727, 39.81946942793729249 ) ) ;
#15194=CARTESIAN_POINT ( 'NONE',  ( 0.5837800304671222351, -45.96535232605464216, 9.296435753618650821 ) ) ;
#15204=ADVANCED_FACE ( 'NONE', ( #18424 ), #2121, .T. ) ;
#15205=CARTESIAN_POINT ( 'NONE',  ( 0.9791128995231617171, -41.06991714040155728, -8.342621909610549835 ) ) ;
#15206=VECTOR ( 'NONE', #20009, 1000.000000000000227 ) ;
#15211=EDGE_CURVE ( 'NONE', #30629, #31192, #30397, .T. ) ;
#15215=CARTESIAN_POINT ( 'NONE',  ( 3.782542959838399721, -42.02453062021629648, 1.084748610081117670 ) ) ;
#15218=CARTESIAN_POINT ( 'NONE',  ( 0.7764139734771249302, 5.581186588129950721, -46.57135200072405468 ) ) ;
#15222=CARTESIAN_POINT ( 'NONE',  ( 0.5824936645240097466, 46.52475202343088512, -5.889450585459719889 ) ) ;
#15227=ORIENTED_EDGE ( 'NONE', *, *, #9696, .T. ) ;
#15240=CARTESIAN_POINT ( 'NONE',  ( 4.956445790444004906, -37.28933980949924631, -28.75835855384189443 ) ) ;
#15246=CARTESIAN_POINT ( 'NONE',  ( 4.962356264823603702, 26.83784316460332420, -32.41860225448503030 ) ) ;
#15253=CARTESIAN_POINT ( 'NONE',  ( 0.5797568665920712627, -44.50349591956066320, -14.78729723578712729 ) ) ;
#15254=EDGE_CURVE ( 'NONE', #58067, #50843, #13198, .T. ) ;
#15266=EDGE_LOOP ( 'NONE', ( #15909, #50400, #60306, #35945 ) ) ;
#15274=B_SPLINE_CURVE_WITH_KNOTS ( 'NONE', 3,
 ( #39365, #5795, #43450, #492 ),
 .UNSPECIFIED., .F., .F.,
 ( 4, 4 ),
 ( 6.505213034913026604E-19, 0.004446298630425053744 ),
 .UNSPECIFIED. ) ;
#15283=CARTESIAN_POINT ( 'NONE',  ( 0.5835871038041856584, -25.11868534319529900, -39.60159213378984333 ) ) ;
#15291=ORIENTED_EDGE ( 'NONE', *, *, #23680, .T. ) ;
#15292=CARTESIAN_POINT ( 'NONE',  ( 5.910764540655178756, 19.00446553125916793, 6.582668785556910152 ) ) ;
#15293=EDGE_CURVE ( 'NONE', #9430, #18146, #22866, .T. ) ;
#15301=ORIENTED_EDGE ( 'NONE', *, *, #4640, .T. ) ;
#15306=B_SPLINE_CURVE_WITH_KNOTS ( 'NONE', 3,
 ( #8616, #27743, #55924, #61238, #46873, #8304, #22422, #46553, #15194, #52456, #58075, #23970, #4520, #766, #28661, #19907 ),
 .UNSPECIFIED., .F., .F.,
 ( 4, 3, 3, 3, 3, 4 ),
 ( 1.214354834101861724E-17, 0.0002732102107931876143, 0.0004098135523333793113, 0.0005464168938824958896, 0.0008195847345945451784, 0.001092771384553108301 ),
 .UNSPECIFIED. ) ;
#15307=ORIENTED_EDGE ( 'NONE', *, *, #47885, .T. ) ;
#15309=ORIENTED_EDGE ( 'NONE', *, *, #35046, .F. ) ;
#15311=CARTESIAN_POINT ( 'NONE',  ( 0.9789889208857698311, 36.00916266840548730, -21.44003502708611464 ) ) ;
#15320=CARTESIAN_POINT ( 'NONE',  ( 4.956445790443991584, 41.78282513192503700, 21.71942849465911252 ) ) ;
#15323=CARTESIAN_POINT ( 'NONE',  ( 2.618530812446115519, 15.57291328060520819, -44.35325423408014700 ) ) ;
#15326=CARTESIAN_POINT ( 'NONE',  ( 0.8560838555295223751, 40.81790744942443183, 23.11430867518979326 ) ) ;
#15329=CARTESIAN_POINT ( 'NONE',  ( 4.962356264823593932, 31.50371261889118557, 27.90612278853270922 ) ) ;
#15335=ADVANCED_FACE ( 'NONE', ( #54679 ), #16763, .F. ) ;
#15339=CARTESIAN_POINT ( 'NONE',  ( 0.9762797500689124330, 4.697980241568662230, 41.64437257103935508 ) ) ;
#15340=CARTESIAN_POINT ( 'NONE',  ( 0.9762797500689124330, -41.77809974471938403, -3.303810967047359881 ) ) ;
#15341=CARTESIAN_POINT ( 'NONE',  ( 0.9780303403264757334, -34.36697018299320661, 23.98439021189286535 ) ) ;
#15346=CARTESIAN_POINT ( 'NONE',  ( 0.9762797500689124330, -6.471194619075235188, -41.40589843715211771 ) ) ;
#15347=DIRECTION ( 'NONE',  ( 0.000000000000000000, 0.000000000000000000, 1.000000000000000000 ) ) ;
#15350=CARTESIAN_POINT ( 'NONE',  ( 5.896782393890504181, -19.93252920631901404, -2.687073932226577533 ) ) ;
#15356=EDGE_CURVE ( 'NONE', #25455, #8551, #26189, .T. ) ;
#15360=ADVANCED_FACE ( 'NONE', ( #31199 ), #23166, .F. ) ;
#15371=ORIENTED_EDGE ( 'NONE', *, *, #22794, .T. ) ;
#15376=CARTESIAN_POINT ( 'NONE',  ( 0.5835226383429296115, 40.44198222182293989, 23.74212603192314575 ) ) ;
#15379=CARTESIAN_POINT ( 'NONE',  ( 0.5848930533535030563, -38.55997537638081951, -26.69084826978085800 ) ) ;
#15382=CARTESIAN_POINT ( 'NONE',  ( 0.5834584762367737154, 32.73240943502174360, -33.58311125538091346 ) ) ;
#15391=ORIENTED_EDGE ( 'NONE', *, *, #40438, .F. ) ;
#15396=CARTESIAN_POINT ( 'NONE',  ( 4.962356264823602814, -25.31392337492848554, -33.62202970123303203 ) ) ;
#15404=CARTESIAN_POINT ( 'NONE',  ( 1.092182651088191792, 20.82421885325586430, 36.37462155946074915 ) ) ;
#15406=DIRECTION ( 'NONE',  ( 0.000000000000000000, 0.000000000000000000, 1.000000000000000000 ) ) ;
#15411=CARTESIAN_POINT ( 'NONE',  ( 0.5837800005270571413, -1.566997147869758411, 46.86981735168539132 ) ) ;
#15413=ORIENTED_EDGE ( 'NONE', *, *, #43659, .T. ) ;
#15416=CARTESIAN_POINT ( 'NONE',  ( 4.962356264823608143, 6.570263404306589727, 41.57002810511892221 ) ) ;
#15428=CARTESIAN_POINT ( 'NONE',  ( 0.7056313189692703380, 28.49521968211951872, 37.25279988437523571 ) ) ;
#15437=CARTESIAN_POINT ( 'NONE',  ( 1.231276596079887931, -37.78837162824473950, -18.14705873423390869 ) ) ;
#15442=VERTEX_POINT ( 'NONE', #45951 ) ;
#15446=CARTESIAN_POINT ( 'NONE',  ( 0.9762797500689124330, 36.31338395866797697, 20.92039508843128814 ) ) ;
#15447=EDGE_CURVE ( 'NONE', #17462, #50427, #46247, .T. ) ;
#15468=CARTESIAN_POINT ( 'NONE',  ( 0.9791128995231628274, 9.710313423905196473, -40.76821368978151128 ) ) ;
#15469=CARTESIAN_POINT ( 'NONE',  ( 4.962356264823608143, 7.429277797797782412, -41.42513040734446861 ) ) ;
#15473=CARTESIAN_POINT ( 'NONE',  ( 0.9775691876210961251, -1.022782437399945232, -41.89615286724711751 ) ) ;
#15478=CARTESIAN_POINT ( 'NONE',  ( 2.618530812446111078, 39.70953715621322999, 25.15709538157219072 ) ) ;
#15480=CARTESIAN_POINT ( 'NONE',  ( 0.5782707292762423457, 37.25243273660916543, 28.49548400908516399 ) ) ;
#15484=EDGE_CURVE ( 'NONE', #36659, #42702, #15306, .T. ) ;
#15485=CARTESIAN_POINT ( 'NONE',  ( 3.782625744892852193, 11.41484085274463567, 40.45910913998868352 ) ) ;
#15492=ORIENTED_EDGE ( 'NONE', *, *, #15160, .F. ) ;
#15493=ORIENTED_EDGE ( 'NONE', *, *, #17200, .T. ) ;
#15496=CARTESIAN_POINT ( 'NONE',  ( 0.9754292589017200532, -34.21816598153960598, 24.19596213741219515 ) ) ;
#15498=ORIENTED_EDGE ( 'NONE', *, *, #56245, .T. ) ;
#15506=EDGE_CURVE ( 'NONE', #59587, #10433, #55658, .T. ) ;
#15511=CARTESIAN_POINT ( 'NONE',  ( 0.9789233960466707796, -41.04249736261641601, -8.476446016578329079 ) ) ;
#15515=ORIENTED_EDGE ( 'NONE', *, *, #20625, .T. ) ;
#15516=VERTEX_POINT ( 'NONE', #18661 ) ;
#15517=CARTESIAN_POINT ( 'NONE',  ( 2.528100132419516477, 33.68154901921120370, 25.05607779159677406 ) ) ;
#15529=CARTESIAN_POINT ( 'NONE',  ( 4.962356264823603702, 17.31942680647464528, -38.35717733303005161 ) ) ;
#15531=CARTESIAN_POINT ( 'NONE',  ( 5.895596859100789899, 17.94951300836806141, 9.074313526372865368 ) ) ;
#15532=EDGE_LOOP ( 'NONE', ( #21426, #35862, #10154, #26934 ) ) ;
#15536=CARTESIAN_POINT ( 'NONE',  ( 2.282803330402963127, -2.882084055115845977, 46.88486428428933550 ) ) ;
#15538=ORIENTED_EDGE ( 'NONE', *, *, #16051, .F. ) ;
#15539=CARTESIAN_POINT ( 'NONE',  ( 0.5848930533535030563, -1.749067435711075591, -46.86377967570363978 ) ) ;
#15540=CARTESIAN_POINT ( 'NONE',  ( 3.238018933889920792, -4.230209958194933506, -12.70876925895034759 ) ) ;
#15541=DIRECTION ( 'NONE',  ( 0.07500201931887537365, -0.9127009170568822771, -0.4016861126571554808 ) ) ;
#15543=CARTESIAN_POINT ( 'NONE',  ( 0.9762797500689124330, 38.38274741215490593, -16.82526333465304091 ) ) ;
#15548=CARTESIAN_POINT ( 'NONE',  ( 5.896782393890504181, -20.11283288166117345, -0.006352352428112362746 ) ) ;
#15549=CARTESIAN_POINT ( 'NONE',  ( 0.9769922540276034795, 41.47347701830330635, 6.023475665958448744 ) ) ;
#15550=CARTESIAN_POINT ( 'NONE',  ( 0.5837157313716023754, 27.89101090674457240, -37.70051159045296885 ) ) ;
#15555=CARTESIAN_POINT ( 'NONE',  ( 3.661933894777891219, 24.23903144487420747, -40.31253551398190638 ) ) ;
#15562=CARTESIAN_POINT ( 'NONE',  ( 5.910764540655177868, -9.651974367317830428, -17.64484710281737634 ) ) ;
#15566=CARTESIAN_POINT ( 'NONE',  ( 0.9787284016396621267, 28.99970135845135033, -30.25480656109806432 ) ) ;
#15573=CARTESIAN_POINT ( 'NONE',  ( 0.5804410086790514622, 22.05813747677497716, -41.38790189066235570 ) ) ;
#15576=CARTESIAN_POINT ( 'NONE',  ( 0.8554163680231738898, -6.900908941296520993, -46.40671211038068833 ) ) ;
#15588=EDGE_CURVE ( 'NONE', #32480, #20677, #48088, .T. ) ;
#15594=ORIENTED_EDGE ( 'NONE', *, *, #39480, .T. ) ;
#15595=CARTESIAN_POINT ( 'NONE',  ( 0.5817216825391120505, -34.47346183105885586, 31.79332290890629764 ) ) ;
#15598=ORIENTED_EDGE ( 'NONE', *, *, #40702, .F. ) ;
#15600=CARTESIAN_POINT ( 'NONE',  ( 5.838029081930957709, 47.13000430274633601, 3.134924652369162956 ) ) ;
#15601=DIRECTION ( 'NONE',  ( 0.000000000000000000, 0.000000000000000000, 1.000000000000000000 ) ) ;
#15603=B_SPLINE_CURVE_WITH_KNOTS ( 'NONE', 3,
 ( #60411, #60724, #56032, #46356, #46663, #27233 ),
 .UNSPECIFIED., .F., .F.,
 ( 4, 2, 4 ),
 ( 0.000000000000000000, 0.0002291459268755698824, 0.0004582918537511397649 ),
 .UNSPECIFIED. ) ;
#15606=LINE ( 'NONE', #34405, #24725 ) ;
#15611=CARTESIAN_POINT ( 'NONE',  ( 1.231276596079887931, -39.86997064245532840, -12.94844438486017779 ) ) ;
#15613=CARTESIAN_POINT ( 'NONE',  ( 1.157643937452369043, -31.63536294457205145, -27.49920155131693988 ) ) ;
#15625=CARTESIAN_POINT ( 'NONE',  ( 0.9780303403264766215, -31.29797956580119944, -27.87070304986538360 ) ) ;
#15627=CARTESIAN_POINT ( 'NONE',  ( 0.8560838555295158248, -38.14845555156047396, -27.29593693413630362 ) ) ;
#15629=CARTESIAN_POINT ( 'NONE',  ( 0.9783242366443545279, -26.85209652948670467, -32.17606878065826947 ) ) ;
#15634=ORIENTED_EDGE ( 'NONE', *, *, #18197, .F. ) ;
#15643=CARTESIAN_POINT ( 'NONE',  ( 0.5804410086790514622, 32.20888702807360460, 34.08969709851039909 ) ) ;
#15654=CARTESIAN_POINT ( 'NONE',  ( 5.896278296736517710, -7.223603833371336158, 18.77089575041337000 ) ) ;
#15656=VERTEX_POINT ( 'NONE', #49004 ) ;
#15660=AXIS2_PLACEMENT_3D ( 'NONE', #35642, #35328, #16210 ) ;
#15665=CARTESIAN_POINT ( 'NONE',  ( 4.960386119450151732, -30.75418163181185705, 31.12260877288193583 ) ) ;
#15670=ORIENTED_EDGE ( 'NONE', *, *, #38573, .F. ) ;
#15676=VERTEX_POINT ( 'NONE', #39626 ) ;
#15678=ORIENTED_EDGE ( 'NONE', *, *, #639, .F. ) ;
#15696=ORIENTED_EDGE ( 'NONE', *, *, #8063, .T. ) ;
#15698=ORIENTED_EDGE ( 'NONE', *, *, #38930, .F. ) ;
#15699=CARTESIAN_POINT ( 'NONE',  ( 1.231276596079887264, -2.246340108599748309, -41.85965512441022440 ) ) ;
#15705=CARTESIAN_POINT ( 'NONE',  ( 0.6064782688330851990, -39.06168768307265537, 25.95224463835178952 ) ) ;
#15708=VERTEX_POINT ( 'NONE', #21114 ) ;
#15713=ADVANCED_FACE ( 'NONE', ( #55765 ), #48166, .T. ) ;
#15727=CARTESIAN_POINT ( 'NONE',  ( 4.956445790443988031, 0.000000000000000000, 0.000000000000000000 ) ) ;
#15733=CARTESIAN_POINT ( 'NONE',  ( 0.9762797500689124330, 38.38274741215490593, -16.82526333465304091 ) ) ;
#15738=VERTEX_POINT ( 'NONE', #51687 ) ;
#15750=CARTESIAN_POINT ( 'NONE',  ( 0.9789889208857698311, -17.72799716457255670, -37.97437312945766053 ) ) ;
#15751=ORIENTED_EDGE ( 'NONE', *, *, #55689, .T. ) ;
#15753=EDGE_CURVE ( 'NONE', #10639, #25145, #11184, .T. ) ;
#15754=CARTESIAN_POINT ( 'NONE',  ( 3.238018933889920792, -0.7223087070292297796, -13.37481822304148871 ) ) ;
#15755=ORIENTED_EDGE ( 'NONE', *, *, #26378, .T. ) ;
#15756=( BOUNDED_SURFACE ( )  B_SPLINE_SURFACE ( 3, 1, ( 
 ( #5270, #53505 ),
 ( #24401, #10940 ),
 ( #6186, #39451 ),
 ( #48826, #19713 ) ),
 .UNSPECIFIED., .F., .F., .F. ) 
 B_SPLINE_SURFACE_WITH_KNOTS ( ( 4, 4 ),
 ( 2, 2 ),
 ( 0.000000000000000000, 1.000000000000000000 ),
 ( 0.000000000000000000, 1.000000000000000000 ),
 .UNSPECIFIED. ) 
 GEOMETRIC_REPRESENTATION_ITEM ( )  RATIONAL_B_SPLINE_SURFACE ( (
 ( 1.000000000000000000, 1.000000000000000000),
 ( 0.9952954269826590483, 0.8620686068821339365),
 ( 0.9952954269826590483, 0.8620686068821339365),
 ( 1.000000000000000000, 1.000000000000000000) ) ) 
 REPRESENTATION_ITEM ( '' )  SURFACE ( )  );
#15758=CARTESIAN_POINT ( 'NONE',  ( 5.838029081930957709, 13.97520979541510044, -45.11938130479024522 ) ) ;
#15759=CARTESIAN_POINT ( 'NONE',  ( 0.9784957157296372277, 36.17631838904543429, 21.15672575817877288 ) ) ;
#15761=B_SPLINE_CURVE_WITH_KNOTS ( 'NONE', 3,
 ( #18769, #38195, #32245, #28449 ),
 .UNSPECIFIED., .F., .F.,
 ( 4, 4 ),
 ( 0.000000000000000000, 0.004447772540403797242 ),
 .UNSPECIFIED. ) ;
#15770=CARTESIAN_POINT ( 'NONE',  ( 2.618530812446111078, -46.97577780651596413, 1.732942200721546699 ) ) ;
#15772=VERTEX_POINT ( 'NONE', #56383 ) ;
#15781=CARTESIAN_POINT ( 'NONE',  ( 0.9790850452238875068, 9.666011576262016902, -40.77873895145319239 ) ) ;
#15785=CARTESIAN_POINT ( 'NONE',  ( 1.231276596079881047, -11.60895935156387537, -40.28037777618035875 ) ) ;
#15789=EDGE_CURVE ( 'NONE', #35743, #24966, #23488, .T. ) ;
#15790=CARTESIAN_POINT ( 'NONE',  ( 1.231276596079881047, 15.85305549123227564, -38.80666698661426040 ) ) ;
#15804=CARTESIAN_POINT ( 'NONE',  ( 3.376099380956842921, 13.21675742563012967, -2.241808819707415079 ) ) ;
#15805=CARTESIAN_POINT ( 'NONE',  ( 5.895881250540457863, -13.98558879082096240, 14.45444526027768184 ) ) ;
#15806=CARTESIAN_POINT ( 'NONE',  ( 1.000433927950260093, -34.17502901178241359, 24.25873182375112691 ) ) ;
#15816=VECTOR ( 'NONE', #44999, 1000.000000000000114 ) ;
#15819=DIRECTION ( 'NONE',  ( -1.000000000000000000, -0.000000000000000000, -0.000000000000000000 ) ) ;
#15825=VERTEX_POINT ( 'NONE', #61381 ) ;
#15833=CARTESIAN_POINT ( 'NONE',  ( 2.282816707992307848, 18.10202035515079544, 43.34528608129922134 ) ) ;
#15836=CARTESIAN_POINT ( 'NONE',  ( 0.5835226383429313879, 46.45302275910173506, -6.431108076244583138 ) ) ;
#15840=CARTESIAN_POINT ( 'NONE',  ( 4.956445790443996025, 13.43466403631381567, 45.13366650706556982 ) ) ;
#15854=CARTESIAN_POINT ( 'NONE',  ( 0.5797568665920714848, 45.39179673982854268, 11.78176970289104197 ) ) ;
#15862=CARTESIAN_POINT ( 'NONE',  ( 0.5806925824938502512, 27.37593026015236219, -38.07598724570169679 ) ) ;
#15871=EDGE_CURVE ( 'NONE', #13524, #28607, #47478, .T. ) ;
#15877=CARTESIAN_POINT ( 'NONE',  ( 0.7056313189692637877, -29.63221772841613344, 36.35492148875172802 ) ) ;
#15905=CARTESIAN_POINT ( 'NONE',  ( 0.5824936645240085253, -20.06997566773453912, 42.38436333999664640 ) ) ;
#15908=EDGE_CURVE ( 'NONE', #7974, #28331, #34069, .T. ) ;
#15909=ORIENTED_EDGE ( 'NONE', *, *, #2337, .F. ) ;
#15914=CARTESIAN_POINT ( 'NONE',  ( 4.956445790443996913, 8.365049606151725214, 46.34181691762049127 ) ) ;
#15916=CARTESIAN_POINT ( 'NONE',  ( 0.9780303403264789530, 4.516970423409048863, 41.66457237977044770 ) ) ;
#15920=CARTESIAN_POINT ( 'NONE',  ( 0.9791128995231609400, 36.05569391225776599, -21.36175017997689451 ) ) ;
#15921=CIRCLE ( 'NONE', #61894, 42.08604991992415023 ) ;
#15922=CARTESIAN_POINT ( 'NONE',  ( 2.618530812446111078, -45.76452502972750125, -10.73941516106192573 ) ) ;
#15929=VERTEX_POINT ( 'NONE', #20053 ) ;
#15930=CARTESIAN_POINT ( 'NONE',  ( 0.9791128995231611620, -31.08508259969504195, -28.10791835081888834 ) ) ;
#15934=CARTESIAN_POINT ( 'NONE',  ( 0.9790320750461896093, -26.99170229640500906, -32.05908825410412533 ) ) ;
#15935=AXIS2_PLACEMENT_3D ( 'NONE', #51886, #4558, #61881 ) ;
#15937=ORIENTED_EDGE ( 'NONE', *, *, #31804, .T. ) ;
#15940=AXIS2_PLACEMENT_3D ( 'NONE', #52829, #61593, #46929 ) ;
#15948=ADVANCED_FACE ( 'NONE', ( #57916 ), #14393, .F. ) ;
#15949=FACE_OUTER_BOUND ( 'NONE', #17411, .T. ) ;
#15950=CARTESIAN_POINT ( 'NONE',  ( 1.231276596079887931, -35.03243822710496858, -23.02183839058345072 ) ) ;
#15952=CARTESIAN_POINT ( 'NONE',  ( 1.231276596079887264, -30.51591784428387655, 28.74118176309011830 ) ) ;
#15962=( BOUNDED_SURFACE ( )  B_SPLINE_SURFACE ( 3, 1, ( 
 ( #12969, #44943 ),
 ( #31433, #12655 ),
 ( #49924, #27045 ),
 ( #46171, #8229 ) ),
 .UNSPECIFIED., .F., .F., .F. ) 
 B_SPLINE_SURFACE_WITH_KNOTS ( ( 4, 4 ),
 ( 2, 2 ),
 ( 0.000000000000000000, 1.000000000000000000 ),
 ( 0.000000000000000000, 1.000000000000000000 ),
 .UNSPECIFIED. ) 
 GEOMETRIC_REPRESENTATION_ITEM ( )  RATIONAL_B_SPLINE_SURFACE ( (
 ( 1.000000000000000000, 1.000000000000000000),
 ( 0.9952954269826590483, 0.8620686068821339365),
 ( 0.9952954269826590483, 0.8620686068821339365),
 ( 1.000000000000000000, 1.000000000000000000) ) ) 
 REPRESENTATION_ITEM ( '' )  SURFACE ( )  );
#15964=CARTESIAN_POINT ( 'NONE',  ( 1.000110580585052089, 24.32719571472549447, 34.12630995916995147 ) ) ;
#15966=CARTESIAN_POINT ( 'NONE',  ( 0.5830082357119570347, -19.49201582728397852, -42.65317519162255167 ) ) ;
#15970=VERTEX_POINT ( 'NONE', #19428 ) ;
#15976=CARTESIAN_POINT ( 'NONE',  ( 1.231276596079881047, 25.54232633153377208, -33.23952972879584422 ) ) ;
#15977=ORIENTED_EDGE ( 'NONE', *, *, #1966, .F. ) ;
#15983=ORIENTED_EDGE ( 'NONE', *, *, #57065, .T. ) ;
#15987=ORIENTED_EDGE ( 'NONE', *, *, #8369, .F. ) ;
#15999=VERTEX_POINT ( 'NONE', #16899 ) ;
#16002=B_SPLINE_CURVE_WITH_KNOTS ( 'NONE', 3,
 ( #37319, #32613, #51699, #47029 ),
 .UNSPECIFIED., .F., .F.,
 ( 4, 4 ),
 ( 0.000000000000000000, 0.004041751736740999482 ),
 .UNSPECIFIED. ) ;
#16004=CARTESIAN_POINT ( 'NONE',  ( 0.5837800005270565862, -46.79128237205272001, -3.132275948988451741 ) ) ;
#16008=CARTESIAN_POINT ( 'NONE',  ( 0.9787464366903542157, 40.46600164325194982, -10.90122488066344886 ) ) ;
#16010=CARTESIAN_POINT ( 'NONE',  ( 0.9785694773339246311, -12.20375881750114999, -40.09243914304710898 ) ) ;
#16013=CARTESIAN_POINT ( 'NONE',  ( 0.9762797500689124330, -22.12212327108586152, -35.59405072711710716 ) ) ;
#16017=CARTESIAN_POINT ( 'NONE',  ( 0.9762797500689124330, -41.84568905980458453, 2.294143041716202092 ) ) ;
#16021=CARTESIAN_POINT ( 'NONE',  ( 0.9754292589017248272, 20.64935455141624487, 36.46822758930269259 ) ) ;
#16023=CARTESIAN_POINT ( 'NONE',  ( 0.5806925824938499181, 43.38503874128572591, -17.80339225430652306 ) ) ;
#16032=EDGE_CURVE ( 'NONE', #4962, #11037, #29186, .T. ) ;
#16035=DIRECTION ( 'NONE',  ( 0.07906939808003034253, -0.9592846432126428402, -0.2711475679102691161 ) ) ;
#16036=CARTESIAN_POINT ( 'NONE',  ( 4.956445790444005794, -36.61936279692559992, -29.60676136437043127 ) ) ;
#16051=EDGE_CURVE ( 'NONE', #33083, #22554, #44386, .T. ) ;
#16052=VERTEX_POINT ( 'NONE', #50386 ) ;
#16054=CARTESIAN_POINT ( 'NONE',  ( 0.9784957157296365615, -17.85167291169407022, -37.91636627165451046 ) ) ;
#16055=VERTEX_POINT ( 'NONE', #21897 ) ;
#16056=ADVANCED_FACE ( 'NONE', ( #41032 ), #18784, .F. ) ;
#16059=CARTESIAN_POINT ( 'NONE',  ( 0.8560838555295158248, -45.77741231505087427, -10.23725333375899105 ) ) ;
#16061=ORIENTED_EDGE ( 'NONE', *, *, #2954, .T. ) ;
#16065=CARTESIAN_POINT ( 'NONE',  ( 0.5782707292762442330, 16.17912178775479504, 44.02240761117701595 ) ) ;
#16068=ORIENTED_EDGE ( 'NONE', *, *, #41173, .F. ) ;
#16069=ADVANCED_FACE ( 'NONE', ( #61014 ), #25161, .F. ) ;
#16070=ORIENTED_EDGE ( 'NONE', *, *, #26132, .T. ) ;
#16072=CARTESIAN_POINT ( 'NONE',  ( 0.5804410086790514622, -14.41595396256412620, -44.62846763227064173 ) ) ;
#16079=CARTESIAN_POINT ( 'NONE',  ( 0.5804410086790514622, 46.89585601637878653, -0.5463884574786393999 ) ) ;
#16085=CARTESIAN_POINT ( 'NONE',  ( 2.282816707992319394, 3.392768508892113566, -46.85067863172353952 ) ) ;
#16093=B_SPLINE_CURVE_WITH_KNOTS ( 'NONE', 3,
 ( #38117, #28995, #37487, #37813, #5470, #23372, #24607, #33097, #56563, #13677, #32786, #51863, #8961, #42498, #57162, #52170, #14296, #9262, #28371 ),
 .UNSPECIFIED., .F., .F.,
 ( 4, 3, 3, 3, 3, 3, 4 ),
 ( 1.250973872328959472E-17, 0.0002732106629380605888, 0.0004098138914053748357, 0.0005464171197651485328, 0.0006830203481512556575, 0.0008196235766963574530, 0.001011968216111140293 ),
 .UNSPECIFIED. ) ;
#16095=CARTESIAN_POINT ( 'NONE',  ( 0.8554163680231738898, 39.89400665120432876, 24.69157156653835017 ) ) ;
#16098=CARTESIAN_POINT ( 'NONE',  ( 0.5830081025819920937, -14.15482648850689529, -44.70875665305972291 ) ) ;
#16107=CARTESIAN_POINT ( 'NONE',  ( 1.231276596079887931, 38.25526645152051941, -17.14092645516095104 ) ) ;
#16109=ORIENTED_EDGE ( 'NONE', *, *, #56062, .F. ) ;
#16113=ORIENTED_EDGE ( 'NONE', *, *, #34215, .T. ) ;
#16119=VERTEX_POINT ( 'NONE', #8386 ) ;
#16123=CARTESIAN_POINT ( 'NONE',  ( 0.5806925824938502512, 17.36345040154772690, 43.56297685531322372 ) ) ;
#16124=FACE_OUTER_BOUND ( 'NONE', #46360, .T. ) ;
#16133=ORIENTED_EDGE ( 'NONE', *, *, #1777, .F. ) ;
#16135=CARTESIAN_POINT ( 'NONE',  ( 0.7764139734771257073, 27.10005299892409170, 38.28351601358438216 ) ) ;
#16139=CARTESIAN_POINT ( 'NONE',  ( 0.5806925824938499181, -38.35106547415185929, -26.98922265166007861 ) ) ;
#16141=CARTESIAN_POINT ( 'NONE',  ( 0.8560838555295223751, 17.70877843982779609, 43.43698884880053157 ) ) ;
#16150=CARTESIAN_POINT ( 'NONE',  ( 0.9762797500689124330, 3.691134646838137190, -41.74566217230977117 ) ) ;
#16153=CARTESIAN_POINT ( 'NONE',  ( 5.896782393890504181, -19.93252920631905667, 2.687073932226298201 ) ) ;
#16162=CARTESIAN_POINT ( 'NONE',  ( 4.956445790444004018, -45.27177431812791042, 12.96165499572219737 ) ) ;
#16163=CARTESIAN_POINT ( 'NONE',  ( 5.896278296736517710, -7.233829247026454468, 18.76695750619285974 ) ) ;
#16169=CARTESIAN_POINT ( 'NONE',  ( 0.9790850452238860635, 15.10954715382613678, 39.09013833525667536 ) ) ;
#16173=CARTESIAN_POINT ( 'NONE',  ( 4.956445790444040433, 46.94638516972321440, -3.684422564748698115 ) ) ;
#16181=CARTESIAN_POINT ( 'NONE',  ( 0.8560838555295158248, 37.37287335782446718, -28.34856559090329142 ) ) ;
#16189=CARTESIAN_POINT ( 'NONE',  ( 5.896782393890504181, 3.351618377817072947, 19.83160964539921167 ) ) ;
#16191=VECTOR ( 'NONE', #31984, 999.9999999999998863 ) ;
#16206=CARTESIAN_POINT ( 'NONE',  ( 0.5830081025819898732, -34.59664839919615531, 31.65918435343287385 ) ) ;
#16210=DIRECTION ( 'NONE',  ( 0.000000000000000000, 0.000000000000000000, 1.000000000000000000 ) ) ;
#16211=EDGE_CURVE ( 'NONE', #11980, #46288, #57219, .T. ) ;
#16214=ORIENTED_EDGE ( 'NONE', *, *, #13379, .F. ) ;
#16217=FACE_OUTER_BOUND ( 'NONE', #42744, .T. ) ;
#16218=VERTEX_POINT ( 'NONE', #47868 ) ;
#16219=CARTESIAN_POINT ( 'NONE',  ( 0.9775691876210979014, 3.818852833867097729, 41.73427933992938677 ) ) ;
#16227=CARTESIAN_POINT ( 'NONE',  ( 5.894904586330512508, -7.227592724925631984, -18.76942501687904041 ) ) ;
#16233=CARTESIAN_POINT ( 'NONE',  ( 0.9775691876210976794, -30.82697754998653039, -28.39068798255189208 ) ) ;
#16235=CARTESIAN_POINT ( 'NONE',  ( 0.9762797500689124330, 38.38274741215490593, -16.82526333465304091 ) ) ;
#16238=CARTESIAN_POINT ( 'NONE',  ( 0.9787464366903561030, 38.51372612363144299, 16.52352543994085110 ) ) ;
#16239=ORIENTED_EDGE ( 'NONE', *, *, #50456, .T. ) ;
#16249=EDGE_CURVE ( 'NONE', #34782, #40429, #24980, .T. ) ;
#16264=CARTESIAN_POINT ( 'NONE',  ( 4.956445790444035104, 41.78282513192535674, -21.71942849465849079 ) ) ;
#16267=CARTESIAN_POINT ( 'NONE',  ( 2.528100132419517809, -33.91014296975959041, 24.74582757562452784 ) ) ;
#16274=DIRECTION ( 'NONE',  ( 0.07500201931887537365, 0.8144017028153685001, 0.5754342391181805905 ) ) ;
#16299=ORIENTED_EDGE ( 'NONE', *, *, #13006, .F. ) ;
#16321=DIRECTION ( 'NONE',  ( 0.07906939808003032866, 0.8860534191553557370, 0.4567902896191699535 ) ) ;
#16322=ADVANCED_FACE ( 'NONE', ( #7377 ), #8210, .T. ) ;
#16337=LINE ( 'NONE', #54524, #50948 ) ;
#16338=B_SPLINE_CURVE_WITH_KNOTS ( 'NONE', 3,
 ( #10589, #29682, #39118, #10906 ),
 .UNSPECIFIED., .F., .F.,
 ( 4, 4 ),
 ( 1.301042606982605321E-18, 0.004446298630425058948 ),
 .UNSPECIFIED. ) ;
#16346=ORIENTED_EDGE ( 'NONE', *, *, #21046, .F. ) ;
#16349=ORIENTED_EDGE ( 'NONE', *, *, #17076, .T. ) ;
#16350=VERTEX_POINT ( 'NONE', #36864 ) ;
#16352=VERTEX_POINT ( 'NONE', #26824 ) ;
#16356=VERTEX_POINT ( 'NONE', #56239 ) ;
#16359=CARTESIAN_POINT ( 'NONE',  ( 5.895596859100789899, -19.93390588528923857, 2.677233529021818104 ) ) ;
#16364=CARTESIAN_POINT ( 'NONE',  ( 0.9780303403264775097, 36.22227486202688596, 21.07810278974036677 ) ) ;
#16366=EDGE_CURVE ( 'NONE', #18623, #6436, #42240, .T. ) ;
#16370=( BOUNDED_SURFACE ( )  B_SPLINE_SURFACE ( 3, 1, ( 
 ( #21076, #59270 ),
 ( #35191, #15770 ),
 ( #34880, #58643 ),
 ( #39589, #39904 ) ),
 .UNSPECIFIED., .F., .F., .F. ) 
 B_SPLINE_SURFACE_WITH_KNOTS ( ( 4, 4 ),
 ( 2, 2 ),
 ( 0.000000000000000000, 1.000000000000000000 ),
 ( 0.000000000000000000, 1.000000000000000000 ),
 .UNSPECIFIED. ) 
 GEOMETRIC_REPRESENTATION_ITEM ( )  RATIONAL_B_SPLINE_SURFACE ( (
 ( 1.000000000000000000, 1.000000000000000000),
 ( 0.7282232189291694135, 0.9929344683865672927),
 ( 0.7282232189291694135, 0.9929344683865672927),
 ( 1.000000000000000000, 1.000000000000000000) ) ) 
 REPRESENTATION_ITEM ( '' )  SURFACE ( )  );
#16371=EDGE_CURVE ( 'NONE', #56097, #4099, #24149, .T. ) ;
#16380=ORIENTED_EDGE ( 'NONE', *, *, #54284, .T. ) ;
#16381=CARTESIAN_POINT ( 'NONE',  ( 0.9780106845699476636, -39.48577557688840045, -14.04296170852301628 ) ) ;
#16384=CARTESIAN_POINT ( 'NONE',  ( 3.661921753702027438, 35.71933374875705880, -30.60654048367672786 ) ) ;
#16387=( BOUNDED_SURFACE ( )  B_SPLINE_SURFACE ( 3, 1, ( 
 ( #38863, #15045 ),
 ( #1520, #30047 ),
 ( #34765, #47937 ),
 ( #34152, #4983 ) ),
 .UNSPECIFIED., .F., .F., .F. ) 
 B_SPLINE_SURFACE_WITH_KNOTS ( ( 4, 4 ),
 ( 2, 2 ),
 ( 0.000000000000000000, 1.000000000000000000 ),
 ( 0.000000000000000000, 1.000000000000000000 ),
 .UNSPECIFIED. ) 
 GEOMETRIC_REPRESENTATION_ITEM ( )  RATIONAL_B_SPLINE_SURFACE ( (
 ( 1.000000000000000000, 1.000000000000000000),
 ( 0.9952954269826590483, 0.8620686068821307169),
 ( 0.9952954269826590483, 0.8620686068821307169),
 ( 1.000000000000000000, 1.000000000000000000) ) ) 
 REPRESENTATION_ITEM ( '' )  SURFACE ( )  );
#16390=CARTESIAN_POINT ( 'NONE',  ( 0.5782707292762442330, -30.83005644796828904, 35.34464560754155826 ) ) ;
#16393=FACE_OUTER_BOUND ( 'NONE', #16603, .T. ) ;
#16394=EDGE_CURVE ( 'NONE', #7929, #40951, #24946, .T. ) ;
#16396=CARTESIAN_POINT ( 'NONE',  ( 0.5782707292762423457, -34.29472224813918757, 31.99388034656949031 ) ) ;
#16398=CARTESIAN_POINT ( 'NONE',  ( 0.5830082357119548142, -13.63298622686205874, -44.87063317445529975 ) ) ;
#16404=ADVANCED_FACE ( 'NONE', ( #7911 ), #27187, .F. ) ;
#16405=CARTESIAN_POINT ( 'NONE',  ( 0.5848930533535030563, 46.50190038545807880, 6.070118856208002178 ) ) ;
#16408=CARTESIAN_POINT ( 'NONE',  ( 4.962356264823609031, 37.75702904547822669, -18.59145920903629090 ) ) ;
#16409=VERTEX_POINT ( 'NONE', #50207 ) ;
#16420=ORIENTED_EDGE ( 'NONE', *, *, #51367, .T. ) ;
#16421=ORIENTED_EDGE ( 'NONE', *, *, #6746, .T. ) ;
#16425=CARTESIAN_POINT ( 'NONE',  ( 0.7764146366350200834, 17.68681966478046874, 43.44210956911165766 ) ) ;
#16428=CARTESIAN_POINT ( 'NONE',  ( 2.618530812446111078, -44.84885430744879642, 14.08215383055557446 ) ) ;
#16435=DIRECTION ( 'NONE',  ( -1.000000000000000000, -0.000000000000000000, -0.000000000000000000 ) ) ;
#16436=CARTESIAN_POINT ( 'NONE',  ( 0.8560838555295158248, 3.785103201470073397, 46.75516899590838449 ) ) ;
#16448=CARTESIAN_POINT ( 'NONE',  ( 0.5797568665920710407, 5.319645520859431542, 46.59320422694997887 ) ) ;
#16453=CARTESIAN_POINT ( 'NONE',  ( 0.6845945791218034371, 37.34424629630233028, -28.38685944719937027 ) ) ;
#16466=CARTESIAN_POINT ( 'NONE',  ( 0.5837799406558231707, 27.74442806126372929, -37.80860035931723928 ) ) ;
#16473=CARTESIAN_POINT ( 'NONE',  ( 5.910764540655177868, 5.973554503640923663, -19.20463186476622397 ) ) ;
#16476=EDGE_CURVE ( 'NONE', #49170, #45083, #11519, .T. ) ;
#16482=CARTESIAN_POINT ( 'NONE',  ( 4.291220156522060236, 44.16776250362654821, 16.38895215469672095 ) ) ;
#16484=ORIENTED_EDGE ( 'NONE', *, *, #20595, .F. ) ;
#16486=CARTESIAN_POINT ( 'NONE',  ( 0.8560838555295223751, -24.46533024579953164, 40.02274915651970133 ) ) ;
#16499=AXIS2_PLACEMENT_3D ( 'NONE', #49849, #55149, #44871 ) ;
#16501=CARTESIAN_POINT ( 'NONE',  ( 3.376099380956838925, 10.79965495504299433, -7.942029745857318801 ) ) ;
#16504=ORIENTED_EDGE ( 'NONE', *, *, #52381, .F. ) ;
#16506=CARTESIAN_POINT ( 'NONE',  ( 0.5848930533535030563, -25.38746244141833230, 39.43031616882030477 ) ) ;
#16512=CARTESIAN_POINT ( 'NONE',  ( 4.960386119450149955, 13.41207489487474724, -41.64796167505215863 ) ) ;
#16515=CARTESIAN_POINT ( 'NONE',  ( 0.5817216825391118284, -19.32621644266162519, 42.72858890975519586 ) ) ;
#16516=DIRECTION ( 'NONE',  ( -0.07906939808003035641, 0.2389416749771256232, 0.9678093336222726162 ) ) ;
#16524=EDGE_CURVE ( 'NONE', #4627, #41301, #16735, .T. ) ;
#16537=ORIENTED_EDGE ( 'NONE', *, *, #6004, .F. ) ;
#16540=CARTESIAN_POINT ( 'NONE',  ( 0.9787464366903561030, 38.65195219007281935, -16.19754872771774501 ) ) ;
#16542=CARTESIAN_POINT ( 'NONE',  ( 0.5837799406558220605, -30.34692608210707121, -35.75342818450186400 ) ) ;
#16551=CARTESIAN_POINT ( 'NONE',  ( 0.5326698147273788431, 0.000000000000000000, -41.88877248453276536 ) ) ;
#16556=CARTESIAN_POINT ( 'NONE',  ( 0.8560838555295158248, 37.37287335782446718, -28.34856559090329142 ) ) ;
#16563=CARTESIAN_POINT ( 'NONE',  ( 5.910764540655178756, 3.329973395294576477, -19.83462920388967987 ) ) ;
#16564=EDGE_CURVE ( 'NONE', #16052, #19210, #30134, .T. ) ;
#16576=CARTESIAN_POINT ( 'NONE',  ( 0.5804410086790514622, 46.55025363952961470, 5.709092568075557317 ) ) ;
#16585=VECTOR ( 'NONE', #42726, 999.9999999999998863 ) ;
#16587=ORIENTED_EDGE ( 'NONE', *, *, #40157, .F. ) ;
#16589=CARTESIAN_POINT ( 'NONE',  ( 0.8560838555295158248, -44.60403252362548443, 14.52078223488980768 ) ) ;
#16597=AXIS2_PLACEMENT_3D ( 'NONE', #7435, #54744, #21875 ) ;
#16601=CARTESIAN_POINT ( 'NONE',  ( 5.895881250540457863, 16.58446435569129918, -11.37906954206300014 ) ) ;
#16603=EDGE_LOOP ( 'NONE', ( #25058, #23124, #38492, #40690 ) ) ;
#16610=CARTESIAN_POINT ( 'NONE',  ( 0.7764139734771235979, -34.18255399381159521, -32.11842887451099671 ) ) ;
#16616=ORIENTED_EDGE ( 'NONE', *, *, #35747, .F. ) ;
#16619=CARTESIAN_POINT ( 'NONE',  ( 0.5830082357119569236, -44.39002986412761231, 15.12472424873239518 ) ) ;
#16626=CARTESIAN_POINT ( 'NONE',  ( 1.231276596079887264, 40.19859528295904738, -11.88905834349085922 ) ) ;
#16627=ORIENTED_EDGE ( 'NONE', *, *, #17116, .T. ) ;
#16633=CARTESIAN_POINT ( 'NONE',  ( 1.231276596079887264, 10.53918392497828727, 40.57341954055075917 ) ) ;
#16642=CARTESIAN_POINT ( 'NONE',  ( 0.5837800304671216800, 32.56903879203510854, 33.74159220224218103 ) ) ;
#16645=CARTESIAN_POINT ( 'NONE',  ( 4.960386119450149955, 35.80440191905969272, 25.14918026279933017 ) ) ;
#16647=CARTESIAN_POINT ( 'NONE',  ( 4.956445790443989807, 46.03642002599014660, 9.908889005849758291 ) ) ;
#16649=CIRCLE ( 'NONE', #14650, 42.08604991992415023 ) ;
#16650=ORIENTED_EDGE ( 'NONE', *, *, #52862, .F. ) ;
#16655=EDGE_CURVE ( 'NONE', #10433, #49383, #18970, .T. ) ;
#16663=ORIENTED_EDGE ( 'NONE', *, *, #35823, .F. ) ;
#16668=ORIENTED_EDGE ( 'NONE', *, *, #28591, .F. ) ;
#16671=CARTESIAN_POINT ( 'NONE',  ( 0.9762797500689124330, -22.12212327108638377, 35.59405072711678741 ) ) ;
#16681=EDGE_CURVE ( 'NONE', #53909, #31128, #3860, .T. ) ;
#16685=EDGE_CURVE ( 'NONE', #17824, #29827, #22270, .T. ) ;
#16695=VECTOR ( 'NONE', #54201, 1000.000000000000114 ) ;
#16698=CARTESIAN_POINT ( 'NONE',  ( 0.9783242366443549720, -39.50104640422178193, -14.00006511335010906 ) ) ;
#16705=CARTESIAN_POINT ( 'NONE',  ( 2.528190830796654964, -2.611642835106711136, 41.89789323885920425 ) ) ;
#16709=CARTESIAN_POINT ( 'NONE',  ( 4.962356264823602814, -15.53171314616136200, -39.11523340858015274 ) ) ;
#16710=CARTESIAN_POINT ( 'NONE',  ( 0.9789233960466705575, 32.80823903839893774, 26.07596935938558502 ) ) ;
#16720=CARTESIAN_POINT ( 'NONE',  ( 0.7056759521545029612, 23.27569225635726724, -40.71843537151615777 ) ) ;
#16730=VERTEX_POINT ( 'NONE', #46498 ) ;
#16735=B_SPLINE_CURVE_WITH_KNOTS ( 'NONE', 3,
 ( #47076, #12948, #32660, #32046, #28554, #36754 ),
 .UNSPECIFIED., .F., .F.,
 ( 4, 2, 4 ),
 ( 0.000000000000000000, 0.0002291459268755699637, 0.0004582918537511399275 ),
 .UNSPECIFIED. ) ;
#16741=ORIENTED_EDGE ( 'NONE', *, *, #18216, .T. ) ;
#16744=( BOUNDED_SURFACE ( )  B_SPLINE_SURFACE ( 3, 1, ( 
 ( #38135, #23391 ),
 ( #24006, #18391 ),
 ( #41907, #18700 ),
 ( #56885, #37512 ) ),
 .UNSPECIFIED., .F., .F., .F. ) 
 B_SPLINE_SURFACE_WITH_KNOTS ( ( 4, 4 ),
 ( 2, 2 ),
 ( 0.000000000000000000, 1.000000000000000000 ),
 ( 0.000000000000000000, 1.000000000000000000 ),
 .UNSPECIFIED. ) 
 GEOMETRIC_REPRESENTATION_ITEM ( )  RATIONAL_B_SPLINE_SURFACE ( (
 ( 1.000000000000000000, 1.000000000000000000),
 ( 0.7282232189291694135, 0.9929344683865672927),
 ( 0.7282232189291694135, 0.9929344683865672927),
 ( 1.000000000000000000, 1.000000000000000000) ) ) 
 REPRESENTATION_ITEM ( '' )  SURFACE ( )  );
#16758=EDGE_CURVE ( 'NONE', #39044, #26356, #31214, .T. ) ;
#16759=ORIENTED_EDGE ( 'NONE', *, *, #17407, .F. ) ;
#16761=CARTESIAN_POINT ( 'NONE',  ( 0.6845945791218023269, -13.06825445484081349, 45.05138450944075146 ) ) ;
#16763=( BOUNDED_SURFACE ( )  B_SPLINE_SURFACE ( 3, 1, ( 
 ( #16189, #15576 ),
 ( #11487, #35002 ),
 ( #40327, #6432 ),
 ( #54991, #11808 ) ),
 .UNSPECIFIED., .F., .F., .F. ) 
 B_SPLINE_SURFACE_WITH_KNOTS ( ( 4, 4 ),
 ( 2, 2 ),
 ( 0.000000000000000000, 1.000000000000000000 ),
 ( 0.000000000000000000, 1.000000000000000000 ),
 .UNSPECIFIED. ) 
 GEOMETRIC_REPRESENTATION_ITEM ( )  RATIONAL_B_SPLINE_SURFACE ( (
 ( 1.000000000000000000, 1.000000000000000000),
 ( 0.7282232189291694135, 0.9929344683865672927),
 ( 0.7282232189291694135, 0.9929344683865672927),
 ( 1.000000000000000000, 1.000000000000000000) ) ) 
 REPRESENTATION_ITEM ( '' )  SURFACE ( )  );
#16765=CARTESIAN_POINT ( 'NONE',  ( 5.917102823773431552, -19.39960706793709733, 5.305182717059529374 ) ) ;
#16773=VERTEX_POINT ( 'NONE', #28603 ) ;
#16776=EDGE_CURVE ( 'NONE', #24375, #36534, #41291, .T. ) ;
#16780=LINE ( 'NONE', #35891, #56462 ) ;
#16781=CARTESIAN_POINT ( 'NONE',  ( 0.5848930533535030563, 22.69711449001784231, 41.03795896745572946 ) ) ;
#16783=EDGE_CURVE ( 'NONE', #54358, #33554, #47268, .T. ) ;
#16787=CARTESIAN_POINT ( 'NONE',  ( 1.231276596079887264, 38.91607545535247681, 15.58254928345742840 ) ) ;
#16795=CARTESIAN_POINT ( 'NONE',  ( 0.5835871038041859915, -34.68875627993142530, -31.55827372739225467 ) ) ;
#16798=CARTESIAN_POINT ( 'NONE',  ( 0.9791128995231611620, -31.07823802939244118, 28.11548603945144009 ) ) ;
#16803=CARTESIAN_POINT ( 'NONE',  ( 4.956445790444011124, -17.42806872899762993, -43.74700527484106516 ) ) ;
#16811=EDGE_CURVE ( 'NONE', #24826, #33742, #48635, .T. ) ;
#16819=VECTOR ( 'NONE', #58039, 1000.000000000000114 ) ;
#16822=ORIENTED_EDGE ( 'NONE', *, *, #58464, .T. ) ;
#16824=ORIENTED_EDGE ( 'NONE', *, *, #59109, .T. ) ;
#16827=B_SPLINE_CURVE_WITH_KNOTS ( 'NONE', 3,
 ( #11295, #40150, #54485, #25385 ),
 .UNSPECIFIED., .F., .F.,
 ( 4, 4 ),
 ( 3.252606517456513784E-19, 0.004446298630425062418 ),
 .UNSPECIFIED. ) ;
#16828=ORIENTED_EDGE ( 'NONE', *, *, #54707, .T. ) ;
#16842=CARTESIAN_POINT ( 'NONE',  ( 0.7056313189692687837, -18.97455749483731324, 42.89189680851932707 ) ) ;
#16848=CARTESIAN_POINT ( 'NONE',  ( 0.9790850452238883950, 4.245257672208578192, 41.69310635536467657 ) ) ;
#16852=CARTESIAN_POINT ( 'NONE',  ( 0.9762797500689124330, 24.45014227842982635, 34.03697001423955726 ) ) ;
#16859=ORIENTED_EDGE ( 'NONE', *, *, #43789, .F. ) ;
#16860=B_SPLINE_CURVE_WITH_KNOTS ( 'NONE', 3,
 ( #46831, #22693, #50880, #46209 ),
 .UNSPECIFIED., .F., .F.,
 ( 4, 4 ),
 ( 0.000000000000000000, 0.004041751736740992543 ),
 .UNSPECIFIED. ) ;
#16869=CARTESIAN_POINT ( 'NONE',  ( 1.231276596079881047, 14.27346765619277846, 39.41503383336979027 ) ) ;
#16870=ORIENTED_EDGE ( 'NONE', *, *, #24415, .F. ) ;
#16881=CARTESIAN_POINT ( 'NONE',  ( 2.528190830796659405, -33.91013147734389577, -24.74585054796578376 ) ) ;
#16889=CARTESIAN_POINT ( 'NONE',  ( 1.231276596079881047, -27.70544295162376258, 31.45926257674180704 ) ) ;
#16890=CARTESIAN_POINT ( 'NONE',  ( 5.895596859100789899, -19.93295055289977213, 2.684337063064242912 ) ) ;
#16895=ORIENTED_EDGE ( 'NONE', *, *, #14173, .F. ) ;
#16897=CARTESIAN_POINT ( 'NONE',  ( 0.5824935313925958535, -20.06998985431518534, -42.38435659888590834 ) ) ;
#16899=CARTESIAN_POINT ( 'NONE',  ( 0.5806925824938499181, 32.99217760300705748, -33.32774488853398509 ) ) ;
#16905=DIRECTION ( 'NONE',  ( -1.000000000000000000, -0.000000000000000000, -0.000000000000000000 ) ) ;
#16907=B_SPLINE_CURVE_WITH_KNOTS ( 'NONE', 3,
 ( #39032, #28985, #19291, #61853 ),
 .UNSPECIFIED., .F., .F.,
 ( 4, 4 ),
 ( 8.673617379884035472E-19, 0.004446298630425055479 ),
 .UNSPECIFIED. ) ;
#16912=CARTESIAN_POINT ( 'NONE',  ( 5.917102823773431552, 3.336722021764336521, 19.83320458728783109 ) ) ;
#16915=ORIENTED_EDGE ( 'NONE', *, *, #39060, .T. ) ;
#16917=CARTESIAN_POINT ( 'NONE',  ( 4.956445790444004018, -45.55738122058057371, -11.91902120403893761 ) ) ;
#16919=LINE ( 'NONE', #17219, #12760 ) ;
#16920=EDGE_CURVE ( 'NONE', #28607, #25211, #34226, .T. ) ;
#16921=ORIENTED_EDGE ( 'NONE', *, *, #44659, .T. ) ;
#16925=ORIENTED_EDGE ( 'NONE', *, *, #50853, .T. ) ;
#16927=CARTESIAN_POINT ( 'NONE',  ( 3.376099380956842921, 5.244649644334445249, 12.33701883520689258 ) ) ;
#16929=B_SPLINE_CURVE_WITH_KNOTS ( 'NONE', 3,
 ( #14254, #8918, #37140, #9523, #61818, #28631, #28329, #52430, #47754, #8279, #18022, #4804, #108, #19257, #13322, #47445, #41841, #32426, #46526 ),
 .UNSPECIFIED., .F., .F.,
 ( 4, 3, 3, 3, 3, 3, 4 ),
 ( 8.891118888688803850E-18, 0.0002732106629380615104, 0.0004098138914053764620, 0.0005464171197651473402, 0.0006830203481512575007, 0.0008196235766963647171, 0.001011968216111141594 ),
 .UNSPECIFIED. ) ;
#16934=EDGE_CURVE ( 'NONE', #25309, #58463, #21375, .T. ) ;
#16938=ORIENTED_EDGE ( 'NONE', *, *, #59562, .T. ) ;
#16943=DIRECTION ( 'NONE',  ( 0.000000000000000000, 0.000000000000000000, 1.000000000000000000 ) ) ;
#16946=ADVANCED_FACE ( 'NONE', ( #20759 ), #61918, .F. ) ;
#16947=ORIENTED_EDGE ( 'NONE', *, *, #16681, .F. ) ;
#16952=CARTESIAN_POINT ( 'NONE',  ( 0.6064515330803585957, -44.06399544130436396, 16.05299479180740363 ) ) ;
#16966=CARTESIAN_POINT ( 'NONE',  ( 0.5806925824938499181, 37.13995815321135296, -28.63295078613577971 ) ) ;
#16967=CARTESIAN_POINT ( 'NONE',  ( 0.5848930533535030563, -14.06811673146533614, 44.73657534967806981 ) ) ;
#16974=CARTESIAN_POINT ( 'NONE',  ( 3.661933894777865017, 31.32117021671156820, 35.09437933925365627 ) ) ;
#16975=CARTESIAN_POINT ( 'NONE',  ( 5.895596859100789899, -4.666058297670689470, 19.56415301451167466 ) ) ;
#16982=CARTESIAN_POINT ( 'NONE',  ( 1.231276596079881047, -6.136529359146127405, -41.46829847537036784 ) ) ;
#16985=CARTESIAN_POINT ( 'NONE',  ( 4.956445790443988031, 47.01859095792194410, 2.605792484304518375 ) ) ;
#16989=ORIENTED_EDGE ( 'NONE', *, *, #52427, .F. ) ;
#16991=ORIENTED_EDGE ( 'NONE', *, *, #55168, .F. ) ;
#16996=CARTESIAN_POINT ( 'NONE',  ( 2.528190830796656741, -35.27991276599423287, 22.75042618011462636 ) ) ;
#16997=VECTOR ( 'NONE', #16274, 999.9999999999998863 ) ;
#17000=CARTESIAN_POINT ( 'NONE',  ( 0.5817216825391123836, -29.92823674778196974, 36.10450937730870180 ) ) ;
#17008=ORIENTED_EDGE ( 'NONE', *, *, #5983, .F. ) ;
#17011=CARTESIAN_POINT ( 'NONE',  ( 5.895881250540457863, -20.11287301435476849, -0.004551564636875675592 ) ) ;
#17015=CARTESIAN_POINT ( 'NONE',  ( 0.7056313189692682286, 21.79704775904467340, -41.52875332763414207 ) ) ;
#17018=EDGE_CURVE ( 'NONE', #37493, #30663, #6002, .T. ) ;
#17027=CARTESIAN_POINT ( 'NONE',  ( 0.9787284016396589070, 33.00560649245351641, 25.82568370816429493 ) ) ;
#17031=CARTESIAN_POINT ( 'NONE',  ( 0.5837157313716019313, -13.80717013915596958, -44.81739747386527739 ) ) ;
#17038=ORIENTED_EDGE ( 'NONE', *, *, #26132, .F. ) ;
#17041=CARTESIAN_POINT ( 'NONE',  ( 1.092182651088186018, -11.67010021001421016, 40.25630317764550625 ) ) ;
#17043=CARTESIAN_POINT ( 'NONE',  ( 1.231276596079887264, -23.26513148155214594, -34.87134107206314582 ) ) ;
#17044=ORIENTED_EDGE ( 'NONE', *, *, #2589, .T. ) ;
#17067=CARTESIAN_POINT ( 'NONE',  ( 0.6845945791218034371, -35.36481895536458353, 30.81778870990308405 ) ) ;
#17074=CARTESIAN_POINT ( 'NONE',  ( 3.376099380956842921, -3.529868236344322341, 12.93245583275328592 ) ) ;
#17076=EDGE_CURVE ( 'NONE', #8104, #53799, #52174, .T. ) ;
#17077=CARTESIAN_POINT ( 'NONE',  ( 0.5804410086790514622, -34.41390132670994717, 31.86225427258510834 ) ) ;
#17078=FACE_OUTER_BOUND ( 'NONE', #49235, .T. ) ;
#17080=CARTESIAN_POINT ( 'NONE',  ( 1.157644175074338033, -21.85425510640531144, -35.76861486307988969 ) ) ;
#17081=FACE_OUTER_BOUND ( 'NONE', #38220, .T. ) ;
#17084=AXIS2_PLACEMENT_3D ( 'NONE', #12352, #39627, #30495 ) ;
#17087=CARTESIAN_POINT ( 'NONE',  ( 1.091591847532191961, 20.82376294252117077, -36.37485241027820138 ) ) ;
#17091=CARTESIAN_POINT ( 'NONE',  ( 5.894904586330512508, -9.666977479134271078, -17.63743060878067581 ) ) ;
#17093=CARTESIAN_POINT ( 'NONE',  ( 0.9762797500689124330, 4.697980241568662230, 41.64437257103935508 ) ) ;
#17100=CARTESIAN_POINT ( 'NONE',  ( 1.231276596079887264, -41.76121777166943616, 3.643825084340432952 ) ) ;
#17101=CARTESIAN_POINT ( 'NONE',  ( 3.782542959838390839, 41.39849740043850801, 7.307685432642670342 ) ) ;
#17106=CARTESIAN_POINT ( 'NONE',  ( 0.9762797500689124330, -41.77809974471938403, -3.303810967047359881 ) ) ;
#17107=CARTESIAN_POINT ( 'NONE',  ( 0.8560838555295167129, -41.44626783305055540, -21.96769712083564841 ) ) ;
#17116=EDGE_CURVE ( 'NONE', #22756, #43281, #6550, .T. ) ;
#17120=EDGE_CURVE ( 'NONE', #5475, #60728, #42651, .T. ) ;
#17121=( BOUNDED_SURFACE ( )  B_SPLINE_SURFACE ( 3, 1, ( 
 ( #55902, #17393 ),
 ( #36515, #55581 ),
 ( #12710, #35898 ),
 ( #49978, #25859 ) ),
 .UNSPECIFIED., .F., .F., .F. ) 
 B_SPLINE_SURFACE_WITH_KNOTS ( ( 4, 4 ),
 ( 2, 2 ),
 ( 0.000000000000000000, 1.000000000000000000 ),
 ( 0.000000000000000000, 1.000000000000000000 ),
 .UNSPECIFIED. ) 
 GEOMETRIC_REPRESENTATION_ITEM ( )  RATIONAL_B_SPLINE_SURFACE ( (
 ( 1.000000000000000000, 1.000000000000000000),
 ( 0.7282232189291693025, 0.9929344683865674037),
 ( 0.7282232189291693025, 0.9929344683865674037),
 ( 1.000000000000000000, 1.000000000000000000) ) ) 
 REPRESENTATION_ITEM ( '' )  SURFACE ( )  );
#17124=CARTESIAN_POINT ( 'NONE',  ( 4.956445790444031552, 34.56007374686835476, -31.98654955994249960 ) ) ;
#17127=CARTESIAN_POINT ( 'NONE',  ( 0.9790724872846771065, 32.91492816068598160, -25.94113941519019306 ) ) ;
#17135=DIRECTION ( 'NONE',  ( -0.07500201931887527651, -0.9957672615368104996, -0.05312492776063274663 ) ) ;
#17145=CARTESIAN_POINT ( 'NONE',  ( 4.962356264823608143, -28.94323483023595145, -30.55363735178127271 ) ) ;
#17153=ORIENTED_EDGE ( 'NONE', *, *, #14403, .T. ) ;
#17161=ADVANCED_FACE ( 'NONE', ( #8811 ), #1918, .F. ) ;
#17162=ORIENTED_EDGE ( 'NONE', *, *, #34117, .T. ) ;
#17165=CARTESIAN_POINT ( 'NONE',  ( 1.231276596079887931, -40.90292846002456173, 9.177538581350681568 ) ) ;
#17166=CARTESIAN_POINT ( 'NONE',  ( 0.5797568665920710407, 27.30868362185057308, -38.12428500894856143 ) ) ;
#17176=CARTESIAN_POINT ( 'NONE',  ( 0.5824936645240093025, 45.13218602318958972, 12.74064220549800552 ) ) ;
#17178=CARTESIAN_POINT ( 'NONE',  ( 5.896782393890504181, 17.95394716461040829, 9.065421561537570838 ) ) ;
#17180=CARTESIAN_POINT ( 'NONE',  ( 5.901463166500145796, -2.027578129543060381, 20.01016734735707914 ) ) ;
#17182=DIRECTION ( 'NONE',  ( -0.07500201931887526263, -0.1791611824598981217, -0.9809566594899399306 ) ) ;
#17188=CARTESIAN_POINT ( 'NONE',  ( 0.5804410086790514622, -38.97211966759181934, 26.09010809617889493 ) ) ;
#17192=EDGE_CURVE ( 'NONE', #15999, #45432, #8022, .T. ) ;
#17194=CARTESIAN_POINT ( 'NONE',  ( 0.5782707292762423457, 3.973746573564317597, -46.73270473529971269 ) ) ;
#17200=EDGE_CURVE ( 'NONE', #14965, #35032, #4338, .T. ) ;
#17202=CARTESIAN_POINT ( 'NONE',  ( 0.9754292580325136797, -0.8180783604022585642, -41.90057535046801007 ) ) ;
#17204=CARTESIAN_POINT ( 'NONE',  ( 0.5782707292762442330, 45.03824936633908038, 13.08787407194444619 ) ) ;
#17209=( BOUNDED_SURFACE ( )  B_SPLINE_SURFACE ( 3, 1, ( 
 ( #53086, #24283 ),
 ( #18993, #9882 ),
 ( #38110, #47794 ),
 ( #8951, #27752 ) ),
 .UNSPECIFIED., .F., .F., .F. ) 
 B_SPLINE_SURFACE_WITH_KNOTS ( ( 4, 4 ),
 ( 2, 2 ),
 ( 0.000000000000000000, 1.000000000000000000 ),
 ( 0.000000000000000000, 1.000000000000000000 ),
 .UNSPECIFIED. ) 
 GEOMETRIC_REPRESENTATION_ITEM ( )  RATIONAL_B_SPLINE_SURFACE ( (
 ( 1.000000000000000000, 1.000000000000000000),
 ( 0.9952954269826590483, 0.8620686068821307169),
 ( 0.9952954269826590483, 0.8620686068821307169),
 ( 1.000000000000000000, 1.000000000000000000) ) ) 
 REPRESENTATION_ITEM ( '' )  SURFACE ( )  );
#17211=FACE_OUTER_BOUND ( 'NONE', #22164, .T. ) ;
#17215=CARTESIAN_POINT ( 'NONE',  ( 2.156380492024271511, -0.2527577876543339874, -46.96604096131991213 ) ) ;
#17219=CARTESIAN_POINT ( 'NONE',  ( 3.238018933889920792, -11.19612451184691615, -7.352162150202732782 ) ) ;
#17225=DIRECTION ( 'NONE',  ( 0.000000000000000000, 0.000000000000000000, 1.000000000000000000 ) ) ;
#17232=CARTESIAN_POINT ( 'NONE',  ( 0.9787464366903567692, -17.80123337693228081, 37.94008543941954059 ) ) ;
#17233=FACE_OUTER_BOUND ( 'NONE', #46069, .T. ) ;
#17239=CARTESIAN_POINT ( 'NONE',  ( 0.5806925824938499181, 36.46274162637902094, 29.49052111156212774 ) ) ;
#17240=EDGE_CURVE ( 'NONE', #28734, #29203, #55832, .T. ) ;
#17241=CARTESIAN_POINT ( 'NONE',  ( 0.5797568665920715958, 36.41064436358183087, -29.55486906806790515 ) ) ;
#17250=CARTESIAN_POINT ( 'NONE',  ( 0.9780106845699489959, 10.02007934243528808, -40.69311067523273806 ) ) ;
#17254=ORIENTED_EDGE ( 'NONE', *, *, #36715, .T. ) ;
#17255=CARTESIAN_POINT ( 'NONE',  ( 5.895881250540457863, 19.00150250643894267, -6.593222588847996057 ) ) ;
#17260=CARTESIAN_POINT ( 'NONE',  ( 0.5824936645240081923, 32.33896082458391419, 33.96218178837067114 ) ) ;
#17263=CARTESIAN_POINT ( 'NONE',  ( 0.7764146366350240802, -6.921054454054549332, 46.39115733534977437 ) ) ;
#17274=ADVANCED_FACE ( 'NONE', ( #50419 ), #30824, .F. ) ;
#17275=ORIENTED_EDGE ( 'NONE', *, *, #57832, .T. ) ;
#17276=CARTESIAN_POINT ( 'NONE',  ( 1.231276596079887931, -39.86997064245532840, -12.94844438486017779 ) ) ;
#17279=ORIENTED_EDGE ( 'NONE', *, *, #9460, .T. ) ;
#17283=ORIENTED_EDGE ( 'NONE', *, *, #21003, .F. ) ;
#17293=ORIENTED_EDGE ( 'NONE', *, *, #23040, .T. ) ;
#17296=ORIENTED_EDGE ( 'NONE', *, *, #34980, .F. ) ;
#17297=CARTESIAN_POINT ( 'NONE',  ( 0.8554163680231738898, 45.48289776771382975, -11.51136324522476428 ) ) ;
#17298=CARTESIAN_POINT ( 'NONE',  ( 5.901463166500146684, 20.06867656024511604, 1.328943738803535224 ) ) ;
#17300=CARTESIAN_POINT ( 'NONE',  ( 0.7764146366350240802, 46.89611481693733452, -0.8915653345649677819 ) ) ;
#17301=ORIENTED_EDGE ( 'NONE', *, *, #5553, .T. ) ;
#17304=CARTESIAN_POINT ( 'NONE',  ( 4.956445790443988031, 0.000000000000000000, 0.000000000000000000 ) ) ;
#17309=ORIENTED_EDGE ( 'NONE', *, *, #53932, .T. ) ;
#17316=CARTESIAN_POINT ( 'NONE',  ( 0.9789233960466710016, -39.54649551180114031, -13.87124434098955028 ) ) ;
#17326=DIRECTION ( 'NONE',  ( -0.07500201931887529039, 0.3457612750068366769, -0.9353201792989060959 ) ) ;
#17327=CARTESIAN_POINT ( 'NONE',  ( 1.157643937452369487, 35.63734160579004850, -22.06767223490007268 ) ) ;
#17331=CARTESIAN_POINT ( 'NONE',  ( 0.5806925824938499181, -29.85799195566266917, -36.16244846134105018 ) ) ;
#17335=CARTESIAN_POINT ( 'NONE',  ( 0.5326698147273788431, 0.000000000000000000, 0.000000000000000000 ) ) ;
#17336=CARTESIAN_POINT ( 'NONE',  ( 0.5804410086790514622, -42.10186154173658934, -20.66284362269238883 ) ) ;
#17337=ORIENTED_EDGE ( 'NONE', *, *, #39916, .F. ) ;
#17340=CARTESIAN_POINT ( 'NONE',  ( 0.9762797500689124330, -11.93232144563832975, 40.17392798947675914 ) ) ;
#17347=CARTESIAN_POINT ( 'NONE',  ( 3.376099380956842921, 2.658192826266324804, -13.13934528545670588 ) ) ;
#17353=CARTESIAN_POINT ( 'NONE',  ( 0.5782707292762423457, 45.42077932512024319, 11.69141390963249627 ) ) ;
#17357=EDGE_LOOP ( 'NONE', ( #48708, #14427, #6672, #45426 ) ) ;
#17361=B_SPLINE_CURVE_WITH_KNOTS ( 'NONE', 3,
 ( #49645, #25846, #44985, #2019 ),
 .UNSPECIFIED., .F., .F.,
 ( 4, 4 ),
 ( 0.000000000000000000, 0.005004948556313793158 ),
 .UNSPECIFIED. ) ;
#17367=ORIENTED_EDGE ( 'NONE', *, *, #56579, .T. ) ;
#17371=CARTESIAN_POINT ( 'NONE',  ( 4.960386119450149955, -21.43901005587166253, 38.14191018416060786 ) ) ;
#17383=( BOUNDED_SURFACE ( )  B_SPLINE_SURFACE ( 3, 1, ( 
 ( #56691, #19137 ),
 ( #38246, #14430 ),
 ( #14736, #10338 ),
 ( #7146, #58851 ) ),
 .UNSPECIFIED., .F., .F., .F. ) 
 B_SPLINE_SURFACE_WITH_KNOTS ( ( 4, 4 ),
 ( 2, 2 ),
 ( 0.000000000000000000, 1.000000000000000000 ),
 ( 0.000000000000000000, 1.000000000000000000 ),
 .UNSPECIFIED. ) 
 GEOMETRIC_REPRESENTATION_ITEM ( )  RATIONAL_B_SPLINE_SURFACE ( (
 ( 1.000000000000000000, 1.000000000000000000),
 ( 0.9729067724841187204, 0.9999501103223794596),
 ( 0.9729067724841187204, 0.9999501103223794596),
 ( 1.000000000000000000, 1.000000000000000000) ) ) 
 REPRESENTATION_ITEM ( '' )  SURFACE ( )  );
#17387=CARTESIAN_POINT ( 'NONE',  ( 1.000433927950263424, 40.58958440049706695, 10.43572306300663044 ) ) ;
#17392=CARTESIAN_POINT ( 'NONE',  ( 5.838029081930955932, 38.95312035650144367, -26.71552867986767055 ) ) ;
#17393=CARTESIAN_POINT ( 'NONE',  ( 5.838029081930955932, 42.16639215765273008, -21.28521624414380042 ) ) ;
#17397=CARTESIAN_POINT ( 'NONE',  ( 1.157644175074338477, -18.38970001308658908, 37.66724318168060393 ) ) ;
#17401=CARTESIAN_POINT ( 'NONE',  ( 4.291220156522059348, 29.64992983783139380, -36.60970715421488109 ) ) ;
#17402=CARTESIAN_POINT ( 'NONE',  ( 5.917102823773431552, 19.70720580609859240, 4.014443593801784615 ) ) ;
#17407=EDGE_CURVE ( 'NONE', #47199, #40254, #4228, .T. ) ;
#17409=CARTESIAN_POINT ( 'NONE',  ( 2.618530812446115519, 43.80811722902085847, 17.04627977145057827 ) ) ;
#17411=EDGE_LOOP ( 'NONE', ( #42146, #21528, #37285, #39968 ) ) ;
#17415=EDGE_CURVE ( 'NONE', #6162, #23761, #38201, .T. ) ;
#17416=ORIENTED_EDGE ( 'NONE', *, *, #61071, .F. ) ;
#17422=VERTEX_POINT ( 'NONE', #8736 ) ;
#17425=CARTESIAN_POINT ( 'NONE',  ( 0.9775691876210976794, 33.12264418954459444, -25.67536077415113382 ) ) ;
#17427=ADVANCED_FACE ( 'NONE', ( #37272 ), #20060, .F. ) ;
#17431=B_SPLINE_CURVE_WITH_KNOTS ( 'NONE', 3,
 ( #48337, #24523, #5398, #14836 ),
 .UNSPECIFIED., .F., .F.,
 ( 4, 4 ),
 ( 0.000000000000000000, 0.004042984057420971090 ),
 .UNSPECIFIED. ) ;
#17439=CARTESIAN_POINT ( 'NONE',  ( 0.8554163680231816613, 21.74163052365391025, -41.57531689939042252 ) ) ;
#17440=FACE_OUTER_BOUND ( 'NONE', #54773, .T. ) ;
#17444=ORIENTED_EDGE ( 'NONE', *, *, #40976, .F. ) ;
#17445=CARTESIAN_POINT ( 'NONE',  ( 1.231276596079887264, -27.70544295162332560, -31.45926257674220494 ) ) ;
#17458=CARTESIAN_POINT ( 'NONE',  ( 0.8560838555295223751, 45.47430759461099115, 11.50913475776684791 ) ) ;
#17459=CARTESIAN_POINT ( 'NONE',  ( 0.5804410086790514622, 43.38796872094602719, 17.80460676694676536 ) ) ;
#17462=VERTEX_POINT ( 'NONE', #33806 ) ;
#17467=CARTESIAN_POINT ( 'NONE',  ( 5.910764540655177868, -19.93482381198526454, 2.665340138569279205 ) ) ;
#17469=ORIENTED_EDGE ( 'NONE', *, *, #57312, .T. ) ;
#17476=CARTESIAN_POINT ( 'NONE',  ( 5.838029081930957709, -40.63013578422388150, 24.08852681897441528 ) ) ;
#17477=CARTESIAN_POINT ( 'NONE',  ( 5.895596859100789899, -17.30333226730986240, 10.25294473112777105 ) ) ;
#17482=CARTESIAN_POINT ( 'NONE',  ( 0.5832655196449142432, 10.64987127965799374, 45.67072831365889840 ) ) ;
#17484=B_SPLINE_CURVE_WITH_KNOTS ( 'NONE', 3,
 ( #39077, #34358, #4889, #14029, #58130, #56903 ),
 .UNSPECIFIED., .F., .F.,
 ( 4, 2, 4 ),
 ( 4.770489558936219510E-18, 0.0002291472222819935318, 0.0004582944445639822932 ),
 .UNSPECIFIED. ) ;
#17490=VECTOR ( 'NONE', #40628, 1000.000000000000000 ) ;
#17491=CARTESIAN_POINT ( 'NONE',  ( 4.956445790443988031, 0.000000000000000000, 0.000000000000000000 ) ) ;
#17493=CARTESIAN_POINT ( 'NONE',  ( 2.528100132419514257, -40.87987497285956806, 9.544087218558223285 ) ) ;
#17497=CARTESIAN_POINT ( 'NONE',  ( 4.956445790443495092, 1.033212179477288384, -47.07940656732829865 ) ) ;
#17499=( BOUNDED_SURFACE ( )  B_SPLINE_SURFACE ( 3, 1, ( 
 ( #23571, #61760 ),
 ( #46475, #47386 ),
 ( #18273, #32996 ),
 ( #8859, #3521 ) ),
 .UNSPECIFIED., .F., .F., .F. ) 
 B_SPLINE_SURFACE_WITH_KNOTS ( ( 4, 4 ),
 ( 2, 2 ),
 ( 0.000000000000000000, 1.000000000000000000 ),
 ( 0.000000000000000000, 1.000000000000000000 ),
 .UNSPECIFIED. ) 
 GEOMETRIC_REPRESENTATION_ITEM ( )  RATIONAL_B_SPLINE_SURFACE ( (
 ( 1.000000000000000000, 1.000000000000000000),
 ( 0.7282232189291694135, 0.9929344683865672927),
 ( 0.7282232189291694135, 0.9929344683865672927),
 ( 1.000000000000000000, 1.000000000000000000) ) ) 
 REPRESENTATION_ITEM ( '' )  SURFACE ( )  );
#17500=EDGE_LOOP ( 'NONE', ( #34785, #53259, #35351, #9191 ) ) ;
#17503=CARTESIAN_POINT ( 'NONE',  ( 5.917102823773431552, -11.93691330175288989, -16.18640846136587896 ) ) ;
#17506=DIRECTION ( 'NONE',  ( 0.07906939808003034253, -0.4719801263061979002, -0.8780562571152528140 ) ) ;
#17510=CIRCLE ( 'NONE', #35544, 47.09074272231896430 ) ;
#17511=CARTESIAN_POINT ( 'NONE',  ( 0.6064782688330897509, 37.24103942229884012, -28.50332312495426734 ) ) ;
#17518=CARTESIAN_POINT ( 'NONE',  ( 1.000110580585053643, 35.71937538688245439, 21.92130709476230876 ) ) ;
#17520=ORIENTED_EDGE ( 'NONE', *, *, #39480, .F. ) ;
#17525=ORIENTED_EDGE ( 'NONE', *, *, #60788, .F. ) ;
#17527=CARTESIAN_POINT ( 'NONE',  ( 5.896782393890504181, -15.78060201202815094, -12.46991126736615385 ) ) ;
#17529=DIRECTION ( 'NONE',  ( -0.07906939808003035641, -0.4122784474075915084, 0.9076202466287580650 ) ) ;
#17535=EDGE_CURVE ( 'NONE', #15999, #9808, #49728, .T. ) ;
#17536=CARTESIAN_POINT ( 'NONE',  ( 0.9780106845699469975, -17.92479137380018273, 37.88183074590216393 ) ) ;
#17537=CARTESIAN_POINT ( 'NONE',  ( 0.5806925824938494740, -34.41156632303759011, 31.86010774524702072 ) ) ;
#17541=EDGE_LOOP ( 'NONE', ( #17594, #15598, #59008, #50425 ) ) ;
#17543=CARTESIAN_POINT ( 'NONE',  ( 4.962356264823593044, 27.50309822711036034, 31.85616401534038644 ) ) ;
#17551=CARTESIAN_POINT ( 'NONE',  ( 1.231276596079881047, -37.78837162824498819, 18.14705873423338289 ) ) ;
#17553=ADVANCED_FACE ( 'NONE', ( #20017 ), #22060, .F. ) ;
#17555=CARTESIAN_POINT ( 'NONE',  ( 0.8560838555295223751, -44.00447048317975174, 16.24744323198866169 ) ) ;
#17568=CARTESIAN_POINT ( 'NONE',  ( 0.6064515330803547100, 32.08788281977977164, -34.20090806076890289 ) ) ;
#17569=CARTESIAN_POINT ( 'NONE',  ( 0.7764139734771289270, -38.15852734697478610, -27.27576326369334581 ) ) ;
#17570=LINE ( 'NONE', #51989, #34137 ) ;
#17571=FACE_OUTER_BOUND ( 'NONE', #29357, .T. ) ;
#17582=CARTESIAN_POINT ( 'NONE',  ( 0.9791128995231621612, -41.81543299240070155, -2.794100553704363055 ) ) ;
#17587=CARTESIAN_POINT ( 'NONE',  ( 5.896782393890504181, -18.51439742298342139, 7.857682542699045314 ) ) ;
#17594=ORIENTED_EDGE ( 'NONE', *, *, #28272, .F. ) ;
#17598=B_SPLINE_CURVE_WITH_KNOTS ( 'NONE', 3,
 ( #1318, #34875, #1022, #53943 ),
 .UNSPECIFIED., .F., .F.,
 ( 4, 4 ),
 ( 0.000000000000000000, 0.004447772540403845815 ),
 .UNSPECIFIED. ) ;
#17603=CARTESIAN_POINT ( 'NONE',  ( 5.910764540655178756, 20.06833201846864512, 1.327888724882238414 ) ) ;
#17618=CARTESIAN_POINT ( 'NONE',  ( 0.5834584762367764910, -1.385012569902221991, -46.87555577477881741 ) ) ;
#17623=CARTESIAN_POINT ( 'NONE',  ( 4.962356264823608143, 12.05238263218917716, 40.32338863178108568 ) ) ;
#17625=CARTESIAN_POINT ( 'NONE',  ( 0.6845945791218034371, 46.90049452736489854, 0.8661026512829932411 ) ) ;
#17627=AXIS2_PLACEMENT_3D ( 'NONE', #52137, #47454, #9228 ) ;
#17628=CARTESIAN_POINT ( 'NONE',  ( 4.956445790444002242, -43.14021684453514638, 18.88014143872134554 ) ) ;
#17634=CARTESIAN_POINT ( 'NONE',  ( 0.9790320750461898314, 32.83655567964974864, 26.04030997587112850 ) ) ;
#17636=CARTESIAN_POINT ( 'NONE',  ( 5.896278296736517710, -18.51903684540627282, 7.846798960905577935 ) ) ;
#17641=CARTESIAN_POINT ( 'NONE',  ( 0.8560838555295223751, -14.76796170096679894, -44.52280473286144513 ) ) ;
#17644=ORIENTED_EDGE ( 'NONE', *, *, #2633, .T. ) ;
#17651=ORIENTED_EDGE ( 'NONE', *, *, #38375, .F. ) ;
#17654=ORIENTED_EDGE ( 'NONE', *, *, #25784, .F. ) ;
#17657=CARTESIAN_POINT ( 'NONE',  ( 0.9762797500689124330, -37.62962005162918899, 18.44821075214967721 ) ) ;
#17665=CARTESIAN_POINT ( 'NONE',  ( 2.282816707992309624, -41.31566379231499297, 22.34978505060748333 ) ) ;
#17667=CARTESIAN_POINT ( 'NONE',  ( 0.8560838555295158248, -45.77741231505087427, -10.23725333375899105 ) ) ;
#17672=EDGE_LOOP ( 'NONE', ( #45157, #1171, #45256, #58887 ) ) ;
#17687=CARTESIAN_POINT ( 'NONE',  ( 1.092182651088184242, -34.99132997457212468, -23.07310146150473074 ) ) ;
#17689=CARTESIAN_POINT ( 'NONE',  ( 5.896278296736517710, 12.98960347168532259, -15.35568888922813180 ) ) ;
#17694=LINE ( 'NONE', #49967, #58863 ) ;
#17695=EDGE_CURVE ( 'NONE', #35106, #56156, #45328, .T. ) ;
#17699=CARTESIAN_POINT ( 'NONE',  ( 0.5837800005270559200, -46.79127812546623488, 3.132339385674594467 ) ) ;
#17700=CARTESIAN_POINT ( 'NONE',  ( 2.528100132419516477, -23.59890196031982157, -34.71808757548846103 ) ) ;
#17721=CARTESIAN_POINT ( 'NONE',  ( 2.282803330402969344, -18.57323392456551758, -43.14547356375118170 ) ) ;
#17722=CARTESIAN_POINT ( 'NONE',  ( 5.901463166500145796, -18.51103891486766173, -7.865068889265479868 ) ) ;
#17723=ORIENTED_EDGE ( 'NONE', *, *, #45861, .F. ) ;
#17726=CARTESIAN_POINT ( 'NONE',  ( 0.5837157313716023754, -7.889940358524325958, 46.22754487014157121 ) ) ;
#17730=CARTESIAN_POINT ( 'NONE',  ( 3.238018933889920792, 12.43622092696273107, 4.974726266180598877 ) ) ;
#17740=FACE_OUTER_BOUND ( 'NONE', #7629, .T. ) ;
#17743=VERTEX_POINT ( 'NONE', #5705 ) ;
#17755=EDGE_LOOP ( 'NONE', ( #36945, #59876, #15538, #41636 ) ) ;
#17757=CARTESIAN_POINT ( 'NONE',  ( 3.376099380956842921, -7.596917057716699340, -11.04514530688664564 ) ) ;
#17758=EDGE_LOOP ( 'NONE', ( #16068, #59430, #5722, #11868 ) ) ;
#17759=CARTESIAN_POINT ( 'NONE',  ( 3.661933894777891663, 18.64962327763467798, -43.18359314084413114 ) ) ;
#17763=ORIENTED_EDGE ( 'NONE', *, *, #39263, .T. ) ;
#17767=B_SPLINE_CURVE_WITH_KNOTS ( 'NONE', 3,
 ( #5946, #58576, #43293, #38287, #52347, #9437, #19476, #28539, #47664, #328, #4710, #30, #57337, #14777, #14471, #33578, #38593, #13087, #16013 ),
 .UNSPECIFIED., .F., .F.,
 ( 4, 3, 3, 3, 3, 3, 4 ),
 ( 9.813676791237319219E-18, 0.0002732106629380678530, 0.0004098138914053834551, 0.0005464171197651561222, 0.0006830203481512647648, 0.0008196235766963767518, 0.001011968216111142462 ),
 .UNSPECIFIED. ) ;
#17769=ORIENTED_EDGE ( 'NONE', *, *, #48499, .F. ) ;
#17774=CARTESIAN_POINT ( 'NONE',  ( 0.5824936645240085253, -42.01860904020938392, 20.82485710314341532 ) ) ;
#17776=ORIENTED_EDGE ( 'NONE', *, *, #51022, .T. ) ;
#17781=VERTEX_POINT ( 'NONE', #43993 ) ;
#17788=CARTESIAN_POINT ( 'NONE',  ( 0.6845945791218034371, 3.832784513612765842, 46.75164471530551680 ) ) ;
#17791=CARTESIAN_POINT ( 'NONE',  ( 1.231276596079887931, -37.78837162824473950, -18.14705873423390869 ) ) ;
#17807=CARTESIAN_POINT ( 'NONE',  ( 0.5835871038041856584, 46.45916567184898582, 6.385951610933906508 ) ) ;
#17809=ORIENTED_EDGE ( 'NONE', *, *, #14810, .F. ) ;
#17818=EDGE_CURVE ( 'NONE', #29994, #54358, #47528, .T. ) ;
#17823=VECTOR ( 'NONE', #24405, 999.9999999999998863 ) ;
#17824=VERTEX_POINT ( 'NONE', #48964 ) ;
#17836=ORIENTED_EDGE ( 'NONE', *, *, #61432, .T. ) ;
#17837=B_SPLINE_CURVE_WITH_KNOTS ( 'NONE', 3,
 ( #55838, #32058, #51137, #24179, #61446, #5051 ),
 .UNSPECIFIED., .F., .F.,
 ( 4, 2, 4 ),
 ( 1.228596259724018017E-16, 0.0002448718616795936384, 0.0004897437233590644368 ),
 .UNSPECIFIED. ) ;
#17840=ORIENTED_EDGE ( 'NONE', *, *, #10963, .T. ) ;
#17848=ORIENTED_EDGE ( 'NONE', *, *, #31768, .F. ) ;
#17850=EDGE_CURVE ( 'NONE', #36503, #8614, #1902, .T. ) ;
#17861=CARTESIAN_POINT ( 'NONE',  ( 0.5804410086790514622, 5.237717535875084707, 46.60564522533493204 ) ) ;
#17868=CARTESIAN_POINT ( 'NONE',  ( 0.5832655196449141322, -41.75240550830532982, -21.35349660461640298 ) ) ;
#17870=( LENGTH_UNIT ( ) NAMED_UNIT ( * ) SI_UNIT ( .MILLI., .METRE. ) );
#17873=( BOUNDED_SURFACE ( )  B_SPLINE_SURFACE ( 3, 1, ( 
 ( #21887, #41024 ),
 ( #60085, #50376 ),
 ( #60686, #7442 ),
 ( #27496, #17188 ) ),
 .UNSPECIFIED., .F., .F., .F. ) 
 B_SPLINE_SURFACE_WITH_KNOTS ( ( 4, 4 ),
 ( 2, 2 ),
 ( 0.000000000000000000, 1.000000000000000000 ),
 ( 0.000000000000000000, 1.000000000000000000 ),
 .UNSPECIFIED. ) 
 GEOMETRIC_REPRESENTATION_ITEM ( )  RATIONAL_B_SPLINE_SURFACE ( (
 ( 1.000000000000000000, 1.000000000000000000),
 ( 0.9729067724841187204, 0.9999501103223794596),
 ( 0.9729067724841187204, 0.9999501103223794596),
 ( 1.000000000000000000, 1.000000000000000000) ) ) 
 REPRESENTATION_ITEM ( '' )  SURFACE ( )  );
#17875=CARTESIAN_POINT ( 'NONE',  ( 1.092182651088185352, 41.63662333493258672, 4.811733752737049841 ) ) ;
#17884=CARTESIAN_POINT ( 'NONE',  ( 0.5824936645240096356, 22.85612023312696905, -40.94918737812936627 ) ) ;
#17897=CARTESIAN_POINT ( 'NONE',  ( 4.960386119450145515, -30.75418163181142361, -31.12260877288235861 ) ) ;
#17898=CARTESIAN_POINT ( 'NONE',  ( 0.9784957157296372277, -41.82994298070580896, -2.566890574853715190 ) ) ;
#17900=ADVANCED_FACE ( 'NONE', ( #26081 ), #47673, .F. ) ;
#17901=B_SPLINE_CURVE_WITH_KNOTS ( 'NONE', 3,
 ( #21962, #18186, #37300, #36689, #37613, #60761 ),
 .UNSPECIFIED., .F., .F.,
 ( 4, 2, 4 ),
 ( 1.053462964043502403E-17, 0.0002448709889506572109, 0.0004897419779013039050 ),
 .UNSPECIFIED. ) ;
#17904=CARTESIAN_POINT ( 'NONE',  ( 0.5837799406558236148, -45.97443208162771811, -9.251764391131139575 ) ) ;
#17912=CARTESIAN_POINT ( 'NONE',  ( 5.894904586330512508, 8.467339502218957037, -18.24372697164165302 ) ) ;
#17920=ORIENTED_EDGE ( 'NONE', *, *, #35553, .T. ) ;
#17923=CARTESIAN_POINT ( 'NONE',  ( 0.5832655196449149093, -44.22601172460468177, -15.59791876849144465 ) ) ;
#17931=CARTESIAN_POINT ( 'NONE',  ( 2.528190830796657629, -26.16753660177270646, -32.82551087718047000 ) ) ;
#17941=CARTESIAN_POINT ( 'NONE',  ( 0.9762797500689124330, -41.77809974471944088, 3.303810967046753255 ) ) ;
#17950=CARTESIAN_POINT ( 'NONE',  ( 5.910764540655177868, -15.79365219732158465, 12.45238084621580121 ) ) ;
#17952=CARTESIAN_POINT ( 'NONE',  ( 4.956445790444004018, -46.73954499432459642, -5.740468958468717631 ) ) ;
#17954=CARTESIAN_POINT ( 'NONE',  ( 1.000433927950262314, 35.71901661376694648, -21.92191893512719147 ) ) ;
#17956=CARTESIAN_POINT ( 'NONE',  ( 5.895596859100789899, -19.93295055289977213, 2.684337063064242912 ) ) ;
#17968=EDGE_LOOP ( 'NONE', ( #26527, #11749, #13511, #54326 ) ) ;
#17979=CARTESIAN_POINT ( 'NONE',  ( 0.9754292589017203863, 19.62773389896157639, -37.02809107808331390 ) ) ;
#17980=EDGE_CURVE ( 'NONE', #38487, #11037, #46762, .T. ) ;
#17984=CARTESIAN_POINT ( 'NONE',  ( 1.231276596079887264, -2.246340108599748309, -41.85965512441022440 ) ) ;
#17992=ORIENTED_EDGE ( 'NONE', *, *, #55762, .T. ) ;
#17993=ORIENTED_EDGE ( 'NONE', *, *, #29802, .T. ) ;
#17994=CARTESIAN_POINT ( 'NONE',  ( 0.7056759521545006297, 10.05083851003305995, 45.81189228095935562 ) ) ;
#17995=VECTOR ( 'NONE', #38370, 999.9999999999998863 ) ;
#17996=ORIENTED_EDGE ( 'NONE', *, *, #34652, .T. ) ;
#17998=CARTESIAN_POINT ( 'NONE',  ( 2.528100132419516477, 23.91661738292092920, -34.49998828392612893 ) ) ;
#18008=CARTESIAN_POINT ( 'NONE',  ( 5.895596859100789899, 3.348897116308617417, -19.83212220910478507 ) ) ;
#18010=ORIENTED_EDGE ( 'NONE', *, *, #29107, .F. ) ;
#18022=CARTESIAN_POINT ( 'NONE',  ( 0.9790320750461898314, 41.90858792809413558, 0.08596752522955294906 ) ) ;
#18039=ORIENTED_EDGE ( 'NONE', *, *, #16776, .T. ) ;
#18043=DIRECTION ( 'NONE',  ( 0.000000000000000000, 0.000000000000000000, 1.000000000000000000 ) ) ;
#18044=EDGE_CURVE ( 'NONE', #16356, #47431, #34769, .T. ) ;
#18046=CARTESIAN_POINT ( 'NONE',  ( 0.5806925824938499181, 22.05663578530122493, 41.38510819338441138 ) ) ;
#18050=ORIENTED_EDGE ( 'NONE', *, *, #50754, .T. ) ;
#18067=EDGE_CURVE ( 'NONE', #13798, #48102, #58695, .T. ) ;
#18068=VERTEX_POINT ( 'NONE', #5635 ) ;
#18077=CARTESIAN_POINT ( 'NONE',  ( 4.956445790444004018, -46.59545590650535019, -6.811867512257778756 ) ) ;
#18078=B_SPLINE_CURVE_WITH_KNOTS ( 'NONE', 3,
 ( #61207, #59436, #13315, #20932, #37438, #2105, #56509, #13625, #55045, #6798, #16542, #54732, #28021, #11866, #59126, #51811 ),
 .UNSPECIFIED., .F., .F.,
 ( 4, 3, 3, 3, 3, 4 ),
 ( 1.250973872328959318E-17, 0.0002732102107931907043, 0.0004098135523333788777, 0.0005464168938824937212, 0.0008195847345945476720, 0.001092771384553104397 ),
 .UNSPECIFIED. ) ;
#18081=CARTESIAN_POINT ( 'NONE',  ( 0.5782707292762442330, 40.71812376972700775, -23.27596937574910285 ) ) ;
#18083=CARTESIAN_POINT ( 'NONE',  ( 0.5837800005270538106, -41.85555320131619794, 21.15060105182773498 ) ) ;
#18084=ORIENTED_EDGE ( 'NONE', *, *, #2563, .T. ) ;
#18092=CARTESIAN_POINT ( 'NONE',  ( 0.5797568599927147570, -42.13545938030424765, 20.58709235131896520 ) ) ;
#18096=CARTESIAN_POINT ( 'NONE',  ( 0.9791128995231611620, -27.05351454939415490, 32.00694900754963612 ) ) ;
#18108=CARTESIAN_POINT ( 'NONE',  ( 4.962356264823594820, 34.94214251265108118, 23.45809613945535332 ) ) ;
#18112=CARTESIAN_POINT ( 'NONE',  ( 4.958415959904823644, -10.03736369554698271, 44.29960816831176373 ) ) ;
#18125=CARTESIAN_POINT ( 'NONE',  ( 3.238018933889920792, -13.17791601574917770, -2.397920317590707118 ) ) ;
#18132=( BOUNDED_SURFACE ( )  B_SPLINE_SURFACE ( 3, 1, ( 
 ( #36596, #21871 ),
 ( #60671, #50664 ),
 ( #45386, #59444 ),
 ( #7119, #17476 ) ),
 .UNSPECIFIED., .F., .F., .F. ) 
 B_SPLINE_SURFACE_WITH_KNOTS ( ( 4, 4 ),
 ( 2, 2 ),
 ( 0.000000000000000000, 1.000000000000000000 ),
 ( 0.000000000000000000, 1.000000000000000000 ),
 .UNSPECIFIED. ) 
 GEOMETRIC_REPRESENTATION_ITEM ( )  RATIONAL_B_SPLINE_SURFACE ( (
 ( 1.000000000000000000, 1.000000000000000000),
 ( 0.7282232189291694135, 0.9929344683865672927),
 ( 0.7282232189291694135, 0.9929344683865672927),
 ( 1.000000000000000000, 1.000000000000000000) ) ) 
 REPRESENTATION_ITEM ( '' )  SURFACE ( )  );
#18133=CARTESIAN_POINT ( 'NONE',  ( 4.962356264823600149, -40.47344704301802665, 11.53844366967928892 ) ) ;
#18139=CARTESIAN_POINT ( 'NONE',  ( 0.5835871038041854364, -7.665477966243003927, -46.26526667436971252 ) ) ;
#18140=CARTESIAN_POINT ( 'NONE',  ( 5.895596859100789899, 12.98270243688412329, 15.36156309259609642 ) ) ;
#18145=CARTESIAN_POINT ( 'NONE',  ( 0.9787284016396597952, -7.155203276473740992, -41.29332954608010198 ) ) ;
#18146=VERTEX_POINT ( 'NONE', #25389 ) ;
#18150=ORIENTED_EDGE ( 'NONE', *, *, #34117, .F. ) ;
#18154=CARTESIAN_POINT ( 'NONE',  ( 2.282816707992305627, 46.71114623179644809, 4.956388213174406587 ) ) ;
#18156=ORIENTED_EDGE ( 'NONE', *, *, #15164, .T. ) ;
#18163=VECTOR ( 'NONE', #11248, 1000.000000000000114 ) ;
#18169=DIRECTION ( 'NONE',  ( 0.07500201931887538753, -0.8647811570515562263, 0.4965161100172509334 ) ) ;
#18174=CARTESIAN_POINT ( 'NONE',  ( 0.5837800005270582515, -41.85558187593742474, -21.15054430667160545 ) ) ;
#18176=EDGE_CURVE ( 'NONE', #44946, #41577, #27325, .T. ) ;
#18180=CARTESIAN_POINT ( 'NONE',  ( 4.291220156522060236, -17.85566473792967557, 43.59546116366188784 ) ) ;
#18186=CARTESIAN_POINT ( 'NONE',  ( 0.5797568665920713737, -8.419848931671534586, -46.13384281164643141 ) ) ;
#18189=CARTESIAN_POINT ( 'NONE',  ( 4.962356264823608143, 0.000000000000000000, 0.000000000000000000 ) ) ;
#18191=B_SPLINE_CURVE_WITH_KNOTS ( 'NONE', 3,
 ( #30606, #58792, #15916, #12154, #2407, #35033, #49111, #16848, #59108, #6466, #35651, #11850, #6163, #25608, #21529, #26218, #16219, #35340, #54401 ),
 .UNSPECIFIED., .F., .F.,
 ( 4, 3, 3, 3, 3, 3, 4 ),
 ( 9.541595121948225732E-18, 0.0002732106629380579325, 0.0004098138914053724505, 0.0005464171197651436539, 0.0006830203481512533807, 0.0008196235766963599467, 0.001011968216111139643 ),
 .UNSPECIFIED. ) ;
#18195=CARTESIAN_POINT ( 'NONE',  ( 4.956445790444011124, -17.42806872899762993, -43.74700527484106516 ) ) ;
#18197=EDGE_CURVE ( 'NONE', #34712, #38898, #1567, .T. ) ;
#18199=CARTESIAN_POINT ( 'NONE',  ( 0.9775691876211000109, -41.78811875591999581, -3.175978562760820356 ) ) ;
#18206=CARTESIAN_POINT ( 'NONE',  ( 0.5837800304671223461, -45.94722522548352828, -9.385618054139468924 ) ) ;
#18214=ORIENTED_EDGE ( 'NONE', *, *, #27942, .F. ) ;
#18216=EDGE_CURVE ( 'NONE', #39044, #47897, #4717, .T. ) ;
#18219=CARTESIAN_POINT ( 'NONE',  ( 4.962356264823608143, 42.01891079680549268, -2.376285612557975213 ) ) ;
#18230=CARTESIAN_POINT ( 'NONE',  ( 4.962356264823603702, -4.645793755590432283, -41.82884409403234116 ) ) ;
#18231=DIRECTION ( 'NONE',  ( 0.000000000000000000, 0.000000000000000000, 1.000000000000000000 ) ) ;
#18232=VERTEX_POINT ( 'NONE', #7187 ) ;
#18234=EDGE_LOOP ( 'NONE', ( #38462, #36088, #61051, #1841 ) ) ;
#18235=CARTESIAN_POINT ( 'NONE',  ( 4.962356264823602814, -25.31392337492848554, -33.62202970123303203 ) ) ;
#18236=CARTESIAN_POINT ( 'NONE',  ( 0.5817217712918340000, 11.31382783192066199, -45.51079271775027024 ) ) ;
#18241=CARTESIAN_POINT ( 'NONE',  ( 0.5832655196449136881, -1.339497008067653150, -46.87686989058363451 ) ) ;
#18245=EDGE_CURVE ( 'NONE', #22599, #29776, #54929, .T. ) ;
#18247=CARTESIAN_POINT ( 'NONE',  ( 0.6845945791218023269, 45.00526092843262660, -13.22622430921391690 ) ) ;
#18249=EDGE_CURVE ( 'NONE', #47523, #48721, #4892, .T. ) ;
#18254=EDGE_CURVE ( 'NONE', #26937, #5500, #32265, .T. ) ;
#18256=CARTESIAN_POINT ( 'NONE',  ( 0.5806925824938499181, 40.62497527030964051, -23.42720099863178973 ) ) ;
#18266=CARTESIAN_POINT ( 'NONE',  ( 0.5835226383429291674, 45.18136229812504467, -12.56530840972593133 ) ) ;
#18271=FACE_OUTER_BOUND ( 'NONE', #7578, .T. ) ;
#18273=CARTESIAN_POINT ( 'NONE',  ( 5.910764540655178756, -2.028561139976813976, -20.00965212517547087 ) ) ;
#18279=EDGE_CURVE ( 'NONE', #4396, #49329, #21939, .T. ) ;
#18292=ADVANCED_FACE ( 'NONE', ( #41372 ), #831, .F. ) ;
#18304=CARTESIAN_POINT ( 'NONE',  ( 0.6064782688330874194, -8.500301393622592627, 46.12027019257743632 ) ) ;
#18307=CARTESIAN_POINT ( 'NONE',  ( 0.5837157313716027085, -38.71448089223815003, 26.46556314962047907 ) ) ;
#18310=CARTESIAN_POINT ( 'NONE',  ( 0.5797568599927134247, 16.26612221817008930, 43.98452655939994571 ) ) ;
#18314=VERTEX_POINT ( 'NONE', #46075 ) ;
#18315=CARTESIAN_POINT ( 'NONE',  ( 1.091591847532197734, -21.89140366521357350, -35.74248783342470404 ) ) ;
#18334=CARTESIAN_POINT ( 'NONE',  ( 0.9789233960466705575, -1.268941605393027805, -41.88945588133657338 ) ) ;
#18357=CARTESIAN_POINT ( 'NONE',  ( 0.5806925824938502512, 23.01490136172913026, 40.85996423950273737 ) ) ;
#18361=ORIENTED_EDGE ( 'NONE', *, *, #23229, .F. ) ;
#18368=CARTESIAN_POINT ( 'NONE',  ( 0.5804410086790514622, 42.96136033320073011, -18.81067170986419157 ) ) ;
#18383=ORIENTED_EDGE ( 'NONE', *, *, #42592, .T. ) ;
#18385=VERTEX_POINT ( 'NONE', #13787 ) ;
#18387=CARTESIAN_POINT ( 'NONE',  ( 0.5830082357119567016, 27.59734378305546798, 37.91594191178936768 ) ) ;
#18391=CARTESIAN_POINT ( 'NONE',  ( 2.618530812446111078, -2.977833924574445401, 46.91331681213611660 ) ) ;
#18392=CARTESIAN_POINT ( 'NONE',  ( 0.5837157313716014873, -41.89656481236102792, 21.06928856192482158 ) ) ;
#18398=LINE ( 'NONE', #36279, #51176 ) ;
#18401=VERTEX_POINT ( 'NONE', #574 ) ;
#18403=CARTESIAN_POINT ( 'NONE',  ( 0.6064782688330866423, -42.17225498498755343, 20.51427200511784577 ) ) ;
#18404=EDGE_CURVE ( 'NONE', #17462, #15825, #25102, .T. ) ;
#18408=CARTESIAN_POINT ( 'NONE',  ( 5.895596859100789899, 10.82540956478658423, 16.95106754653271608 ) ) ;
#18409=CARTESIAN_POINT ( 'NONE',  ( 0.9780303403264778428, -26.80931777084100887, 32.21180054044096863 ) ) ;
#18411=CARTESIAN_POINT ( 'NONE',  ( 0.5797568599927138688, -7.179075611191181316, -46.34313522022226550 ) ) ;
#18423=CARTESIAN_POINT ( 'NONE',  ( 1.231276596079881047, -16.87422718933157739, -38.37365278131454005 ) ) ;
#18424=FACE_OUTER_BOUND ( 'NONE', #56301, .T. ) ;
#18434=CARTESIAN_POINT ( 'NONE',  ( 0.6845945791218034371, 45.00526092843242054, 13.22622430921456349 ) ) ;
#18441=ORIENTED_EDGE ( 'NONE', *, *, #17415, .F. ) ;
#18442=CARTESIAN_POINT ( 'NONE',  ( 3.782542959838398389, -29.99487845573544931, -29.45411889400579142 ) ) ;
#18444=ORIENTED_EDGE ( 'NONE', *, *, #45080, .F. ) ;
#18445=CARTESIAN_POINT ( 'NONE',  ( 0.5817216825391123836, -8.248784698831615358, -46.16484055208877635 ) ) ;
#18451=DIRECTION ( 'NONE',  ( 0.07906939808003035641, -0.7773121955653229387, -0.6241264142084348432 ) ) ;
#18452=ORIENTED_EDGE ( 'NONE', *, *, #53573, .T. ) ;
#18457=CARTESIAN_POINT ( 'NONE',  ( 3.782625744892854414, 41.39849240246781648, -7.307730899384353940 ) ) ;
#18459=CARTESIAN_POINT ( 'NONE',  ( 0.8554163680231738898, -30.98316862405949124, 35.23136010892731207 ) ) ;
#18462=EDGE_LOOP ( 'NONE', ( #55432, #2946, #18444, #35383 ) ) ;
#18466=CARTESIAN_POINT ( 'NONE',  ( 4.956445790443495092, 1.033212179477288384, -47.07940656732829865 ) ) ;
#18476=CARTESIAN_POINT ( 'NONE',  ( 0.5835871038041861025, -41.79378696274027050, -21.27237232220663543 ) ) ;
#18482=LINE ( 'NONE', #42309, #26609 ) ;
#18483=( BOUNDED_SURFACE ( )  B_SPLINE_SURFACE ( 3, 1, ( 
 ( #24557, #38987 ),
 ( #18953, #107 ),
 ( #19255, #57420 ),
 ( #48664, #33661 ) ),
 .UNSPECIFIED., .F., .F., .F. ) 
 B_SPLINE_SURFACE_WITH_KNOTS ( ( 4, 4 ),
 ( 2, 2 ),
 ( 0.000000000000000000, 1.000000000000000000 ),
 ( 0.000000000000000000, 1.000000000000000000 ),
 .UNSPECIFIED. ) 
 GEOMETRIC_REPRESENTATION_ITEM ( )  RATIONAL_B_SPLINE_SURFACE ( (
 ( 1.000000000000000000, 1.000000000000000000),
 ( 0.9952954269826590483, 0.8620686068821339365),
 ( 0.9952954269826590483, 0.8620686068821339365),
 ( 1.000000000000000000, 1.000000000000000000) ) ) 
 REPRESENTATION_ITEM ( '' )  SURFACE ( )  );
#18484=CARTESIAN_POINT ( 'NONE',  ( 2.282803330402962683, -9.105509439560925955, 46.08238931851357023 ) ) ;
#18487=CARTESIAN_POINT ( 'NONE',  ( 0.9790320750461898314, 29.07273748896853860, 30.18464953316030730 ) ) ;
#18494=DIRECTION ( 'NONE',  ( 0.000000000000000000, 0.000000000000000000, 1.000000000000000000 ) ) ;
#18498=CARTESIAN_POINT ( 'NONE',  ( 0.9783242366443545279, 19.90500434199885760, 36.87987652299737107 ) ) ;
#18513=CONICAL_SURFACE ( 'NONE', #60474, 42.08604991992415023, 1.569615340895231137 ) ;
#18525=CARTESIAN_POINT ( 'NONE',  ( 4.958415959904818315, 45.28449214630087738, -3.538181012081164312 ) ) ;
#18529=EDGE_LOOP ( 'NONE', ( #1193, #18985, #45824, #14989 ) ) ;
#18532=CARTESIAN_POINT ( 'NONE',  ( 0.5837799406558225046, 43.13924169579550494, -18.39155717955778968 ) ) ;
#18537=CARTESIAN_POINT ( 'NONE',  ( 0.8554163680231708922, 39.89400665120431455, 24.69157156653835372 ) ) ;
#18540=CARTESIAN_POINT ( 'NONE',  ( 0.5837800005270554760, -1.567060691030147446, -46.86981522720579107 ) ) ;
#18544=CARTESIAN_POINT ( 'NONE',  ( 0.9790724872846771065, -41.81774720698464876, 2.758845503862258575 ) ) ;
#18562=CARTESIAN_POINT ( 'NONE',  ( 3.782542959838397056, 37.99691774666566602, 17.98532999835400759 ) ) ;
#18568=CARTESIAN_POINT ( 'NONE',  ( 0.5824936645240085253, 45.32464743504566229, -12.03804443957227477 ) ) ;
#18576=ORIENTED_EDGE ( 'NONE', *, *, #56371, .F. ) ;
#18578=CARTESIAN_POINT ( 'NONE',  ( 0.8560838555295223751, 17.70877843982779609, 43.43698884880053157 ) ) ;
#18580=( BOUNDED_SURFACE ( )  B_SPLINE_SURFACE ( 3, 1, ( 
 ( #43136, #5181 ),
 ( #8982, #47511 ),
 ( #58116, #43767 ),
 ( #43446, #19947 ) ),
 .UNSPECIFIED., .F., .F., .F. ) 
 B_SPLINE_SURFACE_WITH_KNOTS ( ( 4, 4 ),
 ( 2, 2 ),
 ( 0.000000000000000000, 1.000000000000000000 ),
 ( 0.000000000000000000, 1.000000000000000000 ),
 .UNSPECIFIED. ) 
 GEOMETRIC_REPRESENTATION_ITEM ( )  RATIONAL_B_SPLINE_SURFACE ( (
 ( 1.000000000000000000, 1.000000000000000000),
 ( 0.9729067724841187204, 0.9999501103223794596),
 ( 0.9729067724841187204, 0.9999501103223794596),
 ( 1.000000000000000000, 1.000000000000000000) ) ) 
 REPRESENTATION_ITEM ( '' )  SURFACE ( )  );
#18584=DIRECTION ( 'NONE',  ( 0.000000000000000000, 0.000000000000000000, 1.000000000000000000 ) ) ;
#18594=CARTESIAN_POINT ( 'NONE',  ( 5.901463166500146684, -4.676581321913868550, -19.56137667650625289 ) ) ;
#18599=CARTESIAN_POINT ( 'NONE',  ( 0.9789233960466710016, -39.63276750765551526, 13.62279217034692991 ) ) ;
#18606=CARTESIAN_POINT ( 'NONE',  ( 0.7056759521544981872, -8.631168086166848497, 46.10045299761512894 ) ) ;
#18611=ORIENTED_EDGE ( 'NONE', *, *, #56371, .T. ) ;
#18612=CARTESIAN_POINT ( 'NONE',  ( 0.8560838555295158248, 16.00311602465144745, 44.09391240957503300 ) ) ;
#18614=CARTESIAN_POINT ( 'NONE',  ( 5.917102823773431552, 18.99629506471987384, 6.605338134103467596 ) ) ;
#18617=CARTESIAN_POINT ( 'NONE',  ( 0.5848930533535030563, -7.979791871080650800, 46.21250917318592855 ) ) ;
#18621=AXIS2_PLACEMENT_3D ( 'NONE', #13178, #51051, #60441 ) ;
#18622=ORIENTED_EDGE ( 'NONE', *, *, #22993, .T. ) ;
#18623=VERTEX_POINT ( 'NONE', #3342 ) ;
#18627=CARTESIAN_POINT ( 'NONE',  ( 0.8560838555295223751, -30.97734773434455491, -35.22466126774295248 ) ) ;
#18635=CARTESIAN_POINT ( 'NONE',  ( 5.901463166500145796, 3.359582080289229111, -19.83005493150324128 ) ) ;
#18639=CARTESIAN_POINT ( 'NONE',  ( 0.6064515330803588178, -46.73949274313381608, 3.841113660336747060 ) ) ;
#18657=VECTOR ( 'NONE', #57718, 1000.000000000000114 ) ;
#18660=CARTESIAN_POINT ( 'NONE',  ( 0.5837799406558225046, 22.61724361227189917, 41.08167281112525870 ) ) ;
#18661=CARTESIAN_POINT ( 'NONE',  ( 0.8560838555295158248, 3.785103201470073397, 46.75516899590838449 ) ) ;
#18665=VERTEX_POINT ( 'NONE', #9925 ) ;
#18666=CARTESIAN_POINT ( 'NONE',  ( 0.9772918015221170318, 24.52412876038616574, -33.98387800552902860 ) ) ;
#18669=CARTESIAN_POINT ( 'NONE',  ( 0.5817216825391117174, 46.89379108365920956, -0.4553130896244175219 ) ) ;
#18693=ORIENTED_EDGE ( 'NONE', *, *, #39177, .F. ) ;
#18695=LINE ( 'NONE', #61575, #31438 ) ;
#18699=CONICAL_SURFACE ( 'NONE', #10695, 42.08604991992415023, 1.569615340895231137 ) ;
#18700=CARTESIAN_POINT ( 'NONE',  ( 4.291220156522059348, -3.725477031303138453, 46.96285572870254299 ) ) ;
#18710=CARTESIAN_POINT ( 'NONE',  ( 0.9780303403264766215, 41.57669851679587936, 5.264765316568995601 ) ) ;
#18712=VERTEX_POINT ( 'NONE', #19637 ) ;
#18718=EDGE_CURVE ( 'NONE', #59625, #47413, #50390, .T. ) ;
#18719=CARTESIAN_POINT ( 'NONE',  ( 0.6064782688330866423, -7.098623077535437531, -46.35670390377050154 ) ) ;
#18724=CARTESIAN_POINT ( 'NONE',  ( 4.962356264823599261, -28.94323483023637777, 30.55363735178087126 ) ) ;
#18729=ORIENTED_EDGE ( 'NONE', *, *, #330, .F. ) ;
#18730=CARTESIAN_POINT ( 'NONE',  ( 4.962356264823608143, 0.000000000000000000, 0.000000000000000000 ) ) ;
#18737=B_SPLINE_CURVE_WITH_KNOTS ( 'NONE', 3,
 ( #40783, #31660, #26643, #37931, #61371, #32910, #41698, #13182, #33215, #32593, #18487, #52286, #3434, #4045, #37611, #56678, #13803, #51987, #9078 ),
 .UNSPECIFIED., .F., .F.,
 ( 4, 3, 3, 3, 3, 3, 4 ),
 ( 1.250973872328959318E-17, 0.0002732106629380557099, 0.0004098138914053726673, 0.0005464171197651425697, 0.0006830203481512468755, 0.0008196235766963536583, 0.001011968216111134222 ),
 .UNSPECIFIED. ) ;
#18740=( GEOMETRIC_REPRESENTATION_CONTEXT ( 3 ) GLOBAL_UNCERTAINTY_ASSIGNED_CONTEXT ( ( #33001 ) ) GLOBAL_UNIT_ASSIGNED_CONTEXT ( ( #8438, #61362, #56362 ) ) REPRESENTATION_CONTEXT ( 'NONE', 'WORKASPACE' ) );
#18741=CONICAL_SURFACE ( 'NONE', #5723, 42.08604991992415023, 1.569615340895231137 ) ;
#18749=CARTESIAN_POINT ( 'NONE',  ( 0.5834584762367747146, 43.10339065662142843, 18.47521861618612604 ) ) ;
#18769=CARTESIAN_POINT ( 'NONE',  ( 4.956445790444004018, -43.56224489968086999, -17.88487823385623443 ) ) ;
#18772=VERTEX_POINT ( 'NONE', #25856 ) ;
#18779=CARTESIAN_POINT ( 'NONE',  ( 5.894904586330512508, -19.39861238634060925, 5.312555839344692998 ) ) ;
#18782=B_SPLINE_CURVE_WITH_KNOTS ( 'NONE', 3,
 ( #4967, #45846, #60210, #27638, #3812, #43227, #60512, #263, #12946, #19411, #2889, #22023, #31729, #41147, #41767, #32045 ),
 .UNSPECIFIED., .F., .F.,
 ( 4, 3, 3, 3, 3, 4 ),
 ( 1.127622383284612036E-17, 0.0002732102107931897827, 0.0004098135523333829976, 0.0005464168938825005517, 0.0008195847345945430100, 0.001092771384553107216 ),
 .UNSPECIFIED. ) ;
#18783=ORIENTED_EDGE ( 'NONE', *, *, #61234, .T. ) ;
#18784=( BOUNDED_SURFACE ( )  B_SPLINE_SURFACE ( 3, 1, ( 
 ( #6512, #35388 ),
 ( #25655, #44800 ),
 ( #1839, #20966 ),
 ( #40110, #59155 ) ),
 .UNSPECIFIED., .F., .F., .F. ) 
 B_SPLINE_SURFACE_WITH_KNOTS ( ( 4, 4 ),
 ( 2, 2 ),
 ( 0.000000000000000000, 1.000000000000000000 ),
 ( 0.000000000000000000, 1.000000000000000000 ),
 .UNSPECIFIED. ) 
 GEOMETRIC_REPRESENTATION_ITEM ( )  RATIONAL_B_SPLINE_SURFACE ( (
 ( 1.000000000000000000, 1.000000000000000000),
 ( 0.9729067724841187204, 0.9999501103223794596),
 ( 0.9729067724841187204, 0.9999501103223794596),
 ( 1.000000000000000000, 1.000000000000000000) ) ) 
 REPRESENTATION_ITEM ( '' )  SURFACE ( )  );
#18787=CARTESIAN_POINT ( 'NONE',  ( 4.956445790443991584, 29.98832127573247774, 36.30755619981999871 ) ) ;
#18791=ORIENTED_EDGE ( 'NONE', *, *, #41212, .F. ) ;
#18804=CARTESIAN_POINT ( 'NONE',  ( 5.838029081930955932, -16.99499549701727119, 44.07079743105724390 ) ) ;
#18807=CARTESIAN_POINT ( 'NONE',  ( 0.9784957157296355623, -34.41894368623801626, 23.90960837228307412 ) ) ;
#18809=CARTESIAN_POINT ( 'NONE',  ( 0.5830081025819940921, 22.29738496909589074, -41.25601359707673055 ) ) ;
#18813=AXIS2_PLACEMENT_3D ( 'NONE', #48395, #5455, #10493 ) ;
#18821=CARTESIAN_POINT ( 'NONE',  ( 4.958415959904820092, -31.93886907500572647, -32.29725369179680428 ) ) ;
#18822=LINE ( 'NONE', #43253, #30972 ) ;
#18826=CARTESIAN_POINT ( 'NONE',  ( 0.5837800005270561421, -45.95629507620387955, -9.340995745136783768 ) ) ;
#18829=ORIENTED_EDGE ( 'NONE', *, *, #35231, .F. ) ;
#18834=B_SPLINE_CURVE_WITH_KNOTS ( 'NONE', 3,
 ( #59728, #6459, #25603, #16842, #40056, #55021 ),
 .UNSPECIFIED., .F., .F.,
 ( 4, 2, 4 ),
 ( 9.913782460405889843E-18, 0.0002448709889506573193, 0.0004897419779013046639 ),
 .UNSPECIFIED. ) ;
#18843=ORIENTED_EDGE ( 'NONE', *, *, #39656, .T. ) ;
#18848=CARTESIAN_POINT ( 'NONE',  ( 0.8554163680231720024, -46.74230100997663584, 4.045092014349757292 ) ) ;
#18850=CIRCLE ( 'NONE', #58777, 47.09074272231896430 ) ;
#18859=CARTESIAN_POINT ( 'NONE',  ( 0.5824936645240106348, 43.31572343942117698, -17.97181910547413608 ) ) ;
#18862=CARTESIAN_POINT ( 'NONE',  ( 0.5837800005270562531, 10.87140793764657332, -45.61850225615763321 ) ) ;
#18864=CARTESIAN_POINT ( 'NONE',  ( 0.5804410086790514622, 40.07081992599715647, 24.36902218624511818 ) ) ;
#18865=CARTESIAN_POINT ( 'NONE',  ( 4.962356264823601926, -38.57439820587641321, 16.83007429920694875 ) ) ;
#18868=VECTOR ( 'NONE', #29174, 1000.000000000000114 ) ;
#18869=ORIENTED_EDGE ( 'NONE', *, *, #24339, .T. ) ;
#18871=CARTESIAN_POINT ( 'NONE',  ( 1.231276596079881935, -41.76121777166937221, -3.643825084341031584 ) ) ;
#18873=CARTESIAN_POINT ( 'NONE',  ( 0.5806925824938511393, 42.95845041307772050, -18.80940989108128747 ) ) ;
#18884=CARTESIAN_POINT ( 'NONE',  ( 0.5797568599927156452, 33.05098809540313454, -33.26946790359784245 ) ) ;
#18888=B_SPLINE_CURVE_WITH_KNOTS ( 'NONE', 3,
 ( #47493, #791, #52791, #23677, #38731, #48714 ),
 .UNSPECIFIED., .F., .F.,
 ( 4, 2, 4 ),
 ( 9.446879437911127976E-18, 0.0002448709889506566688, 0.0004897419779013039050 ),
 .UNSPECIFIED. ) ;
#18889=( BOUNDED_SURFACE ( )  B_SPLINE_SURFACE ( 3, 1, ( 
 ( #53173, #43821 ),
 ( #58471, #34399 ),
 ( #24996, #9649 ),
 ( #4935, #15600 ) ),
 .UNSPECIFIED., .F., .F., .F. ) 
 B_SPLINE_SURFACE_WITH_KNOTS ( ( 4, 4 ),
 ( 2, 2 ),
 ( 0.000000000000000000, 1.000000000000000000 ),
 ( 0.000000000000000000, 1.000000000000000000 ),
 .UNSPECIFIED. ) 
 GEOMETRIC_REPRESENTATION_ITEM ( )  RATIONAL_B_SPLINE_SURFACE ( (
 ( 1.000000000000000000, 1.000000000000000000),
 ( 0.7282232189291694135, 0.9929344683865672927),
 ( 0.7282232189291694135, 0.9929344683865672927),
 ( 1.000000000000000000, 1.000000000000000000) ) ) 
 REPRESENTATION_ITEM ( '' )  SURFACE ( )  );
#18891=CARTESIAN_POINT ( 'NONE',  ( 0.5830081025819929819, 45.15677286343053254, -12.65297984439984980 ) ) ;
#18895=CARTESIAN_POINT ( 'NONE',  ( 0.5782707292762442330, 43.45719891954342273, -17.64109451748540280 ) ) ;
#18900=CARTESIAN_POINT ( 'NONE',  ( 5.895881250540457863, -15.78739120953167330, -12.46137875218881952 ) ) ;
#18906=VERTEX_POINT ( 'NONE', #22393 ) ;
#18908=CARTESIAN_POINT ( 'NONE',  ( 1.091591847532194626, -41.86498133637820018, 2.020477334826483951 ) ) ;
#18910=ADVANCED_FACE ( 'NONE', ( #40920 ), #57765, .T. ) ;
#18912=LINE ( 'NONE', #31524, #47708 ) ;
#18913=ORIENTED_EDGE ( 'NONE', *, *, #33919, .F. ) ;
#18921=VECTOR ( 'NONE', #25188, 1000.000000000000000 ) ;
#18922=ORIENTED_EDGE ( 'NONE', *, *, #17818, .T. ) ;
#18927=CARTESIAN_POINT ( 'NONE',  ( 3.238018933889920792, -3.704930136113386840, 12.87171259212121299 ) ) ;
#18932=CARTESIAN_POINT ( 'NONE',  ( 4.962356264823608143, 0.000000000000000000, 0.000000000000000000 ) ) ;
#18933=CARTESIAN_POINT ( 'NONE',  ( 0.5830082357119558134, 36.97260366664089304, -28.84889275254475649 ) ) ;
#18936=ORIENTED_EDGE ( 'NONE', *, *, #46935, .T. ) ;
#18938=CARTESIAN_POINT ( 'NONE',  ( 2.528190830796659405, 41.74865909485399129, -4.393586227066999861 ) ) ;
#18953=CARTESIAN_POINT ( 'NONE',  ( 5.895881250540457863, 19.00150250643885386, 6.593222588848265175 ) ) ;
#18961=CARTESIAN_POINT ( 'NONE',  ( 5.896782393890504181, -15.78060201202815094, -12.46991126736615385 ) ) ;
#18970=B_SPLINE_CURVE_WITH_KNOTS ( 'NONE', 3,
 ( #36488, #8890, #31781, #60563 ),
 .UNSPECIFIED., .F., .F.,
 ( 4, 4 ),
 ( 0.002290414566844504660, 0.004042984057420971958 ),
 .UNSPECIFIED. ) ;
#18971=CARTESIAN_POINT ( 'NONE',  ( 0.7056313189692693388, 10.05087499617880908, -45.81188225524841329 ) ) ;
#18980=CARTESIAN_POINT ( 'NONE',  ( 0.8554163680231816613, -41.45413358837884488, 21.97180651536553952 ) ) ;
#18985=ORIENTED_EDGE ( 'NONE', *, *, #15178, .F. ) ;
#18987=CARTESIAN_POINT ( 'NONE',  ( 0.9754292589017242721, 33.24763086278803570, 25.51318304146031579 ) ) ;
#18988=EDGE_CURVE ( 'NONE', #27840, #33545, #6726, .T. ) ;
#18991=CARTESIAN_POINT ( 'NONE',  ( 0.5830082357119539260, 17.10941071709084937, -43.66348703267112086 ) ) ;
#18993=CARTESIAN_POINT ( 'NONE',  ( 5.896278296736517710, 14.91306641426024093, 13.49545959714773424 ) ) ;
#18994=CARTESIAN_POINT ( 'NONE',  ( 1.231276596079887264, -6.136529359146732254, 41.46829847537028257 ) ) ;
#18995=ADVANCED_FACE ( 'NONE', ( #38072 ), #14784, .T. ) ;
#18999=CARTESIAN_POINT ( 'NONE',  ( 0.8560838555295223751, -44.60403252362528548, -14.52078223489045072 ) ) ;
#19000=ORIENTED_EDGE ( 'NONE', *, *, #43902, .T. ) ;
#19009=CARTESIAN_POINT ( 'NONE',  ( 5.896782393890504181, 0.6657210432558627877, -20.10181341000305366 ) ) ;
#19019=CARTESIAN_POINT ( 'NONE',  ( 0.9754292580325135686, -30.68784781142436557, -28.54090859813089054 ) ) ;
#19029=ORIENTED_EDGE ( 'NONE', *, *, #58638, .T. ) ;
#19030=CARTESIAN_POINT ( 'NONE',  ( 0.7056759521545010738, -42.23392822606338370, 20.39715999134963198 ) ) ;
#19033=VECTOR ( 'NONE', #24877, 1000.000000000000000 ) ;
#19036=CARTESIAN_POINT ( 'NONE',  ( 0.5806925824938499181, -34.41156632303712826, -31.86010774524751454 ) ) ;
#19038=CARTESIAN_POINT ( 'NONE',  ( 5.901463166500146684, 14.92627229327871596, 13.48051429907393306 ) ) ;
#19040=CARTESIAN_POINT ( 'NONE',  ( 1.000433927950264090, -6.320470408796723838, 41.43030691974620083 ) ) ;
#19042=DIRECTION ( 'NONE',  ( 0.000000000000000000, 0.000000000000000000, 1.000000000000000000 ) ) ;
#19049=DIRECTION ( 'NONE',  ( 0.07906939808003032866, -0.9208896734047763433, 0.3817201064965091151 ) ) ;
#19050=ORIENTED_EDGE ( 'NONE', *, *, #48933, .T. ) ;
#19054=CARTESIAN_POINT ( 'NONE',  ( 0.5806925824938502512, 23.01490136172913026, 40.85996423950273737 ) ) ;
#19057=B_SPLINE_CURVE_WITH_KNOTS ( 'NONE', 3,
 ( #22312, #36123, #51407, #56113 ),
 .UNSPECIFIED., .F., .F.,
 ( 4, 4 ),
 ( 1.387948177032400748E-17, 0.005004948556313828720 ),
 .UNSPECIFIED. ) ;
#19058=ORIENTED_EDGE ( 'NONE', *, *, #38941, .F. ) ;
#19077=CARTESIAN_POINT ( 'NONE',  ( 0.9780303403264770656, 40.50400539199167582, 10.75942194546684760 ) ) ;
#19078=CARTESIAN_POINT ( 'NONE',  ( 0.8560838555295158248, -29.58154842764465542, -36.40473632241614155 ) ) ;
#19081=B_SPLINE_CURVE_WITH_KNOTS ( 'NONE', 3,
 ( #28152, #18457, #42284, #57250 ),
 .UNSPECIFIED., .F., .F.,
 ( 4, 4 ),
 ( 3.127317220692750759E-18, 0.004042984057420974560 ),
 .UNSPECIFIED. ) ;
#19089=CARTESIAN_POINT ( 'NONE',  ( 0.9780106845699467755, -37.54462564979032635, 18.62075001906600136 ) ) ;
#19094=CARTESIAN_POINT ( 'NONE',  ( 5.838029081930955932, -22.68231883182838260, -41.43159990350605426 ) ) ;
#19096=VERTEX_POINT ( 'NONE', #37138 ) ;
#19098=CARTESIAN_POINT ( 'NONE',  ( 4.958415959904816539, 42.74072562871904779, -15.37642112304408037 ) ) ;
#19103=CARTESIAN_POINT ( 'NONE',  ( 0.9784957157296367836, 38.67345032168838515, 16.14612328728703616 ) ) ;
#19108=CARTESIAN_POINT ( 'NONE',  ( 4.962356264823608143, -19.84272732133934269, -37.11471096901227185 ) ) ;
#19125=CARTESIAN_POINT ( 'NONE',  ( 0.9785694773339252972, -34.67671301199700906, 23.53425121813456045 ) ) ;
#19126=CARTESIAN_POINT ( 'NONE',  ( 0.6845945791218034371, -6.946890923033673282, -46.39124084584735641 ) ) ;
#19137=CARTESIAN_POINT ( 'NONE',  ( 0.5804410086790514622, 11.40290849443471899, 45.49168638029310330 ) ) ;
#19141=CARTESIAN_POINT ( 'NONE',  ( 0.6845945791218034371, -29.61886432665992430, -36.37484565895580602 ) ) ;
#19148=CARTESIAN_POINT ( 'NONE',  ( 5.895596859100789899, 8.462961974658767872, -18.24572437114973056 ) ) ;
#19150=ORIENTED_EDGE ( 'NONE', *, *, #38232, .T. ) ;
#19151=CARTESIAN_POINT ( 'NONE',  ( 4.291220156522060236, 31.16808953869651333, -35.32618280841412428 ) ) ;
#19159=CARTESIAN_POINT ( 'NONE',  ( 4.956445790444040433, 46.94638516972321440, -3.684422564748698115 ) ) ;
#19163=CARTESIAN_POINT ( 'NONE',  ( 0.5848930533535030563, -1.749067435711754159, 46.86377967570361847 ) ) ;
#19165=B_SPLINE_CURVE_WITH_KNOTS ( 'NONE', 3,
 ( #45470, #17569, #41392, #3138, #27268, #60449 ),
 .UNSPECIFIED., .F., .F.,
 ( 4, 2, 4 ),
 ( 1.238878783205199297E-16, 0.0002448718616795882716, 0.0004897437233590527274 ),
 .UNSPECIFIED. ) ;
#19166=VERTEX_POINT ( 'NONE', #57730 ) ;
#19168=ORIENTED_EDGE ( 'NONE', *, *, #39411, .F. ) ;
#19172=CARTESIAN_POINT ( 'NONE',  ( 0.9791128995231609400, -34.55414444086503778, -23.71388909913344634 ) ) ;
#19183=CARTESIAN_POINT ( 'NONE',  ( 4.962356264823608143, 0.000000000000000000, 0.000000000000000000 ) ) ;
#19193=CIRCLE ( 'NONE', #57153, 12.50000000000000000 ) ;
#19206=EDGE_CURVE ( 'NONE', #36885, #47523, #23493, .T. ) ;
#19210=VERTEX_POINT ( 'NONE', #53048 ) ;
#19217=LINE ( 'NONE', #23288, #59676 ) ;
#19226=CARTESIAN_POINT ( 'NONE',  ( 0.9788927965476029724, -39.54311573103250765, 13.88087212367969236 ) ) ;
#19228=VERTEX_POINT ( 'NONE', #53349 ) ;
#19241=CARTESIAN_POINT ( 'NONE',  ( 0.9762797500689124330, -34.83496347773922963, -23.29914386174477059 ) ) ;
#19245=ORIENTED_EDGE ( 'NONE', *, *, #47676, .F. ) ;
#19249=CARTESIAN_POINT ( 'NONE',  ( 5.895596859100789899, -11.93344155749905866, 16.19015613903219730 ) ) ;
#19255=CARTESIAN_POINT ( 'NONE',  ( 5.896278296736517710, 19.00178995741540788, 6.592340861078921144 ) ) ;
#19257=CARTESIAN_POINT ( 'NONE',  ( 0.9785694773339239649, 41.90806447728379425, 0.2225701743215739437 ) ) ;
#19259=VERTEX_POINT ( 'NONE', #22562 ) ;
#19270=CARTESIAN_POINT ( 'NONE',  ( 1.231276596079887931, -7.805643096901414779, -41.18675402191659174 ) ) ;
#19284=AXIS2_PLACEMENT_3D ( 'NONE', #53323, #23602, #43664 ) ;
#19289=CARTESIAN_POINT ( 'NONE',  ( 0.5837799406558208393, 46.89600465499675863, -0.09108773643912386475 ) ) ;
#19291=CARTESIAN_POINT ( 'NONE',  ( 3.661921753702001237, -12.12682059594439821, 45.44855713955956134 ) ) ;
#19296=CARTESIAN_POINT ( 'NONE',  ( 4.956445790444004018, -45.27177431812773278, -12.96165499572285817 ) ) ;
#19299=CARTESIAN_POINT ( 'NONE',  ( 4.962356264823602814, 6.570263404307167932, -41.57002810511882274 ) ) ;
#19302=VERTEX_POINT ( 'NONE', #4340 ) ;
#19311=CARTESIAN_POINT ( 'NONE',  ( 2.528190830796658517, 39.10452951792409237, -15.26728225110188930 ) ) ;
#19314=CARTESIAN_POINT ( 'NONE',  ( 5.896782393890504181, -17.30187591025968530, 10.25529994022543079 ) ) ;
#19315=FACE_OUTER_BOUND ( 'NONE', #44558, .T. ) ;
#19331=CARTESIAN_POINT ( 'NONE',  ( 0.6845945791218034371, -24.50629722878996830, -39.99809891542528106 ) ) ;
#19334=B_SPLINE_CURVE_WITH_KNOTS ( 'NONE', 3,
 ( #48071, #12805, #60998, #22490, #32208, #60681 ),
 .UNSPECIFIED., .F., .F.,
 ( 4, 2, 4 ),
 ( 0.000000000000000000, 0.0002291459268755696927, 0.0004582918537511393854 ),
 .UNSPECIFIED. ) ;
#19337=CARTESIAN_POINT ( 'NONE',  ( 0.6845945791218034371, 33.22744374803217227, -33.11107824709581138 ) ) ;
#19343=CARTESIAN_POINT ( 'NONE',  ( 1.231276596079881047, -11.60895935156387537, -40.28037777618035875 ) ) ;
#19365=ORIENTED_EDGE ( 'NONE', *, *, #21599, .F. ) ;
#19375=VECTOR ( 'NONE', #13141, 1000.000000000000227 ) ;
#19381=ORIENTED_EDGE ( 'NONE', *, *, #14704, .T. ) ;
#19383=ORIENTED_EDGE ( 'NONE', *, *, #58603, .T. ) ;
#19384=CARTESIAN_POINT ( 'NONE',  ( 5.917102823773431552, 8.458006992051032569, -18.24696785151324008 ) ) ;
#19386=CARTESIAN_POINT ( 'NONE',  ( 3.238018933889920792, -11.82813123897611796, 6.285125596295605632 ) ) ;
#19388=ORIENTED_EDGE ( 'NONE', *, *, #8724, .F. ) ;
#19402=EDGE_CURVE ( 'NONE', #57645, #53012, #56979, .T. ) ;
#19405=VERTEX_POINT ( 'NONE', #14406 ) ;
#19407=CARTESIAN_POINT ( 'NONE',  ( 0.9762797500689124330, -41.16654106227479559, 7.851158013551082782 ) ) ;
#19411=CARTESIAN_POINT ( 'NONE',  ( 0.5837800005270546988, 4.694056397113588019, -46.66048749405113227 ) ) ;
#19421=LINE ( 'NONE', #23804, #15116 ) ;
#19425=CARTESIAN_POINT ( 'NONE',  ( 1.231276596079881935, -39.31472542100197387, -14.54747868495734053 ) ) ;
#19428=CARTESIAN_POINT ( 'NONE',  ( 0.9762797500689124330, 4.697980241569248427, -41.64437257103928403 ) ) ;
#19429=CARTESIAN_POINT ( 'NONE',  ( 4.962356264823608143, 0.000000000000000000, 0.000000000000000000 ) ) ;
#19433=B_SPLINE_CURVE_WITH_KNOTS ( 'NONE', 3,
 ( #9227, #47453, #3273, #4504 ),
 .UNSPECIFIED., .F., .F.,
 ( 4, 4 ),
 ( 1.250926888277100334E-16, 0.005004948556313948416 ),
 .UNSPECIFIED. ) ;
#19434=CARTESIAN_POINT ( 'NONE',  ( 5.838029081930955932, -22.71741985886587045, 41.41236401256183086 ) ) ;
#19437=FACE_OUTER_BOUND ( 'NONE', #7833, .T. ) ;
#19438=ORIENTED_EDGE ( 'NONE', *, *, #38573, .T. ) ;
#19440=VERTEX_POINT ( 'NONE', #54742 ) ;
#19454=ORIENTED_EDGE ( 'NONE', *, *, #15753, .F. ) ;
#19458=CARTESIAN_POINT ( 'NONE',  ( 0.5835226383429290564, 17.02466281517259716, 43.69671990636877013 ) ) ;
#19463=AXIS2_PLACEMENT_3D ( 'NONE', #58865, #10976, #50401 ) ;
#19467=B_SPLINE_CURVE_WITH_KNOTS ( 'NONE', 3,
 ( #20066, #44813, #1850, #20364, #45119, #39809 ),
 .UNSPECIFIED., .F., .F.,
 ( 4, 2, 4 ),
 ( 3.471140604459641645E-18, 0.0002291459268755725658, 0.0004582918537511416622 ),
 .UNSPECIFIED. ) ;
#19469=CARTESIAN_POINT ( 'NONE',  ( 4.956445790443998689, -22.15545010017797622, 41.55326799420426198 ) ) ;
#19472=ORIENTED_EDGE ( 'NONE', *, *, #53770, .T. ) ;
#19473=CARTESIAN_POINT ( 'NONE',  ( 0.8560838555295158248, 27.08392101972004440, 38.29926965725714894 ) ) ;
#19474=CARTESIAN_POINT ( 'NONE',  ( 3.782625744892851749, 37.01847680236511451, 19.92160835193178414 ) ) ;
#19476=CARTESIAN_POINT ( 'NONE',  ( 0.9789889208857696090, -22.63130747653287855, -35.27263556845443304 ) ) ;
#19481=CARTESIAN_POINT ( 'NONE',  ( 5.895881250540457863, 10.81854556178491222, -16.95543433639743114 ) ) ;
#19482=B_SPLINE_CURVE_WITH_KNOTS ( 'NONE', 3,
 ( #19906, #14895, #39019, #20500 ),
 .UNSPECIFIED., .F., .F.,
 ( 4, 4 ),
 ( 8.673617379884035472E-19, 0.004042984057420975427 ),
 .UNSPECIFIED. ) ;
#19485=AXIS2_PLACEMENT_3D ( 'NONE', #4202, #13964, #6346 ) ;
#19486=CARTESIAN_POINT ( 'NONE',  ( 4.956445790443994248, 24.88142650099509723, 39.98065363916922621 ) ) ;
#19492=CARTESIAN_POINT ( 'NONE',  ( 0.7764146366350277439, 33.24270218630520191, 33.09022854290649462 ) ) ;
#19494=CARTESIAN_POINT ( 'NONE',  ( 4.960386119450149955, 1.932332837766998379, -43.71158375621306647 ) ) ;
#19496=( BOUNDED_SURFACE ( )  B_SPLINE_SURFACE ( 3, 1, ( 
 ( #37839, #56890 ),
 ( #61887, #51891 ),
 ( #42834, #33121 ),
 ( #14321, #38441 ) ),
 .UNSPECIFIED., .F., .F., .F. ) 
 B_SPLINE_SURFACE_WITH_KNOTS ( ( 4, 4 ),
 ( 2, 2 ),
 ( 0.000000000000000000, 1.000000000000000000 ),
 ( 0.000000000000000000, 1.000000000000000000 ),
 .UNSPECIFIED. ) 
 GEOMETRIC_REPRESENTATION_ITEM ( )  RATIONAL_B_SPLINE_SURFACE ( (
 ( 1.000000000000000000, 1.000000000000000000),
 ( 0.7282232189291694135, 0.9929344683865672927),
 ( 0.7282232189291694135, 0.9929344683865672927),
 ( 1.000000000000000000, 1.000000000000000000) ) ) 
 REPRESENTATION_ITEM ( '' )  SURFACE ( )  );
#19500=CARTESIAN_POINT ( 'NONE',  ( 3.376099380956838925, 13.04318434631702139, -3.095759315589272642 ) ) ;
#19501=VERTEX_POINT ( 'NONE', #22483 ) ;
#19503=AXIS2_PLACEMENT_3D ( 'NONE', #40323, #25571, #21185 ) ;
#19510=( BOUNDED_SURFACE ( )  B_SPLINE_SURFACE ( 3, 1, ( 
 ( #61043, #24302 ),
 ( #39048, #56340 ),
 ( #43437, #58104 ),
 ( #57795, #477 ) ),
 .UNSPECIFIED., .F., .F., .F. ) 
 B_SPLINE_SURFACE_WITH_KNOTS ( ( 4, 4 ),
 ( 2, 2 ),
 ( 0.000000000000000000, 1.000000000000000000 ),
 ( 0.000000000000000000, 1.000000000000000000 ),
 .UNSPECIFIED. ) 
 GEOMETRIC_REPRESENTATION_ITEM ( )  RATIONAL_B_SPLINE_SURFACE ( (
 ( 1.000000000000000000, 1.000000000000000000),
 ( 0.9952954269826590483, 0.8620686068821339365),
 ( 0.9952954269826590483, 0.8620686068821339365),
 ( 1.000000000000000000, 1.000000000000000000) ) ) 
 REPRESENTATION_ITEM ( '' )  SURFACE ( )  );
#19517=VERTEX_POINT ( 'NONE', #3661 ) ;
#19518=DIRECTION ( 'NONE',  ( 0.07500201931887538753, -0.4910262002617780674, 0.8679101150203120119 ) ) ;
#19522=LINE ( 'NONE', #5383, #33106 ) ;
#19540=ORIENTED_EDGE ( 'NONE', *, *, #48237, .F. ) ;
#19543=CARTESIAN_POINT ( 'NONE',  ( 5.917102823773431552, 10.82912387347610128, 16.94756012482775986 ) ) ;
#19547=CARTESIAN_POINT ( 'NONE',  ( 5.901463166500146684, -19.93509711719964272, -2.666415809369400591 ) ) ;
#19549=CARTESIAN_POINT ( 'NONE',  ( 0.9762797500689124330, -11.93232144563776487, -40.17392798947692256 ) ) ;
#19557=CARTESIAN_POINT ( 'NONE',  ( 5.895596859100789899, 18.99884588797230478, 6.600911917119146821 ) ) ;
#19562=CARTESIAN_POINT ( 'NONE',  ( 5.894904586330512508, 12.98452142685960631, 15.36006560458211467 ) ) ;
#19572=CARTESIAN_POINT ( 'NONE',  ( 0.8560838555295158248, 45.47430759461114747, -11.50913475776619599 ) ) ;
#19581=VERTEX_POINT ( 'NONE', #17791 ) ;
#19584=FACE_OUTER_BOUND ( 'NONE', #7168, .T. ) ;
#19586=EDGE_LOOP ( 'NONE', ( #3939, #2556, #37213, #15391 ) ) ;
#19587=FACE_OUTER_BOUND ( 'NONE', #49492, .T. ) ;
#19608=ORIENTED_EDGE ( 'NONE', *, *, #61071, .T. ) ;
#19611=EDGE_CURVE ( 'NONE', #10729, #33488, #48143, .T. ) ;
#19613=CARTESIAN_POINT ( 'NONE',  ( 5.896278296736517710, 3.339955767731461300, 19.83359965018909676 ) ) ;
#19617=CARTESIAN_POINT ( 'NONE',  ( 5.896278296736517710, 0.6665948613555030544, -20.10180665774094422 ) ) ;
#19618=CARTESIAN_POINT ( 'NONE',  ( 4.960386119450153508, -15.28553149072512340, -40.99742664751524046 ) ) ;
#19634=DIRECTION ( 'NONE',  ( 0.000000000000000000, 0.000000000000000000, 1.000000000000000000 ) ) ;
#19637=CARTESIAN_POINT ( 'NONE',  ( 0.5806925824938499181, 40.62497527030964051, -23.42720099863178973 ) ) ;
#19640=CARTESIAN_POINT ( 'NONE',  ( 1.231276596079881047, -39.86997064245551314, 12.94844438485960580 ) ) ;
#19641=CARTESIAN_POINT ( 'NONE',  ( 0.5804410086790514622, 37.14246315962257938, -28.63489623329332545 ) ) ;
#19644=CARTESIAN_POINT ( 'NONE',  ( 0.5782707292762442330, -24.62356639979741502, -39.91761931105593675 ) ) ;
#19647=CARTESIAN_POINT ( 'NONE',  ( 0.5782707292762442330, -45.81184706829294129, -10.05042396612988931 ) ) ;
#19652=CARTESIAN_POINT ( 'NONE',  ( 0.9784957157296367836, -6.740996248989422845, 41.36293058480602269 ) ) ;
#19654=CARTESIAN_POINT ( 'NONE',  ( 1.091591847532196624, -11.67058309673969774, -40.25613594395188244 ) ) ;
#19656=ORIENTED_EDGE ( 'NONE', *, *, #22929, .T. ) ;
#19659=FACE_OUTER_BOUND ( 'NONE', #14917, .T. ) ;
#19670=CARTESIAN_POINT ( 'NONE',  ( 2.528190830796656741, -18.76089685257605311, 37.55373330895358208 ) ) ;
#19673=EDGE_CURVE ( 'NONE', #46030, #53909, #33941, .T. ) ;
#19682=EDGE_CURVE ( 'NONE', #5752, #57645, #40732, .T. ) ;
#19690=ORIENTED_EDGE ( 'NONE', *, *, #9540, .F. ) ;
#19692=CARTESIAN_POINT ( 'NONE',  ( 5.901463166500145796, 0.6865185226679980657, -20.10090949829560714 ) ) ;
#19694=AXIS2_PLACEMENT_3D ( 'NONE', #58058, #14878, #48371 ) ;
#19696=ORIENTED_EDGE ( 'NONE', *, *, #9385, .F. ) ;
#19700=ORIENTED_EDGE ( 'NONE', *, *, #29798, .F. ) ;
#19707=CARTESIAN_POINT ( 'NONE',  ( 0.9769922540276050338, -26.71843606007641725, -32.28709850063540188 ) ) ;
#19710=CARTESIAN_POINT ( 'NONE',  ( 0.9785694773339250752, -41.82934473077335724, 2.577076853490416486 ) ) ;
#19713=CARTESIAN_POINT ( 'NONE',  ( 0.8554163680231708922, -0.6539261334248972490, -46.91244881397519606 ) ) ;
#19731=EDGE_CURVE ( 'NONE', #19405, #46003, #10746, .T. ) ;
#19740=CARTESIAN_POINT ( 'NONE',  ( 4.956445790444027999, 19.33052208089617352, -42.94029536716791995 ) ) ;
#19747=CARTESIAN_POINT ( 'NONE',  ( 0.5782707292762442330, -29.72436028066389824, -36.27945368404695614 ) ) ;
#19755=EDGE_CURVE ( 'NONE', #52026, #15046, #56060, .T. ) ;
#19761=ORIENTED_EDGE ( 'NONE', *, *, #20374, .T. ) ;
#19762=CARTESIAN_POINT ( 'NONE',  ( 0.5804410086790514622, 45.08525424748427213, 12.91664435118883958 ) ) ;
#19763=EDGE_CURVE ( 'NONE', #27747, #18385, #32381, .T. ) ;
#19765=CARTESIAN_POINT ( 'NONE',  ( 0.5832655196449142432, 40.23291104114027661, 24.09456478397196477 ) ) ;
#19768=ORIENTED_EDGE ( 'NONE', *, *, #6607, .F. ) ;
#19772=CARTESIAN_POINT ( 'NONE',  ( 4.962356264823608143, 17.31942680647409460, 38.35717733303029320 ) ) ;
#19777=ADVANCED_FACE ( 'NONE', ( #26637 ), #41652, .F. ) ;
#19783=LINE ( 'NONE', #4394, #20516 ) ;
#19789=CARTESIAN_POINT ( 'NONE',  ( 0.8560838555295158248, -39.18289055412748922, 25.78902716088759206 ) ) ;
#19790=ORIENTED_EDGE ( 'NONE', *, *, #47376, .T. ) ;
#19792=CARTESIAN_POINT ( 'NONE',  ( 4.291220156522060236, -16.00047830133216564, -44.30997282141229476 ) ) ;
#19794=CARTESIAN_POINT ( 'NONE',  ( 0.9772918015221170318, 41.47740498993091052, -5.996810073025064192 ) ) ;
#19799=CARTESIAN_POINT ( 'NONE',  ( 0.6064782688330865312, 43.44828147745647584, -17.65166516435432342 ) ) ;
#19812=LINE ( 'NONE', #19500, #61193 ) ;
#19817=CARTESIAN_POINT ( 'NONE',  ( 0.9791128995231621612, -1.395278494606673636, 41.88544654374177156 ) ) ;
#19818=CARTESIAN_POINT ( 'NONE',  ( 0.9762797500689124330, -30.73989051779348003, 28.48480149377514437 ) ) ;
#19819=ORIENTED_EDGE ( 'NONE', *, *, #55504, .T. ) ;
#19822=B_SPLINE_CURVE_WITH_KNOTS ( 'NONE', 3,
 ( #21960, #36687, #60759, #37005 ),
 .UNSPECIFIED., .F., .F.,
 ( 4, 4 ),
 ( 0.000000000000000000, 0.004041751736740985604 ),
 .UNSPECIFIED. ) ;
#19824=VERTEX_POINT ( 'NONE', #8763 ) ;
#19836=CARTESIAN_POINT ( 'NONE',  ( 3.376099380956842921, -1.774645281739918090, 13.28755123249070635 ) ) ;
#19839=CARTESIAN_POINT ( 'NONE',  ( 1.231276596079881047, -13.22565419922034557, 39.77887431816932917 ) ) ;
#19845=CARTESIAN_POINT ( 'NONE',  ( 1.000110580585050535, -37.10379152213305787, -19.48656299746027543 ) ) ;
#19854=FACE_OUTER_BOUND ( 'NONE', #17968, .T. ) ;
#19858=CARTESIAN_POINT ( 'NONE',  ( 2.282803330402958242, 46.36091562948769251, 7.560582613298351795 ) ) ;
#19862=ORIENTED_EDGE ( 'NONE', *, *, #27256, .T. ) ;
#19867=FACE_OUTER_BOUND ( 'NONE', #559, .T. ) ;
#19868=CARTESIAN_POINT ( 'NONE',  ( 0.7764146366350237471, -20.54893576326343307, -42.16374879759197825 ) ) ;
#19871=CARTESIAN_POINT ( 'NONE',  ( 2.618530812446111078, -29.26021975733388203, -36.79084572214571125 ) ) ;
#19882=CARTESIAN_POINT ( 'NONE',  ( 3.238018933889920792, 1.614035038994356519, -13.29670572963662423 ) ) ;
#19895=CARTESIAN_POINT ( 'NONE',  ( 0.9762797500689124330, -37.17323042682988188, 19.35137526946117958 ) ) ;
#19905=VERTEX_POINT ( 'NONE', #15950 ) ;
#19906=CARTESIAN_POINT ( 'NONE',  ( 4.962356264823609919, 39.89814050050791394, -13.39305724859256763 ) ) ;
#19907=CARTESIAN_POINT ( 'NONE',  ( 0.5806925824938511393, -45.84420715090610798, 9.875780123533177246 ) ) ;
#19908=CARTESIAN_POINT ( 'NONE',  ( 5.895881250540457863, -19.39704354167987077, 5.318118412603870304 ) ) ;
#19909=B_SPLINE_CURVE_WITH_KNOTS ( 'NONE', 3,
 ( #60121, #11930, #41658, #31941 ),
 .UNSPECIFIED., .F., .F.,
 ( 4, 4 ),
 ( 0.000000000000000000, 0.004447772540403785099 ),
 .UNSPECIFIED. ) ;
#19915=CIRCLE ( 'NONE', #27890, 12.50000000000000000 ) ;
#19925=CARTESIAN_POINT ( 'NONE',  ( 3.782625744892850861, 34.03288848122618049, 24.67793763099795967 ) ) ;
#19940=ORIENTED_EDGE ( 'NONE', *, *, #26723, .T. ) ;
#19941=CARTESIAN_POINT ( 'NONE',  ( 0.6064782688330857541, -44.06397689832020603, -16.05304912853237553 ) ) ;
#19942=CARTESIAN_POINT ( 'NONE',  ( 4.956445790444011124, -16.41925925744418180, -44.13554095710700409 ) ) ;
#19947=CARTESIAN_POINT ( 'NONE',  ( 0.5804410086790514622, -34.41390132670950663, -31.86225427258558440 ) ) ;
#19954=CARTESIAN_POINT ( 'NONE',  ( 0.9787464366903548818, 41.51074110666462502, 5.761281599256292907 ) ) ;
#19957=VECTOR ( 'NONE', #58458, 1000.000000000000000 ) ;
#19960=EDGE_CURVE ( 'NONE', #26927, #38058, #23388, .T. ) ;
#19997=AXIS2_PLACEMENT_3D ( 'NONE', #36482, #22061, #12366 ) ;
#20002=CARTESIAN_POINT ( 'NONE',  ( 0.9791128995231607179, 40.42097734080745397, 11.06715975578630839 ) ) ;
#20005=EDGE_LOOP ( 'NONE', ( #31215, #28501, #43640, #29163 ) ) ;
#20006=DIRECTION ( 'NONE',  ( 0.07906939808003035641, 0.4122784474075788519, 0.9076202466287637272 ) ) ;
#20009=DIRECTION ( 'NONE',  ( 0.07906939808003032866, 0.9784699099467771832, -0.1906427696399925209 ) ) ;
#20010=EDGE_CURVE ( 'NONE', #20493, #31086, #21258, .T. ) ;
#20017=FACE_OUTER_BOUND ( 'NONE', #3384, .T. ) ;
#20024=ORIENTED_EDGE ( 'NONE', *, *, #5224, .F. ) ;
#20032=CARTESIAN_POINT ( 'NONE',  ( 1.231276596079881935, -40.90292846002442673, -9.177538581351248226 ) ) ;
#20041=EDGE_CURVE ( 'NONE', #8823, #3829, #29367, .T. ) ;
#20046=CARTESIAN_POINT ( 'NONE',  ( 0.9783242366443545279, -34.70225378719274545, 23.49655447710985001 ) ) ;
#20053=CARTESIAN_POINT ( 'NONE',  ( 4.956445790444001354, -28.36659270909979114, 37.58822246682706947 ) ) ;
#20059=CARTESIAN_POINT ( 'NONE',  ( 1.157644175074338699, 38.26069983002199137, 17.12078047275106485 ) ) ;
#20060=( BOUNDED_SURFACE ( )  B_SPLINE_SURFACE ( 3, 1, ( 
 ( #42583, #37902 ),
 ( #56959, #23455 ),
 ( #9046, #38504 ),
 ( #57557, #52884 ) ),
 .UNSPECIFIED., .F., .F., .F. ) 
 B_SPLINE_SURFACE_WITH_KNOTS ( ( 4, 4 ),
 ( 2, 2 ),
 ( 0.000000000000000000, 1.000000000000000000 ),
 ( 0.000000000000000000, 1.000000000000000000 ),
 .UNSPECIFIED. ) 
 GEOMETRIC_REPRESENTATION_ITEM ( )  RATIONAL_B_SPLINE_SURFACE ( (
 ( 1.000000000000000000, 1.000000000000000000),
 ( 0.9952954269826590483, 0.8620686068821307169),
 ( 0.9952954269826590483, 0.8620686068821307169),
 ( 1.000000000000000000, 1.000000000000000000) ) ) 
 REPRESENTATION_ITEM ( '' )  SURFACE ( )  );
#20066=CARTESIAN_POINT ( 'NONE',  ( 0.9762797500689124330, -26.66896101499549587, -32.32787193067855469 ) ) ;
#20068=CARTESIAN_POINT ( 'NONE',  ( 0.5806925824938502512, -25.69265091979982429, -39.23149310256842170 ) ) ;
#20072=ORIENTED_EDGE ( 'NONE', *, *, #52661, .F. ) ;
#20073=CARTESIAN_POINT ( 'NONE',  ( 4.956445790444004018, -47.08764048036452721, -0.5405220916603282744 ) ) ;
#20075=FACE_OUTER_BOUND ( 'NONE', #57600, .T. ) ;
#20079=ORIENTED_EDGE ( 'NONE', *, *, #54314, .T. ) ;
#20082=CARTESIAN_POINT ( 'NONE',  ( 3.661921753702006566, -39.81514960208500042, -25.04765430130383308 ) ) ;
#20088=CARTESIAN_POINT ( 'NONE',  ( 0.5830082357119563685, -46.77220610048276939, -3.404815917535003233 ) ) ;
#20093=CARTESIAN_POINT ( 'NONE',  ( 0.9790724872846782167, 40.43026749430960365, -11.03307211614352745 ) ) ;
#20094=ORIENTED_EDGE ( 'NONE', *, *, #26212, .T. ) ;
#20098=CARTESIAN_POINT ( 'NONE',  ( 0.8560838555295223751, 39.88643293834682879, -24.68694597426934223 ) ) ;
#20099=CARTESIAN_POINT ( 'NONE',  ( 0.5806925824938499181, -38.96949031362449745, 26.08833430941674436 ) ) ;
#20104=CARTESIAN_POINT ( 'NONE',  ( 1.231276596079887264, 20.88402890667827450, 36.34740854095507245 ) ) ;
#20113=CARTESIAN_POINT ( 'NONE',  ( 0.5806925824938499181, -19.24316026636448029, -42.76591101925195204 ) ) ;
#20114=FACE_OUTER_BOUND ( 'NONE', #51023, .T. ) ;
#20115=CARTESIAN_POINT ( 'NONE',  ( 0.5824936645240087474, -1.931019941530967454, 46.85626255929636841 ) ) ;
#20118=CARTESIAN_POINT ( 'NONE',  ( 0.9762797500689124330, -37.62962005162893320, -18.44821075215020656 ) ) ;
#20119=ORIENTED_EDGE ( 'NONE', *, *, #43840, .F. ) ;
#20121=CARTESIAN_POINT ( 'NONE',  ( 0.9775691876210974574, -1.777855953716244608, 41.87090800541382407 ) ) ;
#20127=B_SPLINE_CURVE_WITH_KNOTS ( 'NONE', 3,
 ( #54944, #12078, #30840, #50260 ),
 .UNSPECIFIED., .F., .F.,
 ( 4, 4 ),
 ( 0.000000000000000000, 0.004447772540403824131 ),
 .UNSPECIFIED. ) ;
#20138=ORIENTED_EDGE ( 'NONE', *, *, #49010, .T. ) ;
#20139=CARTESIAN_POINT ( 'NONE',  ( 0.5848930533535030563, -46.77916419324616015, -3.314042813373960339 ) ) ;
#20145=ORIENTED_EDGE ( 'NONE', *, *, #22957, .T. ) ;
#20147=( BOUNDED_SURFACE ( )  B_SPLINE_SURFACE ( 3, 1, ( 
 ( #1550, #25686 ),
 ( #20992, #6861 ),
 ( #49802, #53254 ),
 ( #29453, #5618 ) ),
 .UNSPECIFIED., .F., .F., .F. ) 
 B_SPLINE_SURFACE_WITH_KNOTS ( ( 4, 4 ),
 ( 2, 2 ),
 ( 0.000000000000000000, 1.000000000000000000 ),
 ( 0.000000000000000000, 1.000000000000000000 ),
 .UNSPECIFIED. ) 
 GEOMETRIC_REPRESENTATION_ITEM ( )  RATIONAL_B_SPLINE_SURFACE ( (
 ( 1.000000000000000000, 1.000000000000000000),
 ( 0.9729067724841187204, 0.9999501103223794596),
 ( 0.9729067724841187204, 0.9999501103223794596),
 ( 1.000000000000000000, 1.000000000000000000) ) ) 
 REPRESENTATION_ITEM ( '' )  SURFACE ( )  );
#20153=( BOUNDED_SURFACE ( )  B_SPLINE_SURFACE ( 3, 1, ( 
 ( #4951, #56962 ),
 ( #33496, #9049 ),
 ( #43518, #52572 ),
 ( #9665, #24385 ) ),
 .UNSPECIFIED., .F., .F., .F. ) 
 B_SPLINE_SURFACE_WITH_KNOTS ( ( 4, 4 ),
 ( 2, 2 ),
 ( 0.000000000000000000, 1.000000000000000000 ),
 ( 0.000000000000000000, 1.000000000000000000 ),
 .UNSPECIFIED. ) 
 GEOMETRIC_REPRESENTATION_ITEM ( )  RATIONAL_B_SPLINE_SURFACE ( (
 ( 1.000000000000000000, 1.000000000000000000),
 ( 0.9952954269826590483, 0.8620686068821307169),
 ( 0.9952954269826590483, 0.8620686068821307169),
 ( 1.000000000000000000, 1.000000000000000000) ) ) 
 REPRESENTATION_ITEM ( '' )  SURFACE ( )  );
#20156=CARTESIAN_POINT ( 'NONE',  ( 0.6064782688330868643, 46.56801696588680528, -5.545650753847469971 ) ) ;
#20165=CARTESIAN_POINT ( 'NONE',  ( 1.000433927950263646, 41.90447303099593057, -0.6586483488038954448 ) ) ;
#20171=CARTESIAN_POINT ( 'NONE',  ( 4.956445790444035104, 35.28522167764516837, -31.18479086508480691 ) ) ;
#20173=VECTOR ( 'NONE', #18451, 999.9999999999998863 ) ;
#20183=ORIENTED_EDGE ( 'NONE', *, *, #46704, .F. ) ;
#20187=CARTESIAN_POINT ( 'NONE',  ( 5.895596859100789899, -15.78235929336518950, -12.46777118604672197 ) ) ;
#20194=CARTESIAN_POINT ( 'NONE',  ( 4.962356264823608143, -15.53171314616189846, 39.11523340857994668 ) ) ;
#20196=CARTESIAN_POINT ( 'NONE',  ( 1.000110580585050979, -27.55712950893854440, 31.57565669941787689 ) ) ;
#20200=CARTESIAN_POINT ( 'NONE',  ( 0.8554163680231738898, -46.15020320557310640, 8.447734441619829227 ) ) ;
#20202=CARTESIAN_POINT ( 'NONE',  ( 1.231276596079887264, -34.07446381689716475, 24.41736444846234733 ) ) ;
#20211=CARTESIAN_POINT ( 'NONE',  ( 5.895881250540457863, 18.99851645375302311, -6.601822033709823678 ) ) ;
#20214=CARTESIAN_POINT ( 'NONE',  ( 0.5824935313925946323, 16.51437437898027838, -43.89206780187871715 ) ) ;
#20215=CARTESIAN_POINT ( 'NONE',  ( 0.9780303403264777318, -41.13220516101565494, -8.030025652960466331 ) ) ;
#20217=CARTESIAN_POINT ( 'NONE',  ( 5.901463166500146684, 18.99503018386013053, -6.611104193315902045 ) ) ;
#20220=VERTEX_POINT ( 'NONE', #20269 ) ;
#20231=EDGE_CURVE ( 'NONE', #26754, #57580, #34070, .T. ) ;
#20232=DIRECTION ( 'NONE',  ( 0.07500201931887538753, 0.4319596767211368871, -0.8987688995426253991 ) ) ;
#20233=( BOUNDED_SURFACE ( )  B_SPLINE_SURFACE ( 3, 1, ( 
 ( #2198, #12569 ),
 ( #46092, #22265 ),
 ( #54831, #60448 ),
 ( #31042, #7841 ) ),
 .UNSPECIFIED., .F., .F., .F. ) 
 B_SPLINE_SURFACE_WITH_KNOTS ( ( 4, 4 ),
 ( 2, 2 ),
 ( 0.000000000000000000, 1.000000000000000000 ),
 ( 0.000000000000000000, 1.000000000000000000 ),
 .UNSPECIFIED. ) 
 GEOMETRIC_REPRESENTATION_ITEM ( )  RATIONAL_B_SPLINE_SURFACE ( (
 ( 1.000000000000000000, 1.000000000000000000),
 ( 0.9729067724841187204, 0.9999501103223794596),
 ( 0.9729067724841187204, 0.9999501103223794596),
 ( 1.000000000000000000, 1.000000000000000000) ) ) 
 REPRESENTATION_ITEM ( '' )  SURFACE ( )  );
#20251=CARTESIAN_POINT ( 'NONE',  ( 0.8560838555295223751, 45.47430759461099115, 11.50913475776684791 ) ) ;
#20259=CARTESIAN_POINT ( 'NONE',  ( 0.9780303403264755113, 15.36406718167910945, 38.99083293585732690 ) ) ;
#20260=VERTEX_POINT ( 'NONE', #20564 ) ;
#20262=CARTESIAN_POINT ( 'NONE',  ( 4.956445790444006683, -32.34643101787064978, -34.22347806032829709 ) ) ;
#20264=CARTESIAN_POINT ( 'NONE',  ( 0.8554163680231708922, -45.78608427674268455, -10.23913862172187628 ) ) ;
#20268=CARTESIAN_POINT ( 'NONE',  ( 5.896782393890504181, -11.92541098582113612, -16.19600752337651883 ) ) ;
#20269=CARTESIAN_POINT ( 'NONE',  ( 1.231276596079881047, -27.70544295162376258, 31.45926257674180704 ) ) ;
#20276=FACE_OUTER_BOUND ( 'NONE', #45618, .T. ) ;
#20277=EDGE_CURVE ( 'NONE', #33488, #26084, #21957, .T. ) ;
#20278=CARTESIAN_POINT ( 'NONE',  ( 4.958415959904816539, 43.07243048339532265, 14.42115411732758012 ) ) ;
#20282=EDGE_CURVE ( 'NONE', #35884, #31400, #7359, .T. ) ;
#20286=CYLINDRICAL_SURFACE ( 'NONE', #53892, 8.000000000000000000 ) ;
#20290=VERTEX_POINT ( 'NONE', #17106 ) ;
#20292=ORIENTED_EDGE ( 'NONE', *, *, #26465, .F. ) ;
#20294=ORIENTED_EDGE ( 'NONE', *, *, #9063, .T. ) ;
#20295=CARTESIAN_POINT ( 'NONE',  ( 4.960386119450153508, -42.07286811692932105, -12.01291942401236668 ) ) ;
#20296=CARTESIAN_POINT ( 'NONE',  ( 5.896278296736517710, 18.99819559441548833, 6.602692160832260626 ) ) ;
#20298=CARTESIAN_POINT ( 'NONE',  ( 4.962356264823608143, 0.000000000000000000, 0.000000000000000000 ) ) ;
#20303=EDGE_CURVE ( 'NONE', #21575, #37980, #26485, .T. ) ;
#20310=CARTESIAN_POINT ( 'NONE',  ( 0.9754292589017187209, -31.46929217701820036, -27.67690583813050864 ) ) ;
#20316=ADVANCED_FACE ( 'NONE', ( #7050 ), #11264, .F. ) ;
#20319=EDGE_LOOP ( 'NONE', ( #26975, #21118, #58563, #50856 ) ) ;
#20321=CARTESIAN_POINT ( 'NONE',  ( 0.9787284016396604613, -31.20693553390243480, -27.97254320779017078 ) ) ;
#20326=CARTESIAN_POINT ( 'NONE',  ( 0.9784957157296365615, -27.23471787112080733, -31.85283660010242812 ) ) ;
#20329=CARTESIAN_POINT ( 'NONE',  ( 5.895881250540457863, -11.92688455204484121, -16.19497164216397422 ) ) ;
#20347=( BOUNDED_SURFACE ( )  B_SPLINE_SURFACE ( 3, 1, ( 
 ( #17587, #30739 ),
 ( #12284, #36708 ),
 ( #12900, #32000 ),
 ( #51077, #8171 ) ),
 .UNSPECIFIED., .F., .F., .F. ) 
 B_SPLINE_SURFACE_WITH_KNOTS ( ( 4, 4 ),
 ( 2, 2 ),
 ( 0.000000000000000000, 1.000000000000000000 ),
 ( 0.000000000000000000, 1.000000000000000000 ),
 .UNSPECIFIED. ) 
 GEOMETRIC_REPRESENTATION_ITEM ( )  RATIONAL_B_SPLINE_SURFACE ( (
 ( 1.000000000000000000, 1.000000000000000000),
 ( 0.7282232189291694135, 0.9929344683865672927),
 ( 0.7282232189291694135, 0.9929344683865672927),
 ( 1.000000000000000000, 1.000000000000000000) ) ) 
 REPRESENTATION_ITEM ( '' )  SURFACE ( )  );
#20353=CARTESIAN_POINT ( 'NONE',  ( 0.8554163680231816613, -30.98316862405899741, -35.23136010892773839 ) ) ;
#20362=CARTESIAN_POINT ( 'NONE',  ( 0.8560838555295158248, 5.603718208094640829, -46.57221463840858888 ) ) ;
#20364=CARTESIAN_POINT ( 'NONE',  ( 1.091591847532196846, -26.46008473750376311, -32.50573651895864202 ) ) ;
#20365=ORIENTED_EDGE ( 'NONE', *, *, #10691, .F. ) ;
#20371=CARTESIAN_POINT ( 'NONE',  ( 0.6845945791218023269, -18.95641467630792931, 42.90758514917615685 ) ) ;
#20373=CARTESIAN_POINT ( 'NONE',  ( 0.5804410086790514622, -38.35366574781981797, -26.99103880105228370 ) ) ;
#20374=EDGE_CURVE ( 'NONE', #52874, #47700, #24047, .T. ) ;
#20388=CARTESIAN_POINT ( 'NONE',  ( 4.962356264823608143, -41.76635909427997717, 5.177532797578748180 ) ) ;
#20391=CARTESIAN_POINT ( 'NONE',  ( 0.9772918015221170318, 40.30802579601094493, -11.47170049202803987 ) ) ;
#20398=EDGE_LOOP ( 'NONE', ( #14211, #27358 ) ) ;
#20401=CARTESIAN_POINT ( 'NONE',  ( -69.95594261585600293, 1.530808498934191521E-15, 12.50000000000000000 ) ) ;
#20403=( BOUNDED_SURFACE ( )  B_SPLINE_SURFACE ( 3, 1, ( 
 ( #31001, #50109 ),
 ( #31307, #26294 ),
 ( #45428, #2476 ),
 ( #59808, #52875 ) ),
 .UNSPECIFIED., .F., .F., .F. ) 
 B_SPLINE_SURFACE_WITH_KNOTS ( ( 4, 4 ),
 ( 2, 2 ),
 ( 0.000000000000000000, 1.000000000000000000 ),
 ( 0.000000000000000000, 1.000000000000000000 ),
 .UNSPECIFIED. ) 
 GEOMETRIC_REPRESENTATION_ITEM ( )  RATIONAL_B_SPLINE_SURFACE ( (
 ( 1.000000000000000000, 1.000000000000000000),
 ( 0.7282232189291694135, 0.9929344683865672927),
 ( 0.7282232189291694135, 0.9929344683865672927),
 ( 1.000000000000000000, 1.000000000000000000) ) ) 
 REPRESENTATION_ITEM ( '' )  SURFACE ( )  );
#20407=CARTESIAN_POINT ( 'NONE',  ( 0.7056759521544990754, 43.50199477485651300, -17.53069535772447551 ) ) ;
#20409=CARTESIAN_POINT ( 'NONE',  ( 0.8554163680231738898, 40.82560365045097228, -23.11872746688500868 ) ) ;
#20425=B_SPLINE_CURVE_WITH_KNOTS ( 'NONE', 3,
 ( #44435, #39731, #40049, #49713 ),
 .UNSPECIFIED., .F., .F.,
 ( 4, 4 ),
 ( 0.000000000000000000, 0.004447772540403797242 ),
 .UNSPECIFIED. ) ;
#20426=ORIENTED_EDGE ( 'NONE', *, *, #52383, .F. ) ;
#20428=CARTESIAN_POINT ( 'NONE',  ( 0.5806925824938511393, 32.99217760300656010, 33.32774488853447536 ) ) ;
#20437=CARTESIAN_POINT ( 'NONE',  ( 0.9790850452238872847, -17.68673899395511739, -37.99363886261624401 ) ) ;
#20439=LINE ( 'NONE', #40499, #57738 ) ;
#20442=ADVANCED_FACE ( 'NONE', ( #13644 ), #52050, .F. ) ;
#20443=VERTEX_POINT ( 'NONE', #42469 ) ;
#20446=CARTESIAN_POINT ( 'NONE',  ( 1.157644175074337145, 14.29172630907547692, 39.40493414010056483 ) ) ;
#20449=EDGE_CURVE ( 'NONE', #55166, #7311, #50229, .T. ) ;
#20453=EDGE_CURVE ( 'NONE', #1908, #45184, #29479, .T. ) ;
#20459=CARTESIAN_POINT ( 'NONE',  ( 4.956445790444022670, -4.175462451061590308, -46.90526157542895191 ) ) ;
#20475=CARTESIAN_POINT ( 'NONE',  ( 3.782542959838394392, -10.79733161176426570, -40.62825966568303215 ) ) ;
#20477=CIRCLE ( 'NONE', #17627, 42.08604991992415023 ) ;
#20480=CARTESIAN_POINT ( 'NONE',  ( 5.895881250540457863, 14.91980774178274061, 13.48803241976162504 ) ) ;
#20489=( BOUNDED_SURFACE ( )  B_SPLINE_SURFACE ( 3, 1, ( 
 ( #17178, #8073 ),
 ( #36601, #55669 ),
 ( #59447, #46309 ),
 ( #22484, #30635 ) ),
 .UNSPECIFIED., .F., .F., .F. ) 
 B_SPLINE_SURFACE_WITH_KNOTS ( ( 4, 4 ),
 ( 2, 2 ),
 ( 0.000000000000000000, 1.000000000000000000 ),
 ( 0.000000000000000000, 1.000000000000000000 ),
 .UNSPECIFIED. ) 
 GEOMETRIC_REPRESENTATION_ITEM ( )  RATIONAL_B_SPLINE_SURFACE ( (
 ( 1.000000000000000000, 1.000000000000000000),
 ( 0.7282232189291694135, 0.9929344683865672927),
 ( 0.7282232189291694135, 0.9929344683865672927),
 ( 1.000000000000000000, 1.000000000000000000) ) ) 
 REPRESENTATION_ITEM ( '' )  SURFACE ( )  );
#20490=CARTESIAN_POINT ( 'NONE',  ( 1.231276596079881047, -27.70544295162376258, 31.45926257674180704 ) ) ;
#20493=VERTEX_POINT ( 'NONE', #19270 ) ;
#20495=CARTESIAN_POINT ( 'NONE',  ( 4.962356264823608143, 0.000000000000000000, 0.000000000000000000 ) ) ;
#20498=ORIENTED_EDGE ( 'NONE', *, *, #23563, .F. ) ;
#20500=CARTESIAN_POINT ( 'NONE',  ( 1.231276596079887264, 40.19859528295904738, -11.88905834349085922 ) ) ;
#20508=EDGE_CURVE ( 'NONE', #18314, #58067, #48669, .T. ) ;
#20516=VECTOR ( 'NONE', #24148, 1000.000000000000000 ) ;
#20518=VERTEX_POINT ( 'NONE', #25180 ) ;
#20521=DIRECTION ( 'NONE',  ( 0.000000000000000000, 0.000000000000000000, 1.000000000000000000 ) ) ;
#20530=ORIENTED_EDGE ( 'NONE', *, *, #40427, .F. ) ;
#20531=CARTESIAN_POINT ( 'NONE',  ( 0.5832655196449136881, -14.11139715999958888, 44.72251841260825245 ) ) ;
#20532=CARTESIAN_POINT ( 'NONE',  ( 0.9762797500689124330, 32.57381952463229169, 26.36799322592426975 ) ) ;
#20547=FACE_OUTER_BOUND ( 'NONE', #61343, .T. ) ;
#20553=CARTESIAN_POINT ( 'NONE',  ( 0.9762797500689124330, -30.73989051779308568, -28.48480149377557424 ) ) ;
#20554=CARTESIAN_POINT ( 'NONE',  ( 0.8560838555295223751, 44.99141268455589682, -13.27198623905683128 ) ) ;
#20563=CARTESIAN_POINT ( 'NONE',  ( 5.838029081930955932, 30.48039787783015342, 36.08338126287622316 ) ) ;
#20564=CARTESIAN_POINT ( 'NONE',  ( 4.962356264823608143, -40.47344704301786322, -11.53844366967987334 ) ) ;
#20591=EDGE_CURVE ( 'NONE', #1466, #15676, #52460, .T. ) ;
#20595=EDGE_CURVE ( 'NONE', #21146, #31192, #2280, .T. ) ;
#20599=CARTESIAN_POINT ( 'NONE',  ( 4.958415959904820092, -43.67231206503760177, -12.48731807541597050 ) ) ;
#20600=CARTESIAN_POINT ( 'NONE',  ( 0.7764139734771249302, 46.89611479102006797, 0.8915651486764878397 ) ) ;
#20601=CARTESIAN_POINT ( 'NONE',  ( 3.782542959838390839, 5.920274717261695407, -41.61956511868813635 ) ) ;
#20607=LINE ( 'NONE', #6462, #143 ) ;
#20624=CARTESIAN_POINT ( 'NONE',  ( 3.376099380956838925, -1.774645281739724023, -13.28755123249073478 ) ) ;
#20625=EDGE_CURVE ( 'NONE', #35006, #14741, #31426, .T. ) ;
#20627=CARTESIAN_POINT ( 'NONE',  ( 0.9789889208857702751, -27.13076157042887004, -31.94145699010782735 ) ) ;
#20642=CARTESIAN_POINT ( 'NONE',  ( 4.956445790444002242, -37.28933980949966553, 28.75835855384135087 ) ) ;
#20643=CARTESIAN_POINT ( 'NONE',  ( 1.157644175074338033, -41.75974213338677998, -3.623011514227223007 ) ) ;
#20646=B_SPLINE_CURVE_WITH_KNOTS ( 'NONE', 3,
 ( #50381, #1832, #7444, #45401, #21574, #12500 ),
 .UNSPECIFIED., .F., .F.,
 ( 4, 2, 4 ),
 ( 6.314488766312914258E-18, 0.0002291472222819940197, 0.0004582944445639816969 ),
 .UNSPECIFIED. ) ;
#20647=CARTESIAN_POINT ( 'NONE',  ( 1.157644175074338033, 3.373327072561506323, 41.78065269883544630 ) ) ;
#20652=CARTESIAN_POINT ( 'NONE',  ( 0.9754292580325131246, 24.38796667030967669, 34.08158665015274380 ) ) ;
#20655=CARTESIAN_POINT ( 'NONE',  ( 0.5806925824938499181, -24.77160101449041463, -39.81946942793766198 ) ) ;
#20656=CIRCLE ( 'NONE', #15660, 47.09074272231896430 ) ;
#20658=CARTESIAN_POINT ( 'NONE',  ( 2.618530812446115519, -31.41152511854568274, -34.97202995145080706 ) ) ;
#20660=AXIS2_PLACEMENT_3D ( 'NONE', #54472, #35414, #17225 ) ;
#20661=EDGE_CURVE ( 'NONE', #36980, #27845, #54456, .T. ) ;
#20666=DIRECTION ( 'NONE',  ( -1.000000000000000000, -0.000000000000000000, -0.000000000000000000 ) ) ;
#20671=LINE ( 'NONE', #41038, #16997 ) ;
#20677=VERTEX_POINT ( 'NONE', #8851 ) ;
#20682=CARTESIAN_POINT ( 'NONE',  ( 0.9783242366443554161, 20.37523131597068371, -36.62218506625746528 ) ) ;
#20688=CARTESIAN_POINT ( 'NONE',  ( 0.5830082357119558134, 32.79753409158529820, -33.51945394020668800 ) ) ;
#20690=ORIENTED_EDGE ( 'NONE', *, *, #39942, .T. ) ;
#20693=ORIENTED_EDGE ( 'NONE', *, *, #16934, .T. ) ;
#20708=CARTESIAN_POINT ( 'NONE',  ( 0.8560838555295223751, 40.81790744942443183, 23.11430867518979326 ) ) ;
#20709=CARTESIAN_POINT ( 'NONE',  ( 0.9769922540276048117, 41.59126474070951218, -5.147645321342566582 ) ) ;
#20711=CARTESIAN_POINT ( 'NONE',  ( 1.157643937452370153, 20.86452789596350854, 36.35483118202194674 ) ) ;
#20712=( BOUNDED_SURFACE ( )  B_SPLINE_SURFACE ( 3, 1, ( 
 ( #28222, #57027 ),
 ( #61106, #47339 ),
 ( #47049, #27611 ),
 ( #8810, #4385 ) ),
 .UNSPECIFIED., .F., .F., .F. ) 
 B_SPLINE_SURFACE_WITH_KNOTS ( ( 4, 4 ),
 ( 2, 2 ),
 ( 0.000000000000000000, 1.000000000000000000 ),
 ( 0.000000000000000000, 1.000000000000000000 ),
 .UNSPECIFIED. ) 
 GEOMETRIC_REPRESENTATION_ITEM ( )  RATIONAL_B_SPLINE_SURFACE ( (
 ( 1.000000000000000000, 1.000000000000000000),
 ( 0.7282232189291693025, 0.9929344683865674037),
 ( 0.7282232189291693025, 0.9929344683865674037),
 ( 1.000000000000000000, 1.000000000000000000) ) ) 
 REPRESENTATION_ITEM ( '' )  SURFACE ( )  );
#20728=CARTESIAN_POINT ( 'NONE',  ( 0.8560838555295158248, -46.14148336882297485, 8.446084690930096173 ) ) ;
#20729=CARTESIAN_POINT ( 'NONE',  ( 0.9762797500689124330, -0.8945891712305065191, 41.89897964629235361 ) ) ;
#20736=CARTESIAN_POINT ( 'NONE',  ( 3.238018933889920792, -0.1726436309640175248, -13.39319553147569408 ) ) ;
#20758=CARTESIAN_POINT ( 'NONE',  ( 1.091591847532194404, 14.33333461224457750, 39.38673012385353189 ) ) ;
#20759=FACE_OUTER_BOUND ( 'NONE', #26295, .T. ) ;
#20766=FACE_OUTER_BOUND ( 'NONE', #25312, .T. ) ;
#20771=CARTESIAN_POINT ( 'NONE',  ( 0.8560838555295223751, -2.480523550130904642, -46.84250032821665854 ) ) ;
#20772=CARTESIAN_POINT ( 'NONE',  ( 5.895596859100789899, -20.11288567981415909, -0.003583743010673907416 ) ) ;
#20773=FILL_AREA_STYLE_COLOUR ( '', #37453 ) ;
#20786=CARTESIAN_POINT ( 'NONE',  ( 5.896782393890504181, 12.98055409426324580, -15.36331026452040049 ) ) ;
#20791=CARTESIAN_POINT ( 'NONE',  ( 1.157644175074336479, 15.83273920285144243, -38.81142415338135976 ) ) ;
#20799=ADVANCED_FACE ( 'NONE', ( #30037 ), #14480, .T. ) ;
#20802=CARTESIAN_POINT ( 'NONE',  ( 4.956445790443988031, 0.000000000000000000, 0.000000000000000000 ) ) ;
#20804=VERTEX_POINT ( 'NONE', #6200 ) ;
#20806=CARTESIAN_POINT ( 'NONE',  ( 0.9762797500689124330, 36.31338395866826829, -20.92039508843077300 ) ) ;
#20813=DIRECTION ( 'NONE',  ( 0.000000000000000000, 0.000000000000000000, 1.000000000000000000 ) ) ;
#20822=EDGE_CURVE ( 'NONE', #21575, #41654, #33057, .T. ) ;
#20832=EDGE_LOOP ( 'NONE', ( #23823, #26150, #26266, #16668 ) ) ;
#20837=ORIENTED_EDGE ( 'NONE', *, *, #16685, .F. ) ;
#20838=CARTESIAN_POINT ( 'NONE',  ( 0.5835871038041837711, -14.02451996763116426, 44.74983008435918919 ) ) ;
#20840=CARTESIAN_POINT ( 'NONE',  ( 4.958415959904820980, -27.34909152584742031, 36.26611568025254684 ) ) ;
#20844=CARTESIAN_POINT ( 'NONE',  ( 5.910764540655178756, 10.80896614705666359, -16.96076322872724162 ) ) ;
#20848=AXIS2_PLACEMENT_3D ( 'NONE', #56747, #5350, #47077 ) ;
#20852=DIRECTION ( 'NONE',  ( -0.07906939808003034253, -0.9951496949144243986, -0.05852448204802653681 ) ) ;
#20860=CARTESIAN_POINT ( 'NONE',  ( 1.157643937452367711, 14.29172636799923701, -39.40493410750726611 ) ) ;
#20862=CARTESIAN_POINT ( 'NONE',  ( 0.9787284016396593511, 15.23687772655018868, 39.04066541537156354 ) ) ;
#20865=CARTESIAN_POINT ( 'NONE',  ( 2.282803330402972453, 23.71786253601074890, -40.54577541717364397 ) ) ;
#20876=ORIENTED_EDGE ( 'NONE', *, *, #38831, .F. ) ;
#20882=( BOUNDED_SURFACE ( )  B_SPLINE_SURFACE ( 3, 1, ( 
 ( #61396, #32935 ),
 ( #17912, #7 ),
 ( #37324, #57305 ),
 ( #19148, #32620 ) ),
 .UNSPECIFIED., .F., .F., .F. ) 
 B_SPLINE_SURFACE_WITH_KNOTS ( ( 4, 4 ),
 ( 2, 2 ),
 ( 0.000000000000000000, 1.000000000000000000 ),
 ( 0.000000000000000000, 1.000000000000000000 ),
 .UNSPECIFIED. ) 
 GEOMETRIC_REPRESENTATION_ITEM ( )  RATIONAL_B_SPLINE_SURFACE ( (
 ( 1.000000000000000000, 1.000000000000000000),
 ( 0.9729067724841187204, 0.9999501103223794596),
 ( 0.9729067724841187204, 0.9999501103223794596),
 ( 1.000000000000000000, 1.000000000000000000) ) ) 
 REPRESENTATION_ITEM ( '' )  SURFACE ( )  );
#20885=CARTESIAN_POINT ( 'NONE',  ( 0.5797568599927167554, 32.14649101875688331, 34.14422972995566141 ) ) ;
#20887=ORIENTED_EDGE ( 'NONE', *, *, #18067, .T. ) ;
#20888=ORIENTED_EDGE ( 'NONE', *, *, #4638, .T. ) ;
#20892=ORIENTED_EDGE ( 'NONE', *, *, #53087, .F. ) ;
#20894=DIRECTION ( 'NONE',  ( -0.07500201931887527651, 0.6023261099427817955, 0.7947187894968175126 ) ) ;
#20909=VERTEX_POINT ( 'NONE', #50676 ) ;
#20910=CARTESIAN_POINT ( 'NONE',  ( 5.895596859100789899, 8.469463536102802337, 18.24270732712424348 ) ) ;
#20914=CARTESIAN_POINT ( 'NONE',  ( 1.231276596079881935, -40.90292846002442673, -9.177538581351248226 ) ) ;
#20917=CONICAL_SURFACE ( 'NONE', #55917, 42.08604991992415023, 1.569615340895231137 ) ;
#20918=B_SPLINE_CURVE_WITH_KNOTS ( 'NONE', 3,
 ( #25156, #58976, #16384, #20171 ),
 .UNSPECIFIED., .F., .F.,
 ( 4, 4 ),
 ( 4.336808689942017736E-19, 0.004446298630425097112 ),
 .UNSPECIFIED. ) ;
#20924=CARTESIAN_POINT ( 'NONE',  ( 5.895596859100789899, -7.232071727009982354, -18.76766692340500242 ) ) ;
#20927=ORIENTED_EDGE ( 'NONE', *, *, #24714, .F. ) ;
#20930=CARTESIAN_POINT ( 'NONE',  ( 0.7764146366350259676, 27.10005286464496521, -38.28351614471450404 ) ) ;
#20932=CARTESIAN_POINT ( 'NONE',  ( 0.5830082357119567016, -30.06822118592455695, -35.98797173574322983 ) ) ;
#20935=ORIENTED_EDGE ( 'NONE', *, *, #12752, .T. ) ;
#20939=AXIS2_PLACEMENT_3D ( 'NONE', #42112, #37712, #42410 ) ;
#20950=FACE_OUTER_BOUND ( 'NONE', #34153, .T. ) ;
#20956=CARTESIAN_POINT ( 'NONE',  ( 0.9791128995231621612, 9.720239283517752682, 40.76584823743178987 ) ) ;
#20966=CARTESIAN_POINT ( 'NONE',  ( 0.5848930533535030563, 32.73270734968706819, -33.58337314724803946 ) ) ;
#20973=ORIENTED_EDGE ( 'NONE', *, *, #38930, .T. ) ;
#20980=DIRECTION ( 'NONE',  ( 0.07906939808003035641, -0.8617947135858070595, 0.5010567851280115503 ) ) ;
#20985=B_SPLINE_CURVE_WITH_KNOTS ( 'NONE', 3,
 ( #5922, #15062, #48261, #20073 ),
 .UNSPECIFIED., .F., .F.,
 ( 4, 4 ),
 ( 4.336808689942017736E-19, 0.004446298630425057213 ),
 .UNSPECIFIED. ) ;
#20992=CARTESIAN_POINT ( 'NONE',  ( 5.894904586330512508, 3.344157678208356188, 19.83295291894080847 ) ) ;
#21003=EDGE_CURVE ( 'NONE', #20493, #50622, #9061, .T. ) ;
#21004=B_SPLINE_CURVE_WITH_KNOTS ( 'NONE', 3,
 ( #59667, #7343, #54036, #49353, #6406, #22117 ),
 .UNSPECIFIED., .F., .F.,
 ( 4, 2, 4 ),
 ( 4.770489558936219510E-18, 0.0002291472222819944263, 0.0004582944445639840821 ),
 .UNSPECIFIED. ) ;
#21007=CARTESIAN_POINT ( 'NONE',  ( 0.9769922540276045897, 40.53405221617700960, -10.64528844242186700 ) ) ;
#21008=ORIENTED_EDGE ( 'NONE', *, *, #35046, .T. ) ;
#21009=CARTESIAN_POINT ( 'NONE',  ( 0.9787464366903556590, -12.24730775580737330, -40.07913978149986178 ) ) ;
#21013=EDGE_CURVE ( 'NONE', #8559, #34089, #24478, .T. ) ;
#21017=DIRECTION ( 'NONE',  ( -0.07906939808003035641, -0.9940710100007921213, 0.07463817631257134433 ) ) ;
#21026=CIRCLE ( 'NONE', #41092, 42.08604991992415023 ) ;
#21039=VERTEX_POINT ( 'NONE', #61308 ) ;
#21045=CARTESIAN_POINT ( 'NONE',  ( 4.956445790443988031, 0.000000000000000000, 0.000000000000000000 ) ) ;
#21046=EDGE_CURVE ( 'NONE', #49073, #19517, #35907, .T. ) ;
#21056=CARTESIAN_POINT ( 'NONE',  ( 0.9772918015221170318, -18.01631053304243935, -37.83846469569905935 ) ) ;
#21058=CARTESIAN_POINT ( 'NONE',  ( 1.092182651088187573, -21.89098211822472351, 35.74277670161973219 ) ) ;
#21063=CARTESIAN_POINT ( 'NONE',  ( 5.895881250540457863, -7.232970327321949000, -18.76730726162869445 ) ) ;
#21075=EDGE_CURVE ( 'NONE', #40574, #789, #25444, .T. ) ;
#21076=CARTESIAN_POINT ( 'NONE',  ( 5.896782393890504181, 20.06749419425504399, -1.349727247095607430 ) ) ;
#21078=ORIENTED_EDGE ( 'NONE', *, *, #1107, .T. ) ;
#21080=CARTESIAN_POINT ( 'NONE',  ( 5.895596859100789899, 0.6756533542676474990, -20.10153416427100836 ) ) ;
#21083=DIRECTION ( 'NONE',  ( -1.000000000000000000, -0.000000000000000000, -0.000000000000000000 ) ) ;
#21084=CARTESIAN_POINT ( 'NONE',  ( 4.960386119450151732, 41.17653976845452490, 14.79625078758883205 ) ) ;
#21090=CARTESIAN_POINT ( 'NONE',  ( 0.5806925824938502512, -2.112975627976310111, -46.84824112321764744 ) ) ;
#21114=CARTESIAN_POINT ( 'NONE',  ( 4.956445790443987143, 47.01859095792193699, -2.605792484304513934 ) ) ;
#21118=ORIENTED_EDGE ( 'NONE', *, *, #24541, .F. ) ;
#21120=CARTESIAN_POINT ( 'NONE',  ( 5.896782393890504181, 18.99788783847860074, -6.603510017755636063 ) ) ;
#21121=CARTESIAN_POINT ( 'NONE',  ( 0.9754292589017257153, 36.35155297207946745, 20.85406587247130261 ) ) ;
#21124=CARTESIAN_POINT ( 'NONE',  ( 0.5804410086790514622, 5.237717535875093589, 46.60564522533491782 ) ) ;
#21125=B_SPLINE_CURVE_WITH_KNOTS ( 'NONE', 3,
 ( #32721, #22079, #60266, #36500 ),
 .UNSPECIFIED., .F., .F.,
 ( 4, 4 ),
 ( 0.000000000000000000, 0.004447772540403792906 ),
 .UNSPECIFIED. ) ;
#21126=CARTESIAN_POINT ( 'NONE',  ( 4.291220156522059348, -45.16379180774727331, 13.40227245104937204 ) ) ;
#21140=CARTESIAN_POINT ( 'NONE',  ( 0.5806925824938502512, -13.37132486740698134, 44.94919391528425479 ) ) ;
#21145=CARTESIAN_POINT ( 'NONE',  ( 5.895881250540457863, 17.94906520685997364, 9.075171613153653283 ) ) ;
#21146=VERTEX_POINT ( 'NONE', #10879 ) ;
#21150=ORIENTED_EDGE ( 'NONE', *, *, #23771, .F. ) ;
#21153=ORIENTED_EDGE ( 'NONE', *, *, #28437, .F. ) ;
#21160=CARTESIAN_POINT ( 'NONE',  ( 5.896782393890504181, -7.234636363571574691, 18.76662259344765715 ) ) ;
#21161=CARTESIAN_POINT ( 'NONE',  ( 4.962356264823608143, 0.000000000000000000, 0.000000000000000000 ) ) ;
#21165=CARTESIAN_POINT ( 'NONE',  ( 0.9790320750461902755, 14.98204902227782931, 39.13917908740874907 ) ) ;
#21169=CARTESIAN_POINT ( 'NONE',  ( 4.958415959904820092, -31.21198115812912022, -33.00024524162255091 ) ) ;
#21172=DIRECTION ( 'NONE',  ( -1.000000000000000000, -0.000000000000000000, -0.000000000000000000 ) ) ;
#21175=B_SPLINE_CURVE_WITH_KNOTS ( 'NONE', 3,
 ( #183, #57496, #33745, #52826, #29027, #12100, #25860, #15550, #1724, #39373, #16466, #39682, #6109, #10856, #58428, #15862 ),
 .UNSPECIFIED., .F., .F.,
 ( 4, 3, 3, 3, 3, 4 ),
 ( 1.551621725782133898E-17, 0.0002732102107931849038, 0.0004098135523333775766, 0.0005464168938825013106, 0.0008195847345945452868, 0.001092771384553108951 ),
 .UNSPECIFIED. ) ;
#21181=CARTESIAN_POINT ( 'NONE',  ( 2.528190830796658517, 41.96176392093605756, 1.210167259777327198 ) ) ;
#21185=DIRECTION ( 'NONE',  ( 0.000000000000000000, 0.000000000000000000, 1.000000000000000000 ) ) ;
#21191=VECTOR ( 'NONE', #45357, 999.9999999999997726 ) ;
#21196=DIRECTION ( 'NONE',  ( -1.000000000000000000, -0.000000000000000000, -0.000000000000000000 ) ) ;
#21199=B_SPLINE_CURVE_WITH_KNOTS ( 'NONE', 3,
 ( #58543, #33856, #34775, #53839, #48544, #10971 ),
 .UNSPECIFIED., .F., .F.,
 ( 4, 2, 4 ),
 ( 6.805474077711127748E-18, 0.0002291472222819933421, 0.0004582944445639799079 ),
 .UNSPECIFIED. ) ;
#21202=CARTESIAN_POINT ( 'NONE',  ( 0.5804410086790514622, -24.77328595090391872, 39.82215658462187946 ) ) ;
#21207=CARTESIAN_POINT ( 'NONE',  ( 1.157644175074337811, 5.016389116425647998, -41.61535913231781336 ) ) ;
#21210=CARTESIAN_POINT ( 'NONE',  ( 0.5806925824938502512, -44.47729014209954101, -14.86583411581937320 ) ) ;
#21211=CARTESIAN_POINT ( 'NONE',  ( 0.6064782688330870863, 46.89167618744689037, 0.7107395798700630873 ) ) ;
#21215=CARTESIAN_POINT ( 'NONE',  ( 4.956445790444002242, -32.34643101787113295, 34.22347806032784234 ) ) ;
#21224=CARTESIAN_POINT ( 'NONE',  ( 0.9783242366443536397, 24.64300816128945115, 33.89773796242378978 ) ) ;
#21226=B_SPLINE_CURVE_WITH_KNOTS ( 'NONE', 3,
 ( #24372, #57545, #19077, #5240, #57863, #14992, #24066, #53174, #20002, #39114, #24997, #29371, #34707, #44135, #24681, #43192, #53768, #1163, #10902 ),
 .UNSPECIFIED., .F., .F.,
 ( 4, 3, 3, 3, 3, 3, 4 ),
 ( 6.939740885162003740E-18, 0.0002732106629380627572, 0.0004098138914053780341, 0.0005464171197651489665, 0.0006830203481512585849, 0.0008196235766963636329, 0.001011968216111138992 ),
 .UNSPECIFIED. ) ;
#21232=FACE_OUTER_BOUND ( 'NONE', #10795, .T. ) ;
#21236=EDGE_CURVE ( 'NONE', #24966, #13518, #38137, .T. ) ;
#21246=CARTESIAN_POINT ( 'NONE',  ( 2.282816707992305627, 41.06969068285943081, 22.79862876627047186 ) ) ;
#21248=ORIENTED_EDGE ( 'NONE', *, *, #32835, .T. ) ;
#21252=CARTESIAN_POINT ( 'NONE',  ( 0.5837800304671214580, 45.21772934546406475, 12.43359501591787719 ) ) ;
#21255=CARTESIAN_POINT ( 'NONE',  ( 5.896278296736517710, -17.30234040492929637, -10.25455977242977568 ) ) ;
#21258=LINE ( 'NONE', #60366, #38720 ) ;
#21261=LINE ( 'NONE', #39158, #58821 ) ;
#21262=CARTESIAN_POINT ( 'NONE',  ( 0.8554163680231738898, -8.703479761965578376, 46.10265624825618858 ) ) ;
#21263=CARTESIAN_POINT ( 'NONE',  ( 0.9790320750461911636, 9.631629496021094639, 40.78687099782926140 ) ) ;
#21267=CARTESIAN_POINT ( 'NONE',  ( 0.6845945791218023269, 3.832784513613418653, -46.75164471530547416 ) ) ;
#21282=ORIENTED_EDGE ( 'NONE', *, *, #537, .T. ) ;
#21296=CARTESIAN_POINT ( 'NONE',  ( 0.9789889208857698311, 20.05614176017457240, -36.79790857831663686 ) ) ;
#21297=CARTESIAN_POINT ( 'NONE',  ( 1.157644175074340254, 28.54093988368000367, 30.69881147594066917 ) ) ;
#21298=ORIENTED_EDGE ( 'NONE', *, *, #43175, .F. ) ;
#21299=EDGE_CURVE ( 'NONE', #1908, #44492, #36856, .T. ) ;
#21303=CARTESIAN_POINT ( 'NONE',  ( 0.6064782688330876415, -44.53025739761609714, 14.71022170196044954 ) ) ;
#21305=CARTESIAN_POINT ( 'NONE',  ( 0.5806925824938499181, 32.99217760300705748, -33.32774488853398509 ) ) ;
#21307=ORIENTED_EDGE ( 'NONE', *, *, #41468, .T. ) ;
#21308=CARTESIAN_POINT ( 'NONE',  ( 0.9780303403264780648, -17.34655100543410811, 38.15018717661756398 ) ) ;
#21316=EDGE_LOOP ( 'NONE', ( #12967, #19168, #34837, #11363 ) ) ;
#21325=FACE_OUTER_BOUND ( 'NONE', #28611, .T. ) ;
#21330=( BOUNDED_SURFACE ( )  B_SPLINE_SURFACE ( 3, 1, ( 
 ( #21160, #45598 ),
 ( #16163, #54034 ),
 ( #44385, #54649 ),
 ( #6715, #39676 ) ),
 .UNSPECIFIED., .F., .F., .F. ) 
 B_SPLINE_SURFACE_WITH_KNOTS ( ( 4, 4 ),
 ( 2, 2 ),
 ( 0.000000000000000000, 1.000000000000000000 ),
 ( 0.000000000000000000, 1.000000000000000000 ),
 .UNSPECIFIED. ) 
 GEOMETRIC_REPRESENTATION_ITEM ( )  RATIONAL_B_SPLINE_SURFACE ( (
 ( 1.000000000000000000, 1.000000000000000000),
 ( 0.9952954269826590483, 0.8620686068821307169),
 ( 0.9952954269826590483, 0.8620686068821307169),
 ( 1.000000000000000000, 1.000000000000000000) ) ) 
 REPRESENTATION_ITEM ( '' )  SURFACE ( )  );
#21336=CARTESIAN_POINT ( 'NONE',  ( 0.5832655196449132440, 32.43772929586945253, 33.86781512145746120 ) ) ;
#21341=CARTESIAN_POINT ( 'NONE',  ( 4.958415959904820092, -45.41969080731321640, 0.5056093261665406402 ) ) ;
#21345=CARTESIAN_POINT ( 'NONE',  ( 4.956445790444003130, -40.78973928653796577, 23.53157918788916803 ) ) ;
#21347=ORIENTED_EDGE ( 'NONE', *, *, #44287, .F. ) ;
#21350=LINE ( 'NONE', #25734, #52959 ) ;
#21351=EDGE_CURVE ( 'NONE', #32860, #59637, #21684, .T. ) ;
#21353=ORIENTED_EDGE ( 'NONE', *, *, #37191, .T. ) ;
#21358=EDGE_CURVE ( 'NONE', #58092, #19302, #41243, .T. ) ;
#21362=ORIENTED_EDGE ( 'NONE', *, *, #10090, .T. ) ;
#21368=CARTESIAN_POINT ( 'NONE',  ( 4.956445790443991584, 35.28522167764473494, 31.18479086508529363 ) ) ;
#21375=LINE ( 'NONE', #54237, #44288 ) ;
#21376=CARTESIAN_POINT ( 'NONE',  ( 0.9788927965476041937, 36.13029534060832049, 21.23530953935432919 ) ) ;
#21386=CARTESIAN_POINT ( 'NONE',  ( 0.6845945791218023269, 46.90049452736490565, -0.8661026512829932411 ) ) ;
#21397=CARTESIAN_POINT ( 'NONE',  ( 2.528100132419517365, 21.22729024012173582, 36.21679068738293950 ) ) ;
#21399=( BOUNDED_SURFACE ( )  B_SPLINE_SURFACE ( 3, 1, ( 
 ( #28287, #23290 ),
 ( #18594, #372 ),
 ( #42416, #28901 ),
 ( #57379, #57083 ) ),
 .UNSPECIFIED., .F., .F., .F. ) 
 B_SPLINE_SURFACE_WITH_KNOTS ( ( 4, 4 ),
 ( 2, 2 ),
 ( 0.000000000000000000, 1.000000000000000000 ),
 ( 0.000000000000000000, 1.000000000000000000 ),
 .UNSPECIFIED. ) 
 GEOMETRIC_REPRESENTATION_ITEM ( )  RATIONAL_B_SPLINE_SURFACE ( (
 ( 1.000000000000000000, 1.000000000000000000),
 ( 0.7282232189291694135, 0.9929344683865672927),
 ( 0.7282232189291694135, 0.9929344683865672927),
 ( 1.000000000000000000, 1.000000000000000000) ) ) 
 REPRESENTATION_ITEM ( '' )  SURFACE ( )  );
#21402=CARTESIAN_POINT ( 'NONE',  ( 5.896782393890504181, -17.30835043929350192, -10.24436879210333906 ) ) ;
#21408=CARTESIAN_POINT ( 'NONE',  ( 0.9780106845699469975, -22.81401109455046949, 35.15468879442924077 ) ) ;
#21424=EDGE_CURVE ( 'NONE', #34231, #60457, #17510, .T. ) ;
#21426=ORIENTED_EDGE ( 'NONE', *, *, #23986, .F. ) ;
#21432=EDGE_CURVE ( 'NONE', #54810, #49073, #55280, .T. ) ;
#21440=CARTESIAN_POINT ( 'NONE',  ( 0.5782707292762423457, -20.39674625896858728, -42.23398034468063145 ) ) ;
#21447=ORIENTED_EDGE ( 'NONE', *, *, #21703, .T. ) ;
#21448=CARTESIAN_POINT ( 'NONE',  ( 0.5817216825391123836, -13.45861452432960625, 44.92327511761540393 ) ) ;
#21456=CARTESIAN_POINT ( 'NONE',  ( 4.956445790443988031, 46.94638516972315756, 3.684422564749393558 ) ) ;
#21458=ORIENTED_EDGE ( 'NONE', *, *, #51925, .T. ) ;
#21462=VECTOR ( 'NONE', #55894, 999.9999999999997726 ) ;
#21463=CARTESIAN_POINT ( 'NONE',  ( 0.8560838555295158248, 33.26091945577399400, -33.07694168205770069 ) ) ;
#21464=CARTESIAN_POINT ( 'NONE',  ( 0.5835871038041865466, -46.80019526881169867, 2.996026652517322475 ) ) ;
#21469=FACE_OUTER_BOUND ( 'NONE', #25266, .T. ) ;
#21474=CARTESIAN_POINT ( 'NONE',  ( 1.091591847532195070, -34.99102718170865245, 23.07351312056237447 ) ) ;
#21475=DIRECTION ( 'NONE',  ( 0.000000000000000000, 0.000000000000000000, 1.000000000000000000 ) ) ;
#21476=CARTESIAN_POINT ( 'NONE',  ( 2.618530812446111078, 29.00550538245418153, -36.99199165639262077 ) ) ;
#21482=CARTESIAN_POINT ( 'NONE',  ( 0.5848930533535030563, -19.90539571549654241, -42.46231627922634289 ) ) ;
#21486=CARTESIAN_POINT ( 'NONE',  ( 1.231276596079887264, -27.70544295162332560, -31.45926257674220494 ) ) ;
#21487=LINE ( 'NONE', #55293, #17490 ) ;
#21490=CARTESIAN_POINT ( 'NONE',  ( 0.8560838555295158248, 42.82099363437792050, 19.15033519931955297 ) ) ;
#21502=CARTESIAN_POINT ( 'NONE',  ( 4.956445790444004018, -43.14021684453488348, -18.88014143872194950 ) ) ;
#21503=ORIENTED_EDGE ( 'NONE', *, *, #16476, .F. ) ;
#21504=ADVANCED_FACE ( 'NONE', ( #19587 ), #8497, .T. ) ;
#21505=VECTOR ( 'NONE', #12453, 1000.000000000000000 ) ;
#21506=ORIENTED_EDGE ( 'NONE', *, *, #35007, .F. ) ;
#21520=CARTESIAN_POINT ( 'NONE',  ( 4.962356264823602814, 6.570263404307167932, -41.57002810511882274 ) ) ;
#21524=CARTESIAN_POINT ( 'NONE',  ( 5.895881250540457863, -15.78739120953184916, 12.46137875218859747 ) ) ;
#21527=CARTESIAN_POINT ( 'NONE',  ( 0.6845945791218023269, 17.66463248440708256, 43.45534811625348226 ) ) ;
#21528=ORIENTED_EDGE ( 'NONE', *, *, #15293, .F. ) ;
#21529=CARTESIAN_POINT ( 'NONE',  ( 0.9783242366443551941, 3.928031727822913322, 41.72415435873735134 ) ) ;
#21535=ORIENTED_EDGE ( 'NONE', *, *, #35754, .T. ) ;
#21546=CARTESIAN_POINT ( 'NONE',  ( 3.376099380956838925, 0.01224625995945537518, -13.40552996569640065 ) ) ;
#21557=EDGE_CURVE ( 'NONE', #60852, #40143, #49003, .T. ) ;
#21565=B_SPLINE_CURVE_WITH_KNOTS ( 'NONE', 3,
 ( #46399, #55764, #14122, #28492, #37016, #12891, #51371, #47620, #27581, #4356, #42324, #56382, #13815, #37623, #18498, #56076, #23194, #61080, #37307 ),
 .UNSPECIFIED., .F., .F.,
 ( 4, 3, 3, 3, 3, 3, 4 ),
 ( 9.813676791237319219E-18, 0.0002732106629380594504, 0.0004098138914053772210, 0.0005464171197651531949, 0.0006830203481512640059, 0.0008196235766963692708, 0.001011968216111140944 ),
 .UNSPECIFIED. ) ;
#21574=CARTESIAN_POINT ( 'NONE',  ( 0.9754292589017186099, 38.80678075739997723, 15.82280740394609708 ) ) ;
#21575=VERTEX_POINT ( 'NONE', #43407 ) ;
#21578=CARTESIAN_POINT ( 'NONE',  ( 0.5824936645240097466, -19.40917689265153001, -42.69100644620676377 ) ) ;
#21579=B_SPLINE_CURVE_WITH_KNOTS ( 'NONE', 3,
 ( #5880, #25027, #38840, #57895 ),
 .UNSPECIFIED., .F., .F.,
 ( 4, 4 ),
 ( 0.002042055671079073039, 0.004446298630425058081 ),
 .UNSPECIFIED. ) ;
#21582=CARTESIAN_POINT ( 'NONE',  ( 5.895881250540457863, -19.93280900245014564, -2.685294561150279868 ) ) ;
#21583=ORIENTED_EDGE ( 'NONE', *, *, #35059, .T. ) ;
#21585=CARTESIAN_POINT ( 'NONE',  ( 1.231276596079887264, -39.31472542100218703, 14.54747868495677743 ) ) ;
#21594=VERTEX_POINT ( 'NONE', #443 ) ;
#21597=CARTESIAN_POINT ( 'NONE',  ( 0.8554163680231738898, 42.82911630180333162, 19.15391004255849694 ) ) ;
#21598=CARTESIAN_POINT ( 'NONE',  ( 4.962356264823603702, -40.70360067759225586, -10.69824704058845022 ) ) ;
#21599=EDGE_CURVE ( 'NONE', #57176, #44029, #19482, .T. ) ;
#21600=CIRCLE ( 'NONE', #26599, 47.09074272231896430 ) ;
#21615=CARTESIAN_POINT ( 'NONE',  ( 1.231276596079887264, 41.91134057782999633, -0.8463462572780159343 ) ) ;
#21622=CARTESIAN_POINT ( 'NONE',  ( 0.8560838555295223751, 28.55542365806889293, 37.21505896528891810 ) ) ;
#21623=ORIENTED_EDGE ( 'NONE', *, *, #18249, .F. ) ;
#21625=CARTESIAN_POINT ( 'NONE',  ( 5.894904586330512508, -2.011994607810698721, -20.01202862679802408 ) ) ;
#21637=CARTESIAN_POINT ( 'NONE',  ( 4.962356264823608143, -38.91448554252697534, 16.02805081171152324 ) ) ;
#21644=CARTESIAN_POINT ( 'NONE',  ( 5.895596859100789899, -18.51552686702056150, -7.855154234585556949 ) ) ;
#21652=VERTEX_POINT ( 'NONE', #12350 ) ;
#21674=VECTOR ( 'NONE', #54956, 1000.000000000000114 ) ;
#21679=CARTESIAN_POINT ( 'NONE',  ( 0.5817216825391127166, -44.44846903654827486, -14.95220895100342418 ) ) ;
#21681=CARTESIAN_POINT ( 'NONE',  ( 0.5834584762367727162, -30.41620954169410496, 35.69439992672450046 ) ) ;
#21683=LINE ( 'NONE', #31707, #54158 ) ;
#21684=B_SPLINE_CURVE_WITH_KNOTS ( 'NONE', 3,
 ( #50916, #54678, #8302, #21490 ),
 .UNSPECIFIED., .F., .F.,
 ( 4, 4 ),
 ( 0.000000000000000000, 0.004447772540403783365 ),
 .UNSPECIFIED. ) ;
#21685=ORIENTED_EDGE ( 'NONE', *, *, #14232, .T. ) ;
#21686=( BOUNDED_SURFACE ( )  B_SPLINE_SURFACE ( 3, 1, ( 
 ( #49588, #7275 ),
 ( #20480, #44615 ),
 ( #6644, #34906 ),
 ( #39929, #1652 ) ),
 .UNSPECIFIED., .F., .F., .F. ) 
 B_SPLINE_SURFACE_WITH_KNOTS ( ( 4, 4 ),
 ( 2, 2 ),
 ( 0.000000000000000000, 1.000000000000000000 ),
 ( 0.000000000000000000, 1.000000000000000000 ),
 .UNSPECIFIED. ) 
 GEOMETRIC_REPRESENTATION_ITEM ( )  RATIONAL_B_SPLINE_SURFACE ( (
 ( 1.000000000000000000, 1.000000000000000000),
 ( 0.9952954269826590483, 0.8620686068821339365),
 ( 0.9952954269826590483, 0.8620686068821339365),
 ( 1.000000000000000000, 1.000000000000000000) ) ) 
 REPRESENTATION_ITEM ( '' )  SURFACE ( )  );
#21689=ORIENTED_EDGE ( 'NONE', *, *, #12064, .F. ) ;
#21691=CARTESIAN_POINT ( 'NONE',  ( 5.901463166500146684, -1.998795974254450103, 20.01306285889146253 ) ) ;
#21696=B_SPLINE_CURVE_WITH_KNOTS ( 'NONE', 3,
 ( #10061, #33880, #29159, #48275 ),
 .UNSPECIFIED., .F., .F.,
 ( 4, 4 ),
 ( 8.673617379884035472E-19, 0.004042984057420971958 ),
 .UNSPECIFIED. ) ;
#21703=EDGE_CURVE ( 'NONE', #10512, #52560, #59285, .T. ) ;
#21705=CARTESIAN_POINT ( 'NONE',  ( 4.962356264823596597, -3.779019546647577776, 41.91604238389407300 ) ) ;
#21711=CARTESIAN_POINT ( 'NONE',  ( 0.9789889208857693870, 32.94939794372522357, 25.89733718335546442 ) ) ;
#21712=DIRECTION ( 'NONE',  ( -0.07500201931887529039, -0.7485533666540304942, -0.6588190604172040610 ) ) ;
#21713=DIRECTION ( 'NONE',  ( 0.000000000000000000, 0.000000000000000000, 1.000000000000000000 ) ) ;
#21715=CARTESIAN_POINT ( 'NONE',  ( 0.9783242366443540838, -22.77582314543713693, 35.17948791915959106 ) ) ;
#21717=VECTOR ( 'NONE', #6770, 1000.000000000000000 ) ;
#21718=ADVANCED_FACE ( 'NONE', ( #45258 ), #13302, .T. ) ;
#21729=EDGE_CURVE ( 'NONE', #12531, #22979, #24567, .T. ) ;
#21738=CARTESIAN_POINT ( 'NONE',  ( 0.9754292580325136797, -37.66327356036682517, 18.37948017820355062 ) ) ;
#21740=CARTESIAN_POINT ( 'NONE',  ( 0.6064515330803550430, 17.51642761181524577, 43.50297805618738778 ) ) ;
#21744=B_SPLINE_CURVE_WITH_KNOTS ( 'NONE', 3,
 ( #4314, #23450, #28145, #47887 ),
 .UNSPECIFIED., .F., .F.,
 ( 4, 4 ),
 ( 9.697399036122160616E-19, 0.004042984057420974560 ),
 .UNSPECIFIED. ) ;
#21748=ORIENTED_EDGE ( 'NONE', *, *, #60712, .T. ) ;
#21752=LINE ( 'NONE', #43348, #4524 ) ;
#21753=ORIENTED_EDGE ( 'NONE', *, *, #44659, .F. ) ;
#21762=CARTESIAN_POINT ( 'NONE',  ( 5.901463166500145796, -19.40182753204453903, 5.299713082557885535 ) ) ;
#21763=ORIENTED_EDGE ( 'NONE', *, *, #42470, .T. ) ;
#21772=CARTESIAN_POINT ( 'NONE',  ( 1.000433927950262536, -41.76690239855643938, 3.456087626537701407 ) ) ;
#21774=DIRECTION ( 'NONE',  ( 0.000000000000000000, 0.000000000000000000, 1.000000000000000000 ) ) ;
#21777=B_SPLINE_CURVE_WITH_KNOTS ( 'NONE', 3,
 ( #20202, #25807, #57760, #15806, #15496, #29887 ),
 .UNSPECIFIED., .F., .F.,
 ( 4, 2, 4 ),
 ( 8.542522420166516410E-18, 0.0002291472222819941282, 0.0004582944445639797453 ),
 .UNSPECIFIED. ) ;
#21792=CARTESIAN_POINT ( 'NONE',  ( 3.782625744892852637, -41.79414713758510658, 4.526297508658760904 ) ) ;
#21793=CARTESIAN_POINT ( 'NONE',  ( 1.231276596079881047, 41.42457922925067493, 6.425029704024775690 ) ) ;
#21795=CARTESIAN_POINT ( 'NONE',  ( 5.901463166500146684, -11.91875711499662138, 16.20065119599684422 ) ) ;
#21796=CARTESIAN_POINT ( 'NONE',  ( 5.838029081930955932, -46.81003243000938596, -6.315530227494003945 ) ) ;
#21799=B_SPLINE_CURVE_WITH_KNOTS ( 'NONE', 3,
 ( #17984, #37101, #56167, #13276, #61168, #56468 ),
 .UNSPECIFIED., .F., .F.,
 ( 4, 2, 4 ),
 ( 6.040475531737861741E-18, 0.0002291472222819937216, 0.0004582944445639813716 ),
 .UNSPECIFIED. ) ;
#21801=CARTESIAN_POINT ( 'NONE',  ( 0.9791128995231614951, -6.965612749997687203, 41.32575072836828411 ) ) ;
#21813=ORIENTED_EDGE ( 'NONE', *, *, #18988, .F. ) ;
#21815=DIRECTION ( 'NONE',  ( -1.000000000000000000, -0.000000000000000000, -0.000000000000000000 ) ) ;
#21818=B_SPLINE_CURVE_WITH_KNOTS ( 'NONE', 3,
 ( #58710, #39979, #59030, #35260 ),
 .UNSPECIFIED., .F., .F.,
 ( 4, 4 ),
 ( 9.757819552369539906E-19, 0.004446298630425105786 ),
 .UNSPECIFIED. ) ;
#21822=FACE_OUTER_BOUND ( 'NONE', #26671, .T. ) ;
#21824=EDGE_CURVE ( 'NONE', #61119, #25777, #24812, .T. ) ;
#21833=CARTESIAN_POINT ( 'NONE',  ( 0.5832655196449136881, -19.94641636755120828, 42.44261604879714866 ) ) ;
#21834=CARTESIAN_POINT ( 'NONE',  ( 0.5797568665920715958, 45.05935952018240442, -12.99536179691886062 ) ) ;
#21845=ORIENTED_EDGE ( 'NONE', *, *, #13665, .F. ) ;
#21852=CARTESIAN_POINT ( 'NONE',  ( 0.5824935313925951874, -41.69004938736499355, 21.47505434528411428 ) ) ;
#21856=CARTESIAN_POINT ( 'NONE',  ( 0.9762797500689124330, 29.49606728235556830, -29.77090526101713763 ) ) ;
#21857=CARTESIAN_POINT ( 'NONE',  ( 4.962356264823608143, 0.000000000000000000, 0.000000000000000000 ) ) ;
#21870=CARTESIAN_POINT ( 'NONE',  ( 4.962356264823602814, -29.56943756613081931, -29.94802096775409339 ) ) ;
#21871=CARTESIAN_POINT ( 'NONE',  ( 0.8554163680231738898, -39.19027442586735788, 25.79395013442155715 ) ) ;
#21875=DIRECTION ( 'NONE',  ( 0.000000000000000000, 0.000000000000000000, 1.000000000000000000 ) ) ;
#21879=B_SPLINE_CURVE_WITH_KNOTS ( 'NONE', 3,
 ( #31146, #1089, #2317, #49634 ),
 .UNSPECIFIED., .F., .F.,
 ( 4, 4 ),
 ( 0.000000000000000000, 0.004447772540403811120 ),
 .UNSPECIFIED. ) ;
#21885=AXIS2_PLACEMENT_3D ( 'NONE', #43381, #33362, #4805 ) ;
#21887=CARTESIAN_POINT ( 'NONE',  ( 5.895596859100789899, 16.58392706178521792, -11.37987462241457948 ) ) ;
#21894=CARTESIAN_POINT ( 'NONE',  ( 0.5806925824938499181, -19.24316026636448029, -42.76591101925195204 ) ) ;
#21895=B_SPLINE_CURVE_WITH_KNOTS ( 'NONE', 3,
 ( #47608, #47296, #18484, #38534 ),
 .UNSPECIFIED., .F., .F.,
 ( 4, 4 ),
 ( 0.000000000000000000, 0.004447772540403798977 ),
 .UNSPECIFIED. ) ;
#21897=CARTESIAN_POINT ( 'NONE',  ( 0.9762797500689124330, -41.84568905980455611, -2.294143041716810050 ) ) ;
#21904=CARTESIAN_POINT ( 'NONE',  ( 4.960386119450145515, -37.88391031994010660, -21.89168343328299216 ) ) ;
#21905=ORIENTED_EDGE ( 'NONE', *, *, #61166, .F. ) ;
#21909=FACE_OUTER_BOUND ( 'NONE', #54734, .T. ) ;
#21911=ORIENTED_EDGE ( 'NONE', *, *, #29576, .T. ) ;
#21912=CARTESIAN_POINT ( 'NONE',  ( 0.7764139734771211554, 42.82684529576456356, 19.12855961434408059 ) ) ;
#21939=LINE ( 'NONE', #36986, #49735 ) ;
#21941=VERTEX_POINT ( 'NONE', #31365 ) ;
#21947=CARTESIAN_POINT ( 'NONE',  ( 0.5782707292762442330, -13.20261929687983837, -45.00474638756754331 ) ) ;
#21948=CARTESIAN_POINT ( 'NONE',  ( 0.9787284016396609054, 9.533035904949169748, -40.81001378784110045 ) ) ;
#21951=VERTEX_POINT ( 'NONE', #11976 ) ;
#21952=CARTESIAN_POINT ( 'NONE',  ( 5.896278296736517710, 19.00178995741550025, -6.592340861078650249 ) ) ;
#21954=CARTESIAN_POINT ( 'NONE',  ( 4.956445790443988031, 0.000000000000000000, 0.000000000000000000 ) ) ;
#21956=VECTOR ( 'NONE', #21017, 1000.000000000000227 ) ;
#21957=B_SPLINE_CURVE_WITH_KNOTS ( 'NONE', 3,
 ( #10245, #57828, #43470, #19652, #29339, #5510, #832, #30874, #21801, #54978, #27113, #40934, #2361, #12410, #55594, #59997, #12725, #22105, #35292 ),
 .UNSPECIFIED., .F., .F.,
 ( 4, 3, 3, 3, 3, 3, 4 ),
 ( 8.674294979774126656E-18, 0.0002732106629380623777, 0.0004098138914053778715, 0.0005464171197651505928, 0.0006830203481512616207, 0.0008196235766963705718, 0.001011968216111141594 ),
 .UNSPECIFIED. ) ;
#21960=CARTESIAN_POINT ( 'NONE',  ( 1.231276596079881047, 32.36747132271556637, 26.63876069172986405 ) ) ;
#21962=CARTESIAN_POINT ( 'NONE',  ( 0.5806925824938502512, -8.338382001837375768, -46.14860504863607105 ) ) ;
#21983=CARTESIAN_POINT ( 'NONE',  ( 0.5804410086790514622, 5.237717535875747288, -46.60564522533483256 ) ) ;
#21993=( BOUNDED_SURFACE ( )  B_SPLINE_SURFACE ( 3, 1, ( 
 ( #37557, #61017 ),
 ( #7782, #27513 ),
 ( #22209, #56011 ),
 ( #12510, #3380 ) ),
 .UNSPECIFIED., .F., .F., .F. ) 
 B_SPLINE_SURFACE_WITH_KNOTS ( ( 4, 4 ),
 ( 2, 2 ),
 ( 0.000000000000000000, 1.000000000000000000 ),
 ( 0.000000000000000000, 1.000000000000000000 ),
 .UNSPECIFIED. ) 
 GEOMETRIC_REPRESENTATION_ITEM ( )  RATIONAL_B_SPLINE_SURFACE ( (
 ( 1.000000000000000000, 1.000000000000000000),
 ( 0.7282232189291694135, 0.9929344683865672927),
 ( 0.7282232189291694135, 0.9929344683865672927),
 ( 1.000000000000000000, 1.000000000000000000) ) ) 
 REPRESENTATION_ITEM ( '' )  SURFACE ( )  );
#21998=CARTESIAN_POINT ( 'NONE',  ( 2.618530812446111078, -46.78761446237182753, -4.543778396737141456 ) ) ;
#22002=CARTESIAN_POINT ( 'NONE',  ( -4.467299999999993609, 0.000000000000000000, 0.000000000000000000 ) ) ;
#22005=CARTESIAN_POINT ( 'NONE',  ( 0.5806925824938502512, -25.69265091979982429, -39.23149310256842170 ) ) ;
#22011=SURFACE_SIDE_STYLE ('',( #2880 ) ) ;
#22012=EDGE_CURVE ( 'NONE', #20260, #14061, #23131, .T. ) ;
#22016=CARTESIAN_POINT ( 'NONE',  ( 5.895881250540457863, 0.6766202122111161232, -20.10148916614707559 ) ) ;
#22023=CARTESIAN_POINT ( 'NONE',  ( 0.5835226383429297226, 4.512830617619511209, -46.67844078761244475 ) ) ;
#22025=CARTESIAN_POINT ( 'NONE',  ( 4.962356264823603702, 12.05238263218972072, -40.32338863178092225 ) ) ;
#22026=CARTESIAN_POINT ( 'NONE',  ( 4.956445790444031552, 34.56007374686835476, -31.98654955994249960 ) ) ;
#22034=CARTESIAN_POINT ( 'NONE',  ( 0.9790850452238870627, -22.50762242264617541, 35.35172220900689410 ) ) ;
#22037=CARTESIAN_POINT ( 'NONE',  ( 0.9762797500689124330, -41.16654106227479559, 7.851158013551082782 ) ) ;
#22042=CARTESIAN_POINT ( 'NONE',  ( 1.000433927950263202, -11.78619540624106854, 40.21820825818511480 ) ) ;
#22043=CARTESIAN_POINT ( 'NONE',  ( 0.8560838555295158248, -18.91252766612255698, -42.92655508376930129 ) ) ;
#22056=ORIENTED_EDGE ( 'NONE', *, *, #6674, .T. ) ;
#22060=( BOUNDED_SURFACE ( )  B_SPLINE_SURFACE ( 3, 1, ( 
 ( #40066, #59113 ),
 ( #39434, #15922 ),
 ( #54404, #11526 ),
 ( #39127, #58186 ) ),
 .UNSPECIFIED., .F., .F., .F. ) 
 B_SPLINE_SURFACE_WITH_KNOTS ( ( 4, 4 ),
 ( 2, 2 ),
 ( 0.000000000000000000, 1.000000000000000000 ),
 ( 0.000000000000000000, 1.000000000000000000 ),
 .UNSPECIFIED. ) 
 GEOMETRIC_REPRESENTATION_ITEM ( )  RATIONAL_B_SPLINE_SURFACE ( (
 ( 1.000000000000000000, 1.000000000000000000),
 ( 0.7282232189291694135, 0.9929344683865672927),
 ( 0.7282232189291694135, 0.9929344683865672927),
 ( 1.000000000000000000, 1.000000000000000000) ) ) 
 REPRESENTATION_ITEM ( '' )  SURFACE ( )  );
#22061=DIRECTION ( 'NONE',  ( -1.000000000000000000, -0.000000000000000000, -0.000000000000000000 ) ) ;
#22067=EDGE_LOOP ( 'NONE', ( #16947, #15040, #61663, #17651 ) ) ;
#22075=CARTESIAN_POINT ( 'NONE',  ( 4.958415959904820980, 37.73202888843250236, -25.28829669600411023 ) ) ;
#22079=CARTESIAN_POINT ( 'NONE',  ( 3.661933894777868570, 9.064104546016615416, 46.15704901453876374 ) ) ;
#22084=ADVANCED_FACE ( 'NONE', ( #8784 ), #47306, .F. ) ;
#22087=EDGE_CURVE ( 'NONE', #32685, #29292, #44017, .T. ) ;
#22089=CARTESIAN_POINT ( 'NONE',  ( 0.5806925824938499181, -46.82446035038572063, 2.586943222941027631 ) ) ;
#22090=CARTESIAN_POINT ( 'NONE',  ( 0.7056313189692764443, 40.77721431583525913, 23.17255783460248963 ) ) ;
#22094=CARTESIAN_POINT ( 'NONE',  ( 5.895596859100789899, -4.666058297670421240, -19.56415301451173150 ) ) ;
#22097=CARTESIAN_POINT ( 'NONE',  ( 1.000110580585048092, -18.23585865330004552, 37.73421447372084714 ) ) ;
#22098=CARTESIAN_POINT ( 'NONE',  ( 0.5806925824938499181, -38.96949031362449745, 26.08833430941674436 ) ) ;
#22099=CARTESIAN_POINT ( 'NONE',  ( 0.5837800304671215690, -34.74999798522668470, -31.49087125193968717 ) ) ;
#22102=CARTESIAN_POINT ( 'NONE',  ( 0.9787464366903554369, -31.20010594550945981, 27.98012476525880032 ) ) ;
#22104=CARTESIAN_POINT ( 'NONE',  ( 5.896782393890504181, 17.94821721415871352, -9.076760749925545824 ) ) ;
#22105=CARTESIAN_POINT ( 'NONE',  ( 0.9769922540276030354, -7.405947219671726423, 41.24904242361952811 ) ) ;
#22107=CARTESIAN_POINT ( 'NONE',  ( 2.528190830796657629, -13.58807975251270861, 39.71924250023358383 ) ) ;
#22111=CARTESIAN_POINT ( 'NONE',  ( 0.5830081025819928708, -7.530652408779095808, 46.28737742279633238 ) ) ;
#22112=LINE ( 'NONE', #41240, #49784 ) ;
#22117=CARTESIAN_POINT ( 'NONE',  ( 0.9762797500689124330, 29.49606728235512776, 29.77090526101756751 ) ) ;
#22120=CARTESIAN_POINT ( 'NONE',  ( 4.958415959904816539, 33.34645430971464464, -30.84182126257697121 ) ) ;
#22139=CARTESIAN_POINT ( 'NONE',  ( 0.9762797500689124330, -22.12212327108638377, 35.59405072711678741 ) ) ;
#22142=CARTESIAN_POINT ( 'NONE',  ( 0.5326698147273788431, 0.000000000000000000, -41.88877248453276536 ) ) ;
#22148=FACE_OUTER_BOUND ( 'NONE', #48759, .T. ) ;
#22150=B_SPLINE_CURVE_WITH_KNOTS ( 'NONE', 3,
 ( #11493, #2688, #22120, #17124 ),
 .UNSPECIFIED., .F., .F.,
 ( 4, 4 ),
 ( 0.000000000000000000, 0.005004948556313797495 ),
 .UNSPECIFIED. ) ;
#22164=EDGE_LOOP ( 'NONE', ( #20426, #31622, #50744, #39972 ) ) ;
#22168=CARTESIAN_POINT ( 'NONE',  ( 0.9790320750461891652, 38.61669752663120647, -16.28151727201333188 ) ) ;
#22172=CARTESIAN_POINT ( 'NONE',  ( 5.896782393890504181, 20.06834277495334362, -1.337050913387380691 ) ) ;
#22174=ORIENTED_EDGE ( 'NONE', *, *, #24415, .T. ) ;
#22177=CARTESIAN_POINT ( 'NONE',  ( 0.7764146366350260786, -42.25777079059512431, -20.35488347986028046 ) ) ;
#22181=CARTESIAN_POINT ( 'NONE',  ( 3.661921753702003013, -45.68403764746661722, 11.20713290984310895 ) ) ;
#22183=FACE_OUTER_BOUND ( 'NONE', #17672, .T. ) ;
#22185=CARTESIAN_POINT ( 'NONE',  ( 0.5824936645240090805, 10.51679990701790679, 45.70158748617006239 ) ) ;
#22187=EDGE_CURVE ( 'NONE', #52958, #16350, #58284, .T. ) ;
#22189=CARTESIAN_POINT ( 'NONE',  ( 1.231276596079887931, -39.86997064245532840, -12.94844438486017779 ) ) ;
#22197=CARTESIAN_POINT ( 'NONE',  ( 0.9754292580325143458, -41.18084053248014698, 7.775978391330924389 ) ) ;
#22202=CARTESIAN_POINT ( 'NONE',  ( 4.956445790443988031, 0.000000000000000000, 0.000000000000000000 ) ) ;
#22207=B_SPLINE_CURVE_WITH_KNOTS ( 'NONE', 3,
 ( #27270, #12882, #17884, #55758, #32596, #56378, #47304, #42316, #37008, #4658, #42618, #51677, #18809, #56682, #13807, #27573 ),
 .UNSPECIFIED., .F., .F.,
 ( 4, 3, 3, 3, 3, 4 ),
 ( 1.250973872328959318E-17, 0.0002732102107931902706, 0.0004098135523333833229, 0.0005464168938825049969, 0.0008195847345945408416, 0.001092771384553101579 ),
 .UNSPECIFIED. ) ;
#22209=CARTESIAN_POINT ( 'NONE',  ( 5.910764540655178756, 16.59011036809707917, 11.36967354164229604 ) ) ;
#22210=ORIENTED_EDGE ( 'NONE', *, *, #561, .T. ) ;
#22217=CARTESIAN_POINT ( 'NONE',  ( 2.528190830796659405, -30.30926884989141712, -29.04483358427122752 ) ) ;
#22218=EDGE_CURVE ( 'NONE', #5679, #36885, #44271, .T. ) ;
#22221=CARTESIAN_POINT ( 'NONE',  ( 4.956445790443988031, 0.000000000000000000, 0.000000000000000000 ) ) ;
#22223=AXIS2_PLACEMENT_3D ( 'NONE', #32353, #57351, #60832 ) ;
#22224=ORIENTED_EDGE ( 'NONE', *, *, #61957, .T. ) ;
#22225=CARTESIAN_POINT ( 'NONE',  ( 3.782542959838393504, 40.96636395946045184, -9.433709627584986990 ) ) ;
#22228=CARTESIAN_POINT ( 'NONE',  ( 0.5804410086790514622, -38.35366574782019455, 26.99103880105172237 ) ) ;
#22229=AXIS2_PLACEMENT_3D ( 'NONE', #39714, #21196, #26505 ) ;
#22239=FACE_OUTER_BOUND ( 'NONE', #8866, .T. ) ;
#22242=( BOUNDED_SURFACE ( )  B_SPLINE_SURFACE ( 3, 1, ( 
 ( #39399, #38787 ),
 ( #29052, #43804 ),
 ( #24979, #48772 ),
 ( #14974, #29974 ) ),
 .UNSPECIFIED., .F., .F., .F. ) 
 B_SPLINE_SURFACE_WITH_KNOTS ( ( 4, 4 ),
 ( 2, 2 ),
 ( 0.000000000000000000, 1.000000000000000000 ),
 ( 0.000000000000000000, 1.000000000000000000 ),
 .UNSPECIFIED. ) 
 GEOMETRIC_REPRESENTATION_ITEM ( )  RATIONAL_B_SPLINE_SURFACE ( (
 ( 1.000000000000000000, 1.000000000000000000),
 ( 0.9729067724841187204, 0.9999501103223794596),
 ( 0.9729067724841187204, 0.9999501103223794596),
 ( 1.000000000000000000, 1.000000000000000000) ) ) 
 REPRESENTATION_ITEM ( '' )  SURFACE ( )  );
#22246=CARTESIAN_POINT ( 'NONE',  ( 0.5837799406558231707, -44.27132707568020464, 15.46910302943734372 ) ) ;
#22258=EDGE_CURVE ( 'NONE', #26853, #7974, #23277, .T. ) ;
#22259=ORIENTED_EDGE ( 'NONE', *, *, #2554, .F. ) ;
#22260=CARTESIAN_POINT ( 'NONE',  ( 5.895596859100789899, 19.00119700155561020, -6.594141014609973261 ) ) ;
#22261=CARTESIAN_POINT ( 'NONE',  ( 0.8554163680231816613, -18.91615390926536477, 42.93465493506153052 ) ) ;
#22265=CARTESIAN_POINT ( 'NONE',  ( 0.5848930533535030563, -45.92005787004959672, 9.519525597363298175 ) ) ;
#22270=CIRCLE ( 'NONE', #51267, 47.09074272231896430 ) ;
#22280=CARTESIAN_POINT ( 'NONE',  ( 0.9789889208857702751, -41.82137578286608459, -2.703225049948740910 ) ) ;
#22288=CARTESIAN_POINT ( 'NONE',  ( 0.5782707292762442330, 5.414380361654997031, -46.58777563918396680 ) ) ;
#22307=EDGE_CURVE ( 'NONE', #32810, #35884, #9855, .T. ) ;
#22312=CARTESIAN_POINT ( 'NONE',  ( 4.956445790443998689, 1.033212179477464909, 47.07940656732852602 ) ) ;
#22316=CARTESIAN_POINT ( 'NONE',  ( 4.956445790444002242, -36.61936279692601204, 29.60676136436992678 ) ) ;
#22323=CARTESIAN_POINT ( 'NONE',  ( 0.5804410086790514622, 45.08525424748444976, -12.91664435118819121 ) ) ;
#22324=B_SPLINE_CURVE_WITH_KNOTS ( 'NONE', 3,
 ( #46020, #8685, #27804, #3060 ),
 .UNSPECIFIED., .F., .F.,
 ( 4, 4 ),
 ( 3.469446951953613804E-18, 0.005004948556313820046 ),
 .UNSPECIFIED. ) ;
#22326=CARTESIAN_POINT ( 'NONE',  ( 0.9762797500689124330, 41.90547441298052433, 0.5059638413352746111 ) ) ;
#22329=DIRECTION ( 'NONE',  ( -1.000000000000000000, -0.000000000000000000, -0.000000000000000000 ) ) ;
#22330=CARTESIAN_POINT ( 'NONE',  ( 0.9780303403264750672, 33.08964503960959291, 25.71798990099589943 ) ) ;
#22331=CARTESIAN_POINT ( 'NONE',  ( 4.962356264823596597, 39.89814050050772920, 13.39305724859313429 ) ) ;
#22333=CARTESIAN_POINT ( 'NONE',  ( 0.5837800005270554760, -13.89417140152258234, -44.79048179811078967 ) ) ;
#22336=B_SPLINE_CURVE_WITH_KNOTS ( 'NONE', 3,
 ( #16486, #25884, #53144, #10251 ),
 .UNSPECIFIED., .F., .F.,
 ( 4, 4 ),
 ( 0.000000000000000000, 0.004446298630425058948 ),
 .UNSPECIFIED. ) ;
#22339=CARTESIAN_POINT ( 'NONE',  ( 0.5848930533535030563, -41.93775812029553407, -20.98803292905613205 ) ) ;
#22347=CARTESIAN_POINT ( 'NONE',  ( 4.956445790443988031, 0.000000000000000000, 0.000000000000000000 ) ) ;
#22350=ORIENTED_EDGE ( 'NONE', *, *, #55081, .T. ) ;
#22351=ORIENTED_EDGE ( 'NONE', *, *, #61664, .T. ) ;
#22353=CARTESIAN_POINT ( 'NONE',  ( 1.000433927950262536, 19.56092357721248831, -37.06465899558902777 ) ) ;
#22355=FACE_OUTER_BOUND ( 'NONE', #3018, .T. ) ;
#22362=EDGE_CURVE ( 'NONE', #56380, #49641, #54645, .T. ) ;
#22366=CARTESIAN_POINT ( 'NONE',  ( 3.661921753701995019, 47.00091123480373057, -1.882941032570424111 ) ) ;
#22367=ORIENTED_EDGE ( 'NONE', *, *, #21599, .T. ) ;
#22369=DIRECTION ( 'NONE',  ( 0.000000000000000000, 0.000000000000000000, 1.000000000000000000 ) ) ;
#22372=CARTESIAN_POINT ( 'NONE',  ( -69.95594261585601714, 0.000000000000000000, 0.000000000000000000 ) ) ;
#22375=EDGE_LOOP ( 'NONE', ( #34370, #38667, #35614, #57003 ) ) ;
#22378=CARTESIAN_POINT ( 'NONE',  ( 0.6845945791218034371, 42.84081778543538377, 19.10682737110132123 ) ) ;
#22380=CARTESIAN_POINT ( 'NONE',  ( 1.157643937452371041, -35.01838089395619846, -23.03725839071476145 ) ) ;
#22383=CARTESIAN_POINT ( 'NONE',  ( 0.8554163680231738898, 46.61139063278412209, -5.346376005279195986 ) ) ;
#22393=CARTESIAN_POINT ( 'NONE',  ( 0.9762797500689124330, 32.57381952463229169, 26.36799322592426975 ) ) ;
#22394=CARTESIAN_POINT ( 'NONE',  ( 4.962356264823596597, 1.841560470688234474, 42.04574000888969465 ) ) ;
#22404=B_SPLINE_CURVE_WITH_KNOTS ( 'NONE', 3,
 ( #53103, #1393, #10209, #53407 ),
 .UNSPECIFIED., .F., .F.,
 ( 4, 4 ),
 ( 2.194270917860438266E-17, 0.005004948556313820046 ),
 .UNSPECIFIED. ) ;
#22410=( BOUNDED_SURFACE ( )  B_SPLINE_SURFACE ( 3, 1, ( 
 ( #29917, #49027 ),
 ( #6078, #25217 ),
 ( #59026, #35256 ),
 ( #25835, #44972 ) ),
 .UNSPECIFIED., .F., .F., .F. ) 
 B_SPLINE_SURFACE_WITH_KNOTS ( ( 4, 4 ),
 ( 2, 2 ),
 ( 0.000000000000000000, 1.000000000000000000 ),
 ( 0.000000000000000000, 1.000000000000000000 ),
 .UNSPECIFIED. ) 
 GEOMETRIC_REPRESENTATION_ITEM ( )  RATIONAL_B_SPLINE_SURFACE ( (
 ( 1.000000000000000000, 1.000000000000000000),
 ( 0.9952954269826590483, 0.8620686068821339365),
 ( 0.9952954269826590483, 0.8620686068821339365),
 ( 1.000000000000000000, 1.000000000000000000) ) ) 
 REPRESENTATION_ITEM ( '' )  SURFACE ( )  );
#22417=LINE ( 'NONE', #35071, #18163 ) ;
#22418=CARTESIAN_POINT ( 'NONE',  ( 4.962356264823608143, 0.000000000000000000, 0.000000000000000000 ) ) ;
#22422=CARTESIAN_POINT ( 'NONE',  ( 0.5835871038041855474, -45.98328870143440383, 9.207150107499908032 ) ) ;
#22425=VERTEX_POINT ( 'NONE', #21585 ) ;
#22436=FACE_OUTER_BOUND ( 'NONE', #29815, .T. ) ;
#22454=ORIENTED_EDGE ( 'NONE', *, *, #9982, .F. ) ;
#22456=ORIENTED_EDGE ( 'NONE', *, *, #3371, .F. ) ;
#22460=CARTESIAN_POINT ( 'NONE',  ( 0.9790320750461898314, 24.79011560905074063, 33.79034330444261514 ) ) ;
#22463=CARTESIAN_POINT ( 'NONE',  ( 4.291220156522060236, -33.45801620160754908, 33.16549636532919010 ) ) ;
#22465=CARTESIAN_POINT ( 'NONE',  ( 1.091591847532192183, 29.69394621724348227, -29.58088147779393040 ) ) ;
#22470=CARTESIAN_POINT ( 'NONE',  ( 4.291220156522060236, 46.35409538318327094, -8.407546521574817078 ) ) ;
#22476=ORIENTED_EDGE ( 'NONE', *, *, #9134, .F. ) ;
#22483=CARTESIAN_POINT ( 'NONE',  ( 1.231276596079887931, -40.90292846002456173, 9.177538581350681568 ) ) ;
#22484=CARTESIAN_POINT ( 'NONE',  ( 5.917102823773431552, 17.95415397368191179, 9.063005745395072310 ) ) ;
#22490=CARTESIAN_POINT ( 'NONE',  ( 1.091591847532193293, 19.45518260472246652, 37.12485502695927408 ) ) ;
#22511=CARTESIAN_POINT ( 'NONE',  ( 5.896782393890504181, 10.81700609697876736, 16.95636948099257424 ) ) ;
#22514=FACE_OUTER_BOUND ( 'NONE', #14582, .T. ) ;
#22526=ORIENTED_EDGE ( 'NONE', *, *, #19402, .F. ) ;
#22533=EDGE_LOOP ( 'NONE', ( #16616, #49701, #33795, #44184 ) ) ;
#22546=CARTESIAN_POINT ( 'NONE',  ( 2.618530812446115519, -42.57172246446581454, -19.93427288883888338 ) ) ;
#22549=VERTEX_POINT ( 'NONE', #53082 ) ;
#22554=VERTEX_POINT ( 'NONE', #49615 ) ;
#22555=CARTESIAN_POINT ( 'NONE',  ( 2.528100132419516033, 35.48725650258067077, -22.42561937945352923 ) ) ;
#22561=CARTESIAN_POINT ( 'NONE',  ( 0.5817217712918333339, -41.64824464290960293, -21.55594285046991487 ) ) ;
#22562=CARTESIAN_POINT ( 'NONE',  ( 0.8560838555295223751, 37.37287335782406217, 28.34856559090382078 ) ) ;
#22563=EDGE_CURVE ( 'NONE', #47431, #50643, #14301, .T. ) ;
#22569=ADVANCED_FACE ( 'NONE', ( #14905 ), #38517, .T. ) ;
#22572=CARTESIAN_POINT ( 'NONE',  ( 0.5848930533535030563, -45.99261677209119625, -9.162547944928565613 ) ) ;
#22595=CARTESIAN_POINT ( 'NONE',  ( 3.661933894777896104, 41.39923993790886669, -22.33235539559372995 ) ) ;
#22599=VERTEX_POINT ( 'NONE', #36475 ) ;
#22605=( BOUNDED_SURFACE ( )  B_SPLINE_SURFACE ( 3, 1, ( 
 ( #60656, #17459 ),
 ( #41285, #31875 ),
 ( #13389, #55650 ),
 ( #3037, #3951 ) ),
 .UNSPECIFIED., .F., .F., .F. ) 
 B_SPLINE_SURFACE_WITH_KNOTS ( ( 4, 4 ),
 ( 2, 2 ),
 ( 0.000000000000000000, 1.000000000000000000 ),
 ( 0.000000000000000000, 1.000000000000000000 ),
 .UNSPECIFIED. ) 
 GEOMETRIC_REPRESENTATION_ITEM ( )  RATIONAL_B_SPLINE_SURFACE ( (
 ( 1.000000000000000000, 1.000000000000000000),
 ( 0.9729067724841187204, 0.9999501103223794596),
 ( 0.9729067724841187204, 0.9999501103223794596),
 ( 1.000000000000000000, 1.000000000000000000) ) ) 
 REPRESENTATION_ITEM ( '' )  SURFACE ( )  );
#22607=CARTESIAN_POINT ( 'NONE',  ( 3.782542959838398833, 8.059551392177747076, 41.25871404628865946 ) ) ;
#22618=CARTESIAN_POINT ( 'NONE',  ( 0.7056313189692702270, -25.94337377925174692, -39.07288063232081754 ) ) ;
#22620=VERTEX_POINT ( 'NONE', #54607 ) ;
#22625=AXIS2_PLACEMENT_3D ( 'NONE', #5540, #53471, #38188 ) ;
#22628=CARTESIAN_POINT ( 'NONE',  ( 0.9784957157296367836, -41.79884784847546797, 3.031398280062871375 ) ) ;
#22633=CARTESIAN_POINT ( 'NONE',  ( 4.962356264823608143, -41.65024625884313991, -6.040909239515997342 ) ) ;
#22636=ADVANCED_FACE ( 'NONE', ( #22355 ), #46981, .T. ) ;
#22660=VERTEX_POINT ( 'NONE', #59628 ) ;
#22664=EDGE_LOOP ( 'NONE', ( #32165, #48785, #33569, #19365 ) ) ;
#22672=VERTEX_POINT ( 'NONE', #26427 ) ;
#22687=ORIENTED_EDGE ( 'NONE', *, *, #44411, .T. ) ;
#22691=CARTESIAN_POINT ( 'NONE',  ( 0.8554163680231708922, 42.82911630180332452, 19.15391004255850405 ) ) ;
#22693=CARTESIAN_POINT ( 'NONE',  ( 2.528190830796656297, -37.99746236544471145, 17.84508307460686183 ) ) ;
#22695=CARTESIAN_POINT ( 'NONE',  ( 3.238018933889920792, -13.06836926121502707, 2.936872012904754747 ) ) ;
#22705=CARTESIAN_POINT ( 'NONE',  ( 5.901463166500145796, -17.31230476672938323, 10.23728352662539542 ) ) ;
#22707=CARTESIAN_POINT ( 'NONE',  ( 0.9787284016396609054, -1.587498718041325363, -41.87858458387827909 ) ) ;
#22708=CARTESIAN_POINT ( 'NONE',  ( 0.5797568599927135358, 11.48244781954172922, -45.46843631292489363 ) ) ;
#22709=ORIENTED_EDGE ( 'NONE', *, *, #5018, .F. ) ;
#22721=CARTESIAN_POINT ( 'NONE',  ( 0.5817217712918332229, -25.61649477199477332, 39.28142244884644896 ) ) ;
#22727=ORIENTED_EDGE ( 'NONE', *, *, #8754, .F. ) ;
#22730=LINE ( 'NONE', #50001, #54776 ) ;
#22733=CARTESIAN_POINT ( 'NONE',  ( 0.5817217712918331118, 22.13702057711616789, 41.34231819790357321 ) ) ;
#22742=CARTESIAN_POINT ( 'NONE',  ( 0.9785694773339259633, 33.02736108081276001, -25.79784537034606018 ) ) ;
#22751=ORIENTED_EDGE ( 'NONE', *, *, #35132, .T. ) ;
#22756=VERTEX_POINT ( 'NONE', #61463 ) ;
#22761=CARTESIAN_POINT ( 'NONE',  ( 4.956445790443998689, -4.175462451062247560, 46.90526157542890218 ) ) ;
#22771=CARTESIAN_POINT ( 'NONE',  ( 4.962356264823593044, 12.88441948660167391, 40.06528837230087703 ) ) ;
#22783=CARTESIAN_POINT ( 'NONE',  ( 0.8554163680231816613, -46.74230100997663584, 4.045092014349752851 ) ) ;
#22786=EDGE_CURVE ( 'NONE', #32724, #37323, #36971, .T. ) ;
#22790=CARTESIAN_POINT ( 'NONE',  ( 0.5848930533535030563, 40.44226001967956563, -23.74229742228383344 ) ) ;
#22793=CARTESIAN_POINT ( 'NONE',  ( 4.956445790443996913, 7.299064093730984304, 46.52162629890795387 ) ) ;
#22794=EDGE_CURVE ( 'NONE', #35559, #46325, #46365, .T. ) ;
#22805=CARTESIAN_POINT ( 'NONE',  ( 0.5848930533535030563, 40.44226001967923878, 23.74229742228440898 ) ) ;
#22812=CARTESIAN_POINT ( 'NONE',  ( 0.8560838555295223751, -38.14845555156087187, 27.29593693413575295 ) ) ;
#22817=CARTESIAN_POINT ( 'NONE',  ( 4.291220156522060236, -3.725477031302460329, -46.96285572870259273 ) ) ;
#22820=ORIENTED_EDGE ( 'NONE', *, *, #47061, .T. ) ;
#22824=CARTESIAN_POINT ( 'NONE',  ( 0.9762797500689124330, 20.58271139965541963, -36.50584578699964311 ) ) ;
#22829=LINE ( 'NONE', #61031, #11716 ) ;
#22843=CARTESIAN_POINT ( 'NONE',  ( -4.467299999999993609, 0.000000000000000000, 0.000000000000000000 ) ) ;
#22849=CARTESIAN_POINT ( 'NONE',  ( 5.895596859100789899, -19.39920506799832722, 5.310275505304355548 ) ) ;
#22856=DIRECTION ( 'NONE',  ( -1.000000000000000000, -0.000000000000000000, -0.000000000000000000 ) ) ;
#22860=AXIS2_PLACEMENT_3D ( 'NONE', #45094, #60682, #59453 ) ;
#22864=CARTESIAN_POINT ( 'NONE',  ( 1.157643937452368599, -16.89177053992790789, 38.36235606191540626 ) ) ;
#22866=B_SPLINE_CURVE_WITH_KNOTS ( 'NONE', 3,
 ( #44414, #7369, #1751, #30574, #20885, #35621 ),
 .UNSPECIFIED., .F., .F.,
 ( 4, 2, 4 ),
 ( 1.208227429106116496E-16, 0.0002448718616795937469, 0.0004897437233590666052 ),
 .UNSPECIFIED. ) ;
#22883=CARTESIAN_POINT ( 'NONE',  ( 3.238018933889920792, 9.111992562714036126, 9.817284955867229712 ) ) ;
#22884=B_SPLINE_CURVE_WITH_KNOTS ( 'NONE', 3,
 ( #3781, #16996, #36727, #54864 ),
 .UNSPECIFIED., .F., .F.,
 ( 4, 4 ),
 ( 1.301042606982605321E-18, 0.004041751736740994277 ),
 .UNSPECIFIED. ) ;
#22889=ORIENTED_EDGE ( 'NONE', *, *, #46774, .F. ) ;
#22896=( BOUNDED_SURFACE ( )  B_SPLINE_SURFACE ( 3, 1, ( 
 ( #53318, #48330 ),
 ( #43039, #47718 ),
 ( #701, #33937 ),
 ( #37725, #10117 ) ),
 .UNSPECIFIED., .F., .F., .F. ) 
 B_SPLINE_SURFACE_WITH_KNOTS ( ( 4, 4 ),
 ( 2, 2 ),
 ( 0.000000000000000000, 1.000000000000000000 ),
 ( 0.000000000000000000, 1.000000000000000000 ),
 .UNSPECIFIED. ) 
 GEOMETRIC_REPRESENTATION_ITEM ( )  RATIONAL_B_SPLINE_SURFACE ( (
 ( 1.000000000000000000, 1.000000000000000000),
 ( 0.7282232189291694135, 0.9929344683865672927),
 ( 0.7282232189291694135, 0.9929344683865672927),
 ( 1.000000000000000000, 1.000000000000000000) ) ) 
 REPRESENTATION_ITEM ( '' )  SURFACE ( )  );
#22898=CARTESIAN_POINT ( 'NONE',  ( 0.9790724872846782167, -41.81234597974636102, -2.839530533634436527 ) ) ;
#22905=ORIENTED_EDGE ( 'NONE', *, *, #5204, .T. ) ;
#22914=FACE_OUTER_BOUND ( 'NONE', #34724, .T. ) ;
#22922=EDGE_LOOP ( 'NONE', ( #12293, #55597, #26307, #57638 ) ) ;
#22924=DIRECTION ( 'NONE',  ( -1.000000000000000000, -0.000000000000000000, -0.000000000000000000 ) ) ;
#22927=CARTESIAN_POINT ( 'NONE',  ( 0.8560838555295223751, 46.89922841446243496, -0.9138972643637069959 ) ) ;
#22929=EDGE_CURVE ( 'NONE', #15738, #36038, #35935, .T. ) ;
#22931=CARTESIAN_POINT ( 'NONE',  ( 5.894904586330512508, 14.91761050190863003, -13.49052663816309661 ) ) ;
#22939=CARTESIAN_POINT ( 'NONE',  ( 0.5830081025819923157, 4.965830163467174430, 46.63231245788532675 ) ) ;
#22942=CARTESIAN_POINT ( 'NONE',  ( 0.5806925824938499181, -1.020860314012482561, -46.88475452172953339 ) ) ;
#22950=DIRECTION ( 'NONE',  ( -1.000000000000000000, -0.000000000000000000, -0.000000000000000000 ) ) ;
#22954=CARTESIAN_POINT ( 'NONE',  ( 0.9762797500689124330, -12.89881610234976961, 39.87411852747928265 ) ) ;
#22957=EDGE_CURVE ( 'NONE', #51700, #6891, #27710, .T. ) ;
#22962=CARTESIAN_POINT ( 'NONE',  ( 0.7056313189692764443, 42.84374994564657868, -19.08302215458729023 ) ) ;
#22963=EDGE_CURVE ( 'NONE', #44029, #15738, #26143, .T. ) ;
#22975=CARTESIAN_POINT ( 'NONE',  ( 1.231276596079881935, -39.31472542100197387, -14.54747868495734053 ) ) ;
#22976=( BOUNDED_SURFACE ( )  B_SPLINE_SURFACE ( 3, 1, ( 
 ( #32972, #61736 ),
 ( #37993, #33581 ),
 ( #52658, #57045 ),
 ( #52350, #42993 ) ),
 .UNSPECIFIED., .F., .F., .F. ) 
 B_SPLINE_SURFACE_WITH_KNOTS ( ( 4, 4 ),
 ( 2, 2 ),
 ( 0.000000000000000000, 1.000000000000000000 ),
 ( 0.000000000000000000, 1.000000000000000000 ),
 .UNSPECIFIED. ) 
 GEOMETRIC_REPRESENTATION_ITEM ( )  RATIONAL_B_SPLINE_SURFACE ( (
 ( 1.000000000000000000, 1.000000000000000000),
 ( 0.9729067724841187204, 0.9999501103223794596),
 ( 0.9729067724841187204, 0.9999501103223794596),
 ( 1.000000000000000000, 1.000000000000000000) ) ) 
 REPRESENTATION_ITEM ( '' )  SURFACE ( )  );
#22978=VECTOR ( 'NONE', #59240, 1000.000000000000114 ) ;
#22979=VERTEX_POINT ( 'NONE', #59199 ) ;
#22993=EDGE_CURVE ( 'NONE', #13851, #23055, #2275, .T. ) ;
#22997=ORIENTED_EDGE ( 'NONE', *, *, #55972, .T. ) ;
#23006=CARTESIAN_POINT ( 'NONE',  ( -69.95594261585600293, 0.000000000000000000, 0.000000000000000000 ) ) ;
#23007=VERTEX_POINT ( 'NONE', #50727 ) ;
#23009=CARTESIAN_POINT ( 'NONE',  ( 0.8560838555295223751, 16.00311602465208694, -44.09391240957481273 ) ) ;
#23032=B_SPLINE_CURVE_WITH_KNOTS ( 'NONE', 3,
 ( #46082, #41084, #16952, #50739, #36672, #17555 ),
 .UNSPECIFIED., .F., .F.,
 ( 4, 2, 4 ),
 ( 1.266058488688919593E-17, 0.0002448709889506565061, 0.0004897419779013003271 ),
 .UNSPECIFIED. ) ;
#23040=EDGE_CURVE ( 'NONE', #16730, #21951, #47140, .T. ) ;
#23048=LINE ( 'NONE', #42781, #3461 ) ;
#23050=ORIENTED_EDGE ( 'NONE', *, *, #53645, .T. ) ;
#23055=VERTEX_POINT ( 'NONE', #18787 ) ;
#23065=ORIENTED_EDGE ( 'NONE', *, *, #35663, .T. ) ;
#23067=CARTESIAN_POINT ( 'NONE',  ( 3.661933894777876120, -33.59527226767167463, -32.92398587979079849 ) ) ;
#23071=EDGE_CURVE ( 'NONE', #19824, #21951, #32892, .T. ) ;
#23072=CARTESIAN_POINT ( 'NONE',  ( 0.6064782688330857541, 46.37855233655766796, 6.954446748947744616 ) ) ;
#23092=ORIENTED_EDGE ( 'NONE', *, *, #20591, .T. ) ;
#23103=FACE_OUTER_BOUND ( 'NONE', #59273, .T. ) ;
#23104=CARTESIAN_POINT ( 'NONE',  ( 0.9790850452238870627, -27.01872131543053968, 32.03632358343099185 ) ) ;
#23112=CARTESIAN_POINT ( 'NONE',  ( 4.962356264823593044, 18.10963840443015016, 37.99048031708913697 ) ) ;
#23116=ORIENTED_EDGE ( 'NONE', *, *, #1228, .F. ) ;
#23120=CARTESIAN_POINT ( 'NONE',  ( 1.091591847532194626, -16.93206997590070628, -38.34141360574806612 ) ) ;
#23124=ORIENTED_EDGE ( 'NONE', *, *, #2787, .F. ) ;
#23131=B_SPLINE_CURVE_WITH_KNOTS ( 'NONE', 3,
 ( #50765, #12585, #50464, #17276 ),
 .UNSPECIFIED., .F., .F.,
 ( 4, 4 ),
 ( 6.992893892674702526E-18, 0.004042984057420977162 ),
 .UNSPECIFIED. ) ;
#23133=EDGE_LOOP ( 'NONE', ( #676, #11609, #24763, #17296 ) ) ;
#23144=CARTESIAN_POINT ( 'NONE',  ( 0.5832655196449137991, -7.575620595315191608, -46.28007298578045692 ) ) ;
#23147=CARTESIAN_POINT ( 'NONE',  ( 0.9789889208857702751, -7.065452030934339156, -41.30876766064238126 ) ) ;
#23148=EDGE_CURVE ( 'NONE', #16218, #35743, #35152, .T. ) ;
#23153=ORIENTED_EDGE ( 'NONE', *, *, #48397, .F. ) ;
#23154=FACE_OUTER_BOUND ( 'NONE', #60178, .T. ) ;
#23164=CIRCLE ( 'NONE', #3155, 42.08604991992415023 ) ;
#23166=( BOUNDED_SURFACE ( )  B_SPLINE_SURFACE ( 3, 1, ( 
 ( #54365, #26498 ),
 ( #45627, #40949 ),
 ( #34682, #2058 ),
 ( #10880, #49079 ) ),
 .UNSPECIFIED., .F., .F., .F. ) 
 B_SPLINE_SURFACE_WITH_KNOTS ( ( 4, 4 ),
 ( 2, 2 ),
 ( 0.000000000000000000, 1.000000000000000000 ),
 ( 0.000000000000000000, 1.000000000000000000 ),
 .UNSPECIFIED. ) 
 GEOMETRIC_REPRESENTATION_ITEM ( )  RATIONAL_B_SPLINE_SURFACE ( (
 ( 1.000000000000000000, 1.000000000000000000),
 ( 0.7282232189291694135, 0.9929344683865672927),
 ( 0.7282232189291694135, 0.9929344683865672927),
 ( 1.000000000000000000, 1.000000000000000000) ) ) 
 REPRESENTATION_ITEM ( '' )  SURFACE ( )  );
#23171=ORIENTED_EDGE ( 'NONE', *, *, #14953, .F. ) ;
#23184=FACE_OUTER_BOUND ( 'NONE', #50504, .T. ) ;
#23185=EDGE_CURVE ( 'NONE', #60457, #44492, #61311, .T. ) ;
#23191=CARTESIAN_POINT ( 'NONE',  ( 5.838029081930957709, 30.51096402024676024, 36.05753919374044614 ) ) ;
#23194=CARTESIAN_POINT ( 'NONE',  ( 0.9775691876210972353, 19.80844148971958774, 36.93182035505898853 ) ) ;
#23200=AXIS2_PLACEMENT_3D ( 'NONE', #5550, #53479, #43829 ) ;
#23203=ORIENTED_EDGE ( 'NONE', *, *, #34467, .F. ) ;
#23206=CARTESIAN_POINT ( 'NONE',  ( 0.8560838555295158248, 40.81790744942473737, -23.11430867518922128 ) ) ;
#23210=ORIENTED_EDGE ( 'NONE', *, *, #26544, .T. ) ;
#23215=FACE_OUTER_BOUND ( 'NONE', #46641, .T. ) ;
#23217=CARTESIAN_POINT ( 'NONE',  ( 0.5797568665920714848, 11.48244725320605042, 45.46843645518516297 ) ) ;
#23220=CARTESIAN_POINT ( 'NONE',  ( 0.5804410086790514622, -20.23572001627559303, -42.30881098870894874 ) ) ;
#23222=ORIENTED_EDGE ( 'NONE', *, *, #36166, .F. ) ;
#23223=CARTESIAN_POINT ( 'NONE',  ( 0.6845945791218034371, 46.36658412396714368, 7.109598961194799394 ) ) ;
#23225=CARTESIAN_POINT ( 'NONE',  ( 0.5804410086790514622, -42.10186154173687356, 20.66284362269179553 ) ) ;
#23226=CARTESIAN_POINT ( 'NONE',  ( 4.962356264823603702, 41.96072444189417183, -3.245489512195726789 ) ) ;
#23227=ORIENTED_EDGE ( 'NONE', *, *, #37519, .F. ) ;
#23228=CARTESIAN_POINT ( 'NONE',  ( 0.5804410086790514622, -2.113107284889295556, 46.85141011173457315 ) ) ;
#23229=EDGE_CURVE ( 'NONE', #13648, #50298, #48556, .T. ) ;
#23236=CARTESIAN_POINT ( 'NONE',  ( 5.896782393890504181, 12.99025607003319038, -15.35510775321938404 ) ) ;
#23239=CARTESIAN_POINT ( 'NONE',  ( 0.9762797500689124330, -34.83496347773922963, -23.29914386174477059 ) ) ;
#23243=ORIENTED_EDGE ( 'NONE', *, *, #330, .T. ) ;
#23245=CARTESIAN_POINT ( 'NONE',  ( 0.9772918015221170318, -41.78532364903834662, 3.213033348067860562 ) ) ;
#23248=CIRCLE ( 'NONE', #22223, 42.08604991992415023 ) ;
#23259=CARTESIAN_POINT ( 'NONE',  ( 1.231276596079881047, 38.25526645152027072, 17.14092645516147684 ) ) ;
#23260=CARTESIAN_POINT ( 'NONE',  ( 1.231276596079881047, -23.26513148155264332, 34.87134107206281186 ) ) ;
#23262=EDGE_CURVE ( 'NONE', #40345, #39908, #41940, .T. ) ;
#23277=B_SPLINE_CURVE_WITH_KNOTS ( 'NONE', 3,
 ( #58536, #48850, #15665, #34767 ),
 .UNSPECIFIED., .F., .F.,
 ( 4, 4 ),
 ( 4.443059973708341306E-17, 0.005004948556313850404 ),
 .UNSPECIFIED. ) ;
#23284=CARTESIAN_POINT ( 'NONE',  ( 0.7056313189692712262, 3.855069639226469391, -46.74277572025726357 ) ) ;
#23288=CARTESIAN_POINT ( 'NONE',  ( 3.238018933889920792, 10.33920672294413912, -8.515180368487779816 ) ) ;
#23290=CARTESIAN_POINT ( 'NONE',  ( 0.8554163680231738898, 9.985124899324343772, 45.84215040611328362 ) ) ;
#23292=AXIS2_PLACEMENT_3D ( 'NONE', #2281, #12041, #31115 ) ;
#23295=CARTESIAN_POINT ( 'NONE',  ( 0.9784957157296367836, -39.51281881580939626, 13.96675360351822981 ) ) ;
#23310=B_SPLINE_CURVE_WITH_KNOTS ( 'NONE', 3,
 ( #32322, #51398, #27303, #3785, #17300, #22927 ),
 .UNSPECIFIED., .F., .F.,
 ( 4, 2, 4 ),
 ( 9.553906862710701093E-18, 0.0002448709889506563977, 0.0004897419779013032545 ),
 .UNSPECIFIED. ) ;
#23315=CARTESIAN_POINT ( 'NONE',  ( 4.291220156522059348, 46.35409538318315015, 8.407546521575474330 ) ) ;
#23322=CARTESIAN_POINT ( 'NONE',  ( 5.896278296736517710, -9.670675947512847870, -17.63533402951529538 ) ) ;
#23324=CARTESIAN_POINT ( 'NONE',  ( 0.5804410086790514622, -44.48029469925780433, -14.86685021524652228 ) ) ;
#23329=CARTESIAN_POINT ( 'NONE',  ( 5.838029081930955932, -4.747847248974867540, 46.99492530745549601 ) ) ;
#23331=FACE_OUTER_BOUND ( 'NONE', #57735, .T. ) ;
#23343=CARTESIAN_POINT ( 'NONE',  ( 0.8560838555295158248, -44.60403252362548443, 14.52078223488980768 ) ) ;
#23352=EDGE_CURVE ( 'NONE', #13765, #49641, #45077, .T. ) ;
#23354=ORIENTED_EDGE ( 'NONE', *, *, #56476, .T. ) ;
#23355=DIRECTION ( 'NONE',  ( 0.000000000000000000, 0.000000000000000000, 1.000000000000000000 ) ) ;
#23367=CARTESIAN_POINT ( 'NONE',  ( 5.896782393890504181, 5.965008392936887560, 19.20793486427431418 ) ) ;
#23369=CARTESIAN_POINT ( 'NONE',  ( 4.962356264823608143, 18.10963840443066530, -37.99048031708887407 ) ) ;
#23372=CARTESIAN_POINT ( 'NONE',  ( 0.9788927965476044157, -37.46797425825765515, -18.77465093188997969 ) ) ;
#23374=CARTESIAN_POINT ( 'NONE',  ( 0.9789233960466710016, 4.325698577799566458, -41.68483007817547303 ) ) ;
#23377=ORIENTED_EDGE ( 'NONE', *, *, #20591, .F. ) ;
#23381=DIRECTION ( 'NONE',  ( 0.000000000000000000, 0.000000000000000000, 1.000000000000000000 ) ) ;
#23383=ORIENTED_EDGE ( 'NONE', *, *, #38525, .F. ) ;
#23387=CARTESIAN_POINT ( 'NONE',  ( 0.5830081025819919827, 28.03721062606959791, 37.59184558772897589 ) ) ;
#23388=B_SPLINE_CURVE_WITH_KNOTS ( 'NONE', 3,
 ( #24720, #5885, #1205, #39460 ),
 .UNSPECIFIED., .F., .F.,
 ( 4, 4 ),
 ( 2.860979249076398407E-17, 0.005004948556313843465 ),
 .UNSPECIFIED. ) ;
#23391=CARTESIAN_POINT ( 'NONE',  ( 0.8554163680231738898, -2.480940174720807079, 46.85136507041471532 ) ) ;
#23402=CARTESIAN_POINT ( 'NONE',  ( 0.5797568599927143129, 40.02504816884456318, 24.43810196706526838 ) ) ;
#23412=CARTESIAN_POINT ( 'NONE',  ( 4.960386119450141962, -30.07757850721755588, 31.77696863790668758 ) ) ;
#23415=ADVANCED_FACE ( 'NONE', ( #55971 ), #53677, .F. ) ;
#23417=CARTESIAN_POINT ( 'NONE',  ( 4.962356264823608143, 0.000000000000000000, 0.000000000000000000 ) ) ;
#23421=CARTESIAN_POINT ( 'NONE',  ( 0.5806925824938499181, 27.37593026015182218, 38.07598724570208049 ) ) ;
#23423=CARTESIAN_POINT ( 'NONE',  ( 0.8560838555295223751, 23.34035564869547841, 40.68907263964295851 ) ) ;
#23424=CARTESIAN_POINT ( 'NONE',  ( 0.5837800304671215690, 46.47150964378750615, 6.295722643737187596 ) ) ;
#23430=CARTESIAN_POINT ( 'NONE',  ( 5.895881250540457863, 10.81854556178467242, 16.95543433639758391 ) ) ;
#23435=CARTESIAN_POINT ( 'NONE',  ( 5.896278296736517710, -19.39967646272022961, -5.308439766651063429 ) ) ;
#23446=CARTESIAN_POINT ( 'NONE',  ( 5.896278296736517710, 12.98123568145678774, 15.36276341667920420 ) ) ;
#23450=CARTESIAN_POINT ( 'NONE',  ( 3.782625744892851749, 42.00313906590235291, -1.724648574484051622 ) ) ;
#23452=ORIENTED_EDGE ( 'NONE', *, *, #57592, .T. ) ;
#23454=CARTESIAN_POINT ( 'NONE',  ( 1.157643937452369487, 28.54093992520408563, -30.69881142293044718 ) ) ;
#23455=CARTESIAN_POINT ( 'NONE',  ( 0.6845945791218023269, -24.50629722879055450, 39.99809891542494000 ) ) ;
#23457=VERTEX_POINT ( 'NONE', #14020 ) ;
#23473=CIRCLE ( 'NONE', #24457, 42.08604991992415023 ) ;
#23479=DIRECTION ( 'NONE',  ( -0.07500201931887529039, 0.8510178133413054402, -0.5197531899602676475 ) ) ;
#23487=VECTOR ( 'NONE', #60292, 1000.000000000000000 ) ;
#23488=B_SPLINE_CURVE_WITH_KNOTS ( 'NONE', 3,
 ( #47021, #57291, #4055, #13498 ),
 .UNSPECIFIED., .F., .F.,
 ( 4, 4 ),
 ( 2.168404344971008868E-19, 0.004041751736740988206 ),
 .UNSPECIFIED. ) ;
#23492=CARTESIAN_POINT ( 'NONE',  ( 0.8560838555295223751, -29.58154842764516701, 36.40473632241573654 ) ) ;
#23493=B_SPLINE_CURVE_WITH_KNOTS ( 'NONE', 3,
 ( #15469, #29244, #6028, #34580 ),
 .UNSPECIFIED., .F., .F.,
 ( 4, 4 ),
 ( 0.000000000000000000, 0.004042984057420971958 ),
 .UNSPECIFIED. ) ;
#23495=CARTESIAN_POINT ( 'NONE',  ( 4.958415959904820092, -16.79601473596521544, -42.20305489904586693 ) ) ;
#23498=CARTESIAN_POINT ( 'NONE',  ( 0.8554163680231720024, -45.78608427674281955, 10.23913862172123679 ) ) ;
#23499=CARTESIAN_POINT ( 'NONE',  ( 5.896782393890504181, -15.78847575145207038, -12.45994062280484016 ) ) ;
#23503=CARTESIAN_POINT ( 'NONE',  ( 0.5837157313716038187, -45.93808755675273403, -9.430226678619181513 ) ) ;
#23505=ORIENTED_EDGE ( 'NONE', *, *, #7847, .T. ) ;
#23522=CARTESIAN_POINT ( 'NONE',  ( 0.5848930533535030563, -41.77346544155656005, 21.31315714272848538 ) ) ;
#23523=CARTESIAN_POINT ( 'NONE',  ( 0.5837800005270540327, 16.85481827636133545, 43.76243091411424047 ) ) ;
#23533=CARTESIAN_POINT ( 'NONE',  ( 3.661933894777871679, -21.49232232567767653, 41.84150147880487225 ) ) ;
#23541=CARTESIAN_POINT ( 'NONE',  ( 0.5817216825391118284, -2.022013777143747859, -46.85238961347116060 ) ) ;
#23545=CARTESIAN_POINT ( 'NONE',  ( 3.782542959838396168, -41.79414908755126135, -4.526251809622206856 ) ) ;
#23553=CIRCLE ( 'NONE', #60518, 42.08604991992415023 ) ;
#23554=CARTESIAN_POINT ( 'NONE',  ( 0.5837800005270556980, 40.34938032117881335, -23.89901182766041643 ) ) ;
#23559=DIRECTION ( 'NONE',  ( 0.000000000000000000, 0.000000000000000000, 1.000000000000000000 ) ) ;
#23562=CARTESIAN_POINT ( 'NONE',  ( 0.5804410086790514622, 17.36461428077188174, -43.56592731407666008 ) ) ;
#23563=EDGE_CURVE ( 'NONE', #4858, #42220, #38442, .T. ) ;
#23570=CARTESIAN_POINT ( 'NONE',  ( 0.5797568599927146460, -19.16764036586056363, -42.79984662911815008 ) ) ;
#23571=CARTESIAN_POINT ( 'NONE',  ( 5.896782393890504181, -2.019528367549316084, -20.01118667272572793 ) ) ;
#23575=CARTESIAN_POINT ( 'NONE',  ( 0.5804410086790514622, 36.46521478791906645, 29.49250688439903811 ) ) ;
#23579=ORIENTED_EDGE ( 'NONE', *, *, #41689, .T. ) ;
#23584=CARTESIAN_POINT ( 'NONE',  ( 0.9762797500689124330, 25.26481495167865532, 33.43671500974846822 ) ) ;
#23594=CARTESIAN_POINT ( 'NONE',  ( 0.9790850452238870627, -39.57319415496242243, 13.79491336097644805 ) ) ;
#23598=CARTESIAN_POINT ( 'NONE',  ( 3.376099380956838925, 5.244649644334623773, -12.33701883520681974 ) ) ;
#23602=DIRECTION ( 'NONE',  ( -1.000000000000000000, -0.000000000000000000, -0.000000000000000000 ) ) ;
#23606=ADVANCED_FACE ( 'NONE', ( #49974 ), #21330, .F. ) ;
#23607=AXIS2_PLACEMENT_3D ( 'NONE', #47999, #44246, #53587 ) ;
#23610=CARTESIAN_POINT ( 'NONE',  ( 0.5806925824938499181, 46.54710689580866756, -5.708695295225145294 ) ) ;
#23612=CARTESIAN_POINT ( 'NONE',  ( 0.8554163680231816613, -44.61245466728215092, -14.52357950615188997 ) ) ;
#23620=EDGE_LOOP ( 'NONE', ( #11998, #52864, #55257, #20365 ) ) ;
#23654=CARTESIAN_POINT ( 'NONE',  ( 5.901463166500146684, 5.945065151443822415, -19.21390305705025270 ) ) ;
#23658=EDGE_LOOP ( 'NONE', ( #26044, #36485, #19381, #36696 ) ) ;
#23664=ORIENTED_EDGE ( 'NONE', *, *, #36444, .T. ) ;
#23666=VECTOR ( 'NONE', #42012, 1000.000000000000114 ) ;
#23669=DIRECTION ( 'NONE',  ( -1.000000000000000000, -0.000000000000000000, -0.000000000000000000 ) ) ;
#23677=CARTESIAN_POINT ( 'NONE',  ( 0.7056313189692706711, -0.7243877018920470423, 46.89588368305800259 ) ) ;
#23680=EDGE_CURVE ( 'NONE', #8101, #32248, #8952, .T. ) ;
#23684=CARTESIAN_POINT ( 'NONE',  ( 5.896278296736517710, 5.964180709076918774, -19.20821511967883310 ) ) ;
#23687=VERTEX_POINT ( 'NONE', #17093 ) ;
#23693=CARTESIAN_POINT ( 'NONE',  ( 0.9762797500689124330, -18.09842611962761083, -37.79909730639192844 ) ) ;
#23698=EDGE_CURVE ( 'NONE', #45872, #12531, #53748, .T. ) ;
#23705=DIRECTION ( 'NONE',  ( -1.000000000000000000, -0.000000000000000000, -0.000000000000000000 ) ) ;
#23715=CARTESIAN_POINT ( 'NONE',  ( 0.6064515330803560422, 16.19003797393982680, -44.01382744592287111 ) ) ;
#23717=CARTESIAN_POINT ( 'NONE',  ( 5.896782393890504181, 14.92098591823861220, 13.48666994130638663 ) ) ;
#23720=CARTESIAN_POINT ( 'NONE',  ( 4.962356264823608143, 0.000000000000000000, 0.000000000000000000 ) ) ;
#23724=CARTESIAN_POINT ( 'NONE',  ( 0.5806925824938502512, 11.40214825760292250, 45.48860711711456872 ) ) ;
#23732=DIRECTION ( 'NONE',  ( 0.000000000000000000, 0.000000000000000000, 1.000000000000000000 ) ) ;
#23734=CARTESIAN_POINT ( 'NONE',  ( 1.231276596079881047, -41.87427716283725943, 1.954912557623087022 ) ) ;
#23746=CARTESIAN_POINT ( 'NONE',  ( 3.238018933889920792, 7.722174679335471303, -10.94419986063316763 ) ) ;
#23747=EDGE_LOOP ( 'NONE', ( #47633, #1295, #58452, #30748 ) ) ;
#23749=ORIENTED_EDGE ( 'NONE', *, *, #59109, .F. ) ;
#23760=CARTESIAN_POINT ( 'NONE',  ( 0.6064515330803558202, -39.06165493752520490, -25.95229179819768106 ) ) ;
#23761=VERTEX_POINT ( 'NONE', #28627 ) ;
#23764=ORIENTED_EDGE ( 'NONE', *, *, #5421, .T. ) ;
#23765=FACE_BOUND ( 'NONE', #30585, .T. ) ;
#23766=CARTESIAN_POINT ( 'NONE',  ( 0.9790724872846766624, -37.42248053063311630, 18.86513082159360621 ) ) ;
#23771=EDGE_CURVE ( 'NONE', #61953, #1809, #105, .T. ) ;
#23784=ADVANCED_FACE ( 'NONE', ( #24555 ), #8494, .F. ) ;
#23790=CARTESIAN_POINT ( 'NONE',  ( 0.9780303403264775097, -41.00319591444414868, 8.664729551278226083 ) ) ;
#23802=CONICAL_SURFACE ( 'NONE', #4752, 42.08604991992415023, 1.569615340895231137 ) ;
#23803=DIRECTION ( 'NONE',  ( 0.07500201931887538753, 0.5251354798924551259, 0.8477071574878980442 ) ) ;
#23804=CARTESIAN_POINT ( 'NONE',  ( 3.376099380956842921, 8.983142335927920996, -9.950454130567432998 ) ) ;
#23814=CARTESIAN_POINT ( 'NONE',  ( 0.5797568665920719289, 42.92520464323349927, -18.88523536889057652 ) ) ;
#23815=ORIENTED_EDGE ( 'NONE', *, *, #12396, .F. ) ;
#23817=CARTESIAN_POINT ( 'NONE',  ( 2.618530812446111078, 36.00211569111120014, 30.22539420689239975 ) ) ;
#23823=ORIENTED_EDGE ( 'NONE', *, *, #4363, .T. ) ;
#23830=CARTESIAN_POINT ( 'NONE',  ( 1.231276596079881047, -6.136529359146127405, -41.46829847537036784 ) ) ;
#23833=CARTESIAN_POINT ( 'NONE',  ( 0.8554163680231816613, 31.95314001164609152, -34.35407277904558043 ) ) ;
#23836=CARTESIAN_POINT ( 'NONE',  ( 0.5824935313925959646, 40.53383721374637361, 23.58487264717254561 ) ) ;
#23843=ORIENTED_EDGE ( 'NONE', *, *, #8623, .F. ) ;
#23865=CARTESIAN_POINT ( 'NONE',  ( 5.896782393890504181, 20.06749419425504399, -1.349727247095607430 ) ) ;
#23867=CARTESIAN_POINT ( 'NONE',  ( 0.8560838555295223751, 23.34035564869547841, 40.68907263964295851 ) ) ;
#23871=CARTESIAN_POINT ( 'NONE',  ( 0.5817217712918331118, 40.57952311434399206, -23.50611107394829702 ) ) ;
#23877=CARTESIAN_POINT ( 'NONE',  ( 3.376099380956842921, -12.80728341440181595, -3.960034744197991508 ) ) ;
#23886=CARTESIAN_POINT ( 'NONE',  ( 0.7056759521544966329, -18.97452373679281479, -42.89191390086098465 ) ) ;
#23887=CARTESIAN_POINT ( 'NONE',  ( 4.956445790443988031, 0.000000000000000000, 0.000000000000000000 ) ) ;
#23909=ORIENTED_EDGE ( 'NONE', *, *, #40293, .T. ) ;
#23912=FACE_OUTER_BOUND ( 'NONE', #44375, .T. ) ;
#23916=DIRECTION ( 'NONE',  ( 0.07500201931887538753, -0.1132404149163173945, 0.9907327114452572081 ) ) ;
#23917=DIRECTION ( 'NONE',  ( 0.000000000000000000, 0.000000000000000000, 1.000000000000000000 ) ) ;
#23930=VECTOR ( 'NONE', #43612, 1000.000000000000000 ) ;
#23943=CARTESIAN_POINT ( 'NONE',  ( 5.895596859100789899, 12.98270243688412329, 15.36156309259609642 ) ) ;
#23950=CARTESIAN_POINT ( 'NONE',  ( 0.7764139734771269286, -45.77880932777608791, -10.21474852544046463 ) ) ;
#23958=CARTESIAN_POINT ( 'NONE',  ( 0.5797568665920713737, 10.25842449096921172, -45.76013587791182857 ) ) ;
#23961=ORIENTED_EDGE ( 'NONE', *, *, #35863, .F. ) ;
#23970=CARTESIAN_POINT ( 'NONE',  ( 0.5835226383429304997, -45.91973687464727050, 9.519466366825529491 ) ) ;
#23971=CARTESIAN_POINT ( 'NONE',  ( 5.896782393890504181, -19.39652907507979052, 5.319844614046219000 ) ) ;
#23972=EDGE_CURVE ( 'NONE', #48721, #7149, #39479, .T. ) ;
#23986=EDGE_CURVE ( 'NONE', #7311, #37701, #13478, .T. ) ;
#23987=CARTESIAN_POINT ( 'NONE',  ( 0.5797568599927143129, 5.319646101103417735, -46.59320416144418431 ) ) ;
#23997=CARTESIAN_POINT ( 'NONE',  ( 0.8560838555295223751, 11.76118766017263972, 45.40977096290989579 ) ) ;
#24000=ORIENTED_EDGE ( 'NONE', *, *, #1934, .F. ) ;
#24006=CARTESIAN_POINT ( 'NONE',  ( 5.901463166500146684, 0.6576072425842132141, -20.10187610784469570 ) ) ;
#24013=B_SPLINE_CURVE_WITH_KNOTS ( 'NONE', 3,
 ( #24651, #48154, #48757, #19654, #5211, #19343 ),
 .UNSPECIFIED., .F., .F.,
 ( 4, 2, 4 ),
 ( 3.476216610979977084E-18, 0.0002291459268755711835, 0.0004582918537511388975 ),
 .UNSPECIFIED. ) ;
#24016=ORIENTED_EDGE ( 'NONE', *, *, #60873, .F. ) ;
#24021=LINE ( 'NONE', #57818, #7914 ) ;
#24025=CARTESIAN_POINT ( 'NONE',  ( 0.9754292589017201642, -6.395579240694774015, 41.41767778462806149 ) ) ;
#24029=CARTESIAN_POINT ( 'NONE',  ( 0.5824935313925952984, 11.22545165556063651, 45.53270705967863563 ) ) ;
#24046=EDGE_CURVE ( 'NONE', #15772, #38898, #58853, .T. ) ;
#24047=B_SPLINE_CURVE_WITH_KNOTS ( 'NONE', 3,
 ( #46542, #23958, #28341, #18971, #52444, #47771 ),
 .UNSPECIFIED., .F., .F.,
 ( 4, 2, 4 ),
 ( 8.805430561888389713E-18, 0.0002448709889506572109, 0.0004897419779013056397 ),
 .UNSPECIFIED. ) ;
#24049=EDGE_CURVE ( 'NONE', #33545, #60706, #5881, .T. ) ;
#24050=CARTESIAN_POINT ( 'NONE',  ( 0.8560838555295223751, 42.82099363437819051, -19.15033519931896322 ) ) ;
#24051=EDGE_LOOP ( 'NONE', ( #29854, #25925, #9170, #3002 ) ) ;
#24053=CARTESIAN_POINT ( 'NONE',  ( 0.5824935313925941882, 43.31572943909446138, 17.97180458977351236 ) ) ;
#24055=ORIENTED_EDGE ( 'NONE', *, *, #33765, .F. ) ;
#24058=ORIENTED_EDGE ( 'NONE', *, *, #31213, .F. ) ;
#24060=B_SPLINE_CURVE_WITH_KNOTS ( 'NONE', 3,
 ( #27251, #26016, #22555, #45151 ),
 .UNSPECIFIED., .F., .F.,
 ( 4, 4 ),
 ( 2.602085213965210642E-18, 0.004042984057420973693 ),
 .UNSPECIFIED. ) ;
#24065=CARTESIAN_POINT ( 'NONE',  ( 0.6845945791218023269, -44.58955076018944652, -14.56634764511800562 ) ) ;
#24066=CARTESIAN_POINT ( 'NONE',  ( 0.9789889208857693870, 40.44490217462196568, 10.97928896275300659 ) ) ;
#24075=CARTESIAN_POINT ( 'NONE',  ( 5.901463166500146684, 8.452982876530629852, -18.25006714589610723 ) ) ;
#24081=CARTESIAN_POINT ( 'NONE',  ( 2.618530812446111078, -31.41152511854616947, 34.97202995145038074 ) ) ;
#24082=DIRECTION ( 'NONE',  ( 0.07906939808003034253, -0.09174470402933210256, -0.9926383730089382018 ) ) ;
#24083=ADVANCED_FACE ( 'NONE', ( #4965 ), #15002, .T. ) ;
#24084=ORIENTED_EDGE ( 'NONE', *, *, #22258, .T. ) ;
#24087=CARTESIAN_POINT ( 'NONE',  ( 3.376099380956838925, 8.983142335927780664, 9.950454130567566224 ) ) ;
#24111=CARTESIAN_POINT ( 'NONE',  ( 0.8560838555295223751, 46.35895890951135812, -7.156798369939577853 ) ) ;
#24123=CARTESIAN_POINT ( 'NONE',  ( 0.9754292580325133466, 25.32584952646948651, -33.39054975088954080 ) ) ;
#24131=ORIENTED_EDGE ( 'NONE', *, *, #49956, .T. ) ;
#24136=CARTESIAN_POINT ( 'NONE',  ( 0.5817217712918331118, 40.11546086164733538, 24.28960176425324846 ) ) ;
#24145=ORIENTED_EDGE ( 'NONE', *, *, #33567, .T. ) ;
#24146=CARTESIAN_POINT ( 'NONE',  ( 0.5806925824938511393, 42.95845041307772050, -18.80940989108128747 ) ) ;
#24148=DIRECTION ( 'NONE',  ( 0.07500201931887538753, 0.4074616462826469721, 0.9101371896075481915 ) ) ;
#24149=B_SPLINE_CURVE_WITH_KNOTS ( 'NONE', 3,
 ( #54572, #60211, #40530, #6639, #54262, #59287 ),
 .UNSPECIFIED., .F., .F.,
 ( 4, 2, 4 ),
 ( 1.137877798855602457E-16, 0.0002448718616795915784, 0.0004897437233590694241 ),
 .UNSPECIFIED. ) ;
#24152=EDGE_LOOP ( 'NONE', ( #2608, #5005, #1230, #46366 ) ) ;
#24155=CARTESIAN_POINT ( 'NONE',  ( 3.661933894777871679, -42.79842724482195138, 19.51732026486564564 ) ) ;
#24165=B_SPLINE_CURVE_WITH_KNOTS ( 'NONE', 3,
 ( #15142, #61791, #24524, #10438, #34249, #53325 ),
 .UNSPECIFIED., .F., .F.,
 ( 4, 2, 4 ),
 ( 1.196073045797343302E-16, 0.0002448718616795927711, 0.0004897437233590659546 ),
 .UNSPECIFIED. ) ;
#24168=CARTESIAN_POINT ( 'NONE',  ( 0.7056313189692711152, 46.58785579558880841, 5.414825604484328814 ) ) ;
#24172=CARTESIAN_POINT ( 'NONE',  ( 5.901463166500146684, -13.97174733644476419, 14.46748584610281263 ) ) ;
#24173=CONICAL_SURFACE ( 'NONE', #23200, 42.08604991992415023, 1.569615340895231137 ) ;
#24174=CARTESIAN_POINT ( 'NONE',  ( 0.5806925824938499181, -2.112975627976999782, 46.84824112321762613 ) ) ;
#24178=EDGE_CURVE ( 'NONE', #41399, #46288, #32041, .T. ) ;
#24179=CARTESIAN_POINT ( 'NONE',  ( 0.6064782688330856431, -13.21402945353875857, -44.99693180673298087 ) ) ;
#24195=VERTEX_POINT ( 'NONE', #49438 ) ;
#24222=CARTESIAN_POINT ( 'NONE',  ( 0.5824935313925962976, 36.57712202577805272, -29.34880442820758972 ) ) ;
#24223=EDGE_CURVE ( 'NONE', #60467, #18665, #45086, .T. ) ;
#24226=CARTESIAN_POINT ( 'NONE',  ( 1.000433927950263646, -34.92054925016447697, -23.17269767894281074 ) ) ;
#24228=CARTESIAN_POINT ( 'NONE',  ( 3.782542959838394392, 41.85823152591767382, -3.889255316797903372 ) ) ;
#24229=CARTESIAN_POINT ( 'NONE',  ( 1.157643937452368155, 41.90847803242347425, -0.8256776614597129971 ) ) ;
#24230=ORIENTED_EDGE ( 'NONE', *, *, #39177, .T. ) ;
#24232=CARTESIAN_POINT ( 'NONE',  ( 1.231276596079887264, 33.41651732065550817, 25.31033664684050777 ) ) ;
#24234=FACE_OUTER_BOUND ( 'NONE', #35438, .T. ) ;
#24235=CARTESIAN_POINT ( 'NONE',  ( 0.8560838555295223751, -41.44626783305086093, 21.96769712083507287 ) ) ;
#24236=CARTESIAN_POINT ( 'NONE',  ( 0.7056313189692705601, -20.50398842223628648, -42.18216569521248971 ) ) ;
#24237=B_SPLINE_CURVE_WITH_KNOTS ( 'NONE', 3,
 ( #47891, #15000, #24692, #43834, #57554, #876 ),
 .UNSPECIFIED., .F., .F.,
 ( 4, 2, 4 ),
 ( 1.010636948379330479E-17, 0.0002448709889506569398, 0.0004897419779013037966 ),
 .UNSPECIFIED. ) ;
#24240=CARTESIAN_POINT ( 'NONE',  ( 5.896782393890504181, 12.99025607003297722, 15.35510775321956345 ) ) ;
#24245=ORIENTED_EDGE ( 'NONE', *, *, #15753, .T. ) ;
#24264=LINE ( 'NONE', #15804, #11910 ) ;
#24265=CARTESIAN_POINT ( 'NONE',  ( 3.661921753702001237, -43.78265665639738558, 17.19622342091600231 ) ) ;
#24268=ORIENTED_EDGE ( 'NONE', *, *, #48237, .T. ) ;
#24270=CARTESIAN_POINT ( 'NONE',  ( 2.891212509700765487, 5.349982771599759140E-15, 41.99381090189422139 ) ) ;
#24283=CARTESIAN_POINT ( 'NONE',  ( 0.8554163680231720024, -35.40260165760457767, -30.78735566729940132 ) ) ;
#24296=CARTESIAN_POINT ( 'NONE',  ( 5.896782393890504181, 3.339090646272624419, 19.83372281075811827 ) ) ;
#24297=ORIENTED_EDGE ( 'NONE', *, *, #20041, .F. ) ;
#24302=CARTESIAN_POINT ( 'NONE',  ( 0.5804410086790514622, 28.25755288515122743, -37.43034272883802771 ) ) ;
#24303=ORIENTED_EDGE ( 'NONE', *, *, #35163, .F. ) ;
#24308=CARTESIAN_POINT ( 'NONE',  ( 0.6845945791218034371, 40.79463988471336933, -23.15607646797048247 ) ) ;
#24310=DIRECTION ( 'NONE',  ( -0.07906939808003035641, -0.3030506235706508233, -0.9496885541274577847 ) ) ;
#24323=ADVANCED_FACE ( 'NONE', ( #28105 ), #30095, .F. ) ;
#24326=CARTESIAN_POINT ( 'NONE',  ( 0.7056759521544998526, 3.855032142332291301, 46.74278079338640879 ) ) ;
#24327=ORIENTED_EDGE ( 'NONE', *, *, #24538, .F. ) ;
#24339=EDGE_CURVE ( 'NONE', #26618, #51034, #43254, .T. ) ;
#24351=CARTESIAN_POINT ( 'NONE',  ( 0.5848930533535030563, 27.67115520191777733, -37.86264983039271215 ) ) ;
#24372=CARTESIAN_POINT ( 'NONE',  ( 0.9762797500689124330, 40.55021165774351743, 10.58324712448433580 ) ) ;
#24375=VERTEX_POINT ( 'NONE', #48147 ) ;
#24377=CARTESIAN_POINT ( 'NONE',  ( 1.157644175074336923, 40.63757550383299844, -10.27568648069094337 ) ) ;
#24378=ORIENTED_EDGE ( 'NONE', *, *, #48316, .T. ) ;
#24381=CARTESIAN_POINT ( 'NONE',  ( 0.9762797500689124330, 35.79768877047989406, -21.79105926469756938 ) ) ;
#24383=CARTESIAN_POINT ( 'NONE',  ( 4.956445790443988031, 46.94638516972315756, 3.684422564749393558 ) ) ;
#24385=CARTESIAN_POINT ( 'NONE',  ( 0.5804410086790514622, 11.40290849443472787, 45.49168638029309619 ) ) ;
#24391=ORIENTED_EDGE ( 'NONE', *, *, #23771, .T. ) ;
#24394=CARTESIAN_POINT ( 'NONE',  ( 0.8554163680231816613, 16.00619315955244204, -44.10223637924629259 ) ) ;
#24401=CARTESIAN_POINT ( 'NONE',  ( 5.895881250540457863, 0.6766202122108295747, 20.10148916614708270 ) ) ;
#24405=DIRECTION ( 'NONE',  ( -0.07906939808003035641, 0.9890184005629925057, 0.1248624588700777416 ) ) ;
#24409=ADVANCED_FACE ( 'NONE', ( #38766 ), #32493, .F. ) ;
#24414=CARTESIAN_POINT ( 'NONE',  ( 2.282816707992318950, 9.607080803701229854, -45.98044111183712346 ) ) ;
#24415=EDGE_CURVE ( 'NONE', #53799, #36392, #13280, .T. ) ;
#24420=CARTESIAN_POINT ( 'NONE',  ( 3.782625744892853525, -29.99484860343034498, 29.45415355009026115 ) ) ;
#24427=CARTESIAN_POINT ( 'NONE',  ( 5.910764540655177868, 10.83508461757094565, -16.94408981914462586 ) ) ;
#24429=ORIENTED_EDGE ( 'NONE', *, *, #36238, .T. ) ;
#24430=CARTESIAN_POINT ( 'NONE',  ( 5.895596859100789899, 12.98817590332804883, 15.35693556399505155 ) ) ;
#24444=CARTESIAN_POINT ( 'NONE',  ( 4.962356264823608143, 0.000000000000000000, 0.000000000000000000 ) ) ;
#24445=CARTESIAN_POINT ( 'NONE',  ( 4.962356264823608143, -10.17958088187436871, 40.83640203215416165 ) ) ;
#24457=AXIS2_PLACEMENT_3D ( 'NONE', #12092, #2028, #31801 ) ;
#24458=ORIENTED_EDGE ( 'NONE', *, *, #11747, .T. ) ;
#24465=CARTESIAN_POINT ( 'NONE',  ( 0.5806925824938502512, -14.41498975133575300, -44.62544602368080859 ) ) ;
#24478=CIRCLE ( 'NONE', #59475, 47.09074272231896430 ) ;
#24482=CARTESIAN_POINT ( 'NONE',  ( 0.8560838555295223751, 46.60258007729417784, 5.345312359546021241 ) ) ;
#24493=CARTESIAN_POINT ( 'NONE',  ( 0.9788927965476029724, -1.258742425780537078, 41.88976223538774235 ) ) ;
#24494=CARTESIAN_POINT ( 'NONE',  ( 1.157643937452370597, 38.26069984755655184, -17.12078040773669230 ) ) ;
#24498=EDGE_LOOP ( 'NONE', ( #44673, #51140, #22224, #1197 ) ) ;
#24502=ORIENTED_EDGE ( 'NONE', *, *, #18245, .T. ) ;
#24503=CARTESIAN_POINT ( 'NONE',  ( 0.8560838555295223751, 28.55542365806889293, 37.21505896528891810 ) ) ;
#24508=DIRECTION ( 'NONE',  ( 0.000000000000000000, 0.000000000000000000, 1.000000000000000000 ) ) ;
#24515=ORIENTED_EDGE ( 'NONE', *, *, #4864, .F. ) ;
#24520=ORIENTED_EDGE ( 'NONE', *, *, #23185, .T. ) ;
#24523=CARTESIAN_POINT ( 'NONE',  ( 3.782625744892851305, 27.96054597547522391, -31.39181378716972404 ) ) ;
#24524=CARTESIAN_POINT ( 'NONE',  ( 0.7056759521544994085, -0.7243499498853074314, -46.89588624034189479 ) ) ;
#24525=( BOUNDED_SURFACE ( )  B_SPLINE_SURFACE ( 3, 1, ( 
 ( #49896, #60204 ),
 ( #59903, #50812 ),
 ( #22016, #45523 ),
 ( #21080, #7903 ) ),
 .UNSPECIFIED., .F., .F., .F. ) 
 B_SPLINE_SURFACE_WITH_KNOTS ( ( 4, 4 ),
 ( 2, 2 ),
 ( 0.000000000000000000, 1.000000000000000000 ),
 ( 0.000000000000000000, 1.000000000000000000 ),
 .UNSPECIFIED. ) 
 GEOMETRIC_REPRESENTATION_ITEM ( )  RATIONAL_B_SPLINE_SURFACE ( (
 ( 1.000000000000000000, 1.000000000000000000),
 ( 0.9952954269826590483, 0.8620686068821307169),
 ( 0.9952954269826590483, 0.8620686068821307169),
 ( 1.000000000000000000, 1.000000000000000000) ) ) 
 REPRESENTATION_ITEM ( '' )  SURFACE ( )  );
#24527=B_SPLINE_CURVE_WITH_KNOTS ( 'NONE', 3,
 ( #7844, #11322, #2204, #35141, #17263, #55139 ),
 .UNSPECIFIED., .F., .F.,
 ( 4, 2, 4 ),
 ( 7.913933220075304459E-18, 0.0002448709889506558556, 0.0004897419779013037966 ),
 .UNSPECIFIED. ) ;
#24530=CARTESIAN_POINT ( 'NONE',  ( 0.9762797500689124330, 41.46413394121034912, 6.086902470967687329 ) ) ;
#24532=CARTESIAN_POINT ( 'NONE',  ( 0.5797568665920715958, -30.75502540147657271, -35.40273606878996304 ) ) ;
#24538=EDGE_CURVE ( 'NONE', #44946, #3395, #28980, .T. ) ;
#24539=CARTESIAN_POINT ( 'NONE',  ( 1.231276596079881935, 41.65019306089989470, -4.747440258479600494 ) ) ;
#24541=EDGE_CURVE ( 'NONE', #29203, #57580, #26690, .T. ) ;
#24550=CARTESIAN_POINT ( 'NONE',  ( 5.896782393890504181, -11.93563916323493146, 16.18847134979287361 ) ) ;
#24555=FACE_OUTER_BOUND ( 'NONE', #11289, .T. ) ;
#24557=CARTESIAN_POINT ( 'NONE',  ( 5.895596859100789899, 19.00119700155552493, 6.594141014610245932 ) ) ;
#24566=CARTESIAN_POINT ( 'NONE',  ( 0.8554163680231720024, 37.37991192211390512, 28.35397075908108988 ) ) ;
#24567=B_SPLINE_CURVE_WITH_KNOTS ( 'NONE', 3,
 ( #36780, #49607, #6667, #1989, #44948, #40256 ),
 .UNSPECIFIED., .F., .F.,
 ( 4, 2, 4 ),
 ( 6.992893892674702526E-18, 0.0002291472222819966218, 0.0004582944445639862505 ),
 .UNSPECIFIED. ) ;
#24570=CARTESIAN_POINT ( 'NONE',  ( 0.5806925824938499181, 45.37089516811292356, -11.86188155343291584 ) ) ;
#24579=ORIENTED_EDGE ( 'NONE', *, *, #53087, .T. ) ;
#24584=DIRECTION ( 'NONE',  ( 0.07906939808003032866, 0.8172634100797984136, 0.5708139353870058663 ) ) ;
#24594=CARTESIAN_POINT ( 'NONE',  ( 0.5837157313716048179, 46.89593559896864861, 0.09103779108274359655 ) ) ;
#24596=CARTESIAN_POINT ( 'NONE',  ( 0.9785694773339255192, -41.02396546051519266, -8.565609354221619398 ) ) ;
#24598=DIRECTION ( 'NONE',  ( -1.000000000000000000, -0.000000000000000000, -0.000000000000000000 ) ) ;
#24599=B_SPLINE_CURVE_WITH_KNOTS ( 'NONE', 3,
 ( #43395, #60685, #17493, #61002 ),
 .UNSPECIFIED., .F., .F.,
 ( 4, 4 ),
 ( 3.878959614448863476E-18, 0.004042984057420973693 ),
 .UNSPECIFIED. ) ;
#24607=CARTESIAN_POINT ( 'NONE',  ( 0.9789889208857711633, -37.44753480729469430, -18.81534041410943559 ) ) ;
#24610=CARTESIAN_POINT ( 'NONE',  ( 0.5806925824938499181, 28.25565086187788921, -37.42780459384738379 ) ) ;
#24621=CARTESIAN_POINT ( 'NONE',  ( 3.661933894777869902, -3.452430679485475107, 46.91174572913485008 ) ) ;
#24627=FACE_OUTER_BOUND ( 'NONE', #49476, .T. ) ;
#24628=FACE_OUTER_BOUND ( 'NONE', #20319, .T. ) ;
#24637=CARTESIAN_POINT ( 'NONE',  ( 5.895596859100789899, -15.78680134203122165, 12.46214614742294913 ) ) ;
#24638=VERTEX_POINT ( 'NONE', #36840 ) ;
#24647=CARTESIAN_POINT ( 'NONE',  ( 3.661921753702016780, -15.72362396054653999, -44.33281824316339481 ) ) ;
#24649=FACE_OUTER_BOUND ( 'NONE', #36404, .T. ) ;
#24651=CARTESIAN_POINT ( 'NONE',  ( 0.9762797500689124330, -11.93232144563776487, -40.17392798947692256 ) ) ;
#24655=CARTESIAN_POINT ( 'NONE',  ( 0.8560838555295223751, -6.899551485032601406, 46.39794201672221163 ) ) ;
#24659=ORIENTED_EDGE ( 'NONE', *, *, #60237, .T. ) ;
#24661=CARTESIAN_POINT ( 'NONE',  ( 2.282803330402959130, 44.93953277324986573, 13.67242851796949665 ) ) ;
#24664=ORIENTED_EDGE ( 'NONE', *, *, #56579, .F. ) ;
#24665=B_SPLINE_CURVE_WITH_KNOTS ( 'NONE', 3,
 ( #7797, #36037, #22225, #27225 ),
 .UNSPECIFIED., .F., .F.,
 ( 4, 4 ),
 ( 6.505213034913026604E-19, 0.004041751736741000349 ),
 .UNSPECIFIED. ) ;
#24671=ADVANCED_FACE ( 'NONE', ( #39299 ), #38920, .F. ) ;
#24679=CARTESIAN_POINT ( 'NONE',  ( 5.896782393890504181, 19.00205529748287248, 6.591508275760228130 ) ) ;
#24680=CARTESIAN_POINT ( 'NONE',  ( 0.5782707292762423457, -44.53844888462747775, -14.69907904118641007 ) ) ;
#24681=CARTESIAN_POINT ( 'NONE',  ( 0.9783242366443547500, 40.34793699461262406, 11.33042234364170397 ) ) ;
#24682=DIRECTION ( 'NONE',  ( 0.000000000000000000, 0.000000000000000000, 1.000000000000000000 ) ) ;
#24684=CARTESIAN_POINT ( 'NONE',  ( 2.618530812446115519, -37.94055228201274588, 27.75322110555919508 ) ) ;
#24687=LINE ( 'NONE', #872, #15206 ) ;
#24690=EDGE_CURVE ( 'NONE', #18401, #15970, #14262, .T. ) ;
#24691=EDGE_LOOP ( 'NONE', ( #43406, #4778, #29598, #60791 ) ) ;
#24692=CARTESIAN_POINT ( 'NONE',  ( 0.6064515330803592619, -46.83442941052457087, -2.422923405243606609 ) ) ;
#24700=B_SPLINE_CURVE_WITH_KNOTS ( 'NONE', 3,
 ( #55707, #31614, #12220, #12523, #7793, #31304 ),
 .UNSPECIFIED., .F., .F.,
 ( 4, 2, 4 ),
 ( 1.738108305489988542E-18, 0.0002291459268755720237, 0.0004582918537511423127 ),
 .UNSPECIFIED. ) ;
#24706=CARTESIAN_POINT ( 'NONE',  ( 0.9788927965476029724, -31.17652977587658825, -28.00643861267721846 ) ) ;
#24714=EDGE_CURVE ( 'NONE', #40578, #18068, #28335, .T. ) ;
#24720=CARTESIAN_POINT ( 'NONE',  ( 4.956445790443998689, -11.44166143952028314, 45.67960632101629415 ) ) ;
#24725=VECTOR ( 'NONE', #20006, 1000.000000000000114 ) ;
#24726=CARTESIAN_POINT ( 'NONE',  ( 0.8560838555295158248, 40.81790744942473737, -23.11430867518922128 ) ) ;
#24727=CARTESIAN_POINT ( 'NONE',  ( 0.9791128995231621612, -34.54836961549908381, 23.72230155691098474 ) ) ;
#24729=( BOUNDED_SURFACE ( )  B_SPLINE_SURFACE ( 3, 1, ( 
 ( #19557, #23324 ),
 ( #57415, #14554 ),
 ( #56815, #10145 ),
 ( #33655, #52734 ) ),
 .UNSPECIFIED., .F., .F., .F. ) 
 B_SPLINE_SURFACE_WITH_KNOTS ( ( 4, 4 ),
 ( 2, 2 ),
 ( 0.000000000000000000, 1.000000000000000000 ),
 ( 0.000000000000000000, 1.000000000000000000 ),
 .UNSPECIFIED. ) 
 GEOMETRIC_REPRESENTATION_ITEM ( )  RATIONAL_B_SPLINE_SURFACE ( (
 ( 1.000000000000000000, 1.000000000000000000),
 ( 0.9729067724841187204, 0.9999501103223794596),
 ( 0.9729067724841187204, 0.9999501103223794596),
 ( 1.000000000000000000, 1.000000000000000000) ) ) 
 REPRESENTATION_ITEM ( '' )  SURFACE ( )  );
#24731=DIRECTION ( 'NONE',  ( 0.07906939808003037029, 0.6374189498684894595, 0.7664496804329778978 ) ) ;
#24733=CARTESIAN_POINT ( 'NONE',  ( 5.896782393890504181, 16.57826022845101122, -11.38803647148056797 ) ) ;
#24744=FACE_OUTER_BOUND ( 'NONE', #61460, .T. ) ;
#24747=ORIENTED_EDGE ( 'NONE', *, *, #59279, .T. ) ;
#24756=B_SPLINE_CURVE_WITH_KNOTS ( 'NONE', 3,
 ( #22326, #47918, #55824, #38225, #51423, #46768 ),
 .UNSPECIFIED., .F., .F.,
 ( 4, 2, 4 ),
 ( 0.000000000000000000, 0.0002291459268755702077, 0.0004582918537511404154 ),
 .UNSPECIFIED. ) ;
#24757=ORIENTED_EDGE ( 'NONE', *, *, #30008, .F. ) ;
#24763=ORIENTED_EDGE ( 'NONE', *, *, #3376, .F. ) ;
#24764=CARTESIAN_POINT ( 'NONE',  ( 5.895881250540457863, 16.57931246612933407, 11.38657454016568416 ) ) ;
#24766=B_SPLINE_CURVE_WITH_KNOTS ( 'NONE', 3,
 ( #49142, #6194, #25336, #55674, #3061, #3357 ),
 .UNSPECIFIED., .F., .F.,
 ( 4, 2, 4 ),
 ( 1.738108305489988542E-18, 0.0002291459268755712377, 0.0004582918537511407406 ),
 .UNSPECIFIED. ) ;
#24767=CARTESIAN_POINT ( 'NONE',  ( 0.5817217712918332229, 32.92749272057849907, -33.39184297316671746 ) ) ;
#24769=CARTESIAN_POINT ( 'NONE',  ( 1.092182651088182688, -18.34815906953977560, -37.68429703737552217 ) ) ;
#24771=EDGE_CURVE ( 'NONE', #29203, #37717, #10158, .T. ) ;
#24778=CARTESIAN_POINT ( 'NONE',  ( 0.9789889208857698311, 40.39408608331138595, -11.16479769348274331 ) ) ;
#24779=ORIENTED_EDGE ( 'NONE', *, *, #37519, .T. ) ;
#24780=CARTESIAN_POINT ( 'NONE',  ( 0.9762797500689124330, -11.93232144563776487, -40.17392798947692256 ) ) ;
#24781=CARTESIAN_POINT ( 'NONE',  ( 4.960386119450144626, -40.09630699761674322, 17.51349850330343472 ) ) ;
#24798=CARTESIAN_POINT ( 'NONE',  ( 5.901463166500145796, -4.648441909663419302, -19.56808263865219288 ) ) ;
#24801=CARTESIAN_POINT ( 'NONE',  ( 0.5837799406558246140, -1.475992047555320541, 46.87285991970995980 ) ) ;
#24803=CARTESIAN_POINT ( 'NONE',  ( 0.5806925824938499181, -1.020860314012482561, -46.88475452172953339 ) ) ;
#24804=CARTESIAN_POINT ( 'NONE',  ( 4.956445790444004018, -47.08764048036452721, 0.5405220916596411573 ) ) ;
#24811=EDGE_CURVE ( 'NONE', #58761, #38098, #54578, .T. ) ;
#24812=LINE ( 'NONE', #43326, #44349 ) ;
#24816=EDGE_LOOP ( 'NONE', ( #40498, #1092, #25002, #27736 ) ) ;
#24817=ORIENTED_EDGE ( 'NONE', *, *, #57754, .T. ) ;
#24826=VERTEX_POINT ( 'NONE', #26100 ) ;
#24828=VERTEX_POINT ( 'NONE', #10785 ) ;
#24834=CARTESIAN_POINT ( 'NONE',  ( 0.9754292580325141238, -34.21816593646880733, -24.19596220133207964 ) ) ;
#24842=CARTESIAN_POINT ( 'NONE',  ( 0.7056759521544981872, -14.69874540808407914, 44.53869904414941061 ) ) ;
#24845=VERTEX_POINT ( 'NONE', #44316 ) ;
#24847=CARTESIAN_POINT ( 'NONE',  ( 0.7056759521545005187, 46.58786211884279993, -5.414788298048260451 ) ) ;
#24861=CARTESIAN_POINT ( 'NONE',  ( 0.9790320750461888322, 15.14249547772530313, -39.07738429385034351 ) ) ;
#24863=ADVANCED_FACE ( 'NONE', ( #1343 ), #21686, .F. ) ;
#24866=CARTESIAN_POINT ( 'NONE',  ( 0.9785694773339257413, 9.931640869912628844, -40.71483655064518103 ) ) ;
#24870=CARTESIAN_POINT ( 'NONE',  ( 0.9762797500689124330, -0.8945891712298984499, -41.89897964629236782 ) ) ;
#24873=AXIS2_PLACEMENT_3D ( 'NONE', #45584, #59649, #18231 ) ;
#24877=DIRECTION ( 'NONE',  ( -0.07906939808003035641, -0.8172634100798066292, 0.5708139353869940980 ) ) ;
#24885=( BOUNDED_SURFACE ( )  B_SPLINE_SURFACE ( 3, 1, ( 
 ( #9866, #20200 ),
 ( #33686, #58069 ),
 ( #43402, #39621 ),
 ( #38700, #10173 ) ),
 .UNSPECIFIED., .F., .F., .F. ) 
 B_SPLINE_SURFACE_WITH_KNOTS ( ( 4, 4 ),
 ( 2, 2 ),
 ( 0.000000000000000000, 1.000000000000000000 ),
 ( 0.000000000000000000, 1.000000000000000000 ),
 .UNSPECIFIED. ) 
 GEOMETRIC_REPRESENTATION_ITEM ( )  RATIONAL_B_SPLINE_SURFACE ( (
 ( 1.000000000000000000, 1.000000000000000000),
 ( 0.7282232189291694135, 0.9929344683865672927),
 ( 0.7282232189291694135, 0.9929344683865672927),
 ( 1.000000000000000000, 1.000000000000000000) ) ) 
 REPRESENTATION_ITEM ( '' )  SURFACE ( )  );
#24902=ORIENTED_EDGE ( 'NONE', *, *, #8681, .T. ) ;
#24905=CARTESIAN_POINT ( 'NONE',  ( 1.157643937452367933, 33.40146143681677415, 25.32478328593544958 ) ) ;
#24907=EDGE_CURVE ( 'NONE', #19440, #35096, #47558, .T. ) ;
#24911=CARTESIAN_POINT ( 'NONE',  ( 1.092182651088185796, -41.22225533107799578, -7.582008300028149073 ) ) ;
#24919=ORIENTED_EDGE ( 'NONE', *, *, #49010, .F. ) ;
#24920=CARTESIAN_POINT ( 'NONE',  ( 1.092182651088182688, -30.55625471937437965, 28.68930954148243728 ) ) ;
#24926=CARTESIAN_POINT ( 'NONE',  ( 2.528100132419516477, -8.172757371798878623, -41.17596162293945383 ) ) ;
#24928=CARTESIAN_POINT ( 'NONE',  ( 0.5817217712918341110, 46.53606702067560974, -5.799087881344962447 ) ) ;
#24929=CARTESIAN_POINT ( 'NONE',  ( 0.6845945791218034371, -2.432797934429833830, 46.84536278997290282 ) ) ;
#24936=CARTESIAN_POINT ( 'NONE',  ( 0.7764139734771232648, -44.00885462842416729, -16.22532542666233013 ) ) ;
#24944=CARTESIAN_POINT ( 'NONE',  ( 0.7056313189692692278, 45.45044948170761501, 11.57606521527523391 ) ) ;
#24946=B_SPLINE_CURVE_WITH_KNOTS ( 'NONE', 3,
 ( #55202, #16705, #45847, #21705 ),
 .UNSPECIFIED., .F., .F.,
 ( 4, 4 ),
 ( 0.000000000000000000, 0.004041751736740989073 ),
 .UNSPECIFIED. ) ;
#24947=EDGE_CURVE ( 'NONE', #4970, #7001, #6457, .T. ) ;
#24950=CARTESIAN_POINT ( 'NONE',  ( 5.901463166500145796, -20.11262442202718148, -0.01446371710611837197 ) ) ;
#24951=CARTESIAN_POINT ( 'NONE',  ( 0.9789889208857702751, 41.54742805390438321, 5.490548255685043344 ) ) ;
#24963=B_SPLINE_CURVE_WITH_KNOTS ( 'NONE', 3,
 ( #50560, #51473, #32093, #41501, #3551, #61187, #60565, #18307, #13605, #32711, #51793, #31783, #7636, #8892, #46823, #37416 ),
 .UNSPECIFIED., .F., .F.,
 ( 4, 3, 3, 3, 3, 4 ),
 ( 9.813676791237319219E-18, 0.0002732102107931875601, 0.0004098135523333743240, 0.0005464168938824992506, 0.0008195847345945445278, 0.001092771384553111553 ),
 .UNSPECIFIED. ) ;
#24966=VERTEX_POINT ( 'NONE', #22331 ) ;
#24967=ORIENTED_EDGE ( 'NONE', *, *, #23972, .F. ) ;
#24976=ORIENTED_EDGE ( 'NONE', *, *, #44411, .F. ) ;
#24979=CARTESIAN_POINT ( 'NONE',  ( 5.894904586330512508, 5.960138742492036457, 19.20953300400320174 ) ) ;
#24980=LINE ( 'NONE', #44118, #25207 ) ;
#24990=CARTESIAN_POINT ( 'NONE',  ( 0.5832655196449132440, -34.93280808371936530, 31.28792262773866995 ) ) ;
#24995=CARTESIAN_POINT ( 'NONE',  ( 4.956445790444004018, -45.27177431812773278, -12.96165499572285817 ) ) ;
#24996=CARTESIAN_POINT ( 'NONE',  ( 5.910764540655178756, -20.11221018249587544, 0.01549336220059224084 ) ) ;
#24997=CARTESIAN_POINT ( 'NONE',  ( 0.9790320750461896093, 40.39682900182685898, 11.15496925766059633 ) ) ;
#25002=ORIENTED_EDGE ( 'NONE', *, *, #59231, .T. ) ;
#25016=CARTESIAN_POINT ( 'NONE',  ( 0.9769922540276034795, -30.78348955484764460, -28.43779748701913235 ) ) ;
#25021=CARTESIAN_POINT ( 'NONE',  ( 0.9780303403264768436, -27.30392181875063784, -31.79363877744474820 ) ) ;
#25024=CARTESIAN_POINT ( 'NONE',  ( 4.956445790443988031, 0.000000000000000000, 0.000000000000000000 ) ) ;
#25026=CARTESIAN_POINT ( 'NONE',  ( 0.8560838555295158248, -8.701885300216421371, 46.09392613244839509 ) ) ;
#25027=CARTESIAN_POINT ( 'NONE',  ( 3.531697314441601065, 0.2975892744534772150, 47.02729111494448944 ) ) ;
#25038=CARTESIAN_POINT ( 'NONE',  ( 5.896782393890504181, 3.351618377817072947, 19.83160964539921167 ) ) ;
#25047=ADVANCED_FACE ( 'NONE', ( #665 ), #60098, .F. ) ;
#25055=ORIENTED_EDGE ( 'NONE', *, *, #41062, .T. ) ;
#25058=ORIENTED_EDGE ( 'NONE', *, *, #43345, .T. ) ;
#25061=ORIENTED_EDGE ( 'NONE', *, *, #51218, .T. ) ;
#25062=CARTESIAN_POINT ( 'NONE',  ( 5.896278296736517710, 8.471169747519724069, -18.24188210473607441 ) ) ;
#25067=VECTOR ( 'NONE', #51150, 1000.000000000000114 ) ;
#25068=ORIENTED_EDGE ( 'NONE', *, *, #13457, .T. ) ;
#25073=EDGE_LOOP ( 'NONE', ( #18214, #4383, #15126, #39096 ) ) ;
#25076=CARTESIAN_POINT ( 'NONE',  ( 0.5834584762367742705, -46.77877185694124051, -3.313984394868909611 ) ) ;
#25077=ORIENTED_EDGE ( 'NONE', *, *, #35199, .F. ) ;
#25089=CARTESIAN_POINT ( 'NONE',  ( 0.9789233960466707796, 41.55206370043617170, -5.455522804208261967 ) ) ;
#25102=B_SPLINE_CURVE_WITH_KNOTS ( 'NONE', 3,
 ( #57889, #61965, #4333, #19103, #38216, #43219, #254, #15016, #44163, #45078, #59127, #39762, #16238, #30017, #35053, #11541, #44465, #43848, #25318 ),
 .UNSPECIFIED., .F., .F.,
 ( 4, 3, 3, 3, 3, 3, 4 ),
 ( 1.250973872328959318E-17, 0.0002732106629380585830, 0.0004098138914053691979, 0.0005464171197651370403, 0.0006830203481512451408, 0.0008196235766963510562, 0.001011968216111142896 ),
 .UNSPECIFIED. ) ;
#25104=CARTESIAN_POINT ( 'NONE',  ( 1.231276596079881047, 38.25526645152027072, 17.14092645516147684 ) ) ;
#25111=CARTESIAN_POINT ( 'NONE',  ( 2.282816707992312288, -35.70555677707368858, -30.52228991486604670 ) ) ;
#25116=DIRECTION ( 'NONE',  ( -0.07906939808003034253, 0.9868658484044072754, -0.1408681210931379824 ) ) ;
#25123=CARTESIAN_POINT ( 'NONE',  ( 0.7764146366350239692, 28.53559796717425456, 37.22579914958128455 ) ) ;
#25129=EDGE_CURVE ( 'NONE', #22672, #4231, #21026, .T. ) ;
#25131=ORIENTED_EDGE ( 'NONE', *, *, #2307, .T. ) ;
#25132=CARTESIAN_POINT ( 'NONE',  ( 1.231276596079881935, -34.07446381689681658, -24.41736444846283405 ) ) ;
#25136=CARTESIAN_POINT ( 'NONE',  ( 0.5782707292762423457, 23.17211662964077235, 40.77731433787596416 ) ) ;
#25145=VERTEX_POINT ( 'NONE', #31043 ) ;
#25151=ORIENTED_EDGE ( 'NONE', *, *, #15211, .T. ) ;
#25152=CARTESIAN_POINT ( 'NONE',  ( 0.9780303403264782869, -39.69490490238998603, -13.44076404767592692 ) ) ;
#25155=CARTESIAN_POINT ( 'NONE',  ( 0.9772918015221170318, 14.67438192764145199, -39.25556483853453926 ) ) ;
#25156=CARTESIAN_POINT ( 'NONE',  ( 0.8560838555295223751, 36.24009790160352651, -29.78301761346427767 ) ) ;
#25161=( BOUNDED_SURFACE ( )  B_SPLINE_SURFACE ( 3, 1, ( 
 ( #22511, #13126 ),
 ( #33151, #32532 ),
 ( #23430, #36621 ),
 ( #60696, #51611 ) ),
 .UNSPECIFIED., .F., .F., .F. ) 
 B_SPLINE_SURFACE_WITH_KNOTS ( ( 4, 4 ),
 ( 2, 2 ),
 ( 0.000000000000000000, 1.000000000000000000 ),
 ( 0.000000000000000000, 1.000000000000000000 ),
 .UNSPECIFIED. ) 
 GEOMETRIC_REPRESENTATION_ITEM ( )  RATIONAL_B_SPLINE_SURFACE ( (
 ( 1.000000000000000000, 1.000000000000000000),
 ( 0.9952954269826590483, 0.8620686068821307169),
 ( 0.9952954269826590483, 0.8620686068821307169),
 ( 1.000000000000000000, 1.000000000000000000) ) ) 
 REPRESENTATION_ITEM ( '' )  SURFACE ( )  );
#25171=CARTESIAN_POINT ( 'NONE',  ( 3.376099380956838925, 9.644725941469024733, -9.310620019419843629 ) ) ;
#25180=CARTESIAN_POINT ( 'NONE',  ( 0.9762797500689124330, 29.49606728235512776, 29.77090526101756751 ) ) ;
#25185=ORIENTED_EDGE ( 'NONE', *, *, #41186, .T. ) ;
#25187=ORIENTED_EDGE ( 'NONE', *, *, #29408, .T. ) ;
#25188=DIRECTION ( 'NONE',  ( -0.07500201931887527651, -0.8960136144483755727, -0.4376463181854141071 ) ) ;
#25189=CARTESIAN_POINT ( 'NONE',  ( 1.231276596079887264, -18.40965318903149495, -37.66113965983570466 ) ) ;
#25192=ORIENTED_EDGE ( 'NONE', *, *, #20449, .T. ) ;
#25203=EDGE_CURVE ( 'NONE', #17743, #48550, #19822, .T. ) ;
#25207=VECTOR ( 'NONE', #1148, 999.9999999999998863 ) ;
#25208=B_SPLINE_CURVE_WITH_KNOTS ( 'NONE', 3,
 ( #20729, #44255, #5055, #38618, #5364, #24493, #43632, #674, #19817, #57988, #53295, #10407, #29500, #48607, #5664, #43952, #20121, #39241, #58290 ),
 .UNSPECIFIED., .F., .F.,
 ( 4, 3, 3, 3, 3, 3, 4 ),
 ( 8.782706832233357974E-18, 0.0002732106629380614562, 0.0004098138914053768957, 0.0005464171197651472318, 0.0006830203481512577175, 0.0008196235766963645003, 0.001011968216111141811 ),
 .UNSPECIFIED. ) ;
#25211=VERTEX_POINT ( 'NONE', #32594 ) ;
#25214=VERTEX_POINT ( 'NONE', #16966 ) ;
#25217=CARTESIAN_POINT ( 'NONE',  ( 0.5782707292762442330, -20.39674625896916993, 42.23398034468034012 ) ) ;
#25219=ORIENTED_EDGE ( 'NONE', *, *, #3323, .F. ) ;
#25223=CARTESIAN_POINT ( 'NONE',  ( 5.896782393890504181, -19.39988559968493576, 5.307591317834223332 ) ) ;
#25228=CARTESIAN_POINT ( 'NONE',  ( 0.7056759521544988534, -44.02266877934305001, -16.17879670004061055 ) ) ;
#25230=B_SPLINE_CURVE_WITH_KNOTS ( 'NONE', 3,
 ( #48588, #19794, #58272, #53887, #5643, #39847, #38916, #26025, #44544, #39222, #30714, #25089, #11309, #58903, #59209, #1573, #53572, #20709, #58581 ),
 .UNSPECIFIED., .F., .F.,
 ( 4, 3, 3, 3, 3, 3, 4 ),
 ( 8.674294979774126656E-18, 0.0002732106629380616188, 0.0004098138914053757031, 0.0005464171197651461476, 0.0006830203481512564165, 0.0008196235766963625487, 0.001011968216111142245 ),
 .UNSPECIFIED. ) ;
#25234=EDGE_CURVE ( 'NONE', #47712, #60852, #19165, .T. ) ;
#25235=LINE ( 'NONE', #49346, #13844 ) ;
#25238=LINE ( 'NONE', #29940, #55814 ) ;
#25242=VERTEX_POINT ( 'NONE', #46093 ) ;
#25250=CARTESIAN_POINT ( 'NONE',  ( 4.960386119450148179, 43.62260476509040785, 3.391875319207611206 ) ) ;
#25255=AXIS2_PLACEMENT_3D ( 'NONE', #18189, #37011, #18494 ) ;
#25266=EDGE_LOOP ( 'NONE', ( #57635, #28991, #6006, #4001 ) ) ;
#25279=EDGE_LOOP ( 'NONE', ( #38255, #32267, #45944, #44072 ) ) ;
#25288=VERTEX_POINT ( 'NONE', #24655 ) ;
#25289=CARTESIAN_POINT ( 'NONE',  ( 0.5837799406558225046, -19.65753372021275069, 42.57728170768891829 ) ) ;
#25297=CARTESIAN_POINT ( 'NONE',  ( 1.231276596079881047, 40.64579686208666232, -10.25650859035628315 ) ) ;
#25301=CARTESIAN_POINT ( 'NONE',  ( 1.231276596079887264, -31.65135013586864332, -27.48579279545554144 ) ) ;
#25309=VERTEX_POINT ( 'NONE', #43796 ) ;
#25312=EDGE_LOOP ( 'NONE', ( #42701, #56961, #52145, #42821 ) ) ;
#25317=CARTESIAN_POINT ( 'NONE',  ( 4.962356264823596597, 41.32726869310139506, 7.955655864260913646 ) ) ;
#25318=CARTESIAN_POINT ( 'NONE',  ( 0.9762797500689124330, 38.38274741215467145, 16.82526333465357382 ) ) ;
#25323=EDGE_LOOP ( 'NONE', ( #27304, #30659, #20927, #23815 ) ) ;
#25336=CARTESIAN_POINT ( 'NONE',  ( 1.000110580585053199, 10.35431645662686151, -40.61041262395552565 ) ) ;
#25337=CARTESIAN_POINT ( 'NONE',  ( 1.157643937452369487, 5.016389049135196565, 41.61535912980291130 ) ) ;
#25340=CARTESIAN_POINT ( 'NONE',  ( 0.9769922540276054779, 9.284899304422724597, 40.86712859980321610 ) ) ;
#25346=( BOUNDED_SURFACE ( )  B_SPLINE_SURFACE ( 3, 1, ( 
 ( #22094, #12398 ),
 ( #32427, #3267 ),
 ( #13632, #27401 ),
 ( #41526, #26789 ) ),
 .UNSPECIFIED., .F., .F., .F. ) 
 B_SPLINE_SURFACE_WITH_KNOTS ( ( 4, 4 ),
 ( 2, 2 ),
 ( 0.000000000000000000, 1.000000000000000000 ),
 ( 0.000000000000000000, 1.000000000000000000 ),
 .UNSPECIFIED. ) 
 GEOMETRIC_REPRESENTATION_ITEM ( )  RATIONAL_B_SPLINE_SURFACE ( (
 ( 1.000000000000000000, 1.000000000000000000),
 ( 0.9952954269826590483, 0.8620686068821339365),
 ( 0.9952954269826590483, 0.8620686068821339365),
 ( 1.000000000000000000, 1.000000000000000000) ) ) 
 REPRESENTATION_ITEM ( '' )  SURFACE ( )  );
#25347=ORIENTED_EDGE ( 'NONE', *, *, #58680, .T. ) ;
#25350=B_SPLINE_CURVE_WITH_KNOTS ( 'NONE', 3,
 ( #30160, #1035, #49270, #1643 ),
 .UNSPECIFIED., .F., .F.,
 ( 4, 4 ),
 ( 8.673617379884035472E-19, 0.004042984057420972825 ),
 .UNSPECIFIED. ) ;
#25358=EDGE_LOOP ( 'NONE', ( #61966, #42343, #47789, #10353 ) ) ;
#25359=CARTESIAN_POINT ( 'NONE',  ( 5.896278296736517710, 12.98960347168511120, 15.35568888922831121 ) ) ;
#25361=CARTESIAN_POINT ( 'NONE',  ( 2.282803330402972453, 6.007211579933096957, -46.58766270688949618 ) ) ;
#25384=ORIENTED_EDGE ( 'NONE', *, *, #58959, .T. ) ;
#25385=CARTESIAN_POINT ( 'NONE',  ( 4.956445790444004018, -46.73954499432468879, 5.740468958468036398 ) ) ;
#25388=CARTESIAN_POINT ( 'NONE',  ( 0.9762797500689124330, -12.89881610234921006, -39.87411852747946028 ) ) ;
#25389=CARTESIAN_POINT ( 'NONE',  ( 0.5806925824938499181, 32.20670061096218006, 34.08739940358331921 ) ) ;
#25393=ORIENTED_EDGE ( 'NONE', *, *, #22957, .F. ) ;
#25408=CARTESIAN_POINT ( 'NONE',  ( 0.5830081025819948692, -1.293956464538003948, 46.87811548100160053 ) ) ;
#25411=ORIENTED_EDGE ( 'NONE', *, *, #48783, .T. ) ;
#25412=CARTESIAN_POINT ( 'NONE',  ( 0.8560838555295158248, 31.94705745926175311, 34.34761059777461867 ) ) ;
#25414=CARTESIAN_POINT ( 'NONE',  ( 0.5804410086790514622, 46.89585601637879364, -0.5463884574786298520 ) ) ;
#25422=EDGE_LOOP ( 'NONE', ( #8042, #38645, #11280, #24747 ) ) ;
#25430=ORIENTED_EDGE ( 'NONE', *, *, #50647, .F. ) ;
#25433=CARTESIAN_POINT ( 'NONE',  ( 0.9787284016396606834, -17.81048079543711538, -37.93577167745763035 ) ) ;
#25434=ORIENTED_EDGE ( 'NONE', *, *, #9385, .T. ) ;
#25440=CARTESIAN_POINT ( 'NONE',  ( 0.9762797500689124330, -37.17323042682959766, -19.35137526946170183 ) ) ;
#25444=B_SPLINE_CURVE_WITH_KNOTS ( 'NONE', 3,
 ( #9315, #46946, #52532, #23120, #37545, #18423 ),
 .UNSPECIFIED., .F., .F.,
 ( 4, 2, 4 ),
 ( 3.471140604459641645E-18, 0.0002291459268755730266, 0.0004582918537511425838 ),
 .UNSPECIFIED. ) ;
#25447=CARTESIAN_POINT ( 'NONE',  ( 0.8554163680231720024, -14.77070554666819291, -44.53124443315552128 ) ) ;
#25452=CARTESIAN_POINT ( 'NONE',  ( 0.8554163680231720024, 46.90810212776801791, -0.9140174411379322628 ) ) ;
#25455=VERTEX_POINT ( 'NONE', #21486 ) ;
#25456=B_SPLINE_CURVE_WITH_KNOTS ( 'NONE', 3,
 ( #54482, #49812, #49192, #20088, #53562, #25076, #6870, #35116, #26010, #16004, #10679, #39206, #58258, #29774, #53871, #5938 ),
 .UNSPECIFIED., .F., .F.,
 ( 4, 3, 3, 3, 3, 4 ),
 ( 1.127622383284612036E-17, 0.0002732102107931881564, 0.0004098135523333793113, 0.0005464168938824963233, 0.0008195847345945414921, 0.001092771384553107000 ),
 .UNSPECIFIED. ) ;
#25457=EDGE_LOOP ( 'NONE', ( #53101, #23961, #37328, #23171 ) ) ;
#25458=CARTESIAN_POINT ( 'NONE',  ( 0.9772918015221172539, -39.72398724205338993, -13.35446342403389863 ) ) ;
#25461=DIRECTION ( 'NONE',  ( 0.000000000000000000, 0.000000000000000000, 1.000000000000000000 ) ) ;
#25464=EDGE_CURVE ( 'NONE', #41690, #50298, #34563, .T. ) ;
#25470=AXIS2_PLACEMENT_3D ( 'NONE', #22418, #51216, #55919 ) ;
#25472=CARTESIAN_POINT ( 'NONE',  ( 4.960386119450144626, 35.80440191906002667, -25.14918026279881502 ) ) ;
#25476=CARTESIAN_POINT ( 'NONE',  ( 5.895596859100789899, 14.91916793517919970, -13.48875870250514630 ) ) ;
#25484=CARTESIAN_POINT ( 'NONE',  ( 4.958415959904820092, -21.38448066593259966, 40.07378121005046268 ) ) ;
#25491=EDGE_LOOP ( 'NONE', ( #54910, #58946, #56534, #14530 ) ) ;
#25492=EDGE_LOOP ( 'NONE', ( #14376, #28694, #43347, #43912 ) ) ;
#25499=CARTESIAN_POINT ( 'NONE',  ( 0.6845945791218034371, -44.58955076018962416, 14.56634764511735547 ) ) ;
#25500=EDGE_CURVE ( 'NONE', #31192, #38487, #54173, .T. ) ;
#25505=CARTESIAN_POINT ( 'NONE',  ( 5.895881250540457863, -2.008683229081808186, -20.01231803898555128 ) ) ;
#25516=AXIS2_PLACEMENT_3D ( 'NONE', #6518, #16905, #26585 ) ;
#25517=ORIENTED_EDGE ( 'NONE', *, *, #37869, .F. ) ;
#25527=CARTESIAN_POINT ( 'NONE',  ( 0.5806925824938502512, 43.38503874128546300, 17.80339225430713057 ) ) ;
#25529=CARTESIAN_POINT ( 'NONE',  ( 5.896782393890504181, 17.94821721415859628, 9.076760749925794514 ) ) ;
#25532=CARTESIAN_POINT ( 'NONE',  ( 0.6064515330803597060, 5.400767718514963178, 46.58504099051251046 ) ) ;
#25533=ORIENTED_EDGE ( 'NONE', *, *, #20010, .T. ) ;
#25540=CARTESIAN_POINT ( 'NONE',  ( 0.5782707292762442330, 27.23478191391665604, 38.18380557001903242 ) ) ;
#25541=FACE_OUTER_BOUND ( 'NONE', #9795, .T. ) ;
#25548=CARTESIAN_POINT ( 'NONE',  ( 4.960386119450146403, 27.88794419592758445, -33.71496749512250091 ) ) ;
#25549=CARTESIAN_POINT ( 'NONE',  ( 0.9783242366443556381, 41.49812954613101823, 5.851472838444232494 ) ) ;
#25565=CARTESIAN_POINT ( 'NONE',  ( 0.5848930533535030563, -19.57496322689408075, -42.61565319285041653 ) ) ;
#25570=AXIS2_PLACEMENT_3D ( 'NONE', #38639, #33624, #29210 ) ;
#25571=DIRECTION ( 'NONE',  ( -1.000000000000000000, -0.000000000000000000, -0.000000000000000000 ) ) ;
#25579=VERTEX_POINT ( 'NONE', #53333 ) ;
#25586=CARTESIAN_POINT ( 'NONE',  ( 3.376099380956838925, -4.408915724533057023, 12.65977273753491517 ) ) ;
#25588=ORIENTED_EDGE ( 'NONE', *, *, #49956, .F. ) ;
#25596=VERTEX_POINT ( 'NONE', #12931 ) ;
#25598=CARTESIAN_POINT ( 'NONE',  ( 0.5806925824938494740, -19.24316026636509136, 42.76591101925167493 ) ) ;
#25603=CARTESIAN_POINT ( 'NONE',  ( 0.6064515330803564863, -19.09368311036443799, 42.83416395026369372 ) ) ;
#25608=CARTESIAN_POINT ( 'NONE',  ( 0.9785694773339246311, 3.973364312730550019, 41.71987274372960997 ) ) ;
#25629=LINE ( 'NONE', #34128, #61672 ) ;
#25630=CARTESIAN_POINT ( 'NONE',  ( 4.956445790444004906, -46.59545590650544966, 6.811867512257108181 ) ) ;
#25638=CARTESIAN_POINT ( 'NONE',  ( 5.895596859100789899, -17.30333226730972385, -10.25294473112801619 ) ) ;
#25645=CARTESIAN_POINT ( 'NONE',  ( 0.9785694773339252972, 9.498626739178066103, 40.81802905315790753 ) ) ;
#25655=CARTESIAN_POINT ( 'NONE',  ( 5.894904586330512508, -13.98322986223381470, 14.45678714934875053 ) ) ;
#25661=B_SPLINE_CURVE_WITH_KNOTS ( 'NONE', 3,
 ( #33672, #22721, #13334, #41854, #28040, #32436, #60919, #46859, #37150, #61525, #4201, #8602, #52139, #27730, #3899, #42168 ),
 .UNSPECIFIED., .F., .F.,
 ( 4, 3, 3, 3, 3, 4 ),
 ( 1.551621725782133898E-17, 0.0002732102107931864759, 0.0004098135523333695535, 0.0005464168938824849392, 0.0008195847345945289153, 0.001092771384553104831 ),
 .UNSPECIFIED. ) ;
#25664=ORIENTED_EDGE ( 'NONE', *, *, #14511, .F. ) ;
#25669=AXIS2_PLACEMENT_3D ( 'NONE', #15727, #34833, #11024 ) ;
#25672=ORIENTED_EDGE ( 'NONE', *, *, #10296, .F. ) ;
#25673=EDGE_CURVE ( 'NONE', #129, #52874, #28019, .T. ) ;
#25680=CARTESIAN_POINT ( 'NONE',  ( 0.6845945791218034371, -38.17654861005505040, -27.25724962167035414 ) ) ;
#25681=B_SPLINE_CURVE_WITH_KNOTS ( 'NONE', 3,
 ( #5869, #54104, #15625, #1187, #20321, #24706, #11535, #34423, #15930, #38828, #39441, #34122, #58494, #34733, #49423, #10299, #16233, #25016, #6479 ),
 .UNSPECIFIED., .F., .F.,
 ( 4, 3, 3, 3, 3, 3, 4 ),
 ( 9.813676791237319219E-18, 0.0002732106629380673651, 0.0004098138914053816120, 0.0005464171197651560138, 0.0006830203481512717037, 0.0008196235766963805465, 0.001011968216111141161 ),
 .UNSPECIFIED. ) ;
#25683=B_SPLINE_CURVE_WITH_KNOTS ( 'NONE', 3,
 ( #58431, #15555, #20865, #34662 ),
 .UNSPECIFIED., .F., .F.,
 ( 4, 4 ),
 ( 0.000000000000000000, 0.004447772540403830202 ),
 .UNSPECIFIED. ) ;
#25686=CARTESIAN_POINT ( 'NONE',  ( 0.5804410086790514622, -8.338934868870362394, -46.15172821366644484 ) ) ;
#25689=CARTESIAN_POINT ( 'NONE',  ( 0.7056759521545044045, -34.21343630614968845, -32.08098510398369996 ) ) ;
#25701=CARTESIAN_POINT ( 'NONE',  ( 0.5806925824938511393, 5.237374507879287044, 46.60249210726590263 ) ) ;
#25702=CARTESIAN_POINT ( 'NONE',  ( 3.782625744892853525, -36.71075882237605015, 20.48312209552882379 ) ) ;
#25705=CIRCLE ( 'NONE', #60692, 47.09074272231896430 ) ;
#25708=LINE ( 'NONE', #2505, #21956 ) ;
#25714=CARTESIAN_POINT ( 'NONE',  ( 0.9762797500689124330, 20.58271139965489738, 36.50584578699993443 ) ) ;
#25725=B_SPLINE_CURVE_WITH_KNOTS ( 'NONE', 3,
 ( #52718, #33946, #53025, #10125, #33637, #9499 ),
 .UNSPECIFIED., .F., .F.,
 ( 4, 2, 4 ),
 ( 1.571494855748036957E-17, 0.0002448709889506572109, 0.0004897419779012987008 ),
 .UNSPECIFIED. ) ;
#25732=ORIENTED_EDGE ( 'NONE', *, *, #49940, .F. ) ;
#25734=CARTESIAN_POINT ( 'NONE',  ( 3.238018933889920792, 13.23534742317154134, -2.057442819521235311 ) ) ;
#25745=ORIENTED_EDGE ( 'NONE', *, *, #7708, .T. ) ;
#25750=CARTESIAN_POINT ( 'NONE',  ( 3.238018933889920792, -13.34321331060664839, -1.168824587054275943 ) ) ;
#25760=CARTESIAN_POINT ( 'NONE',  ( 0.9754292580325130135, 14.51724361431902999, 39.31382841630305336 ) ) ;
#25762=CARTESIAN_POINT ( 'NONE',  ( 4.956445790443988031, 46.25174887658550915, 8.849507104743643993 ) ) ;
#25772=CARTESIAN_POINT ( 'NONE',  ( 4.291220156522059348, 6.853930411218122742, -46.60914754877926924 ) ) ;
#25774=( LENGTH_UNIT ( ) NAMED_UNIT ( * ) SI_UNIT ( .MILLI., .METRE. ) );
#25775=ORIENTED_EDGE ( 'NONE', *, *, #35163, .T. ) ;
#25777=VERTEX_POINT ( 'NONE', #55417 ) ;
#25781=CARTESIAN_POINT ( 'NONE',  ( 4.956445790443989807, 44.30493387627029733, 15.95653108789479191 ) ) ;
#25784=EDGE_CURVE ( 'NONE', #30302, #59869, #29492, .T. ) ;
#25788=( BOUNDED_SURFACE ( )  B_SPLINE_SURFACE ( 3, 1, ( 
 ( #57005, #43559 ),
 ( #10031, #4362 ),
 ( #53228, #33229 ),
 ( #52301, #33852 ) ),
 .UNSPECIFIED., .F., .F., .F. ) 
 B_SPLINE_SURFACE_WITH_KNOTS ( ( 4, 4 ),
 ( 2, 2 ),
 ( 0.000000000000000000, 1.000000000000000000 ),
 ( 0.000000000000000000, 1.000000000000000000 ),
 .UNSPECIFIED. ) 
 GEOMETRIC_REPRESENTATION_ITEM ( )  RATIONAL_B_SPLINE_SURFACE ( (
 ( 1.000000000000000000, 1.000000000000000000),
 ( 0.9729067724841187204, 0.9999501103223794596),
 ( 0.9729067724841187204, 0.9999501103223794596),
 ( 1.000000000000000000, 1.000000000000000000) ) ) 
 REPRESENTATION_ITEM ( '' )  SURFACE ( )  );
#25792=FACE_OUTER_BOUND ( 'NONE', #48378, .T. ) ;
#25805=DIRECTION ( 'NONE',  ( -0.07906939808003035641, -0.6374189498685002286, 0.7664496804329689050 ) ) ;
#25807=CARTESIAN_POINT ( 'NONE',  ( 1.157643937452369487, -34.08380114724293009, 24.39870434982061553 ) ) ;
#25808=ORIENTED_EDGE ( 'NONE', *, *, #53010, .T. ) ;
#25813=ORIENTED_EDGE ( 'NONE', *, *, #15789, .T. ) ;
#25818=CARTESIAN_POINT ( 'NONE',  ( 0.5806925824938499181, -38.35106547415185929, -26.98922265166007861 ) ) ;
#25824=ADVANCED_FACE ( 'NONE', ( #17233 ), #61364, .F. ) ;
#25826=ORIENTED_EDGE ( 'NONE', *, *, #38865, .T. ) ;
#25829=CARTESIAN_POINT ( 'NONE',  ( 0.6064782688330874194, 27.24299735947540313, 38.17268056202479443 ) ) ;
#25830=CARTESIAN_POINT ( 'NONE',  ( 4.962356264823608143, -29.56943756613123497, 29.94802096775367772 ) ) ;
#25832=ORIENTED_EDGE ( 'NONE', *, *, #24907, .T. ) ;
#25835=CARTESIAN_POINT ( 'NONE',  ( 5.896782393890504181, 8.460428369634545476, -18.24684188237228000 ) ) ;
#25839=CARTESIAN_POINT ( 'NONE',  ( 4.956445790444004018, -40.78973928653763181, -23.53157918788973291 ) ) ;
#25841=CARTESIAN_POINT ( 'NONE',  ( 2.618530812446115519, 44.94501346709303391, -13.77216590232000115 ) ) ;
#25846=CARTESIAN_POINT ( 'NONE',  ( 4.960386119450136633, 13.41207489487415572, 41.64796167505232916 ) ) ;
#25847=CARTESIAN_POINT ( 'NONE',  ( 0.8560838555295167129, -41.44626783305055540, -21.96769712083564841 ) ) ;
#25852=CARTESIAN_POINT ( 'NONE',  ( 4.962356264823608143, -25.31392337492896161, 33.62202970123266965 ) ) ;
#25856=CARTESIAN_POINT ( 'NONE',  ( 4.956445790444011124, -17.42806872899762993, -43.74700527484106516 ) ) ;
#25859=CARTESIAN_POINT ( 'NONE',  ( 0.8554163680231816613, 42.82911630180360163, -19.15391004255791074 ) ) ;
#25860=CARTESIAN_POINT ( 'NONE',  ( 0.5835871038041858805, 27.92758718982630839, -37.67339016674964114 ) ) ;
#25861=ORIENTED_EDGE ( 'NONE', *, *, #18254, .F. ) ;
#25869=CARTESIAN_POINT ( 'NONE',  ( 0.9789889208857696090, -31.01704594793936565, 28.18293382005832726 ) ) ;
#25870=EDGE_CURVE ( 'NONE', #31937, #9918, #33499, .T. ) ;
#25871=B_SPLINE_CURVE_WITH_KNOTS ( 'NONE', 3,
 ( #46193, #50253, #22366, #7314 ),
 .UNSPECIFIED., .F., .F.,
 ( 4, 4 ),
 ( 0.000000000000000000, 0.004446298630425043336 ),
 .UNSPECIFIED. ) ;
#25881=EDGE_LOOP ( 'NONE', ( #4445, #36407, #50811, #42511 ) ) ;
#25884=CARTESIAN_POINT ( 'NONE',  ( 2.282816707992309624, -24.15823995494712761, 40.28494022196337454 ) ) ;
#25890=( BOUNDED_SURFACE ( )  B_SPLINE_SURFACE ( 3, 1, ( 
 ( #53712, #10844 ),
 ( #34965, #25540 ),
 ( #53417, #9915 ),
 ( #10524, #44675 ) ),
 .UNSPECIFIED., .F., .F., .F. ) 
 B_SPLINE_SURFACE_WITH_KNOTS ( ( 4, 4 ),
 ( 2, 2 ),
 ( 0.000000000000000000, 1.000000000000000000 ),
 ( 0.000000000000000000, 1.000000000000000000 ),
 .UNSPECIFIED. ) 
 GEOMETRIC_REPRESENTATION_ITEM ( )  RATIONAL_B_SPLINE_SURFACE ( (
 ( 1.000000000000000000, 1.000000000000000000),
 ( 0.9952954269826590483, 0.8620686068821339365),
 ( 0.9952954269826590483, 0.8620686068821339365),
 ( 1.000000000000000000, 1.000000000000000000) ) ) 
 REPRESENTATION_ITEM ( '' )  SURFACE ( )  );
#25897=B_SPLINE_CURVE_WITH_KNOTS ( 'NONE', 3,
 ( #15326, #21246, #5876, #6487 ),
 .UNSPECIFIED., .F., .F.,
 ( 4, 4 ),
 ( 8.673617379884035472E-19, 0.004446298630425045070 ),
 .UNSPECIFIED. ) ;
#25903=CARTESIAN_POINT ( 'NONE',  ( 4.956445790443991584, 25.79263028817558023, 39.39896284113483915 ) ) ;
#25904=EDGE_LOOP ( 'NONE', ( #40377, #22456, #36798, #11185 ) ) ;
#25906=( BOUNDED_SURFACE ( )  B_SPLINE_SURFACE ( 3, 1, ( 
 ( #48343, #43673 ),
 ( #53029, #33644 ),
 ( #9821, #28924 ),
 ( #19543, #713 ) ),
 .UNSPECIFIED., .F., .F., .F. ) 
 B_SPLINE_SURFACE_WITH_KNOTS ( ( 4, 4 ),
 ( 2, 2 ),
 ( 0.000000000000000000, 1.000000000000000000 ),
 ( 0.000000000000000000, 1.000000000000000000 ),
 .UNSPECIFIED. ) 
 GEOMETRIC_REPRESENTATION_ITEM ( )  RATIONAL_B_SPLINE_SURFACE ( (
 ( 1.000000000000000000, 1.000000000000000000),
 ( 0.7282232189291694135, 0.9929344683865672927),
 ( 0.7282232189291694135, 0.9929344683865672927),
 ( 1.000000000000000000, 1.000000000000000000) ) ) 
 REPRESENTATION_ITEM ( '' )  SURFACE ( )  );
#25909=ORIENTED_EDGE ( 'NONE', *, *, #6740, .F. ) ;
#25914=CARTESIAN_POINT ( 'NONE',  ( 0.5817217712918332229, -20.15223009300066792, 42.34527808725705000 ) ) ;
#25915=CARTESIAN_POINT ( 'NONE',  ( 3.238018933889920792, 3.371911215444494125, 12.96293589904742838 ) ) ;
#25925=ORIENTED_EDGE ( 'NONE', *, *, #13623, .F. ) ;
#25927=CARTESIAN_POINT ( 'NONE',  ( 0.9787284016396613495, 25.00986318006678744, 33.62800533250774748 ) ) ;
#25930=ORIENTED_EDGE ( 'NONE', *, *, #43760, .T. ) ;
#25934=ORIENTED_EDGE ( 'NONE', *, *, #5691, .T. ) ;
#25942=ORIENTED_EDGE ( 'NONE', *, *, #14781, .T. ) ;
#25943=DIRECTION ( 'NONE',  ( 0.07500201931887537365, -0.08636880102338072296, -0.9934360207420882549 ) ) ;
#25958=CARTESIAN_POINT ( 'NONE',  ( 1.231276596079887264, 19.39962232756291272, -37.16088568059149111 ) ) ;
#25963=CARTESIAN_POINT ( 'NONE',  ( 0.9775691876210983455, 9.347414102159763871, 40.85290147092045032 ) ) ;
#25979=CARTESIAN_POINT ( 'NONE',  ( 4.960386119450140185, -15.28553149072569006, 40.99742664751502019 ) ) ;
#25980=ORIENTED_EDGE ( 'NONE', *, *, #47037, .F. ) ;
#25985=CARTESIAN_POINT ( 'NONE',  ( 5.894904586330512508, 20.06808393774118215, 1.342169560605994905 ) ) ;
#25988=ORIENTED_EDGE ( 'NONE', *, *, #17818, .F. ) ;
#25991=ORIENTED_EDGE ( 'NONE', *, *, #41212, .T. ) ;
#26004=EDGE_LOOP ( 'NONE', ( #5441, #4944, #51833, #12088 ) ) ;
#26010=CARTESIAN_POINT ( 'NONE',  ( 0.5837800304671226792, -46.78824101889156850, -3.177709007698712007 ) ) ;
#26016=CARTESIAN_POINT ( 'NONE',  ( 3.782625744892853970, 35.26065757000644396, -22.88938906624093761 ) ) ;
#26025=CARTESIAN_POINT ( 'NONE',  ( 0.9790850452238881729, 41.52796822506905983, -5.636061156592599986 ) ) ;
#26026=ADVANCED_FACE ( 'NONE', ( #12162 ), #6101, .F. ) ;
#26027=CARTESIAN_POINT ( 'NONE',  ( 2.891212509700765487, 5.349982771599759140E-15, 41.99381090189422139 ) ) ;
#26037=CARTESIAN_POINT ( 'NONE',  ( 0.5837799406558230597, 32.66722334661169214, 33.64663532063480744 ) ) ;
#26039=CARTESIAN_POINT ( 'NONE',  ( 0.5848930533535030563, -13.72019472029311160, 44.84450177251164149 ) ) ;
#26040=CARTESIAN_POINT ( 'NONE',  ( 3.238018933889920792, -7.437505510345073567, 11.13961418323092545 ) ) ;
#26041=B_SPLINE_CURVE_WITH_KNOTS ( 'NONE', 3,
 ( #48530, #20652, #15964, #57912, #39794, #58219 ),
 .UNSPECIFIED., .F., .F.,
 ( 4, 2, 4 ),
 ( 0.000000000000000000, 0.0002291459268755687982, 0.0004582918537511375965 ),
 .UNSPECIFIED. ) ;
#26043=CARTESIAN_POINT ( 'NONE',  ( 3.661921753702023441, 20.93653541326595757, -42.12235283935475394 ) ) ;
#26044=ORIENTED_EDGE ( 'NONE', *, *, #206, .T. ) ;
#26067=CARTESIAN_POINT ( 'NONE',  ( 5.896278296736517710, -19.93412839397023006, 2.675351339000858975 ) ) ;
#26072=CARTESIAN_POINT ( 'NONE',  ( 0.9790320750461904975, 36.01440475631515881, 21.43128047015612125 ) ) ;
#26080=EDGE_LOOP ( 'NONE', ( #15670, #22210, #17644, #25055 ) ) ;
#26081=FACE_OUTER_BOUND ( 'NONE', #46580, .T. ) ;
#26084=VERTEX_POINT ( 'NONE', #34728 ) ;
#26097=ADVANCED_FACE ( 'NONE', ( #21232 ), #22605, .F. ) ;
#26100=CARTESIAN_POINT ( 'NONE',  ( 0.8560838555295158248, 5.603718208094640829, -46.57221463840858888 ) ) ;
#26101=CARTESIAN_POINT ( 'NONE',  ( 0.5804410086790514622, -34.41390132670994007, 31.86225427258511544 ) ) ;
#26110=ORIENTED_EDGE ( 'NONE', *, *, #22187, .T. ) ;
#26111=VERTEX_POINT ( 'NONE', #42219 ) ;
#26112=EDGE_CURVE ( 'NONE', #55162, #23761, #46642, .T. ) ;
#26123=VERTEX_POINT ( 'NONE', #36273 ) ;
#26132=EDGE_CURVE ( 'NONE', #14444, #16055, #40740, .T. ) ;
#26135=ORIENTED_EDGE ( 'NONE', *, *, #27579, .F. ) ;
#26141=CARTESIAN_POINT ( 'NONE',  ( 5.894904586330512508, -11.93156318452989950, -16.19157842939388914 ) ) ;
#26143=B_SPLINE_CURVE_WITH_KNOTS ( 'NONE', 3,
 ( #40761, #7183, #55424, #12548, #31640, #11614 ),
 .UNSPECIFIED., .F., .F.,
 ( 4, 2, 4 ),
 ( 6.106282077343213345E-18, 0.0002291472222819927729, 0.0004582944445639794743 ),
 .UNSPECIFIED. ) ;
#26144=VERTEX_POINT ( 'NONE', #26545 ) ;
#26148=CARTESIAN_POINT ( 'NONE',  ( 0.5848930533535030563, -34.90273318373206735, 31.32207366527264725 ) ) ;
#26150=ORIENTED_EDGE ( 'NONE', *, *, #44242, .T. ) ;
#26169=ORIENTED_EDGE ( 'NONE', *, *, #16366, .F. ) ;
#26171=CARTESIAN_POINT ( 'NONE',  ( 0.8560838555295223751, 46.89922841446243496, -0.9138972643637069959 ) ) ;
#26174=CARTESIAN_POINT ( 'NONE',  ( 0.5824936645240084143, -34.53516756923718134, -31.72633574816064694 ) ) ;
#26180=CARTESIAN_POINT ( 'NONE',  ( 5.917102823773431552, -18.51268610137615056, -7.859400191086862719 ) ) ;
#26189=LINE ( 'NONE', #45026, #32206 ) ;
#26198=ORIENTED_EDGE ( 'NONE', *, *, #47910, .F. ) ;
#26208=CARTESIAN_POINT ( 'NONE',  ( 5.838029081930955932, 42.14833990873909642, 21.32094043634829461 ) ) ;
#26211=VERTEX_POINT ( 'NONE', #31553 ) ;
#26212=EDGE_CURVE ( 'NONE', #9808, #6747, #38443, .T. ) ;
#26216=CARTESIAN_POINT ( 'NONE',  ( 3.238018933889920792, 8.164940828002086093, -10.61796749113866767 ) ) ;
#26218=CARTESIAN_POINT ( 'NONE',  ( 0.9780106845699481077, 3.882692594035769496, 41.72835899811612848 ) ) ;
#26224=ORIENTED_EDGE ( 'NONE', *, *, #53242, .F. ) ;
#26234=CARTESIAN_POINT ( 'NONE',  ( 0.9790850452238875068, 38.56342381347958792, -16.40730550837503898 ) ) ;
#26240=CARTESIAN_POINT ( 'NONE',  ( 4.962356264823600149, -40.47344704301802665, 11.53844366967928892 ) ) ;
#26250=CARTESIAN_POINT ( 'NONE',  ( 4.291220156522060236, 2.567299637375230592, -47.04038658299514708 ) ) ;
#26259=DIRECTION ( 'NONE',  ( 0.000000000000000000, 0.000000000000000000, 1.000000000000000000 ) ) ;
#26260=CARTESIAN_POINT ( 'NONE',  ( 0.9787464366903563251, 9.542966726804086974, 40.80766813898550538 ) ) ;
#26261=ADVANCED_FACE ( 'NONE', ( #24628 ), #18580, .F. ) ;
#26265=( BOUNDED_SURFACE ( )  B_SPLINE_SURFACE ( 3, 1, ( 
 ( #60186, #17297 ),
 ( #8483, #31388 ),
 ( #35799, #36416 ),
 ( #55482, #31700 ) ),
 .UNSPECIFIED., .F., .F., .F. ) 
 B_SPLINE_SURFACE_WITH_KNOTS ( ( 4, 4 ),
 ( 2, 2 ),
 ( 0.000000000000000000, 1.000000000000000000 ),
 ( 0.000000000000000000, 1.000000000000000000 ),
 .UNSPECIFIED. ) 
 GEOMETRIC_REPRESENTATION_ITEM ( )  RATIONAL_B_SPLINE_SURFACE ( (
 ( 1.000000000000000000, 1.000000000000000000),
 ( 0.7282232189291694135, 0.9929344683865672927),
 ( 0.7282232189291694135, 0.9929344683865672927),
 ( 1.000000000000000000, 1.000000000000000000) ) ) 
 REPRESENTATION_ITEM ( '' )  SURFACE ( )  );
#26266=ORIENTED_EDGE ( 'NONE', *, *, #40389, .F. ) ;
#26272=CARTESIAN_POINT ( 'NONE',  ( 0.5782707292762423457, 46.57382484760229602, 5.533099743586860519 ) ) ;
#26287=CARTESIAN_POINT ( 'NONE',  ( 3.782625744892855746, -35.60519336021494041, -22.34968254532283183 ) ) ;
#26292=EDGE_LOOP ( 'NONE', ( #22259, #6952, #27656, #36658 ) ) ;
#26294=CARTESIAN_POINT ( 'NONE',  ( 2.618530812446111078, 21.34567399517355213, 41.88184560033108284 ) ) ;
#26295=EDGE_LOOP ( 'NONE', ( #51605, #60356, #44496, #27162 ) ) ;
#26303=EDGE_CURVE ( 'NONE', #40451, #35096, #42950, .T. ) ;
#26304=CARTESIAN_POINT ( 'NONE',  ( 0.5797568599927139799, -44.50349610438583170, 14.78729668187938806 ) ) ;
#26307=ORIENTED_EDGE ( 'NONE', *, *, #42124, .T. ) ;
#26315=CARTESIAN_POINT ( 'NONE',  ( 0.9785694773339231878, 40.47783839118113747, -10.85725586380356766 ) ) ;
#26321=EDGE_LOOP ( 'NONE', ( #41544, #27662, #366, #7862 ) ) ;
#26328=AXIS2_PLACEMENT_3D ( 'NONE', #50609, #21815, #49384 ) ;
#26329=ADVANCED_FACE ( 'NONE', ( #25541 ), #35843, .T. ) ;
#26330=ORIENTED_EDGE ( 'NONE', *, *, #29823, .F. ) ;
#26332=CARTESIAN_POINT ( 'NONE',  ( 2.528100132419517365, -11.27643546515609962, 40.43631760969642386 ) ) ;
#26341=CARTESIAN_POINT ( 'NONE',  ( 4.958415959904820092, 37.15973263041097141, 26.12198737958135197 ) ) ;
#26343=CARTESIAN_POINT ( 'NONE',  ( 4.291220156522060236, 45.95810865397713485, 10.35573494518514792 ) ) ;
#26356=VERTEX_POINT ( 'NONE', #49651 ) ;
#26374=CARTESIAN_POINT ( 'NONE',  ( 0.8560838555295158248, -6.899551485031924614, -46.39794201672231111 ) ) ;
#26376=CARTESIAN_POINT ( 'NONE',  ( 0.5806925824938502512, 27.37593026015236219, -38.07598724570169679 ) ) ;
#26378=EDGE_CURVE ( 'NONE', #59637, #57224, #53713, .T. ) ;
#26387=CARTESIAN_POINT ( 'NONE',  ( 3.661921753701995463, 45.82839444823501651, 10.60138604763640835 ) ) ;
#26389=( NAMED_UNIT ( * ) SI_UNIT ( $, .STERADIAN. ) SOLID_ANGLE_UNIT ( ) );
#26390=B_SPLINE_CURVE_WITH_KNOTS ( 'NONE', 3,
 ( #47738, #57404, #13934, #4175 ),
 .UNSPECIFIED., .F., .F.,
 ( 4, 4 ),
 ( 0.000000000000000000, 0.005004948556313794025 ),
 .UNSPECIFIED. ) ;
#26406=CARTESIAN_POINT ( 'NONE',  ( 0.5835871038041854364, -13.76363918287266586, -44.83075606484005959 ) ) ;
#26413=CARTESIAN_POINT ( 'NONE',  ( 0.5806925824938499181, 23.01490136172973067, -40.85996423950240342 ) ) ;
#26415=ORIENTED_EDGE ( 'NONE', *, *, #35059, .F. ) ;
#26422=CIRCLE ( 'NONE', #30398, 42.08604991992415023 ) ;
#26427=CARTESIAN_POINT ( 'NONE',  ( 4.962356264823609031, -20.60668162140307658, 36.69605251817252878 ) ) ;
#26434=EDGE_CURVE ( 'NONE', #16055, #61015, #25235, .T. ) ;
#26439=VERTEX_POINT ( 'NONE', #59043 ) ;
#26442=CARTESIAN_POINT ( 'NONE',  ( 0.5806925824938499181, -44.11884900496058748, -15.89809815106991309 ) ) ;
#26453=CARTESIAN_POINT ( 'NONE',  ( 2.282816707992306959, 12.16314365252773300, 45.37130043205660712 ) ) ;
#26458=CARTESIAN_POINT ( 'NONE',  ( 0.8554163680231738898, -26.01084021241273092, 39.04666009476549959 ) ) ;
#26465=EDGE_CURVE ( 'NONE', #13205, #11980, #30941, .T. ) ;
#26474=CARTESIAN_POINT ( 'NONE',  ( 2.282816707992324723, 44.93953228679972511, -13.67243227270301809 ) ) ;
#26475=EDGE_LOOP ( 'NONE', ( #17254, #2767, #4179, #12120 ) ) ;
#26482=CARTESIAN_POINT ( 'NONE',  ( 4.291220156522060236, -46.54716543045775978, -7.262946213162822851 ) ) ;
#26485=CIRCLE ( 'NONE', #48484, 42.08604991992415023 ) ;
#26492=ORIENTED_EDGE ( 'NONE', *, *, #54374, .F. ) ;
#26496=ORIENTED_EDGE ( 'NONE', *, *, #9460, .F. ) ;
#26497=DIRECTION ( 'NONE',  ( 0.9990097760809871774, 0.000000000000000000, -0.04449120468829421277 ) ) ;
#26498=CARTESIAN_POINT ( 'NONE',  ( 0.8554163680231738898, -35.40260165760500399, 30.78735566729891815 ) ) ;
#26500=ORIENTED_EDGE ( 'NONE', *, *, #43667, .T. ) ;
#26505=DIRECTION ( 'NONE',  ( 0.000000000000000000, 0.000000000000000000, 1.000000000000000000 ) ) ;
#26510=CARTESIAN_POINT ( 'NONE',  ( 5.895596859100789899, -18.51832497669328959, 7.848555489391991991 ) ) ;
#26516=VERTEX_POINT ( 'NONE', #42149 ) ;
#26521=CARTESIAN_POINT ( 'NONE',  ( 4.962356264823609031, -32.75738977283769771, -26.42326651140497873 ) ) ;
#26522=CARTESIAN_POINT ( 'NONE',  ( 0.5835871038041856584, -19.86395462753460350, 42.48126362829555092 ) ) ;
#26525=LINE ( 'NONE', #22142, #41435 ) ;
#26527=ORIENTED_EDGE ( 'NONE', *, *, #53849, .F. ) ;
#26532=CARTESIAN_POINT ( 'NONE',  ( 5.896278296736517710, -7.223603833371068816, -18.77089575041346947 ) ) ;
#26544=EDGE_CURVE ( 'NONE', #19096, #37493, #61540, .T. ) ;
#26545=CARTESIAN_POINT ( 'NONE',  ( 4.962356264823601926, -38.91448554252674796, -16.02805081171206680 ) ) ;
#26550=CARTESIAN_POINT ( 'NONE',  ( 0.9789233960466703355, 38.63436055929081903, -16.23954774638314191 ) ) ;
#26556=CARTESIAN_POINT ( 'NONE',  ( 5.910764540655177868, 20.06833201846866288, -1.327888724881951754 ) ) ;
#26571=CARTESIAN_POINT ( 'NONE',  ( 4.962356264823608143, 18.10963840443066530, -37.99048031708887407 ) ) ;
#26572=CARTESIAN_POINT ( 'NONE',  ( 5.896782393890504181, 17.95394716461040829, 9.065421561537570838 ) ) ;
#26585=DIRECTION ( 'NONE',  ( 0.000000000000000000, 0.000000000000000000, 1.000000000000000000 ) ) ;
#26591=CARTESIAN_POINT ( 'NONE',  ( 0.5804410086790514622, -46.75463715370013773, -3.677466040800468239 ) ) ;
#26593=VERTEX_POINT ( 'NONE', #33967 ) ;
#26597=CARTESIAN_POINT ( 'NONE',  ( 0.5797568599927158672, 42.92520440875660626, 18.88523590367528726 ) ) ;
#26598=CARTESIAN_POINT ( 'NONE',  ( 0.9762797500689124330, -7.469026406145721886, -41.23758515880873432 ) ) ;
#26599=AXIS2_PLACEMENT_3D ( 'NONE', #30477, #12644, #40855 ) ;
#26605=ORIENTED_EDGE ( 'NONE', *, *, #39459, .T. ) ;
#26609=VECTOR ( 'NONE', #23479, 1000.000000000000114 ) ;
#26610=CARTESIAN_POINT ( 'NONE',  ( 1.092182651088185352, -37.75446286322829792, -18.20334360361852433 ) ) ;
#26616=ADVANCED_FACE ( 'NONE', ( #24234 ), #9787, .F. ) ;
#26618=VERTEX_POINT ( 'NONE', #28018 ) ;
#26619=( BOUNDED_SURFACE ( )  B_SPLINE_SURFACE ( 3, 1, ( 
 ( #31802, #8587 ),
 ( #13317, #16781 ),
 ( #17091, #27713 ),
 ( #35893, #12093 ) ),
 .UNSPECIFIED., .F., .F., .F. ) 
 B_SPLINE_SURFACE_WITH_KNOTS ( ( 4, 4 ),
 ( 2, 2 ),
 ( 0.000000000000000000, 1.000000000000000000 ),
 ( 0.000000000000000000, 1.000000000000000000 ),
 .UNSPECIFIED. ) 
 GEOMETRIC_REPRESENTATION_ITEM ( )  RATIONAL_B_SPLINE_SURFACE ( (
 ( 1.000000000000000000, 1.000000000000000000),
 ( 0.9729067724841187204, 0.9999501103223794596),
 ( 0.9729067724841187204, 0.9999501103223794596),
 ( 1.000000000000000000, 1.000000000000000000) ) ) 
 REPRESENTATION_ITEM ( '' )  SURFACE ( )  );
#26620=ORIENTED_EDGE ( 'NONE', *, *, #54010, .F. ) ;
#26622=CARTESIAN_POINT ( 'NONE',  ( 0.9783242366443547500, 40.48960050396856047, -10.81326690855047623 ) ) ;
#26626=( BOUNDED_SURFACE ( )  B_SPLINE_SURFACE ( 3, 1, ( 
 ( #44434, #26208 ),
 ( #45349, #2394 ),
 ( #29675, #30290 ),
 ( #48789, #1462 ) ),
 .UNSPECIFIED., .F., .F., .F. ) 
 B_SPLINE_SURFACE_WITH_KNOTS ( ( 4, 4 ),
 ( 2, 2 ),
 ( 0.000000000000000000, 1.000000000000000000 ),
 ( 0.000000000000000000, 1.000000000000000000 ),
 .UNSPECIFIED. ) 
 GEOMETRIC_REPRESENTATION_ITEM ( )  RATIONAL_B_SPLINE_SURFACE ( (
 ( 1.000000000000000000, 1.000000000000000000),
 ( 0.7282232189291693025, 0.9929344683865674037),
 ( 0.7282232189291693025, 0.9929344683865674037),
 ( 1.000000000000000000, 1.000000000000000000) ) ) 
 REPRESENTATION_ITEM ( '' )  SURFACE ( )  );
#26627=B_SPLINE_CURVE_WITH_KNOTS ( 'NONE', 3,
 ( #7980, #60583, #36826, #32110, #40602, #44993 ),
 .UNSPECIFIED., .F., .F.,
 ( 4, 2, 4 ),
 ( 3.476216610979977084E-18, 0.0002291459268755703161, 0.0004582918537511371628 ),
 .UNSPECIFIED. ) ;
#26632=CARTESIAN_POINT ( 'NONE',  ( 0.9762797500689124330, 19.69530149098661909, 36.99215976885973589 ) ) ;
#26637=FACE_OUTER_BOUND ( 'NONE', #37819, .T. ) ;
#26643=CARTESIAN_POINT ( 'NONE',  ( 0.9780303403264780648, 29.36652971755217933, 29.89893887319762200 ) ) ;
#26647=CARTESIAN_POINT ( 'NONE',  ( 0.5804410086790514622, -13.37224000219899800, 44.95223074752782821 ) ) ;
#26651=EDGE_CURVE ( 'NONE', #8551, #3462, #50347, .T. ) ;
#26656=CARTESIAN_POINT ( 'NONE',  ( 0.5797568599927147570, -46.07736688617723786, 8.723621352834124210 ) ) ;
#26657=FACE_OUTER_BOUND ( 'NONE', #60927, .T. ) ;
#26659=ORIENTED_EDGE ( 'NONE', *, *, #8711, .T. ) ;
#26671=EDGE_LOOP ( 'NONE', ( #12422, #29075, #27261, #2568 ) ) ;
#26672=VERTEX_POINT ( 'NONE', #38066 ) ;
#26676=EDGE_LOOP ( 'NONE', ( #35056, #3554, #41350, #25980 ) ) ;
#26690=B_SPLINE_CURVE_WITH_KNOTS ( 'NONE', 3,
 ( #11789, #49987, #26174, #45311, #2353, #59681, #16795, #3272, #22099, #3582, #13638, #8286, #13030, #37773, #51508, #41227 ),
 .UNSPECIFIED., .F., .F.,
 ( 4, 3, 3, 3, 3, 4 ),
 ( 1.962735358247463844E-17, 0.0002732102107931921680, 0.0004098135523333891776, 0.0005464168938825009854, 0.0008195847345945413837, 0.001092771384553105265 ),
 .UNSPECIFIED. ) ;
#26699=PRESENTATION_STYLE_ASSIGNMENT (( #36129 ) ) ;
#26706=VECTOR ( 'NONE', #511, 1000.000000000000114 ) ;
#26717=CARTESIAN_POINT ( 'NONE',  ( 0.5817216825391134938, -14.32835586215152901, -44.65347881738895808 ) ) ;
#26723=EDGE_CURVE ( 'NONE', #37975, #46746, #18850, .T. ) ;
#26734=EDGE_CURVE ( 'NONE', #30011, #13746, #45176, .T. ) ;
#26738=DIRECTION ( 'NONE',  ( 0.000000000000000000, 0.000000000000000000, 1.000000000000000000 ) ) ;
#26743=EDGE_CURVE ( 'NONE', #46325, #34231, #33172, .T. ) ;
#26744=( BOUNDED_SURFACE ( )  B_SPLINE_SURFACE ( 3, 1, ( 
 ( #41336, #51931 ),
 ( #46039, #17204 ),
 ( #23435, #18434 ),
 ( #8097, #4297 ) ),
 .UNSPECIFIED., .F., .F., .F. ) 
 B_SPLINE_SURFACE_WITH_KNOTS ( ( 4, 4 ),
 ( 2, 2 ),
 ( 0.000000000000000000, 1.000000000000000000 ),
 ( 0.000000000000000000, 1.000000000000000000 ),
 .UNSPECIFIED. ) 
 GEOMETRIC_REPRESENTATION_ITEM ( )  RATIONAL_B_SPLINE_SURFACE ( (
 ( 1.000000000000000000, 1.000000000000000000),
 ( 0.9952954269826590483, 0.8620686068821339365),
 ( 0.9952954269826590483, 0.8620686068821339365),
 ( 1.000000000000000000, 1.000000000000000000) ) ) 
 REPRESENTATION_ITEM ( '' )  SURFACE ( )  );
#26745=CARTESIAN_POINT ( 'NONE',  ( 0.8554163680231720024, 45.48289776771366633, 11.51136324522541088 ) ) ;
#26754=VERTEX_POINT ( 'NONE', #40844 ) ;
#26773=CARTESIAN_POINT ( 'NONE',  ( 5.895596859100789899, 12.98817590332826200, -15.35693556399487392 ) ) ;
#26775=CARTESIAN_POINT ( 'NONE',  ( 5.838029081930957709, 47.12733084333035549, -3.174861530240974172 ) ) ;
#26789=CARTESIAN_POINT ( 'NONE',  ( 0.8554163680231708922, 9.985124899324334891, 45.84215040611327652 ) ) ;
#26793=CARTESIAN_POINT ( 'NONE',  ( 0.9762797500689124330, 41.59901070109202692, -5.084003725031680077 ) ) ;
#26808=ORIENTED_EDGE ( 'NONE', *, *, #15484, .T. ) ;
#26810=FACE_OUTER_BOUND ( 'NONE', #55297, .T. ) ;
#26812=CARTESIAN_POINT ( 'NONE',  ( 0.5804410086790514622, 23.01644811389264689, -40.86273324284469055 ) ) ;
#26824=CARTESIAN_POINT ( 'NONE',  ( 0.8560838555295158248, -13.02223058219810881, -45.06433561859972059 ) ) ;
#26830=ORIENTED_EDGE ( 'NONE', *, *, #35863, .T. ) ;
#26838=B_SPLINE_CURVE_WITH_KNOTS ( 'NONE', 3,
 ( #28689, #39047, #39347, #5478 ),
 .UNSPECIFIED., .F., .F.,
 ( 4, 4 ),
 ( 1.430489624538199204E-17, 0.005004948556313822648 ),
 .UNSPECIFIED. ) ;
#26843=VERTEX_POINT ( 'NONE', #50509 ) ;
#26846=ORIENTED_EDGE ( 'NONE', *, *, #47930, .F. ) ;
#26853=VERTEX_POINT ( 'NONE', #36436 ) ;
#26860=CARTESIAN_POINT ( 'NONE',  ( 3.238018933889920792, 1.614035038994167559, 13.29670572963665087 ) ) ;
#26861=CARTESIAN_POINT ( 'NONE',  ( 4.962356264823608143, 6.570263404306589727, 41.57002810511892221 ) ) ;
#26866=CARTESIAN_POINT ( 'NONE',  ( 5.901463166500145796, 20.06867656024513380, -1.328943738803248786 ) ) ;
#26873=CARTESIAN_POINT ( 'NONE',  ( 0.5797568665920720399, -42.13545912329951904, -20.58709287564965607 ) ) ;
#26874=CARTESIAN_POINT ( 'NONE',  ( 0.5835226383429291674, 45.27760575932801146, 12.21396296248002500 ) ) ;
#26878=CARTESIAN_POINT ( 'NONE',  ( 0.8560838555295223751, 5.603718208093996012, 46.57221463840868125 ) ) ;
#26883=EDGE_CURVE ( 'NONE', #16119, #3024, #2523, .T. ) ;
#26886=CONICAL_SURFACE ( 'NONE', #21885, 42.08604991992415023, 1.569615340895231137 ) ;
#26909=VERTEX_POINT ( 'NONE', #51736 ) ;
#26914=CARTESIAN_POINT ( 'NONE',  ( 4.962356264823608143, 0.000000000000000000, 0.000000000000000000 ) ) ;
#26927=VERTEX_POINT ( 'NONE', #57648 ) ;
#26934=ORIENTED_EDGE ( 'NONE', *, *, #37497, .F. ) ;
#26935=CARTESIAN_POINT ( 'NONE',  ( 0.9790850452238860635, -17.59487447451424913, 38.03626851426523814 ) ) ;
#26937=VERTEX_POINT ( 'NONE', #3808 ) ;
#26942=CARTESIAN_POINT ( 'NONE',  ( 0.5817217712918332229, -44.44846655092862164, 14.95221640023155807 ) ) ;
#26947=DIRECTION ( 'NONE',  ( -0.07500201931887527651, -0.4074616462826595731, 0.9101371896075425294 ) ) ;
#26963=CARTESIAN_POINT ( 'NONE',  ( 5.896278296736517710, -18.51475911848188716, -7.856887067979012151 ) ) ;
#26967=ADVANCED_FACE ( 'NONE', ( #37359 ), #22976, .F. ) ;
#26973=CARTESIAN_POINT ( 'NONE',  ( 0.8560838555295158248, -18.91252766612255698, -42.92655508376930129 ) ) ;
#26975=ORIENTED_EDGE ( 'NONE', *, *, #20231, .T. ) ;
#26979=B_SPLINE_CURVE_WITH_KNOTS ( 'NONE', 3,
 ( #47642, #56706, #38264, #33555 ),
 .UNSPECIFIED., .F., .F.,
 ( 4, 4 ),
 ( 3.127317220692750759E-18, 0.004042984057420972825 ),
 .UNSPECIFIED. ) ;
#26990=ORIENTED_EDGE ( 'NONE', *, *, #17240, .T. ) ;
#26998=AXIS2_PLACEMENT_3D ( 'NONE', #57607, #44197, #1229 ) ;
#27006=B_SPLINE_CURVE_WITH_KNOTS ( 'NONE', 3,
 ( #57223, #19670, #14360, #535 ),
 .UNSPECIFIED., .F., .F.,
 ( 4, 4 ),
 ( 8.673617379884035472E-19, 0.004041751736740995145 ),
 .UNSPECIFIED. ) ;
#27008=B_SPLINE_CURVE_WITH_KNOTS ( 'NONE', 3,
 ( #13828, #32931, #12904, #4070 ),
 .UNSPECIFIED., .F., .F.,
 ( 4, 4 ),
 ( 1.192622389734054877E-18, 0.004446298630425097979 ),
 .UNSPECIFIED. ) ;
#27010=CARTESIAN_POINT ( 'NONE',  ( 3.782542959838394392, -25.80139896681886924, -33.18924019545502091 ) ) ;
#27021=VERTEX_POINT ( 'NONE', #2110 ) ;
#27022=CARTESIAN_POINT ( 'NONE',  ( 0.9790724872846777727, -39.57652792371481354, -13.78526922061647575 ) ) ;
#27030=CARTESIAN_POINT ( 'NONE',  ( 0.9790850452238869517, 32.92126328992468132, 25.93314006553496398 ) ) ;
#27033=CARTESIAN_POINT ( 'NONE',  ( 0.5835226383429282793, -14.06802566813686717, -44.73626189509590745 ) ) ;
#27041=ORIENTED_EDGE ( 'NONE', *, *, #15178, .T. ) ;
#27045=CARTESIAN_POINT ( 'NONE',  ( 0.6845945791218034371, -8.654967045698466421, 46.10312425586597129 ) ) ;
#27067=ORIENTED_EDGE ( 'NONE', *, *, #16655, .T. ) ;
#27069=CARTESIAN_POINT ( 'NONE',  ( 4.956445790443988031, 0.000000000000000000, 0.000000000000000000 ) ) ;
#27071=CARTESIAN_POINT ( 'NONE',  ( 5.895596859100789899, -2.009647457887034694, 20.01223376606159121 ) ) ;
#27072=DIRECTION ( 'NONE',  ( 1.000000000000000000, -0.000000000000000000, -0.000000000000000000 ) ) ;
#27073=EDGE_CURVE ( 'NONE', #11037, #21146, #5385, .T. ) ;
#27074=B_SPLINE_CURVE_WITH_KNOTS ( 'NONE', 3,
 ( #12042, #31116, #20196, #58364, #1354, #20490 ),
 .UNSPECIFIED., .F., .F.,
 ( 4, 2, 4 ),
 ( 3.476216610979977084E-18, 0.0002291459268755713190, 0.0004582918537511391686 ),
 .UNSPECIFIED. ) ;
#27080=CARTESIAN_POINT ( 'NONE',  ( 5.896782393890504181, -18.51935720350329362, -7.845985957613155648 ) ) ;
#27084=ADVANCED_FACE ( 'NONE', ( #12173 ), #8146, .F. ) ;
#27085=CARTESIAN_POINT ( 'NONE',  ( 0.5848930533535030563, -7.620589013870455730, 46.27309915565668064 ) ) ;
#27086=CARTESIAN_POINT ( 'NONE',  ( 2.618530812446111078, 46.75512741918802107, -4.866708252370782084 ) ) ;
#27090=CARTESIAN_POINT ( 'NONE',  ( 5.896782393890504181, -15.78060201202832324, 12.46991126736593003 ) ) ;
#27092=CARTESIAN_POINT ( 'NONE',  ( 3.661933894777893439, 34.02818518232189149, -32.47635721797108488 ) ) ;
#27109=CARTESIAN_POINT ( 'NONE',  ( 0.9772918015221170318, -30.80181925274452226, 28.41803628810295734 ) ) ;
#27111=CARTESIAN_POINT ( 'NONE',  ( 0.8554163680231708922, -42.27859581856526461, 20.34025095032543007 ) ) ;
#27113=CARTESIAN_POINT ( 'NONE',  ( 0.9790320750461904975, -7.055398401008414311, 41.31051301963263001 ) ) ;
#27115=DIRECTION ( 'NONE',  ( -0.07500201931887529039, 0.9970919462213602147, -0.01350362464641123410 ) ) ;
#27118=CARTESIAN_POINT ( 'NONE',  ( 0.9762797500689124330, 3.691134646837550104, 41.74566217230983511 ) ) ;
#27127=ADVANCED_FACE ( 'NONE', ( #56284 ), #23802, .T. ) ;
#27130=CARTESIAN_POINT ( 'NONE',  ( 0.9790724872846775506, 24.89190385731563282, -33.71540200471602589 ) ) ;
#27149=CARTESIAN_POINT ( 'NONE',  ( 3.782625744892852637, -28.43542810602084359, -30.96230825572154544 ) ) ;
#27156=EDGE_CURVE ( 'NONE', #44940, #25242, #13641, .T. ) ;
#27159=CARTESIAN_POINT ( 'NONE',  ( 0.9788927965476029724, 24.97331521197592963, 33.65516513040856239 ) ) ;
#27162=ORIENTED_EDGE ( 'NONE', *, *, #28249, .F. ) ;
#27187=( BOUNDED_SURFACE ( )  B_SPLINE_SURFACE ( 3, 1, ( 
 ( #44924, #11705 ),
 ( #2891, #16390 ),
 ( #59912, #36138 ),
 ( #20786, #2583 ) ),
 .UNSPECIFIED., .F., .F., .F. ) 
 B_SPLINE_SURFACE_WITH_KNOTS ( ( 4, 4 ),
 ( 2, 2 ),
 ( 0.000000000000000000, 1.000000000000000000 ),
 ( 0.000000000000000000, 1.000000000000000000 ),
 .UNSPECIFIED. ) 
 GEOMETRIC_REPRESENTATION_ITEM ( )  RATIONAL_B_SPLINE_SURFACE ( (
 ( 1.000000000000000000, 1.000000000000000000),
 ( 0.9952954269826590483, 0.8620686068821339365),
 ( 0.9952954269826590483, 0.8620686068821339365),
 ( 1.000000000000000000, 1.000000000000000000) ) ) 
 REPRESENTATION_ITEM ( '' )  SURFACE ( )  );
#27192=CARTESIAN_POINT ( 'NONE',  ( 1.000110580585050979, 9.074284568952180052, 40.91545969842667319 ) ) ;
#27196=B_SPLINE_CURVE_WITH_KNOTS ( 'NONE', 3,
 ( #61851, #28060, #455, #18991, #38107, #4840, #14287, #9881, #57152, #43415, #33391, #28982, #5148, #20214, #41413, #49312 ),
 .UNSPECIFIED., .F., .F.,
 ( 4, 3, 3, 3, 3, 4 ),
 ( 6.939740885162003740E-18, 0.0002732102107932001369, 0.0004098135523333949239, 0.0005464168938825121526, 0.0008195847345945504910, 0.001092771384553109168 ),
 .UNSPECIFIED. ) ;
#27200=B_SPLINE_CURVE_WITH_KNOTS ( 'NONE', 3,
 ( #6298, #1930, #1611, #15437 ),
 .UNSPECIFIED., .F., .F.,
 ( 4, 4 ),
 ( 7.757919228897728493E-18, 0.004042984057420976295 ),
 .UNSPECIFIED. ) ;
#27208=DIRECTION ( 'NONE',  ( -0.07906939808003034253, -0.9784699099467746297, -0.1906427696400062044 ) ) ;
#27215=B_SPLINE_CURVE_WITH_KNOTS ( 'NONE', 3,
 ( #41645, #46968, #13439, #28140, #23144, #13762, #18139, #47570, #4005, #42272, #60710, #32239, #61330, #42889, #18445, #28442 ),
 .UNSPECIFIED., .F., .F.,
 ( 4, 3, 3, 3, 3, 4 ),
 ( 1.040890552917501732E-17, 0.0002732102107931885359, 0.0004098135523333784440, 0.0005464168938824964317, 0.0008195847345945472383, 0.001092771384553108951 ),
 .UNSPECIFIED. ) ;
#27225=CARTESIAN_POINT ( 'NONE',  ( 4.962356264823602814, 41.15374796524927348, -8.809348799717806600 ) ) ;
#27228=CARTESIAN_POINT ( 'NONE',  ( 5.896782393890504181, 16.58545041924871910, -11.37756218478521930 ) ) ;
#27230=EDGE_CURVE ( 'NONE', #15516, #31937, #12988, .T. ) ;
#27233=CARTESIAN_POINT ( 'NONE',  ( 1.231276596079881047, -7.805643096902013411, 41.18675402191647805 ) ) ;
#27239=CARTESIAN_POINT ( 'NONE',  ( 1.231276596079887264, -39.31472542100218703, 14.54747868495677743 ) ) ;
#27248=B_SPLINE_CURVE_WITH_KNOTS ( 'NONE', 3,
 ( #35367, #50362, #30021, #44469, #45385, #35988, #40692, #31263, #55052, #6807, #58822, #49133, #54739, #7429, #2429, #6185 ),
 .UNSPECIFIED., .F., .F.,
 ( 4, 3, 3, 3, 3, 4 ),
 ( 9.813676791237317679E-18, 0.0002732102107931819765, 0.0004098135523333702041, 0.0005464168938824769161, 0.0008195847345945384563, 0.001092771384553104397 ),
 .UNSPECIFIED. ) ;
#27251=CARTESIAN_POINT ( 'NONE',  ( 4.962356264823608143, 34.94214251265138671, -23.45809613945485950 ) ) ;
#27252=CARTESIAN_POINT ( 'NONE',  ( 0.5848930533535030563, 4.512869149483607956, 46.67876491968481645 ) ) ;
#27253=ADVANCED_FACE ( 'NONE', ( #39072 ), #48224, .F. ) ;
#27255=CARTESIAN_POINT ( 'NONE',  ( 120.0000507999999968, 9.797174393178825657E-16, -8.000000000000000000 ) ) ;
#27256=EDGE_CURVE ( 'NONE', #45995, #43148, #53124, .T. ) ;
#27261=ORIENTED_EDGE ( 'NONE', *, *, #14603, .T. ) ;
#27262=CARTESIAN_POINT ( 'NONE',  ( 1.157643937452368821, 41.64460120238013729, 4.767542898545625185 ) ) ;
#27268=CARTESIAN_POINT ( 'NONE',  ( 0.5797568599927128696, -38.30338218405706385, -27.05690710212579830 ) ) ;
#27270=CARTESIAN_POINT ( 'NONE',  ( 0.5806925824938499181, 23.01490136172973067, -40.85996423950240342 ) ) ;
#27274=ORIENTED_EDGE ( 'NONE', *, *, #43305, .T. ) ;
#27282=CARTESIAN_POINT ( 'NONE',  ( 4.956445790444004018, -46.73954499432468879, 5.740468958468036398 ) ) ;
#27283=ORIENTED_EDGE ( 'NONE', *, *, #35132, .F. ) ;
#27289=ORIENTED_EDGE ( 'NONE', *, *, #61166, .T. ) ;
#27291=CARTESIAN_POINT ( 'NONE',  ( 0.9754292580325137907, -6.395579163414738311, -41.41767779666673732 ) ) ;
#27297=DIRECTION ( 'NONE',  ( 0.07906939808003034253, -0.8535645278111539946, -0.5149520629629358304 ) ) ;
#27298=EDGE_CURVE ( 'NONE', #51245, #61317, #21175, .T. ) ;
#27302=CARTESIAN_POINT ( 'NONE',  ( 0.5806925824938499181, -44.11884900496058748, -15.89809815106991309 ) ) ;
#27303=CARTESIAN_POINT ( 'NONE',  ( 0.6064515330803583737, 46.89167588063442338, -0.7106821670863709972 ) ) ;
#27304=ORIENTED_EDGE ( 'NONE', *, *, #20282, .T. ) ;
#27309=CARTESIAN_POINT ( 'NONE',  ( 0.7056759521544992975, -30.91982873080885952, 35.26631566203700885 ) ) ;
#27316=CARTESIAN_POINT ( 'NONE',  ( 4.962356264823601926, -41.65024625884322518, 6.040909239515423579 ) ) ;
#27322=CARTESIAN_POINT ( 'NONE',  ( 5.896278296736517710, -20.11285533178147844, 0.005478796673511841103 ) ) ;
#27325=B_SPLINE_CURVE_WITH_KNOTS ( 'NONE', 3,
 ( #1882, #25702, #39523, #11947 ),
 .UNSPECIFIED., .F., .F.,
 ( 4, 4 ),
 ( 4.906538933386797396E-18, 0.004042984057420978897 ),
 .UNSPECIFIED. ) ;
#27332=B_SPLINE_CURVE_WITH_KNOTS ( 'NONE', 3,
 ( #35364, #6183, #44467, #34431 ),
 .UNSPECIFIED., .F., .F.,
 ( 4, 4 ),
 ( 0.000000000000000000, 0.005004948556313802699 ),
 .UNSPECIFIED. ) ;
#27335=CARTESIAN_POINT ( 'NONE',  ( 0.9754292589017201642, 35.75786470076489820, -21.85640818929475415 ) ) ;
#27336=CARTESIAN_POINT ( 'NONE',  ( 5.895881250540457863, -18.51869114342267508, 7.847659520061995408 ) ) ;
#27338=CARTESIAN_POINT ( 'NONE',  ( 4.958415959904820092, -43.93947138327082058, 11.51202885599944459 ) ) ;
#27348=CARTESIAN_POINT ( 'NONE',  ( 4.962356264823608143, -15.53171314616189846, 39.11523340857994668 ) ) ;
#27351=ORIENTED_EDGE ( 'NONE', *, *, #19682, .T. ) ;
#27358=ORIENTED_EDGE ( 'NONE', *, *, #18988, .T. ) ;
#27359=EDGE_LOOP ( 'NONE', ( #11728, #40380, #51874, #21685 ) ) ;
#27360=FACE_OUTER_BOUND ( 'NONE', #35472, .T. ) ;
#27366=CIRCLE ( 'NONE', #6359, 42.08604991992415023 ) ;
#27372=CARTESIAN_POINT ( 'NONE',  ( 0.5797568599927138688, 10.25842392134313208, 45.76013600636498779 ) ) ;
#27376=CARTESIAN_POINT ( 'NONE',  ( 0.7056759521544966329, -20.50402326997429014, 42.18215095109947299 ) ) ;
#27378=EDGE_CURVE ( 'NONE', #20909, #37975, #11414, .T. ) ;
#27380=CARTESIAN_POINT ( 'NONE',  ( 1.231276596079881047, 28.52807286890743654, 30.71523773966879745 ) ) ;
#27382=EDGE_CURVE ( 'NONE', #37898, #715, #172, .T. ) ;
#27386=CARTESIAN_POINT ( 'NONE',  ( 5.896782393890504181, 12.99025607003319038, -15.35510775321938404 ) ) ;
#27387=DIRECTION ( 'NONE',  ( 0.000000000000000000, 0.000000000000000000, 1.000000000000000000 ) ) ;
#27390=CARTESIAN_POINT ( 'NONE',  ( 0.8554163680231738898, 37.37991192211431013, -28.35397075908056408 ) ) ;
#27400=CARTESIAN_POINT ( 'NONE',  ( 0.9780303403264770656, -1.723996957088520299, -41.87323068366033851 ) ) ;
#27401=CARTESIAN_POINT ( 'NONE',  ( 0.6845945791218034371, 10.02997083120958166, 45.82364243312646579 ) ) ;
#27403=CARTESIAN_POINT ( 'NONE',  ( 0.5797568599927145350, -46.74494067847413703, -3.759764572009656636 ) ) ;
#27404=CARTESIAN_POINT ( 'NONE',  ( 0.5806925824938499181, -25.69265091980040339, 39.23149310256803801 ) ) ;
#27405=CARTESIAN_POINT ( 'NONE',  ( 0.5806925824938502512, 23.01490136172913026, 40.85996423950273737 ) ) ;
#27432=CARTESIAN_POINT ( 'NONE',  ( 0.9790850452238858415, 32.85849888024883825, -26.01261966046257257 ) ) ;
#27438=CARTESIAN_POINT ( 'NONE',  ( 5.910764540655178756, 5.973554503640659874, 19.20463186476631279 ) ) ;
#27444=EDGE_LOOP ( 'NONE', ( #52247, #6779, #15634, #8382 ) ) ;
#27447=CARTESIAN_POINT ( 'NONE',  ( 5.917102823773431552, -9.672968949171048436, 17.63301987068904353 ) ) ;
#27448=CARTESIAN_POINT ( 'NONE',  ( 0.9762797500689124330, 3.691134646838137190, -41.74566217230977117 ) ) ;
#27450=AXIS2_PLACEMENT_3D ( 'NONE', #43688, #38674, #1038 ) ;
#27452=ORIENTED_EDGE ( 'NONE', *, *, #36805, .F. ) ;
#27456=ADVANCED_FACE ( 'NONE', ( #55582 ), #25346, .F. ) ;
#27457=CARTESIAN_POINT ( 'NONE',  ( 0.5806925824938502512, 4.150136846023314341, -46.71186922509998141 ) ) ;
#27463=CARTESIAN_POINT ( 'NONE',  ( 0.8560838555295158248, 46.35895890951125153, 7.156798369940231552 ) ) ;
#27467=CARTESIAN_POINT ( 'NONE',  ( 0.9754292580325136797, 29.55040404863208892, -29.71701679958123066 ) ) ;
#27468=EDGE_CURVE ( 'NONE', #31086, #46849, #12208, .T. ) ;
#27473=EDGE_CURVE ( 'NONE', #41472, #129, #1733, .T. ) ;
#27479=CARTESIAN_POINT ( 'NONE',  ( 0.7764139734771239310, 39.89513478963794313, 24.66614463233940668 ) ) ;
#27483=CARTESIAN_POINT ( 'NONE',  ( 5.910764540655178756, 14.92665574186491462, 13.47947279506933072 ) ) ;
#27484=CARTESIAN_POINT ( 'NONE',  ( 1.231276596079887264, 32.36747132271594296, -26.63876069172940930 ) ) ;
#27487=DIRECTION ( 'NONE',  ( -1.000000000000000000, -0.000000000000000000, -0.000000000000000000 ) ) ;
#27496=CARTESIAN_POINT ( 'NONE',  ( 5.895596859100789899, 16.57987064389777743, -11.38578379577375088 ) ) ;
#27513=CARTESIAN_POINT ( 'NONE',  ( 2.618530812446111078, -37.94055228201235508, -27.75322110555974930 ) ) ;
#27520=CARTESIAN_POINT ( 'NONE',  ( 0.9762797500689124330, -37.17323042682988188, 19.35137526946117958 ) ) ;
#27527=CARTESIAN_POINT ( 'NONE',  ( 3.376099380956842921, 6.035099650301375185, -11.97021118623223046 ) ) ;
#27540=CARTESIAN_POINT ( 'NONE',  ( 5.917102823773431552, 19.00193826451969770, -6.589086449814119284 ) ) ;
#27542=ORIENTED_EDGE ( 'NONE', *, *, #10423, .T. ) ;
#27544=CARTESIAN_POINT ( 'NONE',  ( 0.9775691876210965692, -17.98273630898676956, 37.85439081310702392 ) ) ;
#27557=CARTESIAN_POINT ( 'NONE',  ( 4.958415959904820092, -27.34909152584691583, -36.26611568025293053 ) ) ;
#27573=CARTESIAN_POINT ( 'NONE',  ( 0.5806925824938502512, 22.05663578530182889, -41.38510819338409163 ) ) ;
#27574=ADVANCED_FACE ( 'NONE', ( #23331 ), #26886, .T. ) ;
#27577=CARTESIAN_POINT ( 'NONE',  ( 0.8560838555295223751, -8.701885300215751684, -46.09392613244852299 ) ) ;
#27579=EDGE_CURVE ( 'NONE', #2564, #61765, #30865, .T. ) ;
#27581=CARTESIAN_POINT ( 'NONE',  ( 0.9791128995231614951, 20.14502082081767398, 36.74936149615371761 ) ) ;
#27591=ORIENTED_EDGE ( 'NONE', *, *, #61318, .T. ) ;
#27597=B_SPLINE_CURVE_WITH_KNOTS ( 'NONE', 3,
 ( #29566, #5730, #2592, #16398, #35524, #60217, #26406, #17031, #40242, #22333, #50827, #27033, #16098, #54902, #26717, #35214 ),
 .UNSPECIFIED., .F., .F.,
 ( 4, 3, 3, 3, 3, 4 ),
 ( 1.040890552917501732E-17, 0.0002732102107931881022, 0.0004098135523333803956, 0.0005464168938824994675, 0.0008195847345945422510, 0.001092771384553105699 ),
 .UNSPECIFIED. ) ;
#27601=ORIENTED_EDGE ( 'NONE', *, *, #61454, .F. ) ;
#27611=CARTESIAN_POINT ( 'NONE',  ( 2.618530812446115519, -45.76452502972762204, 10.73941516106128979 ) ) ;
#27612=CARTESIAN_POINT ( 'NONE',  ( 0.5837157313716042628, -44.27127822390313128, -15.46903319550977685 ) ) ;
#27615=CARTESIAN_POINT ( 'NONE',  ( 0.8560838555295223751, 43.53454501559562573, 17.46757637357886850 ) ) ;
#27617=ORIENTED_EDGE ( 'NONE', *, *, #13232, .F. ) ;
#27627=CARTESIAN_POINT ( 'NONE',  ( 0.5835871038041876568, -1.430526113707234037, -46.87417250405064806 ) ) ;
#27631=CARTESIAN_POINT ( 'NONE',  ( 0.5797568599927139799, 45.05935935907746881, 12.99536235818467667 ) ) ;
#27637=DIRECTION ( 'NONE',  ( 0.000000000000000000, 0.000000000000000000, 1.000000000000000000 ) ) ;
#27638=CARTESIAN_POINT ( 'NONE',  ( 0.5830082357119558134, 4.965806736280845790, -46.63231495858044440 ) ) ;
#27641=CARTESIAN_POINT ( 'NONE',  ( 0.9783242366443558602, -12.67232041183570246, 39.94679944108532510 ) ) ;
#27655=ORIENTED_EDGE ( 'NONE', *, *, #53113, .F. ) ;
#27656=ORIENTED_EDGE ( 'NONE', *, *, #10264, .T. ) ;
#27662=ORIENTED_EDGE ( 'NONE', *, *, #60509, .F. ) ;
#27664=LINE ( 'NONE', #50846, #25067 ) ;
#27692=CARTESIAN_POINT ( 'NONE',  ( 5.894904586330512508, -2.011994607810974500, 20.01202862679799210 ) ) ;
#27693=DIRECTION ( 'NONE',  ( 0.000000000000000000, 0.000000000000000000, 1.000000000000000000 ) ) ;
#27696=DIRECTION ( 'NONE',  ( -1.000000000000000000, -0.000000000000000000, -0.000000000000000000 ) ) ;
#27710=B_SPLINE_CURVE_WITH_KNOTS ( 'NONE', 3,
 ( #36362, #17241, #54487, #54180, #11944, #45753 ),
 .UNSPECIFIED., .F., .F.,
 ( 4, 2, 4 ),
 ( 3.576224061345498009E-18, 0.0002448709889506552593, 0.0004897419779013069407 ),
 .UNSPECIFIED. ) ;
#27713=CARTESIAN_POINT ( 'NONE',  ( 0.5848930533535030563, 22.37766167358058667, 41.21302391732886150 ) ) ;
#27715=CARTESIAN_POINT ( 'NONE',  ( 4.962356264823608143, 0.000000000000000000, 0.000000000000000000 ) ) ;
#27718=CARTESIAN_POINT ( 'NONE',  ( 0.9790850452238862855, -1.450985114059958114, -41.88355252914887217 ) ) ;
#27730=CARTESIAN_POINT ( 'NONE',  ( 0.5824935313925957425, -24.92613923739933313, 39.72311367165993801 ) ) ;
#27734=CARTESIAN_POINT ( 'NONE',  ( 3.782625744892853525, -42.02453477873416432, -1.084703058889718186 ) ) ;
#27736=ORIENTED_EDGE ( 'NONE', *, *, #35443, .T. ) ;
#27737=ORIENTED_EDGE ( 'NONE', *, *, #44042, .T. ) ;
#27739=CARTESIAN_POINT ( 'NONE',  ( 4.291220156522060236, -41.03139692541923722, 23.14764488353824134 ) ) ;
#27743=CARTESIAN_POINT ( 'NONE',  ( 0.5817217712918340000, -46.04480998170284067, 8.894404294681674372 ) ) ;
#27747=VERTEX_POINT ( 'NONE', #3202 ) ;
#27752=CARTESIAN_POINT ( 'NONE',  ( 0.5804410086790514622, -35.14691939471148885, -31.05179397260405239 ) ) ;
#27761=CONICAL_SURFACE ( 'NONE', #31750, 42.08604991992415023, 1.569615340895231137 ) ;
#27778=CARTESIAN_POINT ( 'NONE',  ( 3.661921753701998128, 38.05323874046504784, 27.65107855392275837 ) ) ;
#27789=ORIENTED_EDGE ( 'NONE', *, *, #17200, .F. ) ;
#27790=ADVANCED_FACE ( 'NONE', ( #55205 ), #33782, .F. ) ;
#27791=CONICAL_SURFACE ( 'NONE', #9761, 42.08604991992415023, 1.569615340895231137 ) ;
#27792=CARTESIAN_POINT ( 'NONE',  ( 5.896278296736517710, 19.70873670457416438, 4.011567913441704825 ) ) ;
#27804=CARTESIAN_POINT ( 'NONE',  ( 4.960386119450151732, 32.76426482034242582, -28.99895542006316518 ) ) ;
#27811=CARTESIAN_POINT ( 'NONE',  ( 0.8560838555295223751, -46.85553835019177882, -2.220666565569921591 ) ) ;
#27814=CARTESIAN_POINT ( 'NONE',  ( 0.5835226383429296115, 46.50157772193422545, 6.070069514995094728 ) ) ;
#27817=VERTEX_POINT ( 'NONE', #45533 ) ;
#27820=CARTESIAN_POINT ( 'NONE',  ( 1.231276596079881047, 29.74482033789362134, -29.53849072116746655 ) ) ;
#27823=ORIENTED_EDGE ( 'NONE', *, *, #44211, .T. ) ;
#27826=CARTESIAN_POINT ( 'NONE',  ( 4.956445790443996913, 2.113652668516264654, 47.04328350079860854 ) ) ;
#27830=CIRCLE ( 'NONE', #51829, 47.09074272231896430 ) ;
#27834=DIRECTION ( 'NONE',  ( -1.000000000000000000, -0.000000000000000000, -0.000000000000000000 ) ) ;
#27840=VERTEX_POINT ( 'NONE', #2586 ) ;
#27845=VERTEX_POINT ( 'NONE', #22026 ) ;
#27855=CARTESIAN_POINT ( 'NONE',  ( 5.901463166500145796, 8.452982876530379386, 18.25006714589622803 ) ) ;
#27856=CARTESIAN_POINT ( 'NONE',  ( 5.895596859100789899, 20.06821053248684805, -1.339816866691640129 ) ) ;
#27861=CARTESIAN_POINT ( 'NONE',  ( 3.782542959838397945, 23.52698454657985039, 34.83846798499559583 ) ) ;
#27872=CARTESIAN_POINT ( 'NONE',  ( 0.9791128995231632715, -41.06788468137693826, 8.352621267798951976 ) ) ;
#27879=CARTESIAN_POINT ( 'NONE',  ( 0.9762797500689124330, 38.77779312671053447, -15.89363222827765831 ) ) ;
#27890=AXIS2_PLACEMENT_3D ( 'NONE', #11327, #30414, #47019 ) ;
#27893=CARTESIAN_POINT ( 'NONE',  ( 4.962356264823608143, 18.10963840443066530, -37.99048031708887407 ) ) ;
#27896=CARTESIAN_POINT ( 'NONE',  ( 0.5797568665920721509, -45.82673094209771847, 9.956708279469337342 ) ) ;
#27902=( BOUNDED_SURFACE ( )  B_SPLINE_SURFACE ( 3, 1, ( 
 ( #49968, #49650 ),
 ( #31798, #50271 ),
 ( #54328, #16453 ),
 ( #27090, #12388 ) ),
 .UNSPECIFIED., .F., .F., .F. ) 
 B_SPLINE_SURFACE_WITH_KNOTS ( ( 4, 4 ),
 ( 2, 2 ),
 ( 0.000000000000000000, 1.000000000000000000 ),
 ( 0.000000000000000000, 1.000000000000000000 ),
 .UNSPECIFIED. ) 
 GEOMETRIC_REPRESENTATION_ITEM ( )  RATIONAL_B_SPLINE_SURFACE ( (
 ( 1.000000000000000000, 1.000000000000000000),
 ( 0.9952954269826590483, 0.8620686068821339365),
 ( 0.9952954269826590483, 0.8620686068821339365),
 ( 1.000000000000000000, 1.000000000000000000) ) ) 
 REPRESENTATION_ITEM ( '' )  SURFACE ( )  );
#27911=VECTOR ( 'NONE', #35209, 1000.000000000000000 ) ;
#27917=CARTESIAN_POINT ( 'NONE',  ( 5.901463166500145796, -13.99254106127034625, 14.44737571288640865 ) ) ;
#27919=CARTESIAN_POINT ( 'NONE',  ( 5.894904586330512508, -19.39796360309176038, -5.314924281188778465 ) ) ;
#27922=CARTESIAN_POINT ( 'NONE',  ( 1.231276596079881047, -18.40965318903201364, 37.66113965983544887 ) ) ;
#27927=ORIENTED_EDGE ( 'NONE', *, *, #39766, .F. ) ;
#27936=CARTESIAN_POINT ( 'NONE',  ( 0.5830082357119554803, 11.13697854971562329, -45.55436031513902151 ) ) ;
#27942=EDGE_CURVE ( 'NONE', #40345, #59818, #47867, .T. ) ;
#27944=AXIS2_PLACEMENT_3D ( 'NONE', #32149, #7698, #45958 ) ;
#27946=CARTESIAN_POINT ( 'NONE',  ( 3.376099380956842921, 12.51418204574263981, 4.806623696325688755 ) ) ;
#27955=CARTESIAN_POINT ( 'NONE',  ( 0.9762797500689124330, -11.93232144563832975, 40.17392798947675914 ) ) ;
#27959=FACE_OUTER_BOUND ( 'NONE', #40420, .T. ) ;
#27963=CARTESIAN_POINT ( 'NONE',  ( 0.8560838555295158248, 16.00311602465144745, 44.09391240957503300 ) ) ;
#27983=ORIENTED_EDGE ( 'NONE', *, *, #3177, .T. ) ;
#27991=CARTESIAN_POINT ( 'NONE',  ( 2.282803330402966235, -45.75239485235542958, -10.64026657237235973 ) ) ;
#28014=EDGE_LOOP ( 'NONE', ( #20876, #4624, #33807, #57297 ) ) ;
#28016=EDGE_CURVE ( 'NONE', #7742, #41497, #61859, .T. ) ;
#28018=CARTESIAN_POINT ( 'NONE',  ( 4.962356264823609031, 31.50371261889155150, -27.90612278853226513 ) ) ;
#28019=B_SPLINE_CURVE_WITH_KNOTS ( 'NONE', 3,
 ( #4395, #18236, #32642, #27936, #13228, #38282, #61726, #33269, #8822, #18862, #13537, #37347, #42984, #56731, #46441, #51727 ),
 .UNSPECIFIED., .F., .F.,
 ( 4, 3, 3, 3, 3, 4 ),
 ( 1.214354834101861570E-17, 0.0002732102107931902164, 0.0004098135523333812629, 0.0005464168938824976243, 0.0008195847345945407331, 0.001092771384553105699 ),
 .UNSPECIFIED. ) ;
#28021=CARTESIAN_POINT ( 'NONE',  ( 0.5830081025819925378, -30.48545850581747985, -35.63521929317017367 ) ) ;
#28024=CARTESIAN_POINT ( 'NONE',  ( 4.956445790444002242, -37.28933980949966553, 28.75835855384135087 ) ) ;
#28028=CARTESIAN_POINT ( 'NONE',  ( 5.910764540655177868, -17.31247307865856300, 10.23618651500086330 ) ) ;
#28032=ORIENTED_EDGE ( 'NONE', *, *, #55439, .T. ) ;
#28040=CARTESIAN_POINT ( 'NONE',  ( 0.5832655196449136881, -25.42549130248452371, 39.40532419611102455 ) ) ;
#28041=CARTESIAN_POINT ( 'NONE',  ( 0.8554163680231816613, -39.19027442586699550, -25.79395013442212203 ) ) ;
#28047=CARTESIAN_POINT ( 'NONE',  ( 2.618530812446111078, -15.26631161698053418, 44.45971793445664133 ) ) ;
#28051=DIRECTION ( 'NONE',  ( -0.07906939808003035641, 0.9208896734047710142, 0.3817201064965217716 ) ) ;
#28054=ORIENTED_EDGE ( 'NONE', *, *, #50413, .F. ) ;
#28057=CARTESIAN_POINT ( 'NONE',  ( 0.9785694773339237429, 25.03819957080264302, -33.60690357601148293 ) ) ;
#28060=CARTESIAN_POINT ( 'NONE',  ( 0.5817217712918331118, 17.27887506707169152, -43.59673646530094970 ) ) ;
#28061=DIRECTION ( 'NONE',  ( 0.000000000000000000, 0.000000000000000000, 1.000000000000000000 ) ) ;
#28063=B_SPLINE_CURVE_WITH_KNOTS ( 'NONE', 3,
 ( #2984, #22107, #41235, #52447 ),
 .UNSPECIFIED., .F., .F.,
 ( 4, 4 ),
 ( 4.336808689942017736E-19, 0.004041751736740994277 ),
 .UNSPECIFIED. ) ;
#28065=ORIENTED_EDGE ( 'NONE', *, *, #6607, .T. ) ;
#28071=CARTESIAN_POINT ( 'NONE',  ( 5.896782393890504181, -9.671431223051156323, 17.63489452692596515 ) ) ;
#28072=CARTESIAN_POINT ( 'NONE',  ( 5.910764540655177868, -13.97071922697925750, -14.46790388238998482 ) ) ;
#28076=CARTESIAN_POINT ( 'NONE',  ( 0.5806925824938499181, 46.54710689580866756, -5.708695295225145294 ) ) ;
#28078=CARTESIAN_POINT ( 'NONE',  ( 4.958415959904818315, -4.043245302073017022, 45.24219403665016159 ) ) ;
#28080=ORIENTED_EDGE ( 'NONE', *, *, #26303, .T. ) ;
#28085=CARTESIAN_POINT ( 'NONE',  ( 0.5806925824938502512, 28.25565086187734920, 37.42780459384778879 ) ) ;
#28088=CARTESIAN_POINT ( 'NONE',  ( 4.962356264823608143, -19.84272732133934269, -37.11471096901227185 ) ) ;
#28095=CARTESIAN_POINT ( 'NONE',  ( 0.9762797500689124330, -40.96497924994823592, 8.842808390834631993 ) ) ;
#28105=FACE_OUTER_BOUND ( 'NONE', #6924, .T. ) ;
#28111=CARTESIAN_POINT ( 'NONE',  ( 0.5817216825391109403, 11.31383544828560517, 45.51079080456168668 ) ) ;
#28113=CARTESIAN_POINT ( 'NONE',  ( 0.5797568665920710407, 32.14649144340224041, -34.14422932914341402 ) ) ;
#28119=CARTESIAN_POINT ( 'NONE',  ( 2.282816707992311400, -26.37306023955149570, -38.87105169671840343 ) ) ;
#28124=CARTESIAN_POINT ( 'NONE',  ( 0.9762797500689124330, 41.90547441298052433, 0.5059638413352746111 ) ) ;
#28129=EDGE_CURVE ( 'NONE', #41690, #29140, #12143, .T. ) ;
#28134=ORIENTED_EDGE ( 'NONE', *, *, #12781, .T. ) ;
#28140=CARTESIAN_POINT ( 'NONE',  ( 0.5830082357119560355, -7.530675664250292556, -46.28737364528480924 ) ) ;
#28145=CARTESIAN_POINT ( 'NONE',  ( 2.528100132419517365, 41.96176039463138352, -1.210141816325795316 ) ) ;
#28152=CARTESIAN_POINT ( 'NONE',  ( 4.962356264823608143, 41.32726869310149453, -7.955655864260332777 ) ) ;
#28159=VECTOR ( 'NONE', #13089, 1000.000000000000000 ) ;
#28163=CARTESIAN_POINT ( 'NONE',  ( 4.956445790444038657, 44.30493387627053181, -15.95653108789415953 ) ) ;
#28171=CARTESIAN_POINT ( 'NONE',  ( 0.9787464366903576574, -41.10375767077415077, 8.174050295461709581 ) ) ;
#28172=EDGE_CURVE ( 'NONE', #8614, #35106, #43909, .T. ) ;
#28195=CARTESIAN_POINT ( 'NONE',  ( 5.895881250540457863, 19.71075194021744181, -4.001742065590352837 ) ) ;
#28209=EDGE_LOOP ( 'NONE', ( #4950, #24000, #14144, #40488 ) ) ;
#28213=ORIENTED_EDGE ( 'NONE', *, *, #55857, .F. ) ;
#28215=ORIENTED_EDGE ( 'NONE', *, *, #46260, .T. ) ;
#28221=CARTESIAN_POINT ( 'NONE',  ( 5.895596859100789899, 20.06821053248684805, -1.339816866691640129 ) ) ;
#28222=CARTESIAN_POINT ( 'NONE',  ( 5.917102823773431552, 19.71063251686273432, -3.997584750438137213 ) ) ;
#28236=CARTESIAN_POINT ( 'NONE',  ( 0.9783242366443540838, -34.39878881041870073, -23.93862607968005207 ) ) ;
#28247=FACE_OUTER_BOUND ( 'NONE', #60320, .T. ) ;
#28249=EDGE_CURVE ( 'NONE', #56267, #37980, #56265, .T. ) ;
#28253=CARTESIAN_POINT ( 'NONE',  ( 0.9787284016396609054, -12.23755578274794509, 40.08214349798376475 ) ) ;
#28262=CARTESIAN_POINT ( 'NONE',  ( 0.5832655196449135770, 45.28935891855852702, -12.17001034179147645 ) ) ;
#28264=CARTESIAN_POINT ( 'NONE',  ( 0.5806925824938502512, -8.338382001837375768, -46.14860504863607105 ) ) ;
#28269=EDGE_CURVE ( 'NONE', #21652, #32480, #21895, .T. ) ;
#28272=EDGE_CURVE ( 'NONE', #20804, #44257, #56987, .T. ) ;
#28277=ADVANCED_FACE ( 'NONE', ( #4043 ), #41836, .F. ) ;
#28278=ORIENTED_EDGE ( 'NONE', *, *, #35199, .T. ) ;
#28287=CARTESIAN_POINT ( 'NONE',  ( 5.896782393890504181, -4.668739246792056541, -19.56345983519980081 ) ) ;
#28301=DIRECTION ( 'NONE',  ( -1.000000000000000000, -0.000000000000000000, -0.000000000000000000 ) ) ;
#28304=B_SPLINE_CURVE_WITH_KNOTS ( 'NONE', 3,
 ( #50145, #36377, #55442, #1577 ),
 .UNSPECIFIED., .F., .F.,
 ( 4, 4 ),
 ( 4.336808689942017736E-19, 0.004041751736740997747 ),
 .UNSPECIFIED. ) ;
#28307=CARTESIAN_POINT ( 'NONE',  ( 0.8560838555295158248, 46.60258007729424889, -5.345312359545362213 ) ) ;
#28309=CARTESIAN_POINT ( 'NONE',  ( 2.618530812446115519, -44.84885430744860457, -14.08215383055621572 ) ) ;
#28311=EDGE_LOOP ( 'NONE', ( #32739, #13127, #51961, #60118 ) ) ;
#28314=LINE ( 'NONE', #22695, #45462 ) ;
#28328=CARTESIAN_POINT ( 'NONE',  ( 5.910764540655177868, 3.360528482495168223, -19.82947520201938829 ) ) ;
#28329=CARTESIAN_POINT ( 'NONE',  ( 0.9789889208857698311, 41.90853909528808430, -0.09617141507911233789 ) ) ;
#28331=VERTEX_POINT ( 'NONE', #15952 ) ;
#28335=LINE ( 'NONE', #57743, #19033 ) ;
#28338=AXIS2_PLACEMENT_3D ( 'NONE', #39450, #9679, #33202 ) ;
#28341=CARTESIAN_POINT ( 'NONE',  ( 0.6064515330803582627, 10.17911311372881755, -45.77903441811543672 ) ) ;
#28350=VECTOR ( 'NONE', #27115, 1000.000000000000000 ) ;
#28362=CARTESIAN_POINT ( 'NONE',  ( 4.960386119450144626, -43.42409617054088500, -5.365103581847961323 ) ) ;
#28365=EDGE_LOOP ( 'NONE', ( #13789, #59399, #42339, #26620 ) ) ;
#28371=CARTESIAN_POINT ( 'NONE',  ( 0.9762797500689124330, -37.17323042682959766, -19.35137526946170183 ) ) ;
#28373=CARTESIAN_POINT ( 'NONE',  ( 0.6064515330803572635, -13.21408419773141496, 44.99691450368958101 ) ) ;
#28375=ADVANCED_FACE ( 'NONE', ( #34443 ), #56982, .F. ) ;
#28380=CARTESIAN_POINT ( 'NONE',  ( 0.7056313189692712262, -2.409529526766163610, -46.83954324518119705 ) ) ;
#28383=ORIENTED_EDGE ( 'NONE', *, *, #7778, .T. ) ;
#28386=CARTESIAN_POINT ( 'NONE',  ( -69.95594261585601714, 0.000000000000000000, 8.000000000000000000 ) ) ;
#28387=CARTESIAN_POINT ( 'NONE',  ( 0.5835871038041845482, 27.70768690911332399, 37.83541382155152633 ) ) ;
#28389=CARTESIAN_POINT ( 'NONE',  ( 1.231276596079881935, -40.90292846002442673, -9.177538581351248226 ) ) ;
#28397=EDGE_CURVE ( 'NONE', #7149, #56267, #24766, .T. ) ;
#28401=ORIENTED_EDGE ( 'NONE', *, *, #25673, .T. ) ;
#28406=B_SPLINE_CURVE_WITH_KNOTS ( 'NONE', 3,
 ( #51707, #37033, #52318, #42043, #52629, #3774 ),
 .UNSPECIFIED., .F., .F.,
 ( 4, 2, 4 ),
 ( 9.948699630566631321E-18, 0.0002291472222819947516, 0.0004582944445639795827 ),
 .UNSPECIFIED. ) ;
#28411=CARTESIAN_POINT ( 'NONE',  ( 0.9789233960466698914, 29.22897439703389466, -30.03337780753075492 ) ) ;
#28420=B_SPLINE_CURVE_WITH_KNOTS ( 'NONE', 3,
 ( #32295, #46106, #51692, #17898, #3154, #31366, #22280, #61085, #17582, #22898, #36704, #37021, #8785, #55770, #13195, #8459, #18199, #56387, #13502 ),
 .UNSPECIFIED., .F., .F.,
 ( 4, 3, 3, 3, 3, 3, 4 ),
 ( 9.541595121948227273E-18, 0.0002732106629380621609, 0.0004098138914053778715, 0.0005464171197651488581, 0.0006830203481512578259, 0.0008196235766963648256, 0.001011968216111141594 ),
 .UNSPECIFIED. ) ;
#28430=B_SPLINE_CURVE_WITH_KNOTS ( 'NONE', 3,
 ( #51087, #32314, #51391, #18219 ),
 .UNSPECIFIED., .F., .F.,
 ( 4, 4 ),
 ( 1.388456241783856658E-17, 0.005004948556313818311 ),
 .UNSPECIFIED. ) ;
#28432=CARTESIAN_POINT ( 'NONE',  ( 0.5832655196449133550, 43.08542359691993795, 18.51705852578387379 ) ) ;
#28437=EDGE_CURVE ( 'NONE', #59248, #44953, #13888, .T. ) ;
#28439=ORIENTED_EDGE ( 'NONE', *, *, #39697, .T. ) ;
#28442=CARTESIAN_POINT ( 'NONE',  ( 0.5806925824938502512, -8.338382001837375768, -46.14860504863607105 ) ) ;
#28448=EDGE_LOOP ( 'NONE', ( #50862, #51777, #52008, #40728 ) ) ;
#28449=CARTESIAN_POINT ( 'NONE',  ( 0.8560838555295158248, -44.00447048317951726, -16.24744323198929052 ) ) ;
#28460=CARTESIAN_POINT ( 'NONE',  ( 0.8560838555295223751, -46.14148336882287538, -8.446084690930739214 ) ) ;
#28478=CARTESIAN_POINT ( 'NONE',  ( 3.238018933889920792, 13.30865154331494438, 1.512377752505517092 ) ) ;
#28486=CARTESIAN_POINT ( 'NONE',  ( 0.8560838555295223751, 37.37287335782406217, 28.34856559090382078 ) ) ;
#28492=CARTESIAN_POINT ( 'NONE',  ( 0.9784957157296378938, 20.34434192463124091, 36.63933417307226392 ) ) ;
#28493=CARTESIAN_POINT ( 'NONE',  ( 2.282803330402962239, -15.16644679234350690, 44.45757302363679742 ) ) ;
#28494=CARTESIAN_POINT ( 'NONE',  ( 0.5806925824938511393, 42.95845041307772050, -18.80940989108128747 ) ) ;
#28496=EDGE_CURVE ( 'NONE', #3952, #217, #36772, .T. ) ;
#28497=CARTESIAN_POINT ( 'NONE',  ( 0.5804410086790514622, -45.84731009780865918, 9.876437042312852910 ) ) ;
#28498=DIRECTION ( 'NONE',  ( 0.07500201931887537365, -0.8510178133412981127, -0.5197531899602795269 ) ) ;
#28501=ORIENTED_EDGE ( 'NONE', *, *, #46928, .F. ) ;
#28521=CARTESIAN_POINT ( 'NONE',  ( 0.5830082357119563685, 40.20946850652512694, 24.13360058841410449 ) ) ;
#28522=( BOUNDED_SURFACE ( )  B_SPLINE_SURFACE ( 3, 1, ( 
 ( #5220, #9952 ),
 ( #48164, #24351 ),
 ( #10881, #53148 ),
 ( #38783, #29350 ) ),
 .UNSPECIFIED., .F., .F., .F. ) 
 B_SPLINE_SURFACE_WITH_KNOTS ( ( 4, 4 ),
 ( 2, 2 ),
 ( 0.000000000000000000, 1.000000000000000000 ),
 ( 0.000000000000000000, 1.000000000000000000 ),
 .UNSPECIFIED. ) 
 GEOMETRIC_REPRESENTATION_ITEM ( )  RATIONAL_B_SPLINE_SURFACE ( (
 ( 1.000000000000000000, 1.000000000000000000),
 ( 0.9729067724841187204, 0.9999501103223794596),
 ( 0.9729067724841187204, 0.9999501103223794596),
 ( 1.000000000000000000, 1.000000000000000000) ) ) 
 REPRESENTATION_ITEM ( '' )  SURFACE ( )  );
#28524=CARTESIAN_POINT ( 'NONE',  ( 0.5804410086790514622, -46.75463715370017326, 3.677466040799799440 ) ) ;
#28528=CARTESIAN_POINT ( 'NONE',  ( 0.5848930533535030563, -1.384993715960175509, 46.87595198813895792 ) ) ;
#28539=CARTESIAN_POINT ( 'NONE',  ( 0.9790850452238870627, -22.59298530334723765, -35.29722857882659781 ) ) ;
#28540=( BOUNDED_SURFACE ( )  B_SPLINE_SURFACE ( 3, 1, ( 
 ( #24296, #10826 ),
 ( #19613, #1388 ),
 ( #43747, #14609 ),
 ( #34631, #53696 ) ),
 .UNSPECIFIED., .F., .F., .F. ) 
 B_SPLINE_SURFACE_WITH_KNOTS ( ( 4, 4 ),
 ( 2, 2 ),
 ( 0.000000000000000000, 1.000000000000000000 ),
 ( 0.000000000000000000, 1.000000000000000000 ),
 .UNSPECIFIED. ) 
 GEOMETRIC_REPRESENTATION_ITEM ( )  RATIONAL_B_SPLINE_SURFACE ( (
 ( 1.000000000000000000, 1.000000000000000000),
 ( 0.9952954269826590483, 0.8620686068821307169),
 ( 0.9952954269826590483, 0.8620686068821307169),
 ( 1.000000000000000000, 1.000000000000000000) ) ) 
 REPRESENTATION_ITEM ( '' )  SURFACE ( )  );
#28554=CARTESIAN_POINT ( 'NONE',  ( 1.157644175074337367, -13.20506553587984477, 39.78226388319673390 ) ) ;
#28555=EDGE_CURVE ( 'NONE', #54380, #26593, #43425, .T. ) ;
#28565=CARTESIAN_POINT ( 'NONE',  ( 0.5848930533535030563, 16.68483824254287384, -43.82795061610497811 ) ) ;
#28570=CARTESIAN_POINT ( 'NONE',  ( 0.8554163680231708922, 43.54276151446883603, -17.47092993535007466 ) ) ;
#28583=CARTESIAN_POINT ( 'NONE',  ( 0.6064515330803588178, 3.986541738855695183, -46.72731343659132364 ) ) ;
#28585=ORIENTED_EDGE ( 'NONE', *, *, #53849, .T. ) ;
#28587=DIRECTION ( 'NONE',  ( -0.07906939808003035641, 0.7773121955653319315, -0.6241264142084236299 ) ) ;
#28591=EDGE_CURVE ( 'NONE', #32404, #40072, #38385, .T. ) ;
#28603=CARTESIAN_POINT ( 'NONE',  ( 0.5806925824938494740, -46.75147433417404841, 3.677228565731047283 ) ) ;
#28607=VERTEX_POINT ( 'NONE', #432 ) ;
#28610=CARTESIAN_POINT ( 'NONE',  ( 5.896278296736517710, 19.70873670457421767, -4.011567913441433042 ) ) ;
#28611=EDGE_LOOP ( 'NONE', ( #9794, #33242, #12066, #56478 ) ) ;
#28618=CARTESIAN_POINT ( 'NONE',  ( 4.956445790444035104, 35.28522167764516837, -31.18479086508480691 ) ) ;
#28627=CARTESIAN_POINT ( 'NONE',  ( 0.5806925824938502512, -41.60618895332704170, 21.63671424046659908 ) ) ;
#28631=CARTESIAN_POINT ( 'NONE',  ( 0.9788927965476030835, 41.90843032204052321, -0.1417059435968782144 ) ) ;
#28632=ADVANCED_FACE ( 'NONE', ( #40588 ), #35795, .F. ) ;
#28641=CARTESIAN_POINT ( 'NONE',  ( 0.8554163680231816613, -13.02474486562579870, 45.07284652978080430 ) ) ;
#28645=EDGE_CURVE ( 'NONE', #27021, #55166, #35883, .T. ) ;
#28646=CARTESIAN_POINT ( 'NONE',  ( 4.291220156522060236, 8.814262783203506757, -46.27848062430671661 ) ) ;
#28652=ORIENTED_EDGE ( 'NONE', *, *, #3196, .F. ) ;
#28660=CARTESIAN_POINT ( 'NONE',  ( 0.5824935313925941882, 22.85613393777071423, 40.94917970451332678 ) ) ;
#28661=CARTESIAN_POINT ( 'NONE',  ( 0.5817216825391123836, -45.86342747968472366, 9.786775363885668710 ) ) ;
#28680=EDGE_LOOP ( 'NONE', ( #55630, #16870, #48575, #35577 ) ) ;
#28689=CARTESIAN_POINT ( 'NONE',  ( 4.956445790444036881, 42.27038699792232279, -20.75457619864872783 ) ) ;
#28694=ORIENTED_EDGE ( 'NONE', *, *, #60517, .F. ) ;
#28720=CARTESIAN_POINT ( 'NONE',  ( 3.238018933889920792, 6.194554405862312763, -11.87581525961332751 ) ) ;
#28724=CARTESIAN_POINT ( 'NONE',  ( 1.231276596079887264, -6.136529359146732254, 41.46829847537028257 ) ) ;
#28733=DIRECTION ( 'NONE',  ( -1.000000000000000000, -0.000000000000000000, -0.000000000000000000 ) ) ;
#28734=VERTEX_POINT ( 'NONE', #19 ) ;
#28740=CARTESIAN_POINT ( 'NONE',  ( 0.9762797500689124330, 10.20671408566037286, -40.64662068068250278 ) ) ;
#28741=ORIENTED_EDGE ( 'NONE', *, *, #53858, .T. ) ;
#28747=B_SPLINE_CURVE_WITH_KNOTS ( 'NONE', 3,
 ( #13355, #32453, #61246, #47481, #34013, #53083, #38405, #24594, #9560, #57773, #19289, #61549, #56855, #43730, #18669, #779 ),
 .UNSPECIFIED., .F., .F.,
 ( 4, 3, 3, 3, 3, 4 ),
 ( 1.105939361823508950E-17, 0.0002732102107931894033, 0.0004098135523333801787, 0.0005464168938824981664, 0.0008195847345945439857, 0.001092771384553107867 ),
 .UNSPECIFIED. ) ;
#28748=B_SPLINE_CURVE_WITH_KNOTS ( 'NONE', 3,
 ( #4781, #24532, #9505, #43358, #89, #29533 ),
 .UNSPECIFIED., .F., .F.,
 ( 4, 2, 4 ),
 ( 1.985955348410164766E-17, 0.0002448709889506577530, 0.0004897419779012956650 ),
 .UNSPECIFIED. ) ;
#28749=CARTESIAN_POINT ( 'NONE',  ( 0.5830082357119567016, -25.00320994349359438, -39.67457028702288113 ) ) ;
#28750=ORIENTED_EDGE ( 'NONE', *, *, #22794, .F. ) ;
#28751=B_SPLINE_CURVE_WITH_KNOTS ( 'NONE', 3,
 ( #41963, #44134, #58169, #38489 ),
 .UNSPECIFIED., .F., .F.,
 ( 4, 4 ),
 ( 2.168404344971008868E-19, 0.004446298630425049407 ),
 .UNSPECIFIED. ) ;
#28752=( BOUNDED_SURFACE ( )  B_SPLINE_SURFACE ( 3, 1, ( 
 ( #26510, #18368 ),
 ( #7382, #31846 ),
 ( #36867, #46261 ),
 ( #60945, #13358 ) ),
 .UNSPECIFIED., .F., .F., .F. ) 
 B_SPLINE_SURFACE_WITH_KNOTS ( ( 4, 4 ),
 ( 2, 2 ),
 ( 0.000000000000000000, 1.000000000000000000 ),
 ( 0.000000000000000000, 1.000000000000000000 ),
 .UNSPECIFIED. ) 
 GEOMETRIC_REPRESENTATION_ITEM ( )  RATIONAL_B_SPLINE_SURFACE ( (
 ( 1.000000000000000000, 1.000000000000000000),
 ( 0.9729067724841187204, 0.9999501103223794596),
 ( 0.9729067724841187204, 0.9999501103223794596),
 ( 1.000000000000000000, 1.000000000000000000) ) ) 
 REPRESENTATION_ITEM ( '' )  SURFACE ( )  );
#28755=VERTEX_POINT ( 'NONE', #29771 ) ;
#28765=ORIENTED_EDGE ( 'NONE', *, *, #29151, .F. ) ;
#28779=ORIENTED_EDGE ( 'NONE', *, *, #19673, .T. ) ;
#28780=CARTESIAN_POINT ( 'NONE',  ( 4.960386119450145515, 41.17653976845473096, -14.79625078758826895 ) ) ;
#28782=CARTESIAN_POINT ( 'NONE',  ( 0.9762797500689124330, 38.77779312671053447, -15.89363222827765831 ) ) ;
#28785=ORIENTED_EDGE ( 'NONE', *, *, #21013, .F. ) ;
#28792=CARTESIAN_POINT ( 'NONE',  ( 0.9780106845699496620, -41.13015066261051800, 8.040021948128993401 ) ) ;
#28797=ORIENTED_EDGE ( 'NONE', *, *, #39532, .T. ) ;
#28806=CARTESIAN_POINT ( 'NONE',  ( 5.896782393890504181, -7.222780579330736472, 18.77118876312459150 ) ) ;
#28816=CARTESIAN_POINT ( 'NONE',  ( 4.958415959904820092, 8.053194174019305152, -44.70290837762330938 ) ) ;
#28817=FACE_OUTER_BOUND ( 'NONE', #47056, .T. ) ;
#28820=ORIENTED_EDGE ( 'NONE', *, *, #10090, .F. ) ;
#28822=DIRECTION ( 'NONE',  ( 0.07500201931887537365, 0.8838330717251207114, 0.4617507968840214860 ) ) ;
#28836=DIRECTION ( 'NONE',  ( 0.000000000000000000, 0.000000000000000000, 1.000000000000000000 ) ) ;
#28838=B_SPLINE_CURVE_WITH_KNOTS ( 'NONE', 3,
 ( #10319, #6195, #44480, #20642 ),
 .UNSPECIFIED., .F., .F.,
 ( 4, 4 ),
 ( 1.301042606982605128E-18, 0.004446298630425060683 ),
 .UNSPECIFIED. ) ;
#28840=FACE_OUTER_BOUND ( 'NONE', #37550, .T. ) ;
#28841=AXIS2_PLACEMENT_3D ( 'NONE', #53891, #44240, #59214 ) ;
#28844=ORIENTED_EDGE ( 'NONE', *, *, #23229, .T. ) ;
#28851=CARTESIAN_POINT ( 'NONE',  ( 1.231276596079887264, 25.54232633153331733, 33.23952972879620660 ) ) ;
#28854=CARTESIAN_POINT ( 'NONE',  ( 0.9780303403264780648, -34.73352412603711770, -23.45041396609195772 ) ) ;
#28870=CARTESIAN_POINT ( 'NONE',  ( 2.282816707992309624, -33.94297373141591123, 32.47108714959165354 ) ) ;
#28879=CARTESIAN_POINT ( 'NONE',  ( 0.5806925824938494740, 45.08220210717442455, -12.91578164539189721 ) ) ;
#28896=ORIENTED_EDGE ( 'NONE', *, *, #44101, .F. ) ;
#28898=EDGE_LOOP ( 'NONE', ( #15977, #54422, #5410, #40001 ) ) ;
#28901=CARTESIAN_POINT ( 'NONE',  ( 4.291220156522059348, 8.814262783202863716, 46.27848062430680898 ) ) ;
#28908=CARTESIAN_POINT ( 'NONE',  ( 0.9790320750461911636, -39.61794717384558595, 13.66584773340351688 ) ) ;
#28921=ORIENTED_EDGE ( 'NONE', *, *, #61075, .T. ) ;
#28924=CARTESIAN_POINT ( 'NONE',  ( 4.291220156522059348, -23.50705364442096013, -40.82655295593802691 ) ) ;
#28926=CARTESIAN_POINT ( 'NONE',  ( 4.956445790444004018, -45.27177431812791042, 12.96165499572219737 ) ) ;
#28938=CARTESIAN_POINT ( 'NONE',  ( 0.8554163680231720024, 27.08908797599197982, -38.30648490452740162 ) ) ;
#28947=CARTESIAN_POINT ( 'NONE',  ( 4.962356264823608143, 6.570263404306589727, 41.57002810511892221 ) ) ;
#28949=VERTEX_POINT ( 'NONE', #47990 ) ;
#28950=CARTESIAN_POINT ( 'NONE',  ( 0.8560838555295223751, -46.73345513967318965, 4.044379407262076676 ) ) ;
#28952=CARTESIAN_POINT ( 'NONE',  ( 0.5806925824938499181, -45.84420715090598009, -9.875780123533834498 ) ) ;
#28969=CARTESIAN_POINT ( 'NONE',  ( 0.5806925824938502512, 46.40146083665138832, -6.791670970259978013 ) ) ;
#28980=CIRCLE ( 'NONE', #38047, 42.08604991992415023 ) ;
#28982=CARTESIAN_POINT ( 'NONE',  ( 0.5835226383429285013, 16.68471544554396147, -43.82764818065410140 ) ) ;
#28985=CARTESIAN_POINT ( 'NONE',  ( 2.282816707992308292, -12.65678178881115734, 45.23607897639210762 ) ) ;
#28990=EDGE_CURVE ( 'NONE', #3915, #37874, #14786, .T. ) ;
#28991=ORIENTED_EDGE ( 'NONE', *, *, #13986, .T. ) ;
#28992=CARTESIAN_POINT ( 'NONE',  ( 4.962356264823600149, -32.75738977283805298, 26.42326651140453109 ) ) ;
#28995=CARTESIAN_POINT ( 'NONE',  ( 0.9772918015221174759, -37.58957372490684179, -18.52999738074653635 ) ) ;
#28998=CARTESIAN_POINT ( 'NONE',  ( 3.782625744892853970, -8.686979669181580377, -41.13118632281627640 ) ) ;
#29001=CARTESIAN_POINT ( 'NONE',  ( 0.5837800304671227902, 46.48363954360758754, -6.205528741328782516 ) ) ;
#29009=CARTESIAN_POINT ( 'NONE',  ( 1.231276596079881935, 38.91607545535268997, -15.58254928345689017 ) ) ;
#29015=LINE ( 'NONE', #15540, #48776 ) ;
#29026=CARTESIAN_POINT ( 'NONE',  ( 0.5782707292762423457, -46.10024953908492762, -8.631532085424908018 ) ) ;
#29027=CARTESIAN_POINT ( 'NONE',  ( 0.5832655196449155754, 28.00069848097898273, -37.61909179593025954 ) ) ;
#29046=ORIENTED_EDGE ( 'NONE', *, *, #56062, .T. ) ;
#29050=FACE_OUTER_BOUND ( 'NONE', #26004, .T. ) ;
#29052=CARTESIAN_POINT ( 'NONE',  ( 5.894904586330512508, 5.957793302349398523, 19.21026056637763091 ) ) ;
#29061=VERTEX_POINT ( 'NONE', #56287 ) ;
#29072=CARTESIAN_POINT ( 'NONE',  ( 0.5804410086790514622, -44.48029469925780433, -14.86685021524651162 ) ) ;
#29075=ORIENTED_EDGE ( 'NONE', *, *, #11372, .F. ) ;
#29082=CARTESIAN_POINT ( 'NONE',  ( 0.9769922540276050338, -37.60142665668843875, 18.50579013357184621 ) ) ;
#29089=ORIENTED_EDGE ( 'NONE', *, *, #40707, .T. ) ;
#29096=VERTEX_POINT ( 'NONE', #42842 ) ;
#29100=CARTESIAN_POINT ( 'NONE',  ( 0.5830081025819942031, -41.97804134881273086, -20.90636455483389611 ) ) ;
#29107=EDGE_CURVE ( 'NONE', #15738, #371, #24021, .T. ) ;
#29117=CARTESIAN_POINT ( 'NONE',  ( 4.962356264823608143, -4.645793755591040686, 41.82884409403227011 ) ) ;
#29119=B_SPLINE_CURVE_WITH_KNOTS ( 'NONE', 3,
 ( #43216, #37593, #27861, #46992 ),
 .UNSPECIFIED., .F., .F.,
 ( 4, 4 ),
 ( 2.168404344971008868E-18, 0.004041751736740980400 ),
 .UNSPECIFIED. ) ;
#29125=ADVANCED_FACE ( 'NONE', ( #23103 ), #48918, .T. ) ;
#29126=DIRECTION ( 'NONE',  ( -1.000000000000000000, -0.000000000000000000, -0.000000000000000000 ) ) ;
#29127=CARTESIAN_POINT ( 'NONE',  ( 5.901463166500146684, -15.79333916981796726, -12.45344563595674714 ) ) ;
#29128=ADVANCED_FACE ( 'NONE', ( #42231 ), #50946, .F. ) ;
#29129=CARTESIAN_POINT ( 'NONE',  ( 0.9762797500689124330, -39.75277516423506086, -13.26806888463731227 ) ) ;
#29134=EDGE_LOOP ( 'NONE', ( #43642, #18693, #10481, #300 ) ) ;
#29138=CARTESIAN_POINT ( 'NONE',  ( 3.376099380956842921, -13.22083125066026099, -2.217657474370683612 ) ) ;
#29139=ADVANCED_FACE ( 'NONE', ( #38763, #47842 ), #57499, .F. ) ;
#29140=VERTEX_POINT ( 'NONE', #37526 ) ;
#29145=FACE_OUTER_BOUND ( 'NONE', #47357, .T. ) ;
#29148=CARTESIAN_POINT ( 'NONE',  ( 0.5806925824938499181, 40.06810415365472977, 24.36738377166168235 ) ) ;
#29151=EDGE_CURVE ( 'NONE', #58288, #15929, #47924, .T. ) ;
#29155=CARTESIAN_POINT ( 'NONE',  ( 0.5806925824938502512, -13.37132486740698134, 44.94919391528425479 ) ) ;
#29156=EDGE_CURVE ( 'NONE', #30940, #9945, #32822, .T. ) ;
#29159=CARTESIAN_POINT ( 'NONE',  ( 2.528100132419516477, 25.86511525564304037, 33.06432505653756238 ) ) ;
#29161=CARTESIAN_POINT ( 'NONE',  ( 2.618530812446115519, -29.26021975733438651, 36.79084572214530624 ) ) ;
#29163=ORIENTED_EDGE ( 'NONE', *, *, #34446, .F. ) ;
#29172=( BOUNDED_SURFACE ( )  B_SPLINE_SURFACE ( 3, 1, ( 
 ( #51865, #8963 ),
 ( #28072, #34325 ),
 ( #53400, #33404 ),
 ( #1090, #10509 ) ),
 .UNSPECIFIED., .F., .F., .F. ) 
 B_SPLINE_SURFACE_WITH_KNOTS ( ( 4, 4 ),
 ( 2, 2 ),
 ( 0.000000000000000000, 1.000000000000000000 ),
 ( 0.000000000000000000, 1.000000000000000000 ),
 .UNSPECIFIED. ) 
 GEOMETRIC_REPRESENTATION_ITEM ( )  RATIONAL_B_SPLINE_SURFACE ( (
 ( 1.000000000000000000, 1.000000000000000000),
 ( 0.7282232189291693025, 0.9929344683865674037),
 ( 0.7282232189291693025, 0.9929344683865674037),
 ( 1.000000000000000000, 1.000000000000000000) ) ) 
 REPRESENTATION_ITEM ( '' )  SURFACE ( )  );
#29174=DIRECTION ( 'NONE',  ( -0.07906939808003034253, 0.6871887087747716727, -0.7221632148065447732 ) ) ;
#29184=CARTESIAN_POINT ( 'NONE',  ( 0.5835226383429310548, -1.384976919776544912, 46.87562600624814024 ) ) ;
#29186=CIRCLE ( 'NONE', #5208, 47.09074272231896430 ) ;
#29187=DIRECTION ( 'NONE',  ( 0.000000000000000000, 0.000000000000000000, -1.000000000000000000 ) ) ;
#29188=DIRECTION ( 'NONE',  ( 0.07500201931887538753, 0.6540624036680682263, -0.7527131387228735981 ) ) ;
#29189=EDGE_LOOP ( 'NONE', ( #27737, #8282, #23843, #47902 ) ) ;
#29191=CARTESIAN_POINT ( 'NONE',  ( 0.8560838555295223751, -35.39593983670150124, -30.78149244527203621 ) ) ;
#29197=ORIENTED_EDGE ( 'NONE', *, *, #28645, .T. ) ;
#29203=VERTEX_POINT ( 'NONE', #19036 ) ;
#29204=EDGE_CURVE ( 'NONE', #4680, #46648, #44936, .T. ) ;
#29208=CARTESIAN_POINT ( 'NONE',  ( 4.291220156522060236, -9.951772474098369514, -46.04727160136066288 ) ) ;
#29210=DIRECTION ( 'NONE',  ( 0.000000000000000000, 0.000000000000000000, 1.000000000000000000 ) ) ;
#29215=ORIENTED_EDGE ( 'NONE', *, *, #30042, .T. ) ;
#29220=FACE_OUTER_BOUND ( 'NONE', #25422, .T. ) ;
#29223=EDGE_LOOP ( 'NONE', ( #48423, #55425, #59706, #50634 ) ) ;
#29228=CARTESIAN_POINT ( 'NONE',  ( 5.895881250540457863, 19.70893872444552386, -4.010662783674629139 ) ) ;
#29237=CARTESIAN_POINT ( 'NONE',  ( 0.9788927965476014181, -39.63608187503911040, -13.61314167365405403 ) ) ;
#29244=CARTESIAN_POINT ( 'NONE',  ( 3.782625744892852637, 8.059507167186435339, -41.25872572337967625 ) ) ;
#29246=FACE_OUTER_BOUND ( 'NONE', #11480, .T. ) ;
#29249=ORIENTED_EDGE ( 'NONE', *, *, #61810, .T. ) ;
#29256=EDGE_CURVE ( 'NONE', #40254, #48086, #45707, .T. ) ;
#29263=( BOUNDED_SURFACE ( )  B_SPLINE_SURFACE ( 3, 1, ( 
 ( #58553, #53852 ),
 ( #25062, #20371 ),
 ( #57621, #58240 ),
 ( #14752, #10354 ) ),
 .UNSPECIFIED., .F., .F., .F. ) 
 B_SPLINE_SURFACE_WITH_KNOTS ( ( 4, 4 ),
 ( 2, 2 ),
 ( 0.000000000000000000, 1.000000000000000000 ),
 ( 0.000000000000000000, 1.000000000000000000 ),
 .UNSPECIFIED. ) 
 GEOMETRIC_REPRESENTATION_ITEM ( )  RATIONAL_B_SPLINE_SURFACE ( (
 ( 1.000000000000000000, 1.000000000000000000),
 ( 0.9952954269826590483, 0.8620686068821307169),
 ( 0.9952954269826590483, 0.8620686068821307169),
 ( 1.000000000000000000, 1.000000000000000000) ) ) 
 REPRESENTATION_ITEM ( '' )  SURFACE ( )  );
#29269=CARTESIAN_POINT ( 'NONE',  ( 5.895596859100789899, -13.98490190264574196, 14.45512718677573538 ) ) ;
#29273=CARTESIAN_POINT ( 'NONE',  ( 3.601691676948239884, 0.2777746788518056786, 42.02545230802814302 ) ) ;
#29280=CARTESIAN_POINT ( 'NONE',  ( 0.9762797500689124330, 33.20096159360316790, 25.57383300261796677 ) ) ;
#29281=EDGE_CURVE ( 'NONE', #38098, #38419, #6043, .T. ) ;
#29285=( BOUNDED_SURFACE ( )  B_SPLINE_SURFACE ( 3, 1, ( 
 ( #47336, #32944 ),
 ( #48797, #49107 ),
 ( #39425, #5851 ),
 ( #37969, #37648 ) ),
 .UNSPECIFIED., .F., .F., .F. ) 
 B_SPLINE_SURFACE_WITH_KNOTS ( ( 4, 4 ),
 ( 2, 2 ),
 ( 0.000000000000000000, 1.000000000000000000 ),
 ( 0.000000000000000000, 1.000000000000000000 ),
 .UNSPECIFIED. ) 
 GEOMETRIC_REPRESENTATION_ITEM ( )  RATIONAL_B_SPLINE_SURFACE ( (
 ( 1.000000000000000000, 1.000000000000000000),
 ( 0.7282232189291694135, 0.9929344683865672927),
 ( 0.7282232189291694135, 0.9929344683865672927),
 ( 1.000000000000000000, 1.000000000000000000) ) ) 
 REPRESENTATION_ITEM ( '' )  SURFACE ( )  );
#29292=VERTEX_POINT ( 'NONE', #39687 ) ;
#29305=CARTESIAN_POINT ( 'NONE',  ( 5.895596859100789899, 0.6684898708304538584, -20.10177366565161350 ) ) ;
#29314=CARTESIAN_POINT ( 'NONE',  ( 0.5804410086790514622, -1.020940616195406880, -46.88792522722240363 ) ) ;
#29319=CARTESIAN_POINT ( 'NONE',  ( 1.000433927950262980, -40.93358531992097227, 8.992233899849193079 ) ) ;
#29323=CARTESIAN_POINT ( 'NONE',  ( 2.618530812446115519, 46.98662296661649407, -1.408563591474231602 ) ) ;
#29326=ORIENTED_EDGE ( 'NONE', *, *, #6740, .T. ) ;
#29331=CARTESIAN_POINT ( 'NONE',  ( 0.5806925824938502512, -44.47729014209954101, -14.86583411581937320 ) ) ;
#29335=EDGE_CURVE ( 'NONE', #34780, #42042, #62, .T. ) ;
#29337=CARTESIAN_POINT ( 'NONE',  ( 5.901463166500145796, 20.06674442072659303, 1.357806574544058398 ) ) ;
#29339=CARTESIAN_POINT ( 'NONE',  ( 0.9787284016396609054, -6.785939174618667913, 41.35561664934046178 ) ) ;
#29343=VERTEX_POINT ( 'NONE', #26171 ) ;
#29350=CARTESIAN_POINT ( 'NONE',  ( 0.5804410086790514622, 28.25755288515122388, -37.43034272883804192 ) ) ;
#29357=EDGE_LOOP ( 'NONE', ( #52697, #53005, #43998, #24502 ) ) ;
#29367=B_SPLINE_CURVE_WITH_KNOTS ( 'NONE', 3,
 ( #45393, #16881, #35998, #55059 ),
 .UNSPECIFIED., .F., .F.,
 ( 4, 4 ),
 ( 8.673617379884035472E-19, 0.004041751736740998614 ),
 .UNSPECIFIED. ) ;
#29371=CARTESIAN_POINT ( 'NONE',  ( 0.9789233960466705575, 40.38468033015125513, 11.19885357810509952 ) ) ;
#29376=CARTESIAN_POINT ( 'NONE',  ( 5.896782393890504181, 16.58545041924871910, -11.37756218478521930 ) ) ;
#29381=B_SPLINE_CURVE_WITH_KNOTS ( 'NONE', 3,
 ( #35643, #37489, #32469, #23072, #36879, #56867 ),
 .UNSPECIFIED., .F., .F.,
 ( 4, 2, 4 ),
 ( 1.208501758069982961E-16, 0.0002448718616795920121, 0.0004897437233590632441 ),
 .UNSPECIFIED. ) ;
#29384=DIRECTION ( 'NONE',  ( -1.000000000000000000, -0.000000000000000000, -0.000000000000000000 ) ) ;
#29385=CARTESIAN_POINT ( 'NONE',  ( 0.9780303403264780648, 35.89220515824327151, -21.63536970503760060 ) ) ;
#29396=CARTESIAN_POINT ( 'NONE',  ( 1.000110580585050979, 38.83619784128909203, -15.75332409379547016 ) ) ;
#29399=DIRECTION ( 'NONE',  ( 0.000000000000000000, 0.000000000000000000, 1.000000000000000000 ) ) ;
#29404=CARTESIAN_POINT ( 'NONE',  ( 0.5817216825391129387, -42.05894263787597964, -20.74319879843310233 ) ) ;
#29408=EDGE_CURVE ( 'NONE', #16773, #7089, #42703, .T. ) ;
#29417=CARTESIAN_POINT ( 'NONE',  ( 0.6064782688330854210, 40.70787696428524782, -23.28525712719063279 ) ) ;
#29419=MECHANICAL_DESIGN_GEOMETRIC_PRESENTATION_REPRESENTATION('',(#56416),#40456);
#29420=CARTESIAN_POINT ( 'NONE',  ( 5.895596859100789899, 3.348897116308330091, 19.83212220910483481 ) ) ;
#29423=CARTESIAN_POINT ( 'NONE',  ( 3.376099380956842921, 11.76186387009555290, 6.431713763329955036 ) ) ;
#29424=CARTESIAN_POINT ( 'NONE',  ( 3.376099380956838925, 3.553490516825327017, -12.92598502161052565 ) ) ;
#29433=CARTESIAN_POINT ( 'NONE',  ( 0.5797568665920711517, -35.19933622554232500, -30.98761103865694011 ) ) ;
#29439=ORIENTED_EDGE ( 'NONE', *, *, #5279, .T. ) ;
#29446=DIRECTION ( 'NONE',  ( 0.000000000000000000, 0.000000000000000000, 1.000000000000000000 ) ) ;
#29449=CARTESIAN_POINT ( 'NONE',  ( 0.5834584762367748256, 40.25629450370218620, 24.05549296614785604 ) ) ;
#29453=CARTESIAN_POINT ( 'NONE',  ( 5.895596859100789899, 3.348897116308330091, 19.83212220910483481 ) ) ;
#29455=CARTESIAN_POINT ( 'NONE',  ( 0.5817216825391131607, 32.27291863391528892, -34.02489786988552112 ) ) ;
#29469=CARTESIAN_POINT ( 'NONE',  ( 3.661933894777899212, 46.83251759290548932, -4.398461192491206262 ) ) ;
#29470=CARTESIAN_POINT ( 'NONE',  ( 0.7764139734771263734, -39.16768475757491075, 25.80567653905045944 ) ) ;
#29475=B_SPLINE_CURVE_WITH_KNOTS ( 'NONE', 3,
 ( #6389, #16448, #25532, #35576, #54634, #30846 ),
 .UNSPECIFIED., .F., .F.,
 ( 4, 2, 4 ),
 ( 1.053462964043502403E-17, 0.0002448709889506573193, 0.0004897419779013041218 ),
 .UNSPECIFIED. ) ;
#29479=CIRCLE ( 'NONE', #19485, 46.67105333295396719 ) ;
#29481=CARTESIAN_POINT ( 'NONE',  ( 2.282816707992306959, 23.71786607569137217, 40.54577407355216678 ) ) ;
#29487=CARTESIAN_POINT ( 'NONE',  ( 5.917102823773431552, -17.29995091781586325, 10.25677416602822767 ) ) ;
#29492=B_SPLINE_CURVE_WITH_KNOTS ( 'NONE', 3,
 ( #17537, #12542, #46363, #13459, #50721, #12858 ),
 .UNSPECIFIED., .F., .F.,
 ( 4, 2, 4 ),
 ( 9.929776742050823831E-18, 0.0002448709889506595419, 0.0004897419779013092176 ),
 .UNSPECIFIED. ) ;
#29499=CIRCLE ( 'NONE', #16499, 47.09074272231896430 ) ;
#29500=CARTESIAN_POINT ( 'NONE',  ( 0.9787464366903554369, -1.577301036837284176, 41.87894595533244768 ) ) ;
#29505=CARTESIAN_POINT ( 'NONE',  ( 5.895596859100789899, -15.78680134203104579, -12.46214614742317295 ) ) ;
#29515=CARTESIAN_POINT ( 'NONE',  ( 0.5848930533535030563, -46.80349522319535538, -2.950579143132510129 ) ) ;
#29516=CARTESIAN_POINT ( 'NONE',  ( 4.956445790443991584, 25.79263028817558023, 39.39896284113483915 ) ) ;
#29517=CARTESIAN_POINT ( 'NONE',  ( 0.9791128995231611620, -17.64544790140575614, -38.01283470888404992 ) ) ;
#29520=EDGE_CURVE ( 'NONE', #19228, #6747, #58984, .T. ) ;
#29521=CARTESIAN_POINT ( 'NONE',  ( 0.9789889208857696090, -39.55815494300130553, 13.83789274231708966 ) ) ;
#29533=CARTESIAN_POINT ( 'NONE',  ( 0.8560838555295223751, -30.97734773434455491, -35.22466126774295248 ) ) ;
#29546=CARTESIAN_POINT ( 'NONE',  ( 0.9791128995231598298, 15.05754411609824928, -39.11020070822854677 ) ) ;
#29554=CARTESIAN_POINT ( 'NONE',  ( 0.5804410086790514622, -29.86002002114359755, -36.16488706179379875 ) ) ;
#29561=CARTESIAN_POINT ( 'NONE',  ( 5.901463166500146684, -17.31230476672924112, -10.23728352662563879 ) ) ;
#29566=CARTESIAN_POINT ( 'NONE',  ( 0.5806925824938499181, -13.37132486740634540, -44.94919391528445374 ) ) ;
#29567=CARTESIAN_POINT ( 'NONE',  ( 4.960386119450143738, -37.40422633003237962, 22.70154878690114941 ) ) ;
#29576=EDGE_CURVE ( 'NONE', #13746, #44371, #6826, .T. ) ;
#29577=CARTESIAN_POINT ( 'NONE',  ( 0.7764146366350265227, -24.48247828494958611, 40.00810831189270544 ) ) ;
#29584=CARTESIAN_POINT ( 'NONE',  ( 5.896278296736517710, -19.39678151694244690, 5.319008027666769500 ) ) ;
#29593=CARTESIAN_POINT ( 'NONE',  ( 0.7056759521544987424, -29.63218968554087240, -36.35494689250850797 ) ) ;
#29598=ORIENTED_EDGE ( 'NONE', *, *, #32587, .T. ) ;
#29602=DIRECTION ( 'NONE',  ( 0.000000000000000000, 0.000000000000000000, 1.000000000000000000 ) ) ;
#29603=CARTESIAN_POINT ( 'NONE',  ( 0.5782707292762423457, -2.290569157858090676, -46.84538020595721264 ) ) ;
#29607=CARTESIAN_POINT ( 'NONE',  ( 1.231276596079881047, -23.26513148155264332, 34.87134107206281186 ) ) ;
#29614=ORIENTED_EDGE ( 'NONE', *, *, #29715, .F. ) ;
#29617=ORIENTED_EDGE ( 'NONE', *, *, #55857, .T. ) ;
#29619=CARTESIAN_POINT ( 'NONE',  ( 0.5806925824938499181, 42.95845041307745760, 18.80940989108190209 ) ) ;
#29621=CARTESIAN_POINT ( 'NONE',  ( 1.231276596079881047, 41.91134057782998212, 0.8463462572780127147 ) ) ;
#29622=CARTESIAN_POINT ( 'NONE',  ( 5.917102823773431552, -7.220356195166569790, 18.77115272077508124 ) ) ;
#29631=ORIENTED_EDGE ( 'NONE', *, *, #21358, .F. ) ;
#29645=B_SPLINE_CURVE_WITH_KNOTS ( 'NONE', 3,
 ( #60859, #55230, #7944, #22353, #17979, #3226 ),
 .UNSPECIFIED., .F., .F.,
 ( 4, 2, 4 ),
 ( 7.757919228897728493E-18, 0.0002291472222819922579, 0.0004582944445639767638 ),
 .UNSPECIFIED. ) ;
#29647=VECTOR ( 'NONE', #6648, 999.9999999999998863 ) ;
#29648=CARTESIAN_POINT ( 'NONE',  ( 0.9788927965476029724, 29.03256182720962641, -30.22328516857536940 ) ) ;
#29656=CARTESIAN_POINT ( 'NONE',  ( 4.962356264823596597, 39.89814050050772920, 13.39305724859313429 ) ) ;
#29665=CARTESIAN_POINT ( 'NONE',  ( 3.376099380956838925, -3.529868236344142929, -12.93245583275333743 ) ) ;
#29666=CARTESIAN_POINT ( 'NONE',  ( 0.5837799406558230597, -25.31068968778611250, -39.47926718045562211 ) ) ;
#29675=CARTESIAN_POINT ( 'NONE',  ( 5.901463166500145796, -17.29756286482720284, -10.26217273670579466 ) ) ;
#29679=EDGE_CURVE ( 'NONE', #7082, #7098, #36446, .T. ) ;
#29682=CARTESIAN_POINT ( 'NONE',  ( 2.282816707992308736, -46.27578434998796553, -8.065280478779142115 ) ) ;
#29683=ORIENTED_EDGE ( 'NONE', *, *, #47185, .F. ) ;
#29698=ORIENTED_EDGE ( 'NONE', *, *, #28269, .T. ) ;
#29707=CARTESIAN_POINT ( 'NONE',  ( 5.896782393890504181, -11.92541098582113612, -16.19600752337651883 ) ) ;
#29711=FACE_OUTER_BOUND ( 'NONE', #21316, .T. ) ;
#29715=EDGE_CURVE ( 'NONE', #41352, #7929, #41151, .T. ) ;
#29716=CARTESIAN_POINT ( 'NONE',  ( 0.8554163680231708922, 31.95314001164559059, 34.35407277904604229 ) ) ;
#29720=CARTESIAN_POINT ( 'NONE',  ( 0.8554163680231720024, -41.45413358837884488, 21.97180651536554308 ) ) ;
#29722=AXIS2_PLACEMENT_3D ( 'NONE', #30695, #44836, #59195 ) ;
#29723=AXIS2_PLACEMENT_3D ( 'NONE', #24444, #51709, #28836 ) ;
#29730=CARTESIAN_POINT ( 'NONE',  ( 4.960386119450151732, -4.847629508247444541, 43.48490488460461023 ) ) ;
#29731=AXIS2_PLACEMENT_3D ( 'NONE', #19429, #57599, #1219 ) ;
#29732=CARTESIAN_POINT ( 'NONE',  ( 0.8554163680231708922, -39.19027442586736498, 25.79395013442155005 ) ) ;
#29734=CARTESIAN_POINT ( 'NONE',  ( 5.910764540655177868, 12.97317151014736503, 15.36873642943569251 ) ) ;
#29740=VERTEX_POINT ( 'NONE', #3203 ) ;
#29742=CARTESIAN_POINT ( 'NONE',  ( 1.000110580585050979, 25.38656982076186353, -33.34575768381163385 ) ) ;
#29744=ORIENTED_EDGE ( 'NONE', *, *, #29755, .F. ) ;
#29748=ORIENTED_EDGE ( 'NONE', *, *, #56427, .F. ) ;
#29751=EDGE_CURVE ( 'NONE', #42659, #13798, #30208, .T. ) ;
#29752=ORIENTED_EDGE ( 'NONE', *, *, #47183, .T. ) ;
#29755=EDGE_CURVE ( 'NONE', #35032, #42568, #51223, .T. ) ;
#29759=B_SPLINE_CURVE_WITH_KNOTS ( 'NONE', 3,
 ( #27820, #46952, #41329, #14901 ),
 .UNSPECIFIED., .F., .F.,
 ( 4, 4 ),
 ( 0.000000000000000000, 0.004041751736741002084 ),
 .UNSPECIFIED. ) ;
#29761=VERTEX_POINT ( 'NONE', #16709 ) ;
#29765=CARTESIAN_POINT ( 'NONE',  ( 0.5837800304671207918, 32.63445599095994965, -33.67832558714280111 ) ) ;
#29771=CARTESIAN_POINT ( 'NONE',  ( 0.8560838555295223751, 27.08392101972057731, -38.29926965725677235 ) ) ;
#29774=CARTESIAN_POINT ( 'NONE',  ( 0.5824935313925976299, -46.81422942724466196, -2.768772324900471649 ) ) ;
#29776=VERTEX_POINT ( 'NONE', #47680 ) ;
#29778=EDGE_CURVE ( 'NONE', #54614, #4627, #13522, .T. ) ;
#29781=CARTESIAN_POINT ( 'NONE',  ( 0.9789233960466698914, -12.29085669408485160, -40.06584041996139689 ) ) ;
#29791=CARTESIAN_POINT ( 'NONE',  ( 3.376099380956842921, 1.798919266859354327, 13.28428669908133486 ) ) ;
#29798=EDGE_CURVE ( 'NONE', #59869, #26853, #41160, .T. ) ;
#29800=CARTESIAN_POINT ( 'NONE',  ( 4.291220156522059348, 34.26497439135438583, -32.33110773335063470 ) ) ;
#29802=EDGE_CURVE ( 'NONE', #18712, #61, #58297, .T. ) ;
#29814=ORIENTED_EDGE ( 'NONE', *, *, #26434, .F. ) ;
#29815=EDGE_LOOP ( 'NONE', ( #55610, #39122, #35402, #13287 ) ) ;
#29823=EDGE_CURVE ( 'NONE', #25579, #35927, #23248, .T. ) ;
#29827=VERTEX_POINT ( 'NONE', #17952 ) ;
#29836=EDGE_CURVE ( 'NONE', #27817, #47199, #7500, .T. ) ;
#29841=ORIENTED_EDGE ( 'NONE', *, *, #10650, .F. ) ;
#29847=ORIENTED_EDGE ( 'NONE', *, *, #27156, .T. ) ;
#29854=ORIENTED_EDGE ( 'NONE', *, *, #35542, .F. ) ;
#29869=LINE ( 'NONE', #48984, #35423 ) ;
#29887=CARTESIAN_POINT ( 'NONE',  ( 0.9762797500689124330, -34.26226594605947895, 24.13341909939818564 ) ) ;
#29895=CARTESIAN_POINT ( 'NONE',  ( 5.896278296736517710, 18.99819559441558070, -6.602692160831987955 ) ) ;
#29915=CARTESIAN_POINT ( 'NONE',  ( 2.282803330402962239, 3.392772187570622044, 46.85067773618895615 ) ) ;
#29917=CARTESIAN_POINT ( 'NONE',  ( 5.895596859100789899, 8.462961974658767872, -18.24572437114973056 ) ) ;
#29920=CARTESIAN_POINT ( 'NONE',  ( 0.5806925824938499181, -14.41498975133639426, 44.62544602368059543 ) ) ;
#29927=ORIENTED_EDGE ( 'NONE', *, *, #8754, .T. ) ;
#29940=CARTESIAN_POINT ( 'NONE',  ( 3.238018933889920792, -7.437505510344910142, -11.13961418323103558 ) ) ;
#29946=CARTESIAN_POINT ( 'NONE',  ( 1.231276596079887264, 14.27346765619334512, -39.41503383336959132 ) ) ;
#29948=EDGE_LOOP ( 'NONE', ( #58940, #58682, #47666, #37102 ) ) ;
#29954=CARTESIAN_POINT ( 'NONE',  ( 0.5804410086790514622, 32.99440095574045273, -33.33000686209395269 ) ) ;
#29957=CARTESIAN_POINT ( 'NONE',  ( 5.901463166500145796, -11.91875711499639934, -16.20065119599700765 ) ) ;
#29963=ORIENTED_EDGE ( 'NONE', *, *, #19960, .F. ) ;
#29974=CARTESIAN_POINT ( 'NONE',  ( 0.5804410086790514622, -13.37224000219836917, -44.95223074752801296 ) ) ;
#29976=CARTESIAN_POINT ( 'NONE',  ( 120.0000507999999968, 0.000000000000000000, 0.000000000000000000 ) ) ;
#29984=ORIENTED_EDGE ( 'NONE', *, *, #48528, .T. ) ;
#29985=CARTESIAN_POINT ( 'NONE',  ( 4.958415959904820980, 18.66009313387939628, 41.41261737752859773 ) ) ;
#29987=CARTESIAN_POINT ( 'NONE',  ( 4.958415959904820092, 13.93965400761620366, -43.23066041561927619 ) ) ;
#29994=VERTEX_POINT ( 'NONE', #59530 ) ;
#30002=CARTESIAN_POINT ( 'NONE',  ( 0.9762797500689124330, -31.41867615533366376, -27.73430319715951242 ) ) ;
#30008=EDGE_CURVE ( 'NONE', #39735, #22660, #11982, .T. ) ;
#30010=ORIENTED_EDGE ( 'NONE', *, *, #40400, .T. ) ;
#30011=VERTEX_POINT ( 'NONE', #45469 ) ;
#30016=CARTESIAN_POINT ( 'NONE',  ( 0.9790724872846766624, -27.02650450976093310, -32.02972469387346166 ) ) ;
#30017=CARTESIAN_POINT ( 'NONE',  ( 0.9785694773339250752, 38.49576580281336646, 16.56536812055855634 ) ) ;
#30021=CARTESIAN_POINT ( 'NONE',  ( 0.5824936645240084143, 36.57713187198718430, 29.34879219081370039 ) ) ;
#30023=CARTESIAN_POINT ( 'NONE',  ( 0.5837799406558258353, -41.89664897202754901, -21.06927512972148975 ) ) ;
#30029=EDGE_CURVE ( 'NONE', #20518, #47447, #18737, .T. ) ;
#30032=CARTESIAN_POINT ( 'NONE',  ( 0.5782707292762423457, -41.52883855096556687, 21.79660345823301881 ) ) ;
#30037=FACE_OUTER_BOUND ( 'NONE', #11945, .T. ) ;
#30042=EDGE_CURVE ( 'NONE', #56097, #21039, #4655, .T. ) ;
#30047=CARTESIAN_POINT ( 'NONE',  ( 0.6845945791218023269, 39.91187923413981764, -24.64646864590107000 ) ) ;
#30049=CARTESIAN_POINT ( 'NONE',  ( 1.231276596079881047, -0.5545928549373742023, -41.91621640586514985 ) ) ;
#30053=CARTESIAN_POINT ( 'NONE',  ( 0.8560838555295223751, -35.39593983670150124, -30.78149244527203621 ) ) ;
#30057=CARTESIAN_POINT ( 'NONE',  ( 4.960386119450141074, -25.57375555595671202, 35.50238712307264421 ) ) ;
#30060=ADVANCED_FACE ( 'NONE', ( #23184 ), #52223, .F. ) ;
#30066=VERTEX_POINT ( 'NONE', #56992 ) ;
#30067=CARTESIAN_POINT ( 'NONE',  ( 5.896278296736517710, 16.58497454171972052, 11.37829508603518391 ) ) ;
#30095=( BOUNDED_SURFACE ( )  B_SPLINE_SURFACE ( 3, 1, ( 
 ( #33132, #4270 ),
 ( #42234, #37217 ),
 ( #61292, #22790 ),
 ( #17477, #32825 ) ),
 .UNSPECIFIED., .F., .F., .F. ) 
 B_SPLINE_SURFACE_WITH_KNOTS ( ( 4, 4 ),
 ( 2, 2 ),
 ( 0.000000000000000000, 1.000000000000000000 ),
 ( 0.000000000000000000, 1.000000000000000000 ),
 .UNSPECIFIED. ) 
 GEOMETRIC_REPRESENTATION_ITEM ( )  RATIONAL_B_SPLINE_SURFACE ( (
 ( 1.000000000000000000, 1.000000000000000000),
 ( 0.9729067724841187204, 0.9999501103223794596),
 ( 0.9729067724841187204, 0.9999501103223794596),
 ( 1.000000000000000000, 1.000000000000000000) ) ) 
 REPRESENTATION_ITEM ( '' )  SURFACE ( )  );
#30101=EDGE_CURVE ( 'NONE', #4396, #18712, #48561, .T. ) ;
#30107=B_SPLINE_CURVE_WITH_KNOTS ( 'NONE', 3,
 ( #1893, #35444, #35133, #44853 ),
 .UNSPECIFIED., .F., .F.,
 ( 4, 4 ),
 ( 9.813077866773596333E-18, 0.005004948556313810505 ),
 .UNSPECIFIED. ) ;
#30115=FACE_OUTER_BOUND ( 'NONE', #13863, .T. ) ;
#30120=ORIENTED_EDGE ( 'NONE', *, *, #25129, .F. ) ;
#30121=ORIENTED_EDGE ( 'NONE', *, *, #26734, .F. ) ;
#30128=EDGE_LOOP ( 'NONE', ( #29631, #39276, #51458, #15987 ) ) ;
#30130=CARTESIAN_POINT ( 'NONE',  ( 0.9775691876210974574, -17.29743328507051103, -38.17240509502285306 ) ) ;
#30134=B_SPLINE_CURVE_WITH_KNOTS ( 'NONE', 3,
 ( #14179, #37999, #51740, #8837 ),
 .UNSPECIFIED., .F., .F.,
 ( 4, 4 ),
 ( 0.000000000000000000, 0.004447772540403795508 ),
 .UNSPECIFIED. ) ;
#30137=CARTESIAN_POINT ( 'NONE',  ( 5.896278296736517710, -9.661066686813860827, -17.64060004895862832 ) ) ;
#30138=CARTESIAN_POINT ( 'NONE',  ( 1.231276596079881047, 14.27346765619277846, 39.41503383336979027 ) ) ;
#30139=CARTESIAN_POINT ( 'NONE',  ( 2.618530812446111078, 12.26263843375577522, -45.38011114840042382 ) ) ;
#30146=CARTESIAN_POINT ( 'NONE',  ( 5.895881250540457863, 5.954605924855886023, 19.21120375947254644 ) ) ;
#30151=CARTESIAN_POINT ( 'NONE',  ( 5.910764540655178756, -1.997730036635652295, 20.01275376278553964 ) ) ;
#30159=CARTESIAN_POINT ( 'NONE',  ( 0.9762797500689124330, 15.53330887509137703, -38.92352888134260525 ) ) ;
#30160=CARTESIAN_POINT ( 'NONE',  ( 4.962356264823608143, -19.84272732133934269, -37.11471096901227185 ) ) ;
#30164=CARTESIAN_POINT ( 'NONE',  ( 0.9790724872846788829, 9.754597114931216950, -40.75761333918888596 ) ) ;
#30171=EDGE_CURVE ( 'NONE', #20290, #16119, #52323, .T. ) ;
#30193=ORIENTED_EDGE ( 'NONE', *, *, #54284, .F. ) ;
#30195=CARTESIAN_POINT ( 'NONE',  ( 3.238018933889920792, -10.88486934301737996, -7.805582089318734873 ) ) ;
#30203=CARTESIAN_POINT ( 'NONE',  ( 0.5835226383429301666, -38.76587123842037386, -26.39033348921869049 ) ) ;
#30205=DIRECTION ( 'NONE',  ( 0.07500201931887537365, -0.9863955245047961728, -0.1462824881351111328 ) ) ;
#30207=CARTESIAN_POINT ( 'NONE',  ( 0.9790724872846777727, -41.06080244794662093, -8.387235081488672250 ) ) ;
#30208=CIRCLE ( 'NONE', #52209, 42.08604991992415023 ) ;
#30213=CARTESIAN_POINT ( 'NONE',  ( 1.231276596079887264, 33.41651732065550817, 25.31033664684050777 ) ) ;
#30225=FACE_OUTER_BOUND ( 'NONE', #27444, .T. ) ;
#30236=CARTESIAN_POINT ( 'NONE',  ( 3.376099380956842921, 13.33943071323250606, 1.329651036526637409 ) ) ;
#30237=CARTESIAN_POINT ( 'NONE',  ( 4.958415959904820092, -43.67231206503777940, 12.48731807541533101 ) ) ;
#30244=VERTEX_POINT ( 'NONE', #55373 ) ;
#30251=VECTOR ( 'NONE', #39165, 1000.000000000000000 ) ;
#30256=EDGE_CURVE ( 'NONE', #44981, #5400, #30966, .T. ) ;
#30280=EDGE_CURVE ( 'NONE', #20220, #40686, #40271, .T. ) ;
#30287=CARTESIAN_POINT ( 'NONE',  ( 0.5834584762367746036, -34.90241844189876730, 31.32183225674696558 ) ) ;
#30290=CARTESIAN_POINT ( 'NONE',  ( 2.618530812446115519, 41.14519205294185866, 22.73323470438666405 ) ) ;
#30296=CARTESIAN_POINT ( 'NONE',  ( 0.8554163680231816613, -38.15570339590838245, 27.30105806512422717 ) ) ;
#30300=B_SPLINE_CURVE_WITH_KNOTS ( 'NONE', 3,
 ( #57853, #49699, #34694, #40036, #1764, #10891 ),
 .UNSPECIFIED., .F., .F.,
 ( 4, 2, 4 ),
 ( 5.854691731421724714E-18, 0.0002291472222819923663, 0.0004582944445639788780 ),
 .UNSPECIFIED. ) ;
#30301=ADVANCED_FACE ( 'NONE', ( #49762 ), #41465, .F. ) ;
#30302=VERTEX_POINT ( 'NONE', #46318 ) ;
#30306=CARTESIAN_POINT ( 'NONE',  ( 0.9783242366443551941, 36.19415619989782584, -21.12622889168628504 ) ) ;
#30313=VERTEX_POINT ( 'NONE', #27811 ) ;
#30340=CARTESIAN_POINT ( 'NONE',  ( 4.956445790443988031, 0.000000000000000000, 0.000000000000000000 ) ) ;
#30350=DIRECTION ( 'NONE',  ( -1.000000000000000000, -0.000000000000000000, -0.000000000000000000 ) ) ;
#30356=ORIENTED_EDGE ( 'NONE', *, *, #55689, .F. ) ;
#30362=LINE ( 'NONE', #49475, #54439 ) ;
#30368=CARTESIAN_POINT ( 'NONE',  ( 0.9785694773339237429, 20.33543408136244324, -36.64431096960669265 ) ) ;
#30370=EDGE_CURVE ( 'NONE', #60419, #19501, #24599, .T. ) ;
#30371=ORIENTED_EDGE ( 'NONE', *, *, #29520, .F. ) ;
#30381=CARTESIAN_POINT ( 'NONE',  ( 4.958415959904820980, -45.08182420577212923, 5.552754280759789829 ) ) ;
#30391=B_SPLINE_CURVE_WITH_KNOTS ( 'NONE', 3,
 ( #7339, #27092, #3261, #21463 ),
 .UNSPECIFIED., .F., .F.,
 ( 4, 4 ),
 ( 0.000000000000000000, 0.004447772540403832804 ),
 .UNSPECIFIED. ) ;
#30397=B_SPLINE_CURVE_WITH_KNOTS ( 'NONE', 3,
 ( #46029, #22197, #41321, #39396, #1142, #4589 ),
 .UNSPECIFIED., .F., .F.,
 ( 4, 2, 4 ),
 ( 1.738108305489988542E-18, 0.0002291459268755701535, 0.0004582918537511385722 ),
 .UNSPECIFIED. ) ;
#30398=AXIS2_PLACEMENT_3D ( 'NONE', #60968, #3944, #37830 ) ;
#30399=CARTESIAN_POINT ( 'NONE',  ( 5.838029081930957709, -43.47829931555697414, 18.45812955799579669 ) ) ;
#30414=DIRECTION ( 'NONE',  ( -1.000000000000000000, 0.000000000000000000, 0.000000000000000000 ) ) ;
#30427=AXIS2_PLACEMENT_3D ( 'NONE', #22843, #57474, #14616 ) ;
#30430=ORIENTED_EDGE ( 'NONE', *, *, #50647, .T. ) ;
#30434=DIRECTION ( 'NONE',  ( -0.07500201931887527651, 0.5805833823197910082, -0.8107389427381679337 ) ) ;
#30436=CARTESIAN_POINT ( 'NONE',  ( 0.9762797500689124330, -18.09842611962761083, -37.79909730639192844 ) ) ;
#30440=ORIENTED_EDGE ( 'NONE', *, *, #60193, .T. ) ;
#30441=CARTESIAN_POINT ( 'NONE',  ( 5.895881250540457863, -9.661888320803921459, -17.64016994489037415 ) ) ;
#30448=ADVANCED_FACE ( 'NONE', ( #1976 ), #7384, .F. ) ;
#30452=ORIENTED_EDGE ( 'NONE', *, *, #2337, .T. ) ;
#30455=EDGE_CURVE ( 'NONE', #33009, #53253, #58994, .T. ) ;
#30457=CARTESIAN_POINT ( 'NONE',  ( 0.5806925824938499181, -35.14454992382352572, 31.04968555388990836 ) ) ;
#30462=CARTESIAN_POINT ( 'NONE',  ( 0.9785694773339264074, 15.26978228898493839, -39.02779976582937849 ) ) ;
#30473=CARTESIAN_POINT ( 'NONE',  ( 0.5804410086790514622, 32.99440095573996246, 33.33000686209444297 ) ) ;
#30477=CARTESIAN_POINT ( 'NONE',  ( 4.956445790443988031, 0.000000000000000000, 0.000000000000000000 ) ) ;
#30478=CARTESIAN_POINT ( 'NONE',  ( 4.958415959904823644, -38.82150677285534357, 23.58165739950832318 ) ) ;
#30479=CARTESIAN_POINT ( 'NONE',  ( 0.9784957157296353403, -22.35374192235875412, 35.44916471598384788 ) ) ;
#30482=CARTESIAN_POINT ( 'NONE',  ( 0.5848930533535030563, 46.45334699384589072, 6.431145734385690815 ) ) ;
#30484=CARTESIAN_POINT ( 'NONE',  ( 0.5848930533535030563, -41.77346544155627583, -21.31315714272907869 ) ) ;
#30495=DIRECTION ( 'NONE',  ( 0.000000000000000000, 0.000000000000000000, 1.000000000000000000 ) ) ;
#30499=DIRECTION ( 'NONE',  ( 0.000000000000000000, 0.000000000000000000, 1.000000000000000000 ) ) ;
#30504=B_SPLINE_CURVE_WITH_KNOTS ( 'NONE', 3,
 ( #19572, #39303, #1054, #53970, #48989, #24570 ),
 .UNSPECIFIED., .F., .F.,
 ( 4, 2, 4 ),
 ( 1.219794421808126673E-16, 0.0002448718616795938011, 0.0004897437233590656294 ),
 .UNSPECIFIED. ) ;
#30510=CARTESIAN_POINT ( 'NONE',  ( 1.000433927950261648, -30.63672940459725780, 28.59736856849475828 ) ) ;
#30517=CARTESIAN_POINT ( 'NONE',  ( 4.962356264823608143, 41.96072444189411499, 3.245489512196318316 ) ) ;
#30523=CARTESIAN_POINT ( 'NONE',  ( 0.9754292580325136797, 32.52564057721537694, 26.42745110573104483 ) ) ;
#30529=EDGE_CURVE ( 'NONE', #52958, #46743, #2161, .T. ) ;
#30549=( BOUNDED_SURFACE ( )  B_SPLINE_SURFACE ( 3, 1, ( 
 ( #41966, #8723 ),
 ( #23446, #61032 ),
 ( #57233, #32240 ),
 ( #18140, #46653 ) ),
 .UNSPECIFIED., .F., .F., .F. ) 
 B_SPLINE_SURFACE_WITH_KNOTS ( ( 4, 4 ),
 ( 2, 2 ),
 ( 0.000000000000000000, 1.000000000000000000 ),
 ( 0.000000000000000000, 1.000000000000000000 ),
 .UNSPECIFIED. ) 
 GEOMETRIC_REPRESENTATION_ITEM ( )  RATIONAL_B_SPLINE_SURFACE ( (
 ( 1.000000000000000000, 1.000000000000000000),
 ( 0.9952954269826590483, 0.8620686068821307169),
 ( 0.9952954269826590483, 0.8620686068821307169),
 ( 1.000000000000000000, 1.000000000000000000) ) ) 
 REPRESENTATION_ITEM ( '' )  SURFACE ( )  );
#30550=CARTESIAN_POINT ( 'NONE',  ( 0.9790724872846773286, 15.02455757522504420, 39.12285623072784801 ) ) ;
#30551=ORIENTED_EDGE ( 'NONE', *, *, #37586, .T. ) ;
#30565=ORIENTED_EDGE ( 'NONE', *, *, #29256, .F. ) ;
#30574=CARTESIAN_POINT ( 'NONE',  ( 0.6064782688330854210, 32.08784176340432737, 34.20094819424595300 ) ) ;
#30585=EDGE_LOOP ( 'NONE', ( #19388, #61334 ) ) ;
#30591=CARTESIAN_POINT ( 'NONE',  ( 1.091591847532194626, 4.971042726581281990, -41.61787747070175669 ) ) ;
#30592=CARTESIAN_POINT ( 'NONE',  ( 0.7056759521544974101, -46.84549373964249952, 2.290970407077026483 ) ) ;
#30596=LINE ( 'NONE', #25915, #35748 ) ;
#30604=CARTESIAN_POINT ( 'NONE',  ( 5.895596859100789899, -7.225383168024946734, -18.77024297359278293 ) ) ;
#30606=CARTESIAN_POINT ( 'NONE',  ( 0.9762797500689124330, 4.697980241568662230, 41.64437257103935508 ) ) ;
#30610=EDGE_CURVE ( 'NONE', #59587, #22620, #43298, .T. ) ;
#30614=EDGE_CURVE ( 'NONE', #57082, #48917, #41469, .T. ) ;
#30620=CARTESIAN_POINT ( 'NONE',  ( 0.9762797500689124330, -18.09842611962814019, 37.79909730639167265 ) ) ;
#30621=CARTESIAN_POINT ( 'NONE',  ( 0.9780303403264796192, 38.45566908893830771, -16.65836511537540332 ) ) ;
#30623=CARTESIAN_POINT ( 'NONE',  ( 0.5848930533535030563, -30.41648929863225703, 35.69468113226040629 ) ) ;
#30626=AXIS2_PLACEMENT_3D ( 'NONE', #57278, #47606, #47923 ) ;
#30627=CARTESIAN_POINT ( 'NONE',  ( 1.000110580585051201, -40.93372354294542959, -8.991538226667278977 ) ) ;
#30628=CARTESIAN_POINT ( 'NONE',  ( 0.8554163680231816613, -14.77070554666818758, -44.53124443315552128 ) ) ;
#30629=VERTEX_POINT ( 'NONE', #22037 ) ;
#30630=CARTESIAN_POINT ( 'NONE',  ( 0.9762797500689124330, -31.41867615533404390, 27.73430319715907544 ) ) ;
#30635=CARTESIAN_POINT ( 'NONE',  ( 5.838029081930957709, -40.65053383315965618, -24.05408816047831877 ) ) ;
#30636=CARTESIAN_POINT ( 'NONE',  ( 0.5782707292762442330, 32.08118243869992625, 34.21306895095013800 ) ) ;
#30638=B_SPLINE_CURVE_WITH_KNOTS ( 'NONE', 3,
 ( #61386, #48245, #61689, #47626 ),
 .UNSPECIFIED., .F., .F.,
 ( 4, 4 ),
 ( 7.589415207398531038E-19, 0.004446298630425094510 ),
 .UNSPECIFIED. ) ;
#30652=DIRECTION ( 'NONE',  ( -1.000000000000000000, -0.000000000000000000, -0.000000000000000000 ) ) ;
#30656=CARTESIAN_POINT ( 'NONE',  ( 4.962356264823603702, 37.36413190407388640, -19.36897635181878030 ) ) ;
#30659=ORIENTED_EDGE ( 'NONE', *, *, #31410, .F. ) ;
#30663=VERTEX_POINT ( 'NONE', #17641 ) ;
#30669=FACE_OUTER_BOUND ( 'NONE', #37719, .T. ) ;
#30671=ORIENTED_EDGE ( 'NONE', *, *, #10418, .T. ) ;
#30674=CARTESIAN_POINT ( 'NONE',  ( 0.9754292580325137907, 35.75786466006411501, 21.85640825608229321 ) ) ;
#30679=CARTESIAN_POINT ( 'NONE',  ( 0.9787284016396600173, 19.97613726806151746, -36.84141607995537981 ) ) ;
#30680=EDGE_CURVE ( 'NONE', #16352, #34782, #17837, .T. ) ;
#30683=EDGE_CURVE ( 'NONE', #35390, #371, #41054, .T. ) ;
#30688=CARTESIAN_POINT ( 'NONE',  ( 0.5824936645240084143, 32.86261044185514635, -33.45574709952209957 ) ) ;
#30689=CARTESIAN_POINT ( 'NONE',  ( 4.960386119450146403, -10.60034705332560101, -42.45078452774922084 ) ) ;
#30695=CARTESIAN_POINT ( 'NONE',  ( 4.962356264823608143, 0.000000000000000000, 0.000000000000000000 ) ) ;
#30696=ORIENTED_EDGE ( 'NONE', *, *, #16685, .T. ) ;
#30706=EDGE_CURVE ( 'NONE', #25288, #8559, #49219, .T. ) ;
#30714=CARTESIAN_POINT ( 'NONE',  ( 0.9790320750461911636, 41.54611640558821506, -5.500667609982005324 ) ) ;
#30719=CARTESIAN_POINT ( 'NONE',  ( 0.8560838555295158248, -24.46533024579895610, -40.02274915652004239 ) ) ;
#30726=CIRCLE ( 'NONE', #30866, 47.09074272231896430 ) ;
#30728=CARTESIAN_POINT ( 'NONE',  ( 0.6845945791218023269, -46.85360930762397658, -2.268439014493842443 ) ) ;
#30737=ORIENTED_EDGE ( 'NONE', *, *, #173, .F. ) ;
#30738=DIRECTION ( 'NONE',  ( 0.000000000000000000, 0.000000000000000000, 1.000000000000000000 ) ) ;
#30739=CARTESIAN_POINT ( 'NONE',  ( 0.8554163680231738898, 43.54276151446884313, -17.47092993535008176 ) ) ;
#30744=CIRCLE ( 'NONE', #9735, 42.08604991992415023 ) ;
#30748=ORIENTED_EDGE ( 'NONE', *, *, #36538, .F. ) ;
#30753=( BOUNDED_SURFACE ( )  B_SPLINE_SURFACE ( 3, 1, ( 
 ( #11023, #346 ),
 ( #24172, #58590 ),
 ( #10708, #29800 ),
 ( #38306, #57356 ) ),
 .UNSPECIFIED., .F., .F., .F. ) 
 B_SPLINE_SURFACE_WITH_KNOTS ( ( 4, 4 ),
 ( 2, 2 ),
 ( 0.000000000000000000, 1.000000000000000000 ),
 ( 0.000000000000000000, 1.000000000000000000 ),
 .UNSPECIFIED. ) 
 GEOMETRIC_REPRESENTATION_ITEM ( )  RATIONAL_B_SPLINE_SURFACE ( (
 ( 1.000000000000000000, 1.000000000000000000),
 ( 0.7282232189291694135, 0.9929344683865672927),
 ( 0.7282232189291694135, 0.9929344683865672927),
 ( 1.000000000000000000, 1.000000000000000000) ) ) 
 REPRESENTATION_ITEM ( '' )  SURFACE ( )  );
#30755=ADVANCED_FACE ( 'NONE', ( #47690 ), #9415, .F. ) ;
#30761=VERTEX_POINT ( 'NONE', #53590 ) ;
#30786=VECTOR ( 'NONE', #53275, 1000.000000000000000 ) ;
#30787=B_SPLINE_CURVE_WITH_KNOTS ( 'NONE', 3,
 ( #28307, #53330, #24847, #20156, #4470, #23610 ),
 .UNSPECIFIED., .F., .F.,
 ( 4, 2, 4 ),
 ( 1.196425325848827598E-16, 0.0002448718616795920663, 0.0004897437233590645452 ),
 .UNSPECIFIED. ) ;
#30789=CARTESIAN_POINT ( 'NONE',  ( 5.895596859100789899, -13.97974974393952508, -14.46010996878344201 ) ) ;
#30791=CARTESIAN_POINT ( 'NONE',  ( 3.238018933889920792, 4.556392162264638834, 12.59550645394246615 ) ) ;
#30812=ADVANCED_FACE ( 'NONE', ( #6579 ), #38295, .F. ) ;
#30818=B_SPLINE_CURVE_WITH_KNOTS ( 'NONE', 3,
 ( #61800, #38661, #57716, #38059 ),
 .UNSPECIFIED., .F., .F.,
 ( 4, 4 ),
 ( 0.000000000000000000, 0.004041751736740986471 ),
 .UNSPECIFIED. ) ;
#30824=( BOUNDED_SURFACE ( )  B_SPLINE_SURFACE ( 3, 1, ( 
 ( #27540, #7485 ),
 ( #3104, #46358 ),
 ( #60413, #45438 ),
 ( #41063, #50715 ) ),
 .UNSPECIFIED., .F., .F., .F. ) 
 B_SPLINE_SURFACE_WITH_KNOTS ( ( 4, 4 ),
 ( 2, 2 ),
 ( 0.000000000000000000, 1.000000000000000000 ),
 ( 0.000000000000000000, 1.000000000000000000 ),
 .UNSPECIFIED. ) 
 GEOMETRIC_REPRESENTATION_ITEM ( )  RATIONAL_B_SPLINE_SURFACE ( (
 ( 1.000000000000000000, 1.000000000000000000),
 ( 0.7282232189291693025, 0.9929344683865674037),
 ( 0.7282232189291693025, 0.9929344683865674037),
 ( 1.000000000000000000, 1.000000000000000000) ) ) 
 REPRESENTATION_ITEM ( '' )  SURFACE ( )  );
#30840=CARTESIAN_POINT ( 'NONE',  ( 2.282803330402972453, 12.16313988363625143, -45.37130079277079631 ) ) ;
#30843=CARTESIAN_POINT ( 'NONE',  ( 4.956445790444001354, -28.36659270909979114, 37.58822246682706947 ) ) ;
#30846=CARTESIAN_POINT ( 'NONE',  ( 0.8560838555295223751, 5.603718208093996012, 46.57221463840868125 ) ) ;
#30850=VERTEX_POINT ( 'NONE', #24803 ) ;
#30863=CARTESIAN_POINT ( 'NONE',  ( 0.9780106845699476636, 14.76917789809602155, 39.21992644906198677 ) ) ;
#30865=B_SPLINE_CURVE_WITH_KNOTS ( 'NONE', 3,
 ( #37766, #38681, #48363, #417, #5423, #56823 ),
 .UNSPECIFIED., .F., .F.,
 ( 4, 2, 4 ),
 ( 6.857096618313869002E-18, 0.0002291472222819941282, 0.0004582944445639813716 ),
 .UNSPECIFIED. ) ;
#30866=AXIS2_PLACEMENT_3D ( 'NONE', #60076, #27487, #51285 ) ;
#30872=CARTESIAN_POINT ( 'NONE',  ( 0.9762797500689124330, -30.73989051779348003, 28.48480149377514437 ) ) ;
#30874=CARTESIAN_POINT ( 'NONE',  ( 0.9790850452238877288, -6.920706823809607222, 41.33329344876927536 ) ) ;
#30876=CARTESIAN_POINT ( 'NONE',  ( 0.9775691876210963471, 29.40491633870845334, -29.86108846146687767 ) ) ;
#30879=ORIENTED_EDGE ( 'NONE', *, *, #46935, .F. ) ;
#30892=ORIENTED_EDGE ( 'NONE', *, *, #41949, .F. ) ;
#30893=ORIENTED_EDGE ( 'NONE', *, *, #51253, .F. ) ;
#30897=AXIS2_PLACEMENT_3D ( 'NONE', #5196, #14954, #53126 ) ;
#30899=FACE_OUTER_BOUND ( 'NONE', #20832, .T. ) ;
#30903=CARTESIAN_POINT ( 'NONE',  ( 5.895596859100789899, 10.82540956478682581, -16.95106754653256331 ) ) ;
#30907=LINE ( 'NONE', #45042, #61936 ) ;
#30908=ORIENTED_EDGE ( 'NONE', *, *, #47782, .T. ) ;
#30910=( BOUNDED_SURFACE ( )  B_SPLINE_SURFACE ( 3, 1, ( 
 ( #58916, #26647 ),
 ( #6898, #26039 ),
 ( #31355, #16967 ),
 ( #54199, #36080 ) ),
 .UNSPECIFIED., .F., .F., .F. ) 
 B_SPLINE_SURFACE_WITH_KNOTS ( ( 4, 4 ),
 ( 2, 2 ),
 ( 0.000000000000000000, 1.000000000000000000 ),
 ( 0.000000000000000000, 1.000000000000000000 ),
 .UNSPECIFIED. ) 
 GEOMETRIC_REPRESENTATION_ITEM ( )  RATIONAL_B_SPLINE_SURFACE ( (
 ( 1.000000000000000000, 1.000000000000000000),
 ( 0.9729067724841187204, 0.9999501103223794596),
 ( 0.9729067724841187204, 0.9999501103223794596),
 ( 1.000000000000000000, 1.000000000000000000) ) ) 
 REPRESENTATION_ITEM ( '' )  SURFACE ( )  );
#30923=EDGE_LOOP ( 'NONE', ( #38034, #4298, #20498, #36712 ) ) ;
#30926=CIRCLE ( 'NONE', #17084, 47.09074272231896430 ) ;
#30932=( BOUNDED_SURFACE ( )  B_SPLINE_SURFACE ( 3, 1, ( 
 ( #33521, #10016 ),
 ( #4346, #57280 ),
 ( #14414, #52598 ),
 ( #56989, #4652 ) ),
 .UNSPECIFIED., .F., .F., .F. ) 
 B_SPLINE_SURFACE_WITH_KNOTS ( ( 4, 4 ),
 ( 2, 2 ),
 ( 0.000000000000000000, 1.000000000000000000 ),
 ( 0.000000000000000000, 1.000000000000000000 ),
 .UNSPECIFIED. ) 
 GEOMETRIC_REPRESENTATION_ITEM ( )  RATIONAL_B_SPLINE_SURFACE ( (
 ( 1.000000000000000000, 1.000000000000000000),
 ( 0.9952954269826590483, 0.8620686068821339365),
 ( 0.9952954269826590483, 0.8620686068821339365),
 ( 1.000000000000000000, 1.000000000000000000) ) ) 
 REPRESENTATION_ITEM ( '' )  SURFACE ( )  );
#30937=( BOUNDED_SURFACE ( )  B_SPLINE_SURFACE ( 3, 1, ( 
 ( #34504, #38291 ),
 ( #10074, #57646 ),
 ( #49202, #5339 ),
 ( #38912, #48586 ) ),
 .UNSPECIFIED., .F., .F., .F. ) 
 B_SPLINE_SURFACE_WITH_KNOTS ( ( 4, 4 ),
 ( 2, 2 ),
 ( 0.000000000000000000, 1.000000000000000000 ),
 ( 0.000000000000000000, 1.000000000000000000 ),
 .UNSPECIFIED. ) 
 GEOMETRIC_REPRESENTATION_ITEM ( )  RATIONAL_B_SPLINE_SURFACE ( (
 ( 1.000000000000000000, 1.000000000000000000),
 ( 0.7282232189291694135, 0.9929344683865672927),
 ( 0.7282232189291694135, 0.9929344683865672927),
 ( 1.000000000000000000, 1.000000000000000000) ) ) 
 REPRESENTATION_ITEM ( '' )  SURFACE ( )  );
#30940=VERTEX_POINT ( 'NONE', #12271 ) ;
#30941=B_SPLINE_CURVE_WITH_KNOTS ( 'NONE', 3,
 ( #31799, #51191, #2963, #17387, #12702, #59979 ),
 .UNSPECIFIED., .F., .F.,
 ( 4, 2, 4 ),
 ( 6.942281208919283290E-18, 0.0002291472222819949955, 0.0004582944445639830521 ),
 .UNSPECIFIED. ) ;
#30945=CARTESIAN_POINT ( 'NONE',  ( 0.5806925824938502512, 27.37593026015236219, -38.07598724570169679 ) ) ;
#30951=CARTESIAN_POINT ( 'NONE',  ( 3.782542959838396168, -40.24477878435767053, 12.14889435276654162 ) ) ;
#30957=CARTESIAN_POINT ( 'NONE',  ( 5.895881250540457863, -2.017740640757076154, -20.01140685496494953 ) ) ;
#30963=CARTESIAN_POINT ( 'NONE',  ( 0.8554163680231738898, -18.91615390926476792, -42.93465493506180053 ) ) ;
#30966=LINE ( 'NONE', #11889, #41246 ) ;
#30969=B_SPLINE_CURVE_WITH_KNOTS ( 'NONE', 3,
 ( #39178, #58231, #25361, #20362 ),
 .UNSPECIFIED., .F., .F.,
 ( 4, 4 ),
 ( 0.000000000000000000, 0.004447772540403827600 ),
 .UNSPECIFIED. ) ;
#30971=EDGE_CURVE ( 'NONE', #8614, #49719, #41703, .T. ) ;
#30972=VECTOR ( 'NONE', #28498, 1000.000000000000000 ) ;
#30975=ADVANCED_FACE ( 'NONE', ( #60155 ), #60623, .F. ) ;
#30982=ADVANCED_FACE ( 'NONE', ( #17571 ), #50289, .T. ) ;
#31001=CARTESIAN_POINT ( 'NONE',  ( 5.896782393890504181, -9.671431223050909409, -17.63489452692610371 ) ) ;
#31019=CARTESIAN_POINT ( 'NONE',  ( 1.231276596079887931, 36.49189576017872128, 20.63051901543724043 ) ) ;
#31021=CARTESIAN_POINT ( 'NONE',  ( 0.9775691876210972353, 40.51774410171000795, -10.70729293044395369 ) ) ;
#31026=( BOUNDED_SURFACE ( )  B_SPLINE_SURFACE ( 3, 1, ( 
 ( #24679, #52869 ),
 ( #48186, #58168 ),
 ( #15292, #14679 ),
 ( #863, #56945 ) ),
 .UNSPECIFIED., .F., .F., .F. ) 
 B_SPLINE_SURFACE_WITH_KNOTS ( ( 4, 4 ),
 ( 2, 2 ),
 ( 0.000000000000000000, 1.000000000000000000 ),
 ( 0.000000000000000000, 1.000000000000000000 ),
 .UNSPECIFIED. ) 
 GEOMETRIC_REPRESENTATION_ITEM ( )  RATIONAL_B_SPLINE_SURFACE ( (
 ( 1.000000000000000000, 1.000000000000000000),
 ( 0.7282232189291694135, 0.9929344683865672927),
 ( 0.7282232189291694135, 0.9929344683865672927),
 ( 1.000000000000000000, 1.000000000000000000) ) ) 
 REPRESENTATION_ITEM ( '' )  SURFACE ( )  );
#31027=ORIENTED_EDGE ( 'NONE', *, *, #31173, .T. ) ;
#31028=CARTESIAN_POINT ( 'NONE',  ( 0.8560838555295223751, 42.82099363437819051, -19.15033519931896322 ) ) ;
#31037=CARTESIAN_POINT ( 'NONE',  ( 0.8560838555295158248, 28.55542365806940452, -37.21505896528851309 ) ) ;
#31042=CARTESIAN_POINT ( 'NONE',  ( 5.895596859100789899, 19.70914391261472076, -4.009716878325650491 ) ) ;
#31043=CARTESIAN_POINT ( 'NONE',  ( 4.962356264823603702, 0.9708976703223142213, -42.07484944210863631 ) ) ;
#31049=CARTESIAN_POINT ( 'NONE',  ( 5.838029081930955932, 46.28366904854783570, 9.427992233631421470 ) ) ;
#31050=CARTESIAN_POINT ( 'NONE',  ( 0.8560838555295223751, 33.26091945577352504, 33.07694168205818386 ) ) ;
#31056=ADVANCED_FACE ( 'NONE', ( #61377 ), #47863, .F. ) ;
#31061=ORIENTED_EDGE ( 'NONE', *, *, #23071, .T. ) ;
#31070=ORIENTED_EDGE ( 'NONE', *, *, #3806, .T. ) ;
#31076=CARTESIAN_POINT ( 'NONE',  ( 0.9754292589017183879, -22.05710651247192899, 35.63441481479315343 ) ) ;
#31082=CARTESIAN_POINT ( 'NONE',  ( 0.5797568599927127586, -14.49376273346966926, 44.59995684411468631 ) ) ;
#31086=VERTEX_POINT ( 'NONE', #27577 ) ;
#31088=CARTESIAN_POINT ( 'NONE',  ( 5.896278296736517710, 5.953715084307535044, 19.21146158701290929 ) ) ;
#31094=CARTESIAN_POINT ( 'NONE',  ( 1.092182651088186018, 41.42847769239433831, -6.359435551451717572 ) ) ;
#31105=CARTESIAN_POINT ( 'NONE',  ( 4.291220156522060236, 35.59851124210567264, -30.85668476442946329 ) ) ;
#31106=B_SPLINE_CURVE_WITH_KNOTS ( 'NONE', 3,
 ( #47521, #4884, #19030, #18403, #18092, #42527 ),
 .UNSPECIFIED., .F., .F.,
 ( 4, 2, 4 ),
 ( 1.159750240187440271E-16, 0.0002448718616795938553, 0.0004897437233590718093 ),
 .UNSPECIFIED. ) ;
#31112=CARTESIAN_POINT ( 'NONE',  ( 0.9789889208857696090, -22.46918319153057553, 35.37613185111973735 ) ) ;
#31115=DIRECTION ( 'NONE',  ( 0.000000000000000000, 0.000000000000000000, 1.000000000000000000 ) ) ;
#31116=CARTESIAN_POINT ( 'NONE',  ( 0.9754292580325131246, -27.49953659056433608, 31.62440440875080583 ) ) ;
#31117=CARTESIAN_POINT ( 'NONE',  ( 0.6064782688330886407, 23.15856706935003473, -40.78008359129716354 ) ) ;
#31119=ORIENTED_EDGE ( 'NONE', *, *, #40120, .F. ) ;
#31120=CARTESIAN_POINT ( 'NONE',  ( 1.231276596079887264, -11.60895935156443848, 40.28037777618019533 ) ) ;
#31122=EDGE_CURVE ( 'NONE', #8559, #20443, #51424, .T. ) ;
#31128=VERTEX_POINT ( 'NONE', #15346 ) ;
#31134=FACE_OUTER_BOUND ( 'NONE', #15266, .T. ) ;
#31140=ORIENTED_EDGE ( 'NONE', *, *, #27382, .F. ) ;
#31142=CARTESIAN_POINT ( 'NONE',  ( 0.6845945791218023269, -20.52768236698738846, -42.17843972166372879 ) ) ;
#31145=CARTESIAN_POINT ( 'NONE',  ( 5.895596859100789899, 14.91436009500259097, -13.49407448360508255 ) ) ;
#31146=CARTESIAN_POINT ( 'NONE',  ( 4.956445790444011124, -11.44166143951963122, -45.67960632101645757 ) ) ;
#31154=CARTESIAN_POINT ( 'NONE',  ( 5.895596859100789899, 14.91436009500259097, -13.49407448360508255 ) ) ;
#31162=ORIENTED_EDGE ( 'NONE', *, *, #16783, .T. ) ;
#31163=DIRECTION ( 'NONE',  ( -1.000000000000000000, -0.000000000000000000, -0.000000000000000000 ) ) ;
#31164=CARTESIAN_POINT ( 'NONE',  ( 1.157644175074336035, 20.86452795889626799, -36.35483115806782450 ) ) ;
#31167=EDGE_CURVE ( 'NONE', #14312, #2143, #53525, .T. ) ;
#31173=EDGE_CURVE ( 'NONE', #47431, #32248, #10327, .T. ) ;
#31183=FACE_OUTER_BOUND ( 'NONE', #45801, .T. ) ;
#31184=CARTESIAN_POINT ( 'NONE',  ( 5.896782393890504181, 5.965008392937153126, -19.20793486427423247 ) ) ;
#31188=EDGE_CURVE ( 'NONE', #58971, #37747, #26041, .T. ) ;
#31192=VERTEX_POINT ( 'NONE', #48843 ) ;
#31194=CARTESIAN_POINT ( 'NONE',  ( 0.5824936645240075261, -8.159118969952315226, 46.18080723281560296 ) ) ;
#31199=FACE_OUTER_BOUND ( 'NONE', #60021, .T. ) ;
#31211=DIRECTION ( 'NONE',  ( -1.000000000000000000, 0.000000000000000000, 0.000000000000000000 ) ) ;
#31212=ORIENTED_EDGE ( 'NONE', *, *, #55652, .T. ) ;
#31213=EDGE_CURVE ( 'NONE', #9908, #26144, #8836, .T. ) ;
#31214=B_SPLINE_CURVE_WITH_KNOTS ( 'NONE', 3,
 ( #41813, #60878, #17998, #56182 ),
 .UNSPECIFIED., .F., .F.,
 ( 4, 4 ),
 ( 3.469446951953614189E-18, 0.004042984057420972825 ),
 .UNSPECIFIED. ) ;
#31215=ORIENTED_EDGE ( 'NONE', *, *, #57759, .F. ) ;
#31227=CARTESIAN_POINT ( 'NONE',  ( 0.8560838555295158248, 46.89922841446242074, 0.9138972643637033322 ) ) ;
#31233=CARTESIAN_POINT ( 'NONE',  ( 5.895881250540457863, -7.224475463583877044, -18.77057899704682953 ) ) ;
#31237=CARTESIAN_POINT ( 'NONE',  ( 4.956445790444006683, -23.10347171912805564, -41.03373788315033721 ) ) ;
#31240=VERTEX_POINT ( 'NONE', #24111 ) ;
#31251=AXIS2_PLACEMENT_3D ( 'NONE', #43046, #52405, #707 ) ;
#31252=CARTESIAN_POINT ( 'NONE',  ( 0.9762797500689124330, 3.691134646837550104, 41.74566217230983511 ) ) ;
#31254=CARTESIAN_POINT ( 'NONE',  ( 0.9775691876210990117, 38.72908157502681803, -16.01224373237266718 ) ) ;
#31260=CARTESIAN_POINT ( 'NONE',  ( 5.838029081930955932, -16.95764376597146850, -44.08518318051234530 ) ) ;
#31263=CARTESIAN_POINT ( 'NONE',  ( 0.5837157313716021534, 36.74748076922353590, 29.13519728262657438 ) ) ;
#31268=CARTESIAN_POINT ( 'NONE',  ( 5.910764540655177868, -2.028561139977089756, 20.00965212517543890 ) ) ;
#31273=ADVANCED_FACE ( 'NONE', ( #55074 ), #5007, .F. ) ;
#31278=DIRECTION ( 'NONE',  ( 0.07500201931887535978, -0.9899952385360587526, 0.1195162113439968143 ) ) ;
#31291=CARTESIAN_POINT ( 'NONE',  ( 0.8554163680231816613, -2.480940174720135172, -46.85136507041474374 ) ) ;
#31292=EDGE_CURVE ( 'NONE', #34772, #40345, #32702, .T. ) ;
#31293=AXIS2_PLACEMENT_3D ( 'NONE', #1906, #39542, #29187 ) ;
#31294=CARTESIAN_POINT ( 'NONE',  ( 4.962356264823608143, 0.000000000000000000, 0.000000000000000000 ) ) ;
#31303=CARTESIAN_POINT ( 'NONE',  ( 1.511324885427794085, -0.4710387770532362128, -46.93530688883296165 ) ) ;
#31304=CARTESIAN_POINT ( 'NONE',  ( 1.231276596079881935, 41.65019306089989470, -4.747440258479600494 ) ) ;
#31307=CARTESIAN_POINT ( 'NONE',  ( 5.901463166500146684, -9.678444301826155893, -17.63081354439112403 ) ) ;
#31320=CARTESIAN_POINT ( 'NONE',  ( 5.910764540655177868, 17.94353875551725253, 9.084638429701733742 ) ) ;
#31323=EDGE_CURVE ( 'NONE', #48040, #37577, #48325, .T. ) ;
#31327=CARTESIAN_POINT ( 'NONE',  ( 0.5824936645240095245, -44.41937930270042756, 15.03851460095492598 ) ) ;
#31330=CARTESIAN_POINT ( 'NONE',  ( 1.000433927950263868, 9.073595347253974097, -40.91562715060270250 ) ) ;
#31344=ORIENTED_EDGE ( 'NONE', *, *, #60835, .T. ) ;
#31345=CARTESIAN_POINT ( 'NONE',  ( 1.092182651088186685, 10.47430941773377455, 40.58386411695983043 ) ) ;
#31350=B_SPLINE_CURVE_WITH_KNOTS ( 'NONE', 3,
 ( #35822, #39288, #58652, #44920 ),
 .UNSPECIFIED., .F., .F.,
 ( 4, 4 ),
 ( 0.000000000000000000, 0.005004948556313813107 ),
 .UNSPECIFIED. ) ;
#31355=CARTESIAN_POINT ( 'NONE',  ( 5.894904586330512508, 5.957793302349664089, -19.21026056637754920 ) ) ;
#31361=CARTESIAN_POINT ( 'NONE',  ( 0.7764139734771251522, -46.13398389262297883, 8.467349118943408470 ) ) ;
#31365=CARTESIAN_POINT ( 'NONE',  ( 4.962356264823608143, -42.08379584346670299, -0.4355746408611892995 ) ) ;
#31366=CARTESIAN_POINT ( 'NONE',  ( 0.9788927965476035276, -41.82430862360842383, -2.657784940308306698 ) ) ;
#31369=EDGE_LOOP ( 'NONE', ( #12152, #17520, #14996, #4068 ) ) ;
#31381=DIRECTION ( 'NONE',  ( 0.000000000000000000, 0.000000000000000000, 1.000000000000000000 ) ) ;
#31384=FACE_OUTER_BOUND ( 'NONE', #50259, .T. ) ;
#31386=LINE ( 'NONE', #37039, #43026 ) ;
#31388=CARTESIAN_POINT ( 'NONE',  ( 2.618530812446111078, 45.68928551531458027, -11.05513357215843229 ) ) ;
#31389=CARTESIAN_POINT ( 'NONE',  ( 4.956445790444018229, -5.251077430595369577, -46.79705371022334504 ) ) ;
#31390=CARTESIAN_POINT ( 'NONE',  ( 0.5817217712918333339, -44.14976367950093561, -15.81244196993600326 ) ) ;
#31393=DIRECTION ( 'NONE',  ( -1.000000000000000000, -0.000000000000000000, -0.000000000000000000 ) ) ;
#31400=VERTEX_POINT ( 'NONE', #22812 ) ;
#31405=CARTESIAN_POINT ( 'NONE',  ( 0.5797568599927133137, -35.19933661194119878, 30.98761060085561070 ) ) ;
#31410=EDGE_CURVE ( 'NONE', #18068, #31400, #55866, .T. ) ;
#31413=CARTESIAN_POINT ( 'NONE',  ( 5.895596859100789899, -19.39920506799832722, 5.310275505304355548 ) ) ;
#31425=CARTESIAN_POINT ( 'NONE',  ( 0.9791128995231607179, -22.54602046135226345, 35.32724721234943388 ) ) ;
#31426=LINE ( 'NONE', #45247, #35495 ) ;
#31433=CARTESIAN_POINT ( 'NONE',  ( 5.895881250540457863, 3.340873024792621937, -19.83346286054237950 ) ) ;
#31438=VECTOR ( 'NONE', #4251, 1000.000000000000227 ) ;
#31443=EDGE_CURVE ( 'NONE', #13518, #48016, #38711, .T. ) ;
#31444=LINE ( 'NONE', #37098, #39591 ) ;
#31446=CARTESIAN_POINT ( 'NONE',  ( 5.838029081930955932, 25.43272996496320815, -39.80252887295205255 ) ) ;
#31463=CARTESIAN_POINT ( 'NONE',  ( 0.5835226383429308328, -13.72009239797509217, 44.84419181050082415 ) ) ;
#31476=ADVANCED_FACE ( 'NONE', ( #10885 ), #22242, .F. ) ;
#31477=CARTESIAN_POINT ( 'NONE',  ( 3.238018933889920792, -6.973938193058539348, 11.43554451904465807 ) ) ;
#31488=CARTESIAN_POINT ( 'NONE',  ( 0.5806925824938499181, -46.75147433417400578, -3.677228565731735621 ) ) ;
#31490=CARTESIAN_POINT ( 'NONE',  ( 4.962356264823596597, 41.32726869310139506, 7.955655864260913646 ) ) ;
#31491=EDGE_CURVE ( 'NONE', #22425, #13149, #53153, .T. ) ;
#31494=CARTESIAN_POINT ( 'NONE',  ( 0.9789233960466696693, -31.16971095351161125, 28.01402944788343063 ) ) ;
#31502=ORIENTED_EDGE ( 'NONE', *, *, #55043, .F. ) ;
#31524=CARTESIAN_POINT ( 'NONE',  ( 3.376099380956838925, 10.22925587767796074, 8.664335394077147257 ) ) ;
#31525=ORIENTED_EDGE ( 'NONE', *, *, #15588, .T. ) ;
#31530=CARTESIAN_POINT ( 'NONE',  ( 4.956445790444004018, -47.08764048036452721, -0.5405220916603282744 ) ) ;
#31534=CARTESIAN_POINT ( 'NONE',  ( 0.5806925824938494740, 45.08220210717442455, -12.91578164539189721 ) ) ;
#31541=CARTESIAN_POINT ( 'NONE',  ( 5.896278296736517710, 8.471169747519471827, 18.24188210473619165 ) ) ;
#31542=ORIENTED_EDGE ( 'NONE', *, *, #56374, .F. ) ;
#31543=CARTESIAN_POINT ( 'NONE',  ( 3.376099380956842921, 0.8831717405837441470, -13.37641175011824046 ) ) ;
#31550=FACE_OUTER_BOUND ( 'NONE', #25279, .T. ) ;
#31552=CARTESIAN_POINT ( 'NONE',  ( 4.962356264823602814, 41.15374796524927348, -8.809348799717806600 ) ) ;
#31553=CARTESIAN_POINT ( 'NONE',  ( 4.956445790444026223, 7.299064093731650438, -46.52162629890785439 ) ) ;
#31554=ORIENTED_EDGE ( 'NONE', *, *, #59686, .F. ) ;
#31569=CONICAL_SURFACE ( 'NONE', #45574, 42.08604991992415023, 1.569615340895231137 ) ;
#31573=EDGE_CURVE ( 'NONE', #39908, #9401, #47562, .T. ) ;
#31577=CARTESIAN_POINT ( 'NONE',  ( 4.956445790444004018, -45.55738122058073003, 11.91902120403828036 ) ) ;
#31586=DIRECTION ( 'NONE',  ( -1.000000000000000000, -0.000000000000000000, -0.000000000000000000 ) ) ;
#31591=ORIENTED_EDGE ( 'NONE', *, *, #14435, .T. ) ;
#31613=DIRECTION ( 'NONE',  ( 0.000000000000000000, 0.000000000000000000, 1.000000000000000000 ) ) ;
#31614=CARTESIAN_POINT ( 'NONE',  ( 0.9754292580325137907, 41.60825679387271236, -5.008036888756832283 ) ) ;
#31621=EDGE_CURVE ( 'NONE', #58203, #48545, #10323, .T. ) ;
#31622=ORIENTED_EDGE ( 'NONE', *, *, #11931, .T. ) ;
#31626=CARTESIAN_POINT ( 'NONE',  ( 0.8560838555295158248, -44.60403252362548443, 14.52078223488980768 ) ) ;
#31633=CARTESIAN_POINT ( 'NONE',  ( 0.5848930533535030563, -46.77916419324618857, 3.314042813373282659 ) ) ;
#31640=CARTESIAN_POINT ( 'NONE',  ( 0.9754292589017213855, 40.26172081468631347, -11.63276854130313431 ) ) ;
#31644=ORIENTED_EDGE ( 'NONE', *, *, #21729, .T. ) ;
#31652=ORIENTED_EDGE ( 'NONE', *, *, #44980, .T. ) ;
#31653=CARTESIAN_POINT ( 'NONE',  ( 0.9762797500689124330, 10.20671408565980975, 40.64662068068264489 ) ) ;
#31655=AXIS2_PLACEMENT_3D ( 'NONE', #12461, #49731, #55034 ) ;
#31660=CARTESIAN_POINT ( 'NONE',  ( 0.9772918015221174759, 29.43140870804984743, 29.83503037052932427 ) ) ;
#31661=CARTESIAN_POINT ( 'NONE',  ( 0.7764146366350225259, 31.96094562988600174, -34.32984748163959665 ) ) ;
#31669=CARTESIAN_POINT ( 'NONE',  ( 4.956445790443995136, 19.33052208089553758, 42.94029536716820417 ) ) ;
#31670=CARTESIAN_POINT ( 'NONE',  ( 5.895881250540457863, -4.666996818433856831, 19.56391633352149739 ) ) ;
#31682=( BOUNDED_SURFACE ( )  B_SPLINE_SURFACE ( 3, 1, ( 
 ( #27386, #12383 ),
 ( #17689, #56193 ),
 ( #13305, #7645 ),
 ( #26773, #45907 ) ),
 .UNSPECIFIED., .F., .F., .F. ) 
 B_SPLINE_SURFACE_WITH_KNOTS ( ( 4, 4 ),
 ( 2, 2 ),
 ( 0.000000000000000000, 1.000000000000000000 ),
 ( 0.000000000000000000, 1.000000000000000000 ),
 .UNSPECIFIED. ) 
 GEOMETRIC_REPRESENTATION_ITEM ( )  RATIONAL_B_SPLINE_SURFACE ( (
 ( 1.000000000000000000, 1.000000000000000000),
 ( 0.9952954269826590483, 0.8620686068821307169),
 ( 0.9952954269826590483, 0.8620686068821307169),
 ( 1.000000000000000000, 1.000000000000000000) ) ) 
 REPRESENTATION_ITEM ( '' )  SURFACE ( )  );
#31684=EDGE_CURVE ( 'NONE', #14, #27845, #22150, .T. ) ;
#31696=CARTESIAN_POINT ( 'NONE',  ( 0.8560838555295158248, -6.899551485031924614, -46.39794201672231111 ) ) ;
#31700=CARTESIAN_POINT ( 'NONE',  ( 5.838029081930957709, 46.28366904854798491, -9.427992233630753560 ) ) ;
#31701=CARTESIAN_POINT ( 'NONE',  ( 5.838029081930957709, -46.81536740852270384, -6.275861100912842439 ) ) ;
#31705=CARTESIAN_POINT ( 'NONE',  ( 0.5837800005270550319, -30.27734249767566155, 35.81225753733249206 ) ) ;
#31707=CARTESIAN_POINT ( 'NONE',  ( 3.376099380956842921, -8.298464850405602888, 10.52824129466312186 ) ) ;
#31709=CARTESIAN_POINT ( 'NONE',  ( 0.8560838555295158248, -30.97734773434503808, 35.22466126774251194 ) ) ;
#31721=ORIENTED_EDGE ( 'NONE', *, *, #1765, .T. ) ;
#31722=CARTESIAN_POINT ( 'NONE',  ( 0.5797568665920713737, 21.98355169411229681, -41.42401191958792595 ) ) ;
#31729=CARTESIAN_POINT ( 'NONE',  ( 0.5830081025819935370, 4.422179700680720416, -46.68700419899666798 ) ) ;
#31732=B_SPLINE_CURVE_WITH_KNOTS ( 'NONE', 3,
 ( #24995, #20599, #20295, #44133 ),
 .UNSPECIFIED., .F., .F.,
 ( 4, 4 ),
 ( 5.051591013050331407E-17, 0.005004948556313863414 ),
 .UNSPECIFIED. ) ;
#31733=DIRECTION ( 'NONE',  ( 0.000000000000000000, 0.000000000000000000, 1.000000000000000000 ) ) ;
#31739=CARTESIAN_POINT ( 'NONE',  ( 0.9790320750461896093, -22.62273297271198658, 35.27816726231058908 ) ) ;
#31745=EDGE_LOOP ( 'NONE', ( #1593, #52938, #47716, #2472 ) ) ;
#31750=AXIS2_PLACEMENT_3D ( 'NONE', #53249, #10667, #29446 ) ;
#31753=EDGE_CURVE ( 'NONE', #29096, #50421, #55747, .T. ) ;
#31754=ORIENTED_EDGE ( 'NONE', *, *, #29520, .T. ) ;
#31756=CARTESIAN_POINT ( 'NONE',  ( 0.9762797500689124330, -39.42083772998312696, -14.22400568939859866 ) ) ;
#31760=B_SPLINE_CURVE_WITH_KNOTS ( 'NONE', 3,
 ( #41183, #46811, #56172, #3233 ),
 .UNSPECIFIED., .F., .F.,
 ( 4, 4 ),
 ( 2.909219710836648185E-18, 0.004042984057420972825 ),
 .UNSPECIFIED. ) ;
#31768=EDGE_CURVE ( 'NONE', #48721, #52874, #9247, .T. ) ;
#31780=CARTESIAN_POINT ( 'NONE',  ( 5.896278296736517710, 14.91306641426042923, -13.49545959714752819 ) ) ;
#31781=CARTESIAN_POINT ( 'NONE',  ( 1.793429038971303680, -0.3977116370890650399, 41.94332992053986686 ) ) ;
#31783=CARTESIAN_POINT ( 'NONE',  ( 0.5835226383429291674, -38.55970297496715204, 26.69066842602997980 ) ) ;
#31787=CARTESIAN_POINT ( 'NONE',  ( 4.956445790444035104, 39.12691469764034480, -26.20348443209818967 ) ) ;
#31793=FACE_OUTER_BOUND ( 'NONE', #19586, .T. ) ;
#31794=AXIS2_PLACEMENT_3D ( 'NONE', #57530, #210, #57220 ) ;
#31796=CARTESIAN_POINT ( 'NONE',  ( 0.9762797500689124330, -12.89881610234921006, -39.87411852747946028 ) ) ;
#31798=CARTESIAN_POINT ( 'NONE',  ( 5.895881250540457863, -15.78174954617524861, 12.46852288244675222 ) ) ;
#31799=CARTESIAN_POINT ( 'NONE',  ( 1.231276596079887931, 40.64579686208652731, 10.25650859035686757 ) ) ;
#31801=DIRECTION ( 'NONE',  ( 0.000000000000000000, 0.000000000000000000, 1.000000000000000000 ) ) ;
#31802=CARTESIAN_POINT ( 'NONE',  ( 5.895596859100789899, -9.662743138698242973, -17.63971593444825103 ) ) ;
#31803=CARTESIAN_POINT ( 'NONE',  ( 0.5806925824938511393, 40.62497527030930655, 23.42720099863236882 ) ) ;
#31804=EDGE_CURVE ( 'NONE', #43662, #4858, #4924, .T. ) ;
#31821=DIRECTION ( 'NONE',  ( -1.000000000000000000, -0.000000000000000000, -0.000000000000000000 ) ) ;
#31837=CARTESIAN_POINT ( 'NONE',  ( 0.9787464366903548818, 25.00166030498751724, -33.63407461019966149 ) ) ;
#31843=ORIENTED_EDGE ( 'NONE', *, *, #13660, .T. ) ;
#31845=CARTESIAN_POINT ( 'NONE',  ( 0.5806925824938494740, 45.08220210717442455, -12.91578164539189721 ) ) ;
#31846=CARTESIAN_POINT ( 'NONE',  ( 0.5848930533535030563, 43.10374212188066423, -18.47540249840228199 ) ) ;
#31848=FACE_OUTER_BOUND ( 'NONE', #12360, .T. ) ;
#31853=ORIENTED_EDGE ( 'NONE', *, *, #46006, .F. ) ;
#31860=CARTESIAN_POINT ( 'NONE',  ( 2.528100132419517365, -28.01580866738180831, -31.26288923539745213 ) ) ;
#31862=VERTEX_POINT ( 'NONE', #53080 ) ;
#31863=CARTESIAN_POINT ( 'NONE',  ( 0.5326698147273822848, 0.000000000000000000, 0.000000000000000000 ) ) ;
#31868=VERTEX_POINT ( 'NONE', #18873 ) ;
#31874=CARTESIAN_POINT ( 'NONE',  ( 1.231276596079887264, -0.5545928549379750550, 41.91621640586514985 ) ) ;
#31875=CARTESIAN_POINT ( 'NONE',  ( 0.5848930533535030563, 43.24595201260119381, 18.14003078584358519 ) ) ;
#31879=CARTESIAN_POINT ( 'NONE',  ( 2.618530812446115519, 46.37964111407213608, -7.658699584659897752 ) ) ;
#31888=CIRCLE ( 'NONE', #59900, 42.08604991992415023 ) ;
#31897=CARTESIAN_POINT ( 'NONE',  ( 0.5835871038041859915, 10.73853903563474255, 45.64995325607297616 ) ) ;
#31900=CARTESIAN_POINT ( 'NONE',  ( 3.782625744892852637, 18.67351185206663544, -37.66348442730344459 ) ) ;
#31901=CARTESIAN_POINT ( 'NONE',  ( 0.9754292580325137907, 9.147692842514130618, 40.89800951834966014 ) ) ;
#31902=B_SPLINE_CURVE_WITH_KNOTS ( 'NONE', 3,
 ( #52198, #4264, #18710, #48743, #5801, #39681, #24951, #1723, #39371, #44087, #34353, #499, #19954, #35280, #25549, #44685, #1416, #15549, #58427 ),
 .UNSPECIFIED., .F., .F.,
 ( 4, 3, 3, 3, 3, 3, 4 ),
 ( 7.807008523764759705E-18, 0.0002732106629380613477, 0.0004098138914053775462, 0.0005464171197651491833, 0.0006830203481512603196, 0.0008196235766963692708, 0.001011968216111142245 ),
 .UNSPECIFIED. ) ;
#31903=FACE_OUTER_BOUND ( 'NONE', #33246, .T. ) ;
#31905=FACE_OUTER_BOUND ( 'NONE', #37732, .T. ) ;
#31915=ADVANCED_FACE ( 'NONE', ( #36752 ), #52049, .F. ) ;
#31928=CARTESIAN_POINT ( 'NONE',  ( 3.376099380956842921, -11.30600709870807208, -7.202956831470656240 ) ) ;
#31929=CARTESIAN_POINT ( 'NONE',  ( 3.376099380956842921, 10.79965495504287887, 7.942029745857468903 ) ) ;
#31932=CARTESIAN_POINT ( 'NONE',  ( 0.9762797500689124330, -27.44172181261435739, 31.67454323498272117 ) ) ;
#31935=FACE_OUTER_BOUND ( 'NONE', #25323, .T. ) ;
#31937=VERTEX_POINT ( 'NONE', #14176 ) ;
#31941=CARTESIAN_POINT ( 'NONE',  ( 0.8560838555295158248, 39.88643293834648063, 24.68694597426990001 ) ) ;
#31945=EDGE_LOOP ( 'NONE', ( #10212, #43967, #48458, #2561 ) ) ;
#31947=CARTESIAN_POINT ( 'NONE',  ( 0.9787284016396619046, -17.47079291802099377, 38.09340354634191783 ) ) ;
#31948=CARTESIAN_POINT ( 'NONE',  ( 0.5804410086790514622, -46.75463715370018036, 3.677466040799790559 ) ) ;
#31949=B_SPLINE_CURVE_WITH_KNOTS ( 'NONE', 3,
 ( #17941, #23245, #46148, #22628, #13237, #13865, #47071, #60821, #55818, #18544, #37673, #32037, #61735, #19710, #38836, #12631, #50813, #37058, #56122 ),
 .UNSPECIFIED., .F., .F.,
 ( 4, 3, 3, 3, 3, 3, 4 ),
 ( 8.240649770922408386E-18, 0.0002732106629380604804, 0.0004098138914053759199, 0.0005464171197651462560, 0.0006830203481512570670, 0.0008196235766963637414, 0.001011968216111141811 ),
 .UNSPECIFIED. ) ;
#31955=CARTESIAN_POINT ( 'NONE',  ( 1.157644175074338255, 40.20129498541808744, 11.86836791536983426 ) ) ;
#31959=CARTESIAN_POINT ( 'NONE',  ( 1.092182651088184686, 8.955214945688501516, -40.94588269556293625 ) ) ;
#31960=ORIENTED_EDGE ( 'NONE', *, *, #57434, .T. ) ;
#31977=CARTESIAN_POINT ( 'NONE',  ( 0.5804410086790514622, -46.06497594411302998, -8.805557513507348943 ) ) ;
#31981=CARTESIAN_POINT ( 'NONE',  ( 0.5806925824938502512, 37.13995815321093374, 28.63295078613632683 ) ) ;
#31982=ADVANCED_FACE ( 'NONE', ( #28247 ), #53856, .F. ) ;
#31984=DIRECTION ( 'NONE',  ( -0.07906939808003032866, 0.9145849808368812228, -0.3965883799544098753 ) ) ;
#31985=ORIENTED_EDGE ( 'NONE', *, *, #48783, .F. ) ;
#31991=EDGE_CURVE ( 'NONE', #6142, #55166, #12513, .T. ) ;
#31994=B_SPLINE_CURVE_WITH_KNOTS ( 'NONE', 3,
 ( #27239, #3405, #12855, #55110, #61047, #3712 ),
 .UNSPECIFIED., .F., .F.,
 ( 4, 2, 4 ),
 ( 5.898697549827395015E-18, 0.0002291472222819930982, 0.0004582944445639802874 ),
 .UNSPECIFIED. ) ;
#32000=CARTESIAN_POINT ( 'NONE',  ( 4.291220156522059348, 44.16776250362676848, -16.38895215469610989 ) ) ;
#32019=ORIENTED_EDGE ( 'NONE', *, *, #4685, .T. ) ;
#32024=CARTESIAN_POINT ( 'NONE',  ( 0.5797568665920713737, -25.76189042052133615, -39.18609843506905577 ) ) ;
#32030=CARTESIAN_POINT ( 'NONE',  ( 0.5835226383429256147, -1.749062421197752570, -46.86345329990871278 ) ) ;
#32037=CARTESIAN_POINT ( 'NONE',  ( 0.9789233960466703355, -41.82366163528425318, 2.667968187515405543 ) ) ;
#32041=B_SPLINE_CURVE_WITH_KNOTS ( 'NONE', 3,
 ( #36292, #44772, #17176, #54425, #35369, #7751, #59445, #11237, #21252, #40383, #40087, #26874, #35990, #2115, #11877, #46014 ),
 .UNSPECIFIED., .F., .F.,
 ( 4, 3, 3, 3, 3, 4 ),
 ( 8.674294979774126656E-18, 0.0002732102107931834944, 0.0004098135523333795282, 0.0005464168938825003348, 0.0008195847345945455036, 0.001092771384553109602 ),
 .UNSPECIFIED. ) ;
#32045=CARTESIAN_POINT ( 'NONE',  ( 0.5806925824938502512, 4.150136846023314341, -46.71186922509998141 ) ) ;
#32046=CARTESIAN_POINT ( 'NONE',  ( 1.091591847532195958, -13.16112942808253017, 39.79376412370536542 ) ) ;
#32050=CARTESIAN_POINT ( 'NONE',  ( 0.9772918015221172539, 33.14542697680284533, 25.64600409958848815 ) ) ;
#32052=FACE_OUTER_BOUND ( 'NONE', #8253, .T. ) ;
#32058=CARTESIAN_POINT ( 'NONE',  ( 0.7764139734771232648, -13.04263755106484624, -45.05474532852694125 ) ) ;
#32059=CIRCLE ( 'NONE', #52063, 8.000000000000000000 ) ;
#32061=CARTESIAN_POINT ( 'NONE',  ( 0.9762797500689124330, 25.26481495167912783, -33.43671500974812716 ) ) ;
#32064=CARTESIAN_POINT ( 'NONE',  ( 0.6845945791218034371, 43.51705215793874260, -17.51207275559303511 ) ) ;
#32072=B_SPLINE_CURVE_WITH_KNOTS ( 'NONE', 3,
 ( #25527, #12615, #37046, #12303, #56109, #27615 ),
 .UNSPECIFIED., .F., .F.,
 ( 4, 2, 4 ),
 ( 9.929776742050823831E-18, 0.0002448709889506581324, 0.0004897419779013063986 ),
 .UNSPECIFIED. ) ;
#32073=EDGE_CURVE ( 'NONE', #46288, #36503, #54179, .T. ) ;
#32083=CARTESIAN_POINT ( 'NONE',  ( 3.661921753702005677, -41.09997312006429127, 22.87844691765657146 ) ) ;
#32084=EDGE_CURVE ( 'NONE', #38640, #16773, #57173, .T. ) ;
#32093=CARTESIAN_POINT ( 'NONE',  ( 0.5824936645240071931, -38.86801570395647332, 26.23957953697626877 ) ) ;
#32110=CARTESIAN_POINT ( 'NONE',  ( 1.091591847532201509, -23.20683314692016452, 34.90274897836625456 ) ) ;
#32116=ADVANCED_FACE ( 'NONE', ( #36510 ), #26619, .F. ) ;
#32119=CARTESIAN_POINT ( 'NONE',  ( 0.8560838555295223751, -8.701885300215751684, -46.09392613244852299 ) ) ;
#32120=ORIENTED_EDGE ( 'NONE', *, *, #10691, .T. ) ;
#32126=FACE_OUTER_BOUND ( 'NONE', #42274, .T. ) ;
#32136=B_SPLINE_CURVE_WITH_KNOTS ( 'NONE', 3,
 ( #25781, #45231, #21084, #49899 ),
 .UNSPECIFIED., .F., .F.,
 ( 4, 4 ),
 ( 1.551583845779545699E-17, 0.005004948556313820913 ),
 .UNSPECIFIED. ) ;
#32147=DIRECTION ( 'NONE',  ( -0.07906939808003032866, 0.2232318573464505962, -0.9715531730960047518 ) ) ;
#32149=CARTESIAN_POINT ( 'NONE',  ( 4.962356264823608143, 0.000000000000000000, 0.000000000000000000 ) ) ;
#32162=CARTESIAN_POINT ( 'NONE',  ( 5.910764540655177868, -9.679148173057056326, 17.62995544841702866 ) ) ;
#32165=ORIENTED_EDGE ( 'NONE', *, *, #35754, .F. ) ;
#32167=CARTESIAN_POINT ( 'NONE',  ( 0.5804410086790514622, 36.46521478791949278, -29.49250688439851231 ) ) ;
#32171=CARTESIAN_POINT ( 'NONE',  ( 1.000433927950263646, -39.80191350348199109, -13.12350407148118059 ) ) ;
#32172=VERTEX_POINT ( 'NONE', #28024 ) ;
#32174=CARTESIAN_POINT ( 'NONE',  ( 0.9791128995231609400, 24.86348713967445789, 33.73639639175184612 ) ) ;
#32180=CARTESIAN_POINT ( 'NONE',  ( 1.231276596079881047, 29.74482033789362134, -29.53849072116746655 ) ) ;
#32186=CARTESIAN_POINT ( 'NONE',  ( 0.8554163680231816613, 46.36773742900852113, -7.158100224664470268 ) ) ;
#32198=CARTESIAN_POINT ( 'NONE',  ( 4.962356264823609031, 31.50371261889155150, -27.90612278853226513 ) ) ;
#32206=VECTOR ( 'NONE', #45330, 1000.000000000000000 ) ;
#32208=CARTESIAN_POINT ( 'NONE',  ( 1.157644175074335591, 19.41637191003240659, 37.14844246170341791 ) ) ;
#32210=CARTESIAN_POINT ( 'NONE',  ( 4.962356264823609031, -32.75738977283769771, -26.42326651140497873 ) ) ;
#32216=CARTESIAN_POINT ( 'NONE',  ( 5.894904586330512508, -17.30455939762460460, -10.25093342655803497 ) ) ;
#32226=ORIENTED_EDGE ( 'NONE', *, *, #35305, .T. ) ;
#32231=CARTESIAN_POINT ( 'NONE',  ( 0.8560838555295158248, 37.37287335782446718, -28.34856559090329142 ) ) ;
#32232=ORIENTED_EDGE ( 'NONE', *, *, #3793, .T. ) ;
#32238=ORIENTED_EDGE ( 'NONE', *, *, #35595, .T. ) ;
#32239=CARTESIAN_POINT ( 'NONE',  ( 0.5835226383429293895, -7.979743399672678095, -46.21218637785216288 ) ) ;
#32240=CARTESIAN_POINT ( 'NONE',  ( 0.5782707292762423457, -30.83005644796779521, -35.34464560754199880 ) ) ;
#32244=ORIENTED_EDGE ( 'NONE', *, *, #34215, .F. ) ;
#32245=CARTESIAN_POINT ( 'NONE',  ( 2.282803330402964015, -43.92595983154121342, -16.64352607877350465 ) ) ;
#32248=VERTEX_POINT ( 'NONE', #20708 ) ;
#32251=DIRECTION ( 'NONE',  ( -1.000000000000000000, -0.000000000000000000, -0.000000000000000000 ) ) ;
#32257=CARTESIAN_POINT ( 'NONE',  ( 5.901463166500145796, 17.94437285245830793, 9.083906278281064672 ) ) ;
#32264=DIRECTION ( 'NONE',  ( 0.000000000000000000, 0.000000000000000000, 1.000000000000000000 ) ) ;
#32265=LINE ( 'NONE', #55427, #41764 ) ;
#32267=ORIENTED_EDGE ( 'NONE', *, *, #30101, .F. ) ;
#32287=CARTESIAN_POINT ( 'NONE',  ( 5.895596859100789899, -7.225383168025214076, 18.77024297359267990 ) ) ;
#32288=ORIENTED_EDGE ( 'NONE', *, *, #3757, .F. ) ;
#32295=CARTESIAN_POINT ( 'NONE',  ( 0.9762797500689124330, -41.84568905980455611, -2.294143041716810050 ) ) ;
#32299=B_SPLINE_CURVE_WITH_KNOTS ( 'NONE', 3,
 ( #45137, #30689, #40142, #6865 ),
 .UNSPECIFIED., .F., .F.,
 ( 4, 4 ),
 ( 0.000000000000000000, 0.005004948556313807036 ),
 .UNSPECIFIED. ) ;
#32305=ORIENTED_EDGE ( 'NONE', *, *, #31188, .F. ) ;
#32311=CARTESIAN_POINT ( 'NONE',  ( 0.5782707292762442330, -14.58551739541110948, 44.57576736317366084 ) ) ;
#32313=ORIENTED_EDGE ( 'NONE', *, *, #31323, .F. ) ;
#32314=CARTESIAN_POINT ( 'NONE',  ( 4.958415959904820092, 45.35203410338238683, -2.529220533737273957 ) ) ;
#32318=ORIENTED_EDGE ( 'NONE', *, *, #18176, .T. ) ;
#32322=CARTESIAN_POINT ( 'NONE',  ( 0.5806925824938499181, 46.89268439822727430, -0.5463627657667492477 ) ) ;
#32329=DIRECTION ( 'NONE',  ( 0.000000000000000000, 0.000000000000000000, 1.000000000000000000 ) ) ;
#32333=ORIENTED_EDGE ( 'NONE', *, *, #36817, .T. ) ;
#32339=ORIENTED_EDGE ( 'NONE', *, *, #61435, .F. ) ;
#32353=CARTESIAN_POINT ( 'NONE',  ( 4.962356264823608143, 0.000000000000000000, 0.000000000000000000 ) ) ;
#32354=CARTESIAN_POINT ( 'NONE',  ( 0.9791128995231609400, 32.89306773298482511, 25.96889542047248511 ) ) ;
#32358=CARTESIAN_POINT ( 'NONE',  ( 2.528190830796654076, 38.15965687918174609, 17.49556295224946822 ) ) ;
#32362=CARTESIAN_POINT ( 'NONE',  ( 0.5817217712918328898, 45.34790564380423916, -11.94999613928816196 ) ) ;
#32375=UNCERTAINTY_MEASURE_WITH_UNIT (LENGTH_MEASURE( 1.000000000000000082E-05 ), #25774, 'distance_accuracy_value', 'NONE');
#32381=B_SPLINE_CURVE_WITH_KNOTS ( 'NONE', 3,
 ( #16633, #12255, #31345, #7513, #55441, #31653 ),
 .UNSPECIFIED., .F., .F.,
 ( 4, 2, 4 ),
 ( 6.732537572691846445E-18, 0.0002291472222819932608, 0.0004582944445639797995 ),
 .UNSPECIFIED. ) ;
#32402=CARTESIAN_POINT ( 'NONE',  ( 4.958415959904820980, -22.27126879049791341, 39.58780797523441208 ) ) ;
#32404=VERTEX_POINT ( 'NONE', #37920 ) ;
#32405=FACE_OUTER_BOUND ( 'NONE', #48812, .T. ) ;
#32406=CARTESIAN_POINT ( 'NONE',  ( 1.231276596079881047, 32.36747132271556637, 26.63876069172986405 ) ) ;
#32417=B_SPLINE_CURVE_WITH_KNOTS ( 'NONE', 3,
 ( #10655, #24123, #29742, #14436, #43261, #15976 ),
 .UNSPECIFIED., .F., .F.,
 ( 4, 2, 4 ),
 ( 3.471140604459641645E-18, 0.0002291459268755744903, 0.0004582918537511455111 ),
 .UNSPECIFIED. ) ;
#32419=CARTESIAN_POINT ( 'NONE',  ( 5.894904586330512508, 12.98639672351335328, -15.35848013968714199 ) ) ;
#32426=CARTESIAN_POINT ( 'NONE',  ( 0.9769922540276041456, 41.90628016062868255, 0.4418576524454907450 ) ) ;
#32427=CARTESIAN_POINT ( 'NONE',  ( 5.895881250540457863, -4.666996818433588601, -19.56391633352155779 ) ) ;
#32436=CARTESIAN_POINT ( 'NONE',  ( 0.5834584762367766020, -25.38722266164445429, 39.43000018439352061 ) ) ;
#32437=CARTESIAN_POINT ( 'NONE',  ( 2.618530812446115519, -39.53489722556178521, -25.43066437516854705 ) ) ;
#32438=CARTESIAN_POINT ( 'NONE',  ( 4.956445790444026223, 2.113652668516905031, -47.04328350079857302 ) ) ;
#32446=CARTESIAN_POINT ( 'NONE',  ( 0.5837157313716030416, 22.45749545691984750, 41.16913845812719330 ) ) ;
#32453=CARTESIAN_POINT ( 'NONE',  ( 0.5817217712918327788, 46.89379117910313255, 0.4553052372231276568 ) ) ;
#32456=EDGE_CURVE ( 'NONE', #38817, #48578, #53409, .T. ) ;
#32459=CARTESIAN_POINT ( 'NONE',  ( 5.901463166500146684, 5.972693816097455866, 19.20533256467557237 ) ) ;
#32464=DIRECTION ( 'NONE',  ( 0.07906939808003035641, -0.5848023231963108692, -0.8073129957280876789 ) ) ;
#32469=CARTESIAN_POINT ( 'NONE',  ( 0.7056759521544981872, 46.36311911575824496, 7.085902551898405122 ) ) ;
#32480=VERTEX_POINT ( 'NONE', #25026 ) ;
#32484=CARTESIAN_POINT ( 'NONE',  ( 3.661933894777862797, 46.33057283091471845, 8.130755568270412681 ) ) ;
#32487=CARTESIAN_POINT ( 'NONE',  ( 2.528190830796656741, 33.68156755522954882, -25.05606000901808983 ) ) ;
#32489=CARTESIAN_POINT ( 'NONE',  ( 0.5806925824938499181, -42.09901922557445175, 20.66143612114793626 ) ) ;
#32490=ADVANCED_BREP_SHAPE_REPRESENTATION ( '', ( #52453, #14677 ), #18740 ) ;
#32493=( BOUNDED_SURFACE ( )  B_SPLINE_SURFACE ( 3, 1, ( 
 ( #53129, #1125 ),
 ( #506, #19647 ),
 ( #10236, #188 ),
 ( #57822, #20264 ) ),
 .UNSPECIFIED., .F., .F., .F. ) 
 B_SPLINE_SURFACE_WITH_KNOTS ( ( 4, 4 ),
 ( 2, 2 ),
 ( 0.000000000000000000, 1.000000000000000000 ),
 ( 0.000000000000000000, 1.000000000000000000 ),
 .UNSPECIFIED. ) 
 GEOMETRIC_REPRESENTATION_ITEM ( )  RATIONAL_B_SPLINE_SURFACE ( (
 ( 1.000000000000000000, 1.000000000000000000),
 ( 0.9952954269826590483, 0.8620686068821339365),
 ( 0.9952954269826590483, 0.8620686068821339365),
 ( 1.000000000000000000, 1.000000000000000000) ) ) 
 REPRESENTATION_ITEM ( '' )  SURFACE ( )  );
#32499=CARTESIAN_POINT ( 'NONE',  ( 0.5797568599927134247, 36.41064399614844405, 29.55486952190357997 ) ) ;
#32500=ORIENTED_EDGE ( 'NONE', *, *, #49508, .T. ) ;
#32513=CARTESIAN_POINT ( 'NONE',  ( 4.956445790444004906, -46.59545590650544966, 6.811867512257108181 ) ) ;
#32517=VECTOR ( 'NONE', #55654, 1000.000000000000000 ) ;
#32518=FACE_OUTER_BOUND ( 'NONE', #49792, .T. ) ;
#32521=CARTESIAN_POINT ( 'NONE',  ( 0.8554163680231708922, -41.45413358837855355, -21.97180651536612928 ) ) ;
#32526=CARTESIAN_POINT ( 'NONE',  ( 0.5837799406558231707, 46.48971530503088445, 6.160350674627294687 ) ) ;
#32532=CARTESIAN_POINT ( 'NONE',  ( 0.6845945791218023269, -25.96635969083004980, -39.06602981005851660 ) ) ;
#32533=VERTEX_POINT ( 'NONE', #19108 ) ;
#32551=ORIENTED_EDGE ( 'NONE', *, *, #15155, .F. ) ;
#32554=ORIENTED_EDGE ( 'NONE', *, *, #37865, .T. ) ;
#32555=CARTESIAN_POINT ( 'NONE',  ( 0.9762797500689124330, -6.471194619075235188, -41.40589843715211771 ) ) ;
#32557=CARTESIAN_POINT ( 'NONE',  ( 0.8560838555295223751, -39.18289055412714106, -25.78902716088815694 ) ) ;
#32582=CARTESIAN_POINT ( 'NONE',  ( 0.9762797500689124330, -17.18051571332144434, 38.22505284509125545 ) ) ;
#32587=EDGE_CURVE ( 'NONE', #26593, #3829, #60329, .T. ) ;
#32591=CARTESIAN_POINT ( 'NONE',  ( 0.5782707292762423457, -7.086273146448189841, 46.36292793387347899 ) ) ;
#32593=CARTESIAN_POINT ( 'NONE',  ( 0.9790724872846768845, 29.10550071523391225, 30.15302701383349060 ) ) ;
#32594=CARTESIAN_POINT ( 'NONE',  ( 0.5806925824938499181, -14.41498975133639426, 44.62544602368059543 ) ) ;
#32596=CARTESIAN_POINT ( 'NONE',  ( 0.5832655196449149093, 22.73672770770176399, -41.01556285264354784 ) ) ;
#32597=CARTESIAN_POINT ( 'NONE',  ( 2.618530812446111078, 31.65223561859532708, 34.75432015653772311 ) ) ;
#32603=CARTESIAN_POINT ( 'NONE',  ( 0.8560838555295223751, 42.82099363437819051, -19.15033519931896322 ) ) ;
#32605=CARTESIAN_POINT ( 'NONE',  ( 0.6845945791218023269, -45.78817307429886796, 10.19066863517794985 ) ) ;
#32606=CIRCLE ( 'NONE', #16597, 42.08604991992415023 ) ;
#32607=CARTESIAN_POINT ( 'NONE',  ( 1.231276596079887264, 35.62927148397050559, -22.08691432816256395 ) ) ;
#32609=ORIENTED_EDGE ( 'NONE', *, *, #49449, .T. ) ;
#32613=CARTESIAN_POINT ( 'NONE',  ( 2.528190830796658517, 25.86513783113687737, -33.06431280291939601 ) ) ;
#32617=VERTEX_POINT ( 'NONE', #30630 ) ;
#32620=CARTESIAN_POINT ( 'NONE',  ( 0.5804410086790514622, -20.23572001627617922, 42.30881098870867874 ) ) ;
#32623=CARTESIAN_POINT ( 'NONE',  ( 0.8554163680231708922, -14.77070554666881286, 44.53124443315531522 ) ) ;
#32625=CARTESIAN_POINT ( 'NONE',  ( 0.5848930533535030563, 45.27791896734265720, 12.21405487028406966 ) ) ;
#32631=CARTESIAN_POINT ( 'NONE',  ( 0.5804410086790514622, 22.05813747677496295, -41.38790189066234859 ) ) ;
#32632=CARTESIAN_POINT ( 'NONE',  ( 0.5830081025819929819, -44.39003745708693316, -15.12470194551506886 ) ) ;
#32633=CARTESIAN_POINT ( 'NONE',  ( 0.5806925824938502512, 17.36345040154772690, 43.56297685531322372 ) ) ;
#32642=CARTESIAN_POINT ( 'NONE',  ( 0.5824936645240081923, 11.22543641052009811, -45.53271083994098234 ) ) ;
#32644=CARTESIAN_POINT ( 'NONE',  ( 0.9787284016396619046, -34.65686640017599274, -23.56348043581808227 ) ) ;
#32655=B_SPLINE_CURVE_WITH_KNOTS ( 'NONE', 3,
 ( #61125, #47667, #55817, #57044 ),
 .UNSPECIFIED., .F., .F.,
 ( 4, 4 ),
 ( 0.000000000000000000, 0.005004948556313801832 ),
 .UNSPECIFIED. ) ;
#32660=CARTESIAN_POINT ( 'NONE',  ( 1.000110580585051867, -13.04367042783479391, 39.82813257663394069 ) ) ;
#32661=CIRCLE ( 'NONE', #25669, 47.09074272231896430 ) ;
#32663=CARTESIAN_POINT ( 'NONE',  ( 3.661921753702002569, -33.59527669226428515, 32.92398074055204660 ) ) ;
#32665=EDGE_CURVE ( 'NONE', #47413, #42220, #27248, .T. ) ;
#32672=DIRECTION ( 'NONE',  ( -1.000000000000000000, -0.000000000000000000, -0.000000000000000000 ) ) ;
#32678=FACE_OUTER_BOUND ( 'NONE', #10121, .T. ) ;
#32679=ORIENTED_EDGE ( 'NONE', *, *, #39411, .T. ) ;
#32683=( BOUNDED_SURFACE ( )  B_SPLINE_SURFACE ( 3, 1, ( 
 ( #39394, #15573 ),
 ( #34679, #10877 ),
 ( #58754, #7683 ),
 ( #55603, #26812 ) ),
 .UNSPECIFIED., .F., .F., .F. ) 
 B_SPLINE_SURFACE_WITH_KNOTS ( ( 4, 4 ),
 ( 2, 2 ),
 ( 0.000000000000000000, 1.000000000000000000 ),
 ( 0.000000000000000000, 1.000000000000000000 ),
 .UNSPECIFIED. ) 
 GEOMETRIC_REPRESENTATION_ITEM ( )  RATIONAL_B_SPLINE_SURFACE ( (
 ( 1.000000000000000000, 1.000000000000000000),
 ( 0.9729067724841187204, 0.9999501103223794596),
 ( 0.9729067724841187204, 0.9999501103223794596),
 ( 1.000000000000000000, 1.000000000000000000) ) ) 
 REPRESENTATION_ITEM ( '' )  SURFACE ( )  );
#32685=VERTEX_POINT ( 'NONE', #21870 ) ;
#32696=CARTESIAN_POINT ( 'NONE',  ( 4.962356264823593044, 27.50309822711036034, 31.85616401534038644 ) ) ;
#32702=B_SPLINE_CURVE_WITH_KNOTS ( 'NONE', 3,
 ( #36618, #40105, #50383, #55682 ),
 .UNSPECIFIED., .F., .F.,
 ( 4, 4 ),
 ( 1.951563910473907981E-18, 0.004446298630425045938 ),
 .UNSPECIFIED. ) ;
#32708=CARTESIAN_POINT ( 'NONE',  ( 0.5806925824938499181, -8.338382001838064994, 46.14860504863594315 ) ) ;
#32711=CARTESIAN_POINT ( 'NONE',  ( 0.5837800005270558090, -38.66299731356561864, 26.54068381509792474 ) ) ;
#32712=FACE_OUTER_BOUND ( 'NONE', #50804, .T. ) ;
#32715=CARTESIAN_POINT ( 'NONE',  ( 4.962356264823608143, -38.91448554252697534, 16.02805081171152324 ) ) ;
#32717=CARTESIAN_POINT ( 'NONE',  ( 5.896278296736517710, -18.51903684540615913, -7.846798960905831066 ) ) ;
#32721=CARTESIAN_POINT ( 'NONE',  ( 4.956445790443996913, 8.365049606151725214, 46.34181691762049127 ) ) ;
#32724=VERTEX_POINT ( 'NONE', #16551 ) ;
#32728=B_SPLINE_CURVE_WITH_KNOTS ( 'NONE', 3,
 ( #37833, #56269, #47207, #22771 ),
 .UNSPECIFIED., .F., .F.,
 ( 4, 4 ),
 ( 0.000000000000000000, 0.004041751736740986471 ),
 .UNSPECIFIED. ) ;
#32739=ORIENTED_EDGE ( 'NONE', *, *, #42614, .F. ) ;
#32740=MECHANICAL_DESIGN_GEOMETRIC_PRESENTATION_REPRESENTATION('',(#43761),#39781);
#32747=CARTESIAN_POINT ( 'NONE',  ( 4.962356264823608143, 0.000000000000000000, 0.000000000000000000 ) ) ;
#32750=CARTESIAN_POINT ( 'NONE',  ( 5.917102823773431552, 16.57624106732469826, 11.38937882984319039 ) ) ;
#32751=EDGE_CURVE ( 'NONE', #11571, #41967, #9255, .T. ) ;
#32756=B_SPLINE_CURVE_WITH_KNOTS ( 'NONE', 3,
 ( #61268, #33111, #51878, #18387, #56264, #56578, #28387, #57178, #14311, #4870, #57479, #13693, #23387, #42513, #8976, #28085 ),
 .UNSPECIFIED., .F., .F.,
 ( 4, 3, 3, 3, 3, 4 ),
 ( 3.469446951953614189E-18, 0.0002732102107931881022, 0.0004098135523333745409, 0.0005464168938824928538, 0.0008195847345945353121, 0.001092771384553107650 ),
 .UNSPECIFIED. ) ;
#32766=EDGE_LOOP ( 'NONE', ( #61419, #20072, #51049, #56848 ) ) ;
#32772=CARTESIAN_POINT ( 'NONE',  ( 4.956445790443988031, 0.000000000000000000, 0.000000000000000000 ) ) ;
#32773=CARTESIAN_POINT ( 'NONE',  ( 0.9772918015221172539, 32.63115054127247561, -26.29724073174774546 ) ) ;
#32776=CARTESIAN_POINT ( 'NONE',  ( 0.8560838555295158248, 42.82099363437792050, 19.15033519931955297 ) ) ;
#32786=CARTESIAN_POINT ( 'NONE',  ( 0.9790320750461911636, -37.36543188631139856, -18.97792487316815979 ) ) ;
#32793=CARTESIAN_POINT ( 'NONE',  ( 0.9762797500689124330, -31.41867615533404390, 27.73430319715907544 ) ) ;
#32794=CARTESIAN_POINT ( 'NONE',  ( 0.8560838555295223751, 3.785103201470721768, -46.75516899590834186 ) ) ;
#32797=( BOUNDED_SURFACE ( )  B_SPLINE_SURFACE ( 3, 1, ( 
 ( #57775, #14909 ),
 ( #20217, #16428 ),
 ( #54612, #21126 ),
 ( #11744, #40268 ) ),
 .UNSPECIFIED., .F., .F., .F. ) 
 B_SPLINE_SURFACE_WITH_KNOTS ( ( 4, 4 ),
 ( 2, 2 ),
 ( 0.000000000000000000, 1.000000000000000000 ),
 ( 0.000000000000000000, 1.000000000000000000 ),
 .UNSPECIFIED. ) 
 GEOMETRIC_REPRESENTATION_ITEM ( )  RATIONAL_B_SPLINE_SURFACE ( (
 ( 1.000000000000000000, 1.000000000000000000),
 ( 0.7282232189291694135, 0.9929344683865672927),
 ( 0.7282232189291694135, 0.9929344683865672927),
 ( 1.000000000000000000, 1.000000000000000000) ) ) 
 REPRESENTATION_ITEM ( '' )  SURFACE ( )  );
#32808=CARTESIAN_POINT ( 'NONE',  ( 1.092182651088184464, -41.86503207152927786, -2.019968834440684979 ) ) ;
#32810=VERTEX_POINT ( 'NONE', #8069 ) ;
#32822=LINE ( 'NONE', #28720, #42956 ) ;
#32823=CARTESIAN_POINT ( 'NONE',  ( 0.9775691876210987896, -27.34475084661038835, 31.75843683380510996 ) ) ;
#32825=CARTESIAN_POINT ( 'NONE',  ( 0.5804410086790514622, 40.62771722849996081, -23.42879520283628025 ) ) ;
#32828=FACE_OUTER_BOUND ( 'NONE', #4293, .T. ) ;
#32835=EDGE_CURVE ( 'NONE', #51034, #5328, #17484, .T. ) ;
#32837=CARTESIAN_POINT ( 'NONE',  ( 0.5837800005270555870, 32.60177022003745861, 33.70993677184314663 ) ) ;
#32839=ORIENTED_EDGE ( 'NONE', *, *, #37410, .F. ) ;
#32850=VECTOR ( 'NONE', #15541, 1000.000000000000114 ) ;
#32853=ORIENTED_EDGE ( 'NONE', *, *, #22963, .T. ) ;
#32860=VERTEX_POINT ( 'NONE', #48747 ) ;
#32870=CARTESIAN_POINT ( 'NONE',  ( 0.9783242366443547500, -6.706126116610328758, -41.36861567317236421 ) ) ;
#32874=ADVANCED_FACE ( 'NONE', ( #9297 ), #55882, .F. ) ;
#32875=ORIENTED_EDGE ( 'NONE', *, *, #50279, .T. ) ;
#32885=CARTESIAN_POINT ( 'NONE',  ( 0.5804410086790514622, 45.08525424748445687, -12.91664435118818410 ) ) ;
#32892=LINE ( 'NONE', #8428, #51953 ) ;
#32894=ORIENTED_EDGE ( 'NONE', *, *, #42468, .T. ) ;
#32898=CARTESIAN_POINT ( 'NONE',  ( 0.9762797500689124330, 10.20671408566037286, -40.64662068068250278 ) ) ;
#32910=CARTESIAN_POINT ( 'NONE',  ( 0.9788927965476033055, 29.23628500401661157, 30.02625937068571815 ) ) ;
#32914=EDGE_CURVE ( 'NONE', #3462, #40188, #34688, .T. ) ;
#32924=CARTESIAN_POINT ( 'NONE',  ( 0.5782707292762423457, -45.81184706829309761, 10.05042396612924982 ) ) ;
#32931=CARTESIAN_POINT ( 'NONE',  ( 2.282816707992322058, 31.69834551989417193, -34.66571588341096088 ) ) ;
#32935=CARTESIAN_POINT ( 'NONE',  ( 0.5804410086790514622, -19.24447200597980512, 42.76879877979338573 ) ) ;
#32938=CARTESIAN_POINT ( 'NONE',  ( 2.618530812446115519, 31.65223561859582802, -34.75432015653727547 ) ) ;
#32940=CARTESIAN_POINT ( 'NONE',  ( 0.7764146366350234141, 11.73874228733617642, 45.41191917526355581 ) ) ;
#32941=ORIENTED_EDGE ( 'NONE', *, *, #8706, .T. ) ;
#32944=CARTESIAN_POINT ( 'NONE',  ( 0.8554163680231738898, 16.00619315955181321, 44.10223637924652706 ) ) ;
#32945=( BOUNDED_SURFACE ( )  B_SPLINE_SURFACE ( 3, 1, ( 
 ( #45312, #60288 ),
 ( #21795, #21476 ),
 ( #7355, #17401 ),
 ( #55590, #11473 ) ),
 .UNSPECIFIED., .F., .F., .F. ) 
 B_SPLINE_SURFACE_WITH_KNOTS ( ( 4, 4 ),
 ( 2, 2 ),
 ( 0.000000000000000000, 1.000000000000000000 ),
 ( 0.000000000000000000, 1.000000000000000000 ),
 .UNSPECIFIED. ) 
 GEOMETRIC_REPRESENTATION_ITEM ( )  RATIONAL_B_SPLINE_SURFACE ( (
 ( 1.000000000000000000, 1.000000000000000000),
 ( 0.7282232189291694135, 0.9929344683865672927),
 ( 0.7282232189291694135, 0.9929344683865672927),
 ( 1.000000000000000000, 1.000000000000000000) ) ) 
 REPRESENTATION_ITEM ( '' )  SURFACE ( )  );
#32947=B_SPLINE_CURVE_WITH_KNOTS ( 'NONE', 3,
 ( #44696, #10866, #24647, #43786 ),
 .UNSPECIFIED., .F., .F.,
 ( 4, 4 ),
 ( 0.000000000000000000, 0.004446298630425077163 ),
 .UNSPECIFIED. ) ;
#32948=CARTESIAN_POINT ( 'NONE',  ( 5.896782393890504181, -19.93422257774822626, -2.674482585249919442 ) ) ;
#32950=CARTESIAN_POINT ( 'NONE',  ( 0.5804410086790514622, -41.60900809504539666, 21.63816760268400330 ) ) ;
#32956=CARTESIAN_POINT ( 'NONE',  ( 0.5830081025819947582, 43.06738386279880615, -18.55889225133284270 ) ) ;
#32957=ORIENTED_EDGE ( 'NONE', *, *, #11931, .F. ) ;
#32961=ORIENTED_EDGE ( 'NONE', *, *, #13623, .T. ) ;
#32962=CARTESIAN_POINT ( 'NONE',  ( 0.9790850452238870627, -34.57988883937719748, -23.67633033473545012 ) ) ;
#32963=CARTESIAN_POINT ( 'NONE',  ( 4.956445790444002242, -43.14021684453514638, 18.88014143872134554 ) ) ;
#32964=CARTESIAN_POINT ( 'NONE',  ( 4.294001357053613965, 0.6022292657941538119, -42.05358333227729162 ) ) ;
#32967=VECTOR ( 'NONE', #3805, 1000.000000000000114 ) ;
#32972=CARTESIAN_POINT ( 'NONE',  ( 5.895596859100789899, -15.78235929336518950, -12.46777118604672197 ) ) ;
#32996=CARTESIAN_POINT ( 'NONE',  ( 4.291220156522059348, 2.567299637374572008, 47.04038658299518261 ) ) ;
#33000=B_SPLINE_CURVE_WITH_KNOTS ( 'NONE', 3,
 ( #59002, #35224, #34921, #10484 ),
 .UNSPECIFIED., .F., .F.,
 ( 4, 4 ),
 ( 5.204170427930421283E-17, 0.005004948556313862547 ),
 .UNSPECIFIED. ) ;
#33001=UNCERTAINTY_MEASURE_WITH_UNIT (LENGTH_MEASURE( 1.000000000000000082E-05 ), #8438, 'distance_accuracy_value', 'NONE');
#33009=VERTEX_POINT ( 'NONE', #7042 ) ;
#33020=CARTESIAN_POINT ( 'NONE',  ( 0.9762797500689124330, -39.42083772998332591, 14.22400568939802845 ) ) ;
#33025=ORIENTED_EDGE ( 'NONE', *, *, #25500, .T. ) ;
#33027=CARTESIAN_POINT ( 'NONE',  ( 0.7764139734771250412, -14.74570975091260117, 44.52644736388372593 ) ) ;
#33030=CARTESIAN_POINT ( 'NONE',  ( 0.5848930533535030563, -38.76613696830671074, -26.39052305169494872 ) ) ;
#33033=CARTESIAN_POINT ( 'NONE',  ( 2.528100132419514257, -16.56545499686994916, 38.57252233622727999 ) ) ;
#33034=CARTESIAN_POINT ( 'NONE',  ( 5.838029081930955932, -45.55059156558374411, -12.49834653777416626 ) ) ;
#33041=ORIENTED_EDGE ( 'NONE', *, *, #23680, .F. ) ;
#33051=CARTESIAN_POINT ( 'NONE',  ( 0.8554163680231816613, 39.89400665120465561, -24.69157156653778529 ) ) ;
#33052=EDGE_CURVE ( 'NONE', #6436, #41264, #25683, .T. ) ;
#33057=B_SPLINE_CURVE_WITH_KNOTS ( 'NONE', 3,
 ( #49455, #2129, #11249, #40396 ),
 .UNSPECIFIED., .F., .F.,
 ( 4, 4 ),
 ( 8.673617379884035472E-19, 0.004042984057420974560 ),
 .UNSPECIFIED. ) ;
#33068=CARTESIAN_POINT ( 'NONE',  ( 2.618530812446115519, 9.522253559614673790, -46.03317799527428633 ) ) ;
#33070=B_SPLINE_CURVE_WITH_KNOTS ( 'NONE', 3,
 ( #25388, #53880, #960, #48579, #44228, #10685, #15083, #39839, #43923, #1881, #34192, #29781, #21009, #16010, #58265, #35124, #10381, #40153, #24780 ),
 .UNSPECIFIED., .F., .F.,
 ( 4, 3, 3, 3, 3, 3, 4 ),
 ( 1.250973872328959318E-17, 0.0002732106629380648714, 0.0004098138914053863283, 0.0005464171197651537370, 0.0006830203481512621628, 0.0008196235766963708971, 0.001011968216111137908 ),
 .UNSPECIFIED. ) ;
#33075=CARTESIAN_POINT ( 'NONE',  ( 0.5848930533535030563, -25.08041605097227134, -39.62632727237903651 ) ) ;
#33077=CARTESIAN_POINT ( 'NONE',  ( 5.910764540655177868, 17.95751408178366759, -9.056982194511830286 ) ) ;
#33079=VERTEX_POINT ( 'NONE', #50585 ) ;
#33083=VERTEX_POINT ( 'NONE', #55277 ) ;
#33097=CARTESIAN_POINT ( 'NONE',  ( 0.9790850452238886170, -37.42709535634217843, -18.85602989630809745 ) ) ;
#33098=CARTESIAN_POINT ( 'NONE',  ( 0.5804410086790514622, -2.113107284888626758, -46.85141011173459447 ) ) ;
#33102=ORIENTED_EDGE ( 'NONE', *, *, #26303, .F. ) ;
#33106=VECTOR ( 'NONE', #30434, 1000.000000000000227 ) ;
#33111=CARTESIAN_POINT ( 'NONE',  ( 0.5817217712918332229, 27.44989446949152523, 38.02286480030341664 ) ) ;
#33115=CARTESIAN_POINT ( 'NONE',  ( 0.5806925824938499181, -46.06186276235273169, 8.804950948514585818 ) ) ;
#33117=ORIENTED_EDGE ( 'NONE', *, *, #33773, .T. ) ;
#33121=CARTESIAN_POINT ( 'NONE',  ( 4.291220156522059348, 44.81988414002803012, 14.51092633087771411 ) ) ;
#33126=CARTESIAN_POINT ( 'NONE',  ( 0.8554163680231720024, -46.15020320557298561, -8.447734441620465162 ) ) ;
#33128=ORIENTED_EDGE ( 'NONE', *, *, #49782, .F. ) ;
#33129=EDGE_CURVE ( 'NONE', #34855, #46145, #55620, .T. ) ;
#33132=CARTESIAN_POINT ( 'NONE',  ( 5.895596859100789899, -17.30698493747188849, 10.24677781483567607 ) ) ;
#33133=CARTESIAN_POINT ( 'NONE',  ( 0.7056759521544990754, -6.968496825407635598, -46.38091074042502271 ) ) ;
#33136=EDGE_CURVE ( 'NONE', #19210, #9240, #57845, .T. ) ;
#33137=CARTESIAN_POINT ( 'NONE',  ( 0.5837799406558236148, 10.96004523085180615, 45.59737885136471647 ) ) ;
#33143=CARTESIAN_POINT ( 'NONE',  ( 1.091591847532195736, -2.180174137653107191, 41.85696873503080440 ) ) ;
#33149=ORIENTED_EDGE ( 'NONE', *, *, #16564, .F. ) ;
#33151=CARTESIAN_POINT ( 'NONE',  ( 5.896278296736517710, 10.81775449038653925, 16.95591835908941647 ) ) ;
#33155=CARTESIAN_POINT ( 'NONE',  ( 0.5835226383429280572, 43.24565384930013323, 18.13989795154533624 ) ) ;
#33156=ORIENTED_EDGE ( 'NONE', *, *, #28129, .T. ) ;
#33158=( BOUNDED_SURFACE ( )  B_SPLINE_SURFACE ( 3, 1, ( 
 ( #59683, #59369 ),
 ( #16473, #12108 ),
 ( #35604, #54665 ),
 ( #31184, #28641 ) ),
 .UNSPECIFIED., .F., .F., .F. ) 
 B_SPLINE_SURFACE_WITH_KNOTS ( ( 4, 4 ),
 ( 2, 2 ),
 ( 0.000000000000000000, 1.000000000000000000 ),
 ( 0.000000000000000000, 1.000000000000000000 ),
 .UNSPECIFIED. ) 
 GEOMETRIC_REPRESENTATION_ITEM ( )  RATIONAL_B_SPLINE_SURFACE ( (
 ( 1.000000000000000000, 1.000000000000000000),
 ( 0.7282232189291693025, 0.9929344683865674037),
 ( 0.7282232189291693025, 0.9929344683865674037),
 ( 1.000000000000000000, 1.000000000000000000) ) ) 
 REPRESENTATION_ITEM ( '' )  SURFACE ( )  );
#33172=B_SPLINE_CURVE_WITH_KNOTS ( 'NONE', 3,
 ( #58975, #16085, #6631, #49576 ),
 .UNSPECIFIED., .F., .F.,
 ( 4, 4 ),
 ( 1.084202172485504434E-19, 0.004446298630425088438 ),
 .UNSPECIFIED. ) ;
#33174=CARTESIAN_POINT ( 'NONE',  ( 0.9790850452238877288, -7.020569879040508887, -41.31644864744191636 ) ) ;
#33181=CARTESIAN_POINT ( 'NONE',  ( 0.9785694773339239649, -37.50411832126101785, 18.70231308313300289 ) ) ;
#33187=CARTESIAN_POINT ( 'NONE',  ( 5.838029081930957709, -32.82243551873150267, 33.96693664096945042 ) ) ;
#33198=ORIENTED_EDGE ( 'NONE', *, *, #45861, .T. ) ;
#33199=EDGE_CURVE ( 'NONE', #17422, #34160, #6230, .T. ) ;
#33202=DIRECTION ( 'NONE',  ( 0.000000000000000000, 0.000000000000000000, 1.000000000000000000 ) ) ;
#33212=CARTESIAN_POINT ( 'NONE',  ( 1.157644175074336923, -39.86048670168759855, 12.96703032246667853 ) ) ;
#33215=CARTESIAN_POINT ( 'NONE',  ( 0.9791128995231609400, 29.13826394149679189, 30.12140449450908619 ) ) ;
#33218=CARTESIAN_POINT ( 'NONE',  ( 4.962356264823608143, 0.000000000000000000, 0.000000000000000000 ) ) ;
#33219=( BOUNDED_SURFACE ( )  B_SPLINE_SURFACE ( 3, 1, ( 
 ( #40221, #25452 ),
 ( #54559, #21386 ),
 ( #17011, #55191 ),
 ( #20772, #16079 ) ),
 .UNSPECIFIED., .F., .F., .F. ) 
 B_SPLINE_SURFACE_WITH_KNOTS ( ( 4, 4 ),
 ( 2, 2 ),
 ( 0.000000000000000000, 1.000000000000000000 ),
 ( 0.000000000000000000, 1.000000000000000000 ),
 .UNSPECIFIED. ) 
 GEOMETRIC_REPRESENTATION_ITEM ( )  RATIONAL_B_SPLINE_SURFACE ( (
 ( 1.000000000000000000, 1.000000000000000000),
 ( 0.9952954269826590483, 0.8620686068821307169),
 ( 0.9952954269826590483, 0.8620686068821307169),
 ( 1.000000000000000000, 1.000000000000000000) ) ) 
 REPRESENTATION_ITEM ( '' )  SURFACE ( )  );
#33226=CARTESIAN_POINT ( 'NONE',  ( 0.5797568599927133137, -2.195683865110441779, 46.84446905490015212 ) ) ;
#33229=CARTESIAN_POINT ( 'NONE',  ( 0.5848930533535030563, -44.36099898510395434, 15.21101086158195237 ) ) ;
#33236=CARTESIAN_POINT ( 'NONE',  ( 0.5830081025819932039, -46.00989229531988656, -9.073138671667642541 ) ) ;
#33238=ORIENTED_EDGE ( 'NONE', *, *, #7532, .F. ) ;
#33242=ORIENTED_EDGE ( 'NONE', *, *, #30680, .F. ) ;
#33243=CARTESIAN_POINT ( 'NONE',  ( 4.962356264823600149, -32.75738977283805298, 26.42326651140453109 ) ) ;
#33246=EDGE_LOOP ( 'NONE', ( #24055, #60578, #49785, #30193 ) ) ;
#33258=CARTESIAN_POINT ( 'NONE',  ( 0.6845945791218023269, 21.77999332122274012, -41.54561844095520939 ) ) ;
#33265=CARTESIAN_POINT ( 'NONE',  ( 0.5830082357119578118, 43.28068137227774770, -18.05587591034304396 ) ) ;
#33266=ORIENTED_EDGE ( 'NONE', *, *, #42404, .F. ) ;
#33269=CARTESIAN_POINT ( 'NONE',  ( 0.5837157313716030416, 10.95998063749551044, -45.59732325485506976 ) ) ;
#33271=CARTESIAN_POINT ( 'NONE',  ( 0.6845945791218034371, 39.91187923413946237, 24.64646864590162068 ) ) ;
#33274=DIRECTION ( 'NONE',  ( -0.07500201931887527651, 0.9652320423656555182, 0.2504032777116073083 ) ) ;
#33288=CARTESIAN_POINT ( 'NONE',  ( 5.917102823773431552, -4.653982686479870345, -19.56604618224355363 ) ) ;
#33290=CARTESIAN_POINT ( 'NONE',  ( 0.5806925824938511393, 32.99217760300656010, 33.32774488853447536 ) ) ;
#33293=DIRECTION ( 'NONE',  ( -0.07500201931887527651, -0.9463514676414596094, -0.3143144870841088623 ) ) ;
#33321=AXIS2_PLACEMENT_3D ( 'NONE', #13241, #41765, #37061 ) ;
#33327=ORIENTED_EDGE ( 'NONE', *, *, #37298, .T. ) ;
#33328=ORIENTED_EDGE ( 'NONE', *, *, #61154, .F. ) ;
#33329=EDGE_CURVE ( 'NONE', #8407, #52560, #53289, .T. ) ;
#33337=CARTESIAN_POINT ( 'NONE',  ( 2.282803330402979114, 43.74200375098541116, -17.12115694997745052 ) ) ;
#33339=VECTOR ( 'NONE', #53663, 1000.000000000000114 ) ;
#33340=VERTEX_POINT ( 'NONE', #53651 ) ;
#33341=CARTESIAN_POINT ( 'NONE',  ( 4.958415959904820092, -42.01301765298963176, 17.26587100357872373 ) ) ;
#33346=CARTESIAN_POINT ( 'NONE',  ( 5.910764540655178756, -19.93482381198522191, -2.665340138569558537 ) ) ;
#33347=CARTESIAN_POINT ( 'NONE',  ( 4.962356264823603702, 41.96072444189417183, -3.245489512195726789 ) ) ;
#33362=DIRECTION ( 'NONE',  ( -1.000000000000000000, -0.000000000000000000, -0.000000000000000000 ) ) ;
#33373=ADVANCED_FACE ( 'NONE', ( #16393 ), #43859, .F. ) ;
#33377=ORIENTED_EDGE ( 'NONE', *, *, #52735, .F. ) ;
#33386=CARTESIAN_POINT ( 'NONE',  ( 0.5804410086790514622, 45.37396088368723213, -11.86269470150086924 ) ) ;
#33389=CARTESIAN_POINT ( 'NONE',  ( 1.092182651088186240, 33.37207687231951070, 25.35873951264696302 ) ) ;
#33391=CARTESIAN_POINT ( 'NONE',  ( 0.5837799406558226156, 16.76978727848185002, -43.79517991984587155 ) ) ;
#33392=CARTESIAN_POINT ( 'NONE',  ( 4.956445790443994248, 24.88142650099509723, 39.98065363916922621 ) ) ;
#33400=ORIENTED_EDGE ( 'NONE', *, *, #61234, .F. ) ;
#33404=CARTESIAN_POINT ( 'NONE',  ( 2.618530812446115519, 33.67725335819500287, 32.79587467115556620 ) ) ;
#33408=ORIENTED_EDGE ( 'NONE', *, *, #3414, .T. ) ;
#33416=CARTESIAN_POINT ( 'NONE',  ( 0.5806925824938499181, -44.11884900496058748, -15.89809815106991309 ) ) ;
#33418=ADVANCED_FACE ( 'NONE', ( #25792 ), #50220, .F. ) ;
#33420=CARTESIAN_POINT ( 'NONE',  ( 4.960386119450153508, -20.61356833094577823, -38.59426466896047003 ) ) ;
#33422=EDGE_CURVE ( 'NONE', #41654, #46648, #29869, .T. ) ;
#33428=CARTESIAN_POINT ( 'NONE',  ( 0.5806925824938502512, 22.05663578530182889, -41.38510819338409163 ) ) ;
#33437=CARTESIAN_POINT ( 'NONE',  ( 5.896782393890504181, -19.93252920631901404, -2.687073932226577533 ) ) ;
#33438=LINE ( 'NONE', #4577, #36863 ) ;
#33446=B_SPLINE_CURVE_WITH_KNOTS ( 'NONE', 3,
 ( #34464, #52616, #928, #48539, #20059, #44194 ),
 .UNSPECIFIED., .F., .F.,
 ( 4, 2, 4 ),
 ( 3.471140604459641645E-18, 0.0002291459268755719424, 0.0004582918537511404154 ),
 .UNSPECIFIED. ) ;
#33447=EDGE_CURVE ( 'NONE', #4858, #18906, #59951, .T. ) ;
#33464=EDGE_LOOP ( 'NONE', ( #59173, #95, #55073, #27289 ) ) ;
#33467=CARTESIAN_POINT ( 'NONE',  ( 0.5830082357119554803, 43.06739319212223194, 18.55887061686358663 ) ) ;
#33477=CARTESIAN_POINT ( 'NONE',  ( 0.5804410086790514622, 10.33990028284824803, -45.74501408892724896 ) ) ;
#33488=VERTEX_POINT ( 'NONE', #45536 ) ;
#33491=B_SPLINE_CURVE_WITH_KNOTS ( 'NONE', 3,
 ( #59693, #50601, #31194, #60300, #40944, #50912, #12416, #17726, #7365, #45621, #2678, #7682, #22111, #9867, #61233, #56229 ),
 .UNSPECIFIED., .F., .F.,
 ( 4, 3, 3, 3, 3, 4 ),
 ( 1.040890552917501732E-17, 0.0002732102107931913006, 0.0004098135523333824013, 0.0005464168938824995759, 0.0008195847345945435521, 0.001092771384553107867 ),
 .UNSPECIFIED. ) ;
#33492=CARTESIAN_POINT ( 'NONE',  ( 0.9772918015221170318, -37.21531972239668562, 19.27062099960642172 ) ) ;
#33496=CARTESIAN_POINT ( 'NONE',  ( 5.896278296736517710, -4.657235598391419096, -19.56622437251140667 ) ) ;
#33499=LINE ( 'NONE', #57562, #48033 ) ;
#33501=EDGE_LOOP ( 'NONE', ( #17469, #55611, #18441, #9312 ) ) ;
#33511=CARTESIAN_POINT ( 'NONE',  ( 0.9783242366443567484, -41.12142888775412075, 8.084712514115880211 ) ) ;
#33519=CARTESIAN_POINT ( 'NONE',  ( 4.962356264823601926, -38.57439820587641321, 16.83007429920694875 ) ) ;
#33521=CARTESIAN_POINT ( 'NONE',  ( 5.895596859100789899, 20.06821053248683029, 1.339816866691926567 ) ) ;
#33525=CARTESIAN_POINT ( 'NONE',  ( 0.5782707292762442330, -7.086273146447505944, -46.36292793387357847 ) ) ;
#33529=ORIENTED_EDGE ( 'NONE', *, *, #32835, .F. ) ;
#33534=CARTESIAN_POINT ( 'NONE',  ( 0.8560838555295158248, -14.76796170096741534, 44.52280473286123907 ) ) ;
#33539=B_SPLINE_CURVE_WITH_KNOTS ( 'NONE', 3,
 ( #33290, #43313, #52360, #9453, #19492, #53285 ),
 .UNSPECIFIED., .F., .F.,
 ( 4, 2, 4 ),
 ( 1.007374941650268034E-17, 0.0002448709889506589456, 0.0004897419779013078081 ),
 .UNSPECIFIED. ) ;
#33545=VERTEX_POINT ( 'NONE', #343 ) ;
#33546=CARTESIAN_POINT ( 'NONE',  ( 4.962356264823609031, -33.29728444345293781, 25.73958909062332268 ) ) ;
#33554=VERTEX_POINT ( 'NONE', #14182 ) ;
#33555=CARTESIAN_POINT ( 'NONE',  ( 1.231276596079887264, 38.91607545535247681, 15.58254928345742840 ) ) ;
#33557=ORIENTED_EDGE ( 'NONE', *, *, #52043, .T. ) ;
#33562=CARTESIAN_POINT ( 'NONE',  ( 5.895881250540457863, -19.93402233083542185, -2.676272654655299288 ) ) ;
#33566=CARTESIAN_POINT ( 'NONE',  ( 0.5806925824938499181, 23.01490136172973067, -40.85996423950240342 ) ) ;
#33567=EDGE_CURVE ( 'NONE', #30011, #4680, #61745, .T. ) ;
#33569=ORIENTED_EDGE ( 'NONE', *, *, #35453, .F. ) ;
#33571=EDGE_LOOP ( 'NONE', ( #53076, #28765, #16663, #53904 ) ) ;
#33572=CARTESIAN_POINT ( 'NONE',  ( 0.9754292589017192761, 25.32584946409135540, 33.39054979807107770 ) ) ;
#33573=CARTESIAN_POINT ( 'NONE',  ( 0.9762797500689124330, 40.28286501695585997, -11.55922018180369548 ) ) ;
#33575=CARTESIAN_POINT ( 'NONE',  ( 0.5837157313716032636, 4.603500525675801924, 46.66952802945544221 ) ) ;
#33578=CARTESIAN_POINT ( 'NONE',  ( 0.9780106845699478857, -22.28528844046299184, -35.49221274562640360 ) ) ;
#33581=CARTESIAN_POINT ( 'NONE',  ( 0.5848930533535030563, 36.91687493861116565, 28.92088219875909516 ) ) ;
#33593=AXIS2_PLACEMENT_3D ( 'NONE', #12244, #46074, #16943 ) ;
#33596=CARTESIAN_POINT ( 'NONE',  ( 4.962356264823608143, -36.43094049105388166, 21.07183363638861096 ) ) ;
#33602=CARTESIAN_POINT ( 'NONE',  ( 5.896278296736517710, -4.657235598391687326, 19.56622437251134627 ) ) ;
#33624=DIRECTION ( 'NONE',  ( -1.000000000000000000, -0.000000000000000000, -0.000000000000000000 ) ) ;
#33637=CARTESIAN_POINT ( 'NONE',  ( 0.7764146366350251904, 39.89513471720565718, -24.66614480548544819 ) ) ;
#33640=ORIENTED_EDGE ( 'NONE', *, *, #53116, .T. ) ;
#33642=CARTESIAN_POINT ( 'NONE',  ( 4.962356264823608143, -15.53171314616189846, 39.11523340857994668 ) ) ;
#33644=CARTESIAN_POINT ( 'NONE',  ( 2.618530812446111078, -24.09540528802407522, -40.36258457041695635 ) ) ;
#33649=ORIENTED_EDGE ( 'NONE', *, *, #52100, .T. ) ;
#33650=ORIENTED_EDGE ( 'NONE', *, *, #51022, .F. ) ;
#33651=CARTESIAN_POINT ( 'NONE',  ( 5.896782393890504181, -15.78060201202832324, 12.46991126736593003 ) ) ;
#33655=CARTESIAN_POINT ( 'NONE',  ( 5.895596859100789899, 19.00119700155552493, 6.594141014610245932 ) ) ;
#33661=CARTESIAN_POINT ( 'NONE',  ( 0.8554163680231708922, -44.01281378489781559, -16.25046755781901098 ) ) ;
#33667=CARTESIAN_POINT ( 'NONE',  ( 0.6064782688330866423, -45.81047758530520753, -10.03666228509350411 ) ) ;
#33672=CARTESIAN_POINT ( 'NONE',  ( 0.5806925824938499181, -25.69265091980040339, 39.23149310256803801 ) ) ;
#33683=ORIENTED_EDGE ( 'NONE', *, *, #40789, .T. ) ;
#33684=VERTEX_POINT ( 'NONE', #59216 ) ;
#33686=CARTESIAN_POINT ( 'NONE',  ( 5.901463166500146684, 19.70672075163023251, -4.020326797401311048 ) ) ;
#33691=ORIENTED_EDGE ( 'NONE', *, *, #34446, .T. ) ;
#33692=CARTESIAN_POINT ( 'NONE',  ( 0.5835871038041865466, 22.41749763088149905, 41.19090012212553376 ) ) ;
#33719=FACE_OUTER_BOUND ( 'NONE', #29134, .T. ) ;
#33727=ORIENTED_EDGE ( 'NONE', *, *, #42197, .T. ) ;
#33728=CARTESIAN_POINT ( 'NONE',  ( 0.9762797500689124330, -34.26226594605912368, -24.13341909939868657 ) ) ;
#33732=DIRECTION ( 'NONE',  ( -1.000000000000000000, -0.000000000000000000, -0.000000000000000000 ) ) ;
#33739=FACE_OUTER_BOUND ( 'NONE', #13145, .T. ) ;
#33742=VERTEX_POINT ( 'NONE', #38926 ) ;
#33745=CARTESIAN_POINT ( 'NONE',  ( 0.5824936645240103017, 28.11017874027236374, -37.53739509116535089 ) ) ;
#33747=DIRECTION ( 'NONE',  ( -0.07906939808003035641, 0.9592846432126468370, -0.2711475679102552938 ) ) ;
#33751=CARTESIAN_POINT ( 'NONE',  ( 0.8560838555295158248, 46.89922841446242074, 0.9138972643637033322 ) ) ;
#33758=ADVANCED_FACE ( 'NONE', ( #49838 ), #39094, .F. ) ;
#33765=EDGE_CURVE ( 'NONE', #15772, #48535, #53583, .T. ) ;
#33773=EDGE_CURVE ( 'NONE', #26516, #56097, #61493, .T. ) ;
#33778=ORIENTED_EDGE ( 'NONE', *, *, #49508, .F. ) ;
#33780=CARTESIAN_POINT ( 'NONE',  ( 2.618530812446115519, 6.104648047582319492, 46.60965631082630267 ) ) ;
#33782=( BOUNDED_SURFACE ( )  B_SPLINE_SURFACE ( 3, 1, ( 
 ( #2894, #8213 ),
 ( #17950, #31105 ),
 ( #37065, #41150 ),
 ( #12327, #7591 ) ),
 .UNSPECIFIED., .F., .F., .F. ) 
 B_SPLINE_SURFACE_WITH_KNOTS ( ( 4, 4 ),
 ( 2, 2 ),
 ( 0.000000000000000000, 1.000000000000000000 ),
 ( 0.000000000000000000, 1.000000000000000000 ),
 .UNSPECIFIED. ) 
 GEOMETRIC_REPRESENTATION_ITEM ( )  RATIONAL_B_SPLINE_SURFACE ( (
 ( 1.000000000000000000, 1.000000000000000000),
 ( 0.7282232189291693025, 0.9929344683865674037),
 ( 0.7282232189291693025, 0.9929344683865674037),
 ( 1.000000000000000000, 1.000000000000000000) ) ) 
 REPRESENTATION_ITEM ( '' )  SURFACE ( )  );
#33791=CARTESIAN_POINT ( 'NONE',  ( 0.5848930533535030563, 10.69427347779520332, -45.66076649783362029 ) ) ;
#33795=ORIENTED_EDGE ( 'NONE', *, *, #48655, .F. ) ;
#33796=B_SPLINE_CURVE_WITH_KNOTS ( 'NONE', 3,
 ( #4399, #29469, #38909, #47355 ),
 .UNSPECIFIED., .F., .F.,
 ( 4, 4 ),
 ( 0.000000000000000000, 0.004447772540403843212 ),
 .UNSPECIFIED. ) ;
#33797=CARTESIAN_POINT ( 'NONE',  ( 0.9775691876210974574, -6.597867306536943310, -41.38601038992914738 ) ) ;
#33803=ORIENTED_EDGE ( 'NONE', *, *, #17407, .T. ) ;
#33804=CARTESIAN_POINT ( 'NONE',  ( 0.8560838555295223751, -0.6537497281626496459, 46.90357604036880446 ) ) ;
#33805=CARTESIAN_POINT ( 'NONE',  ( 0.9784957157296372277, -37.29867915761859365, 19.10867839724658168 ) ) ;
#33806=CARTESIAN_POINT ( 'NONE',  ( 0.9762797500689124330, 38.77779312671030709, 15.89363222827819300 ) ) ;
#33807=ORIENTED_EDGE ( 'NONE', *, *, #25129, .T. ) ;
#33814=LINE ( 'NONE', #20624, #35828 ) ;
#33815=CARTESIAN_POINT ( 'NONE',  ( 1.157644175074336257, 38.90537128965222280, -15.60046025902721389 ) ) ;
#33816=CARTESIAN_POINT ( 'NONE',  ( 0.9762797500689124330, -26.66896101499549587, -32.32787193067855469 ) ) ;
#33818=ORIENTED_EDGE ( 'NONE', *, *, #27942, .T. ) ;
#33822=CARTESIAN_POINT ( 'NONE',  ( 0.9787284016396613495, -41.03117890019433389, 8.531023208799519253 ) ) ;
#33823=DIRECTION ( 'NONE',  ( 0.000000000000000000, 0.000000000000000000, 1.000000000000000000 ) ) ;
#33834=VECTOR ( 'NONE', #58126, 1000.000000000000000 ) ;
#33850=EDGE_CURVE ( 'NONE', #18146, #58874, #45786, .T. ) ;
#33852=CARTESIAN_POINT ( 'NONE',  ( 0.5804410086790514622, -44.48029469925801749, 14.86685021524587746 ) ) ;
#33856=CARTESIAN_POINT ( 'NONE',  ( 1.157643937452369265, 15.83273913728741888, 38.81142416873363032 ) ) ;
#33872=ORIENTED_EDGE ( 'NONE', *, *, #56716, .T. ) ;
#33873=DIRECTION ( 'NONE',  ( 0.000000000000000000, 0.000000000000000000, 1.000000000000000000 ) ) ;
#33876=CARTESIAN_POINT ( 'NONE',  ( 0.5824935313925951874, 17.19420832410670030, 43.63023466772849446 ) ) ;
#33880=CARTESIAN_POINT ( 'NONE',  ( 3.782625744892852637, 26.30387422842974843, 32.79244279815019070 ) ) ;
#33881=ADVANCED_FACE ( 'NONE', ( #11964 ), #20233, .F. ) ;
#33884=CARTESIAN_POINT ( 'NONE',  ( 0.9780303403264780648, 40.33289069370958657, -11.38409160558530608 ) ) ;
#33885=ORIENTED_EDGE ( 'NONE', *, *, #21424, .T. ) ;
#33886=CARTESIAN_POINT ( 'NONE',  ( 0.5837800304671231233, 4.648813602424494817, 46.66503899354860607 ) ) ;
#33888=EDGE_CURVE ( 'NONE', #45432, #57208, #38238, .T. ) ;
#33904=ADVANCED_FACE ( 'NONE', ( #55754 ), #624, .F. ) ;
#33917=CARTESIAN_POINT ( 'NONE',  ( 1.000433927950261870, 38.32221909574490581, -16.96544138036415461 ) ) ;
#33919=EDGE_CURVE ( 'NONE', #29140, #13648, #4583, .T. ) ;
#33924=VERTEX_POINT ( 'NONE', #1133 ) ;
#33926=ORIENTED_EDGE ( 'NONE', *, *, #10075, .T. ) ;
#33927=CARTESIAN_POINT ( 'NONE',  ( 0.5797568665920712627, 28.32170371298940736, 37.37788660953842168 ) ) ;
#33937=CARTESIAN_POINT ( 'NONE',  ( 4.291220156522059348, 24.50578158393244976, -40.23500548361207052 ) ) ;
#33941=B_SPLINE_CURVE_WITH_KNOTS ( 'NONE', 3,
 ( #14336, #9607, #33133, #18719, #18411, #61598 ),
 .UNSPECIFIED., .F., .F.,
 ( 4, 2, 4 ),
 ( 1.210102227977247116E-16, 0.0002448718616795922832, 0.0004897437233590635694 ),
 .UNSPECIFIED. ) ;
#33946=CARTESIAN_POINT ( 'NONE',  ( 0.5797568665920713737, 40.02504847250913400, -24.43810146830487895 ) ) ;
#33950=DIRECTION ( 'NONE',  ( -1.000000000000000000, -0.000000000000000000, -0.000000000000000000 ) ) ;
#33952=( BOUNDED_SURFACE ( )  B_SPLINE_SURFACE ( 3, 1, ( 
 ( #49222, #39543 ),
 ( #40473, #30728 ),
 ( #34523, #58287 ),
 ( #34835, #53591 ) ),
 .UNSPECIFIED., .F., .F., .F. ) 
 B_SPLINE_SURFACE_WITH_KNOTS ( ( 4, 4 ),
 ( 2, 2 ),
 ( 0.000000000000000000, 1.000000000000000000 ),
 ( 0.000000000000000000, 1.000000000000000000 ),
 .UNSPECIFIED. ) 
 GEOMETRIC_REPRESENTATION_ITEM ( )  RATIONAL_B_SPLINE_SURFACE ( (
 ( 1.000000000000000000, 1.000000000000000000),
 ( 0.9952954269826590483, 0.8620686068821307169),
 ( 0.9952954269826590483, 0.8620686068821307169),
 ( 1.000000000000000000, 1.000000000000000000) ) ) 
 REPRESENTATION_ITEM ( '' )  SURFACE ( )  );
#33953=CARTESIAN_POINT ( 'NONE',  ( 0.5837157313716038187, 36.86032209105336932, -28.99230447766828433 ) ) ;
#33954=ORIENTED_EDGE ( 'NONE', *, *, #16758, .T. ) ;
#33960=CARTESIAN_POINT ( 'NONE',  ( 1.092182651088185130, 41.90646141200330277, -0.7808177550258036392 ) ) ;
#33962=VECTOR ( 'NONE', #6482, 1000.000000000000227 ) ;
#33964=EDGE_LOOP ( 'NONE', ( #18050, #8482, #48112, #53913 ) ) ;
#33967=CARTESIAN_POINT ( 'NONE',  ( 4.962356264823609031, -32.75738977283769771, -26.42326651140497873 ) ) ;
#33969=CARTESIAN_POINT ( 'NONE',  ( 0.8560838555295158248, 46.35895890951125153, 7.156798369940231552 ) ) ;
#33985=CARTESIAN_POINT ( 'NONE',  ( 1.231276596079887264, 10.53918392497828727, 40.57341954055075917 ) ) ;
#33987=EDGE_CURVE ( 'NONE', #40429, #24828, #24013, .T. ) ;
#33994=ORIENTED_EDGE ( 'NONE', *, *, #39656, .F. ) ;
#34012=B_SPLINE_CURVE_WITH_KNOTS ( 'NONE', 3,
 ( #12290, #59559, #50780, #7871, #7548, #54855 ),
 .UNSPECIFIED., .F., .F.,
 ( 4, 2, 4 ),
 ( 1.177386153108680874E-16, 0.0002448718616795951563, 0.0004897437233590725683 ),
 .UNSPECIFIED. ) ;
#34013=CARTESIAN_POINT ( 'NONE',  ( 0.5832655196449119117, 46.89545140795105738, 0.2276405452299705978 ) ) ;
#34014=CARTESIAN_POINT ( 'NONE',  ( 0.6845945791218023269, 5.556290360844593934, 46.57825842751027068 ) ) ;
#34028=ORIENTED_EDGE ( 'NONE', *, *, #9346, .T. ) ;
#34030=CARTESIAN_POINT ( 'NONE',  ( 0.5837800005270559200, -13.89411067738082473, 44.79050063491671807 ) ) ;
#34032=EDGE_CURVE ( 'NONE', #2702, #9808, #42015, .T. ) ;
#34039=CARTESIAN_POINT ( 'NONE',  ( 0.5782707292762442330, 23.17211662964134433, -40.77731433787561599 ) ) ;
#34056=( BOUNDED_SURFACE ( )  B_SPLINE_SURFACE ( 3, 1, ( 
 ( #4687, #9410 ),
 ( #8799, #32311 ),
 ( #51388, #56400 ),
 ( #60790, #32623 ) ),
 .UNSPECIFIED., .F., .F., .F. ) 
 B_SPLINE_SURFACE_WITH_KNOTS ( ( 4, 4 ),
 ( 2, 2 ),
 ( 0.000000000000000000, 1.000000000000000000 ),
 ( 0.000000000000000000, 1.000000000000000000 ),
 .UNSPECIFIED. ) 
 GEOMETRIC_REPRESENTATION_ITEM ( )  RATIONAL_B_SPLINE_SURFACE ( (
 ( 1.000000000000000000, 1.000000000000000000),
 ( 0.9952954269826590483, 0.8620686068821339365),
 ( 0.9952954269826590483, 0.8620686068821339365),
 ( 1.000000000000000000, 1.000000000000000000) ) ) 
 REPRESENTATION_ITEM ( '' )  SURFACE ( )  );
#34060=CARTESIAN_POINT ( 'NONE',  ( 0.5804410086790514622, -24.77328595090333252, -39.82215658462223473 ) ) ;
#34062=CARTESIAN_POINT ( 'NONE',  ( 4.962356264823608143, -42.08379584346670299, -0.4355746408611892995 ) ) ;
#34068=CARTESIAN_POINT ( 'NONE',  ( 5.910764540655177868, 20.06626233353475541, 1.358806252166760986 ) ) ;
#34069=B_SPLINE_CURVE_WITH_KNOTS ( 'NONE', 3,
 ( #9703, #24420, #10333, #48846 ),
 .UNSPECIFIED., .F., .F.,
 ( 4, 4 ),
 ( 1.734723475976807094E-18, 0.004042984057420971090 ),
 .UNSPECIFIED. ) ;
#34070=LINE ( 'NONE', #44698, #26706 ) ;
#34077=CARTESIAN_POINT ( 'NONE',  ( 0.6845945791218034371, 46.59746449482855724, -5.392849280958651903 ) ) ;
#34082=( BOUNDED_SURFACE ( )  B_SPLINE_SURFACE ( 3, 1, ( 
 ( #27447, #41570 ),
 ( #32162, #61255 ),
 ( #41267, #55321 ),
 ( #28071, #17439 ) ),
 .UNSPECIFIED., .F., .F., .F. ) 
 B_SPLINE_SURFACE_WITH_KNOTS ( ( 4, 4 ),
 ( 2, 2 ),
 ( 0.000000000000000000, 1.000000000000000000 ),
 ( 0.000000000000000000, 1.000000000000000000 ),
 .UNSPECIFIED. ) 
 GEOMETRIC_REPRESENTATION_ITEM ( )  RATIONAL_B_SPLINE_SURFACE ( (
 ( 1.000000000000000000, 1.000000000000000000),
 ( 0.7282232189291693025, 0.9929344683865674037),
 ( 0.7282232189291693025, 0.9929344683865674037),
 ( 1.000000000000000000, 1.000000000000000000) ) ) 
 REPRESENTATION_ITEM ( '' )  SURFACE ( )  );
#34089=VERTEX_POINT ( 'NONE', #59066 ) ;
#34091=CARTESIAN_POINT ( 'NONE',  ( 0.5830081025819922047, -25.46374175752871594, -39.38057757433394812 ) ) ;
#34108=ORIENTED_EDGE ( 'NONE', *, *, #60077, .F. ) ;
#34109=ADVANCED_FACE ( 'NONE', ( #53737 ), #13462, .F. ) ;
#34117=EDGE_CURVE ( 'NONE', #18772, #58158, #39024, .T. ) ;
#34122=CARTESIAN_POINT ( 'NONE',  ( 0.9789233960466705575, -30.99329158749494084, -28.20908724870154671 ) ) ;
#34128=CARTESIAN_POINT ( 'NONE',  ( 3.376099380956838925, 0.8831717405835582957, 13.37641175011825823 ) ) ;
#34137=VECTOR ( 'NONE', #55756, 1000.000000000000227 ) ;
#34144=CARTESIAN_POINT ( 'NONE',  ( 0.8560838555295223751, 9.983184696771347788, -45.83349056521751663 ) ) ;
#34149=CARTESIAN_POINT ( 'NONE',  ( 5.896278296736517710, 16.57877312360428235, -11.38732898139155481 ) ) ;
#34152=CARTESIAN_POINT ( 'NONE',  ( 5.895596859100789899, -17.30698493747188849, 10.24677781483567607 ) ) ;
#34153=EDGE_LOOP ( 'NONE', ( #19696, #18150, #67, #442 ) ) ;
#34156=CARTESIAN_POINT ( 'NONE',  ( 2.618530812446115519, -24.09540528802465076, 40.36258457041660108 ) ) ;
#34160=VERTEX_POINT ( 'NONE', #2983 ) ;
#34164=EDGE_LOOP ( 'NONE', ( #24131, #33400, #21150, #16504 ) ) ;
#34167=EDGE_LOOP ( 'NONE', ( #54093, #52814, #42727, #46054 ) ) ;
#34178=CARTESIAN_POINT ( 'NONE',  ( 4.956445790443998689, -5.251077430596073903, 46.79705371022326688 ) ) ;
#34187=CARTESIAN_POINT ( 'NONE',  ( 0.6064515330803599280, 46.37855968485794733, -6.954389807535533485 ) ) ;
#34192=CARTESIAN_POINT ( 'NONE',  ( 0.9790320750461907195, -12.33438343446691476, -40.05246706301296911 ) ) ;
#34202=B_SPLINE_CURVE_WITH_KNOTS ( 'NONE', 3,
 ( #10400, #14489, #19494, #52673 ),
 .UNSPECIFIED., .F., .F.,
 ( 4, 4 ),
 ( 1.111881969766579830E-16, 0.005004948556313921527 ),
 .UNSPECIFIED. ) ;
#34205=DIRECTION ( 'NONE',  ( -1.000000000000000000, -0.000000000000000000, -0.000000000000000000 ) ) ;
#34211=FACE_OUTER_BOUND ( 'NONE', #49231, .T. ) ;
#34215=EDGE_CURVE ( 'NONE', #21941, #14444, #9804, .T. ) ;
#34217=( BOUNDED_SURFACE ( )  B_SPLINE_SURFACE ( 3, 1, ( 
 ( #18614, #33034 ),
 ( #37745, #56803 ),
 ( #13931, #28309 ),
 ( #4471, #23612 ) ),
 .UNSPECIFIED., .F., .F., .F. ) 
 B_SPLINE_SURFACE_WITH_KNOTS ( ( 4, 4 ),
 ( 2, 2 ),
 ( 0.000000000000000000, 1.000000000000000000 ),
 ( 0.000000000000000000, 1.000000000000000000 ),
 .UNSPECIFIED. ) 
 GEOMETRIC_REPRESENTATION_ITEM ( )  RATIONAL_B_SPLINE_SURFACE ( (
 ( 1.000000000000000000, 1.000000000000000000),
 ( 0.7282232189291693025, 0.9929344683865674037),
 ( 0.7282232189291693025, 0.9929344683865674037),
 ( 1.000000000000000000, 1.000000000000000000) ) ) 
 REPRESENTATION_ITEM ( '' )  SURFACE ( )  );
#34222=CARTESIAN_POINT ( 'NONE',  ( 1.231276596079887931, 38.25526645152051941, -17.14092645516095104 ) ) ;
#34226=B_SPLINE_CURVE_WITH_KNOTS ( 'NONE', 3,
 ( #5694, #33027, #24842, #52096, #31082, #1312 ),
 .UNSPECIFIED., .F., .F.,
 ( 4, 2, 4 ),
 ( 1.222833943671018430E-16, 0.0002448718616795911990, 0.0004897437233590601000 ),
 .UNSPECIFIED. ) ;
#34229=CARTESIAN_POINT ( 'NONE',  ( 4.962356264823603702, 30.91935898304086550, -28.55221248765493414 ) ) ;
#34231=VERTEX_POINT ( 'NONE', #32438 ) ;
#34240=ORIENTED_EDGE ( 'NONE', *, *, #26743, .T. ) ;
#34245=VERTEX_POINT ( 'NONE', #17107 ) ;
#34247=CARTESIAN_POINT ( 'NONE',  ( 1.000110580585050979, 14.44681620832066216, 39.34090726222393641 ) ) ;
#34249=CARTESIAN_POINT ( 'NONE',  ( 0.5797568599927140909, -0.9380848280338333067, -46.88651517788902368 ) ) ;
#34256=CARTESIAN_POINT ( 'NONE',  ( 0.6845945791218034371, -46.13320409389251608, 8.493173773401963444 ) ) ;
#34262=CARTESIAN_POINT ( 'NONE',  ( 0.6064782688330851990, -35.25406363906476770, 30.92709885119426616 ) ) ;
#34268=CARTESIAN_POINT ( 'NONE',  ( 0.9762797500689124330, 14.58899758184696971, -39.28722355604386252 ) ) ;
#34287=CARTESIAN_POINT ( 'NONE',  ( 4.956445790443998689, -17.42806872899825521, 43.74700527484080936 ) ) ;
#34290=CARTESIAN_POINT ( 'NONE',  ( 3.376099380956838925, 7.576724406378373189, 11.05900677736737237 ) ) ;
#34293=CARTESIAN_POINT ( 'NONE',  ( 0.5797568665920705966, -24.70127861128346325, 39.86316775633390819 ) ) ;
#34294=DIRECTION ( 'NONE',  ( -1.000000000000000000, -0.000000000000000000, -0.000000000000000000 ) ) ;
#34300=CARTESIAN_POINT ( 'NONE',  ( 0.5782707292762442330, 45.42077932512039951, -11.69141390963183902 ) ) ;
#34309=CARTESIAN_POINT ( 'NONE',  ( 1.000433927950264534, 36.39033293409891456, 20.78851477615176435 ) ) ;
#34314=( BOUNDED_SURFACE ( )  B_SPLINE_SURFACE ( 3, 1, ( 
 ( #57031, #52023 ),
 ( #10058, #28528 ),
 ( #14156, #19163 ),
 ( #47651, #23228 ) ),
 .UNSPECIFIED., .F., .F., .F. ) 
 B_SPLINE_SURFACE_WITH_KNOTS ( ( 4, 4 ),
 ( 2, 2 ),
 ( 0.000000000000000000, 1.000000000000000000 ),
 ( 0.000000000000000000, 1.000000000000000000 ),
 .UNSPECIFIED. ) 
 GEOMETRIC_REPRESENTATION_ITEM ( )  RATIONAL_B_SPLINE_SURFACE ( (
 ( 1.000000000000000000, 1.000000000000000000),
 ( 0.9729067724841187204, 0.9999501103223794596),
 ( 0.9729067724841187204, 0.9999501103223794596),
 ( 1.000000000000000000, 1.000000000000000000) ) ) 
 REPRESENTATION_ITEM ( '' )  SURFACE ( )  );
#34321=CARTESIAN_POINT ( 'NONE',  ( 4.962356264823601926, -42.08379584346671720, 0.4355746408606013254 ) ) ;
#34325=CARTESIAN_POINT ( 'NONE',  ( 4.291220156522060236, 34.26497439135391687, 32.33110773335113208 ) ) ;
#34327=B_SPLINE_CURVE_WITH_KNOTS ( 'NONE', 3,
 ( #3248, #40285, #59337, #40586 ),
 .UNSPECIFIED., .F., .F.,
 ( 4, 4 ),
 ( 1.734723475976807094E-18, 0.004042984057420972825 ),
 .UNSPECIFIED. ) ;
#34329=CARTESIAN_POINT ( 'NONE',  ( 0.5837800005270565862, 46.47757032468152971, -6.250657193932968703 ) ) ;
#34332=EDGE_CURVE ( 'NONE', #41577, #6162, #1575, .T. ) ;
#34333=CARTESIAN_POINT ( 'NONE',  ( 4.962356264823608143, -14.71877352713578269, -39.42833123173278409 ) ) ;
#34337=ORIENTED_EDGE ( 'NONE', *, *, #14457, .T. ) ;
#34342=LINE ( 'NONE', #48425, #45709 ) ;
#34347=CARTESIAN_POINT ( 'NONE',  ( 5.901463166500146684, -7.215136289071354625, 18.77390952014955872 ) ) ;
#34353=CARTESIAN_POINT ( 'NONE',  ( 0.9790320750461911636, 41.52319970619036837, 5.671068567917366465 ) ) ;
#34358=CARTESIAN_POINT ( 'NONE',  ( 1.157643937452369043, 32.37803415880393487, -26.62076592823879650 ) ) ;
#34362=CARTESIAN_POINT ( 'NONE',  ( 5.895596859100789899, -13.97974974393973291, 14.46010996878324129 ) ) ;
#34370=ORIENTED_EDGE ( 'NONE', *, *, #25870, .F. ) ;
#34385=EDGE_CURVE ( 'NONE', #4231, #54025, #6068, .T. ) ;
#34389=CARTESIAN_POINT ( 'NONE',  ( 0.5837800304671217910, -25.19555850426963417, -39.55276430083521433 ) ) ;
#34395=CARTESIAN_POINT ( 'NONE',  ( 0.5835871038041858805, -34.87197729266512169, 31.35569569633796405 ) ) ;
#34397=VERTEX_POINT ( 'NONE', #34597 ) ;
#34399=CARTESIAN_POINT ( 'NONE',  ( 2.618530812446111078, 46.98662296661650828, 1.408563591474228938 ) ) ;
#34403=B_SPLINE_CURVE_WITH_KNOTS ( 'NONE', 3,
 ( #49109, #1170, #58790, #15914 ),
 .UNSPECIFIED., .F., .F.,
 ( 4, 4 ),
 ( 0.000000000000000000, 0.005004948556313788821 ),
 .UNSPECIFIED. ) ;
#34405=CARTESIAN_POINT ( 'NONE',  ( 3.238018933889920792, -5.387504234938196745, -12.26304572633470791 ) ) ;
#34407=ORIENTED_EDGE ( 'NONE', *, *, #50208, .T. ) ;
#34413=CARTESIAN_POINT ( 'NONE',  ( 0.9790850452238872847, 36.03246141061279673, -21.40091247951577813 ) ) ;
#34423=CARTESIAN_POINT ( 'NONE',  ( 0.9790850452238869517, -31.11560338686072669, -28.07412609743672860 ) ) ;
#34431=CARTESIAN_POINT ( 'NONE',  ( 4.956445790444004018, -43.56224489968086999, -17.88487823385623443 ) ) ;
#34436=B_SPLINE_CURVE_WITH_KNOTS ( 'NONE', 3,
 ( #28494, #23814, #42942, #22962, #56384, #32603 ),
 .UNSPECIFIED., .F., .F.,
 ( 4, 2, 4 ),
 ( 1.889500315511339631E-17, 0.0002448709889506574277, 0.0004897419779012958819 ),
 .UNSPECIFIED. ) ;
#34440=CARTESIAN_POINT ( 'NONE',  ( 5.896278296736517710, -13.98624301437808448, -14.45378794493484520 ) ) ;
#34443=FACE_OUTER_BOUND ( 'NONE', #33501, .T. ) ;
#34446=EDGE_CURVE ( 'NONE', #41967, #20220, #27074, .T. ) ;
#34447=CARTESIAN_POINT ( 'NONE',  ( 0.9769922540276052558, -34.79934705825704100, 23.35245167868034244 ) ) ;
#34458=CARTESIAN_POINT ( 'NONE',  ( 0.8554163680231720024, 46.61139063278402972, 5.346376005279848798 ) ) ;
#34461=CARTESIAN_POINT ( 'NONE',  ( 4.962356264823608143, 0.000000000000000000, 0.000000000000000000 ) ) ;
#34464=CARTESIAN_POINT ( 'NONE',  ( 0.9762797500689124330, 38.38274741215467145, 16.82526333465357382 ) ) ;
#34465=ORIENTED_EDGE ( 'NONE', *, *, #14479, .T. ) ;
#34467=EDGE_CURVE ( 'NONE', #46849, #56041, #60673, .T. ) ;
#34468=CARTESIAN_POINT ( 'NONE',  ( 3.376099380956838925, -11.75009321188407618, -6.453192476914276554 ) ) ;
#34482=CARTESIAN_POINT ( 'NONE',  ( 0.5804410086790514622, -38.35366574781983218, -26.99103880105228370 ) ) ;
#34488=LINE ( 'NONE', #6867, #61759 ) ;
#34490=VECTOR ( 'NONE', #10527, 1000.000000000000000 ) ;
#34498=ORIENTED_EDGE ( 'NONE', *, *, #58759, .T. ) ;
#34500=CARTESIAN_POINT ( 'NONE',  ( 4.960386119450145515, -26.33153931528478608, -34.94404816216851373 ) ) ;
#34504=CARTESIAN_POINT ( 'NONE',  ( 5.896782393890504181, 0.6784186533438157918, 20.10138888258240186 ) ) ;
#34507=CARTESIAN_POINT ( 'NONE',  ( 5.917102823773431552, 17.94639498788077248, -9.078360258918451109 ) ) ;
#34514=ADVANCED_FACE ( 'NONE', ( #60531 ), #41461, .F. ) ;
#34520=CIRCLE ( 'NONE', #2480, 42.08604991992415023 ) ;
#34523=CARTESIAN_POINT ( 'NONE',  ( 5.895881250540457863, 20.06765451668684008, 1.347933161250673972 ) ) ;
#34528=CARTESIAN_POINT ( 'NONE',  ( 3.782625744892852193, 5.920320325620187951, 41.61956164277864190 ) ) ;
#34537=ORIENTED_EDGE ( 'NONE', *, *, #48849, .T. ) ;
#34544=CARTESIAN_POINT ( 'NONE',  ( 5.901463166500145796, 3.331057597887998156, 19.83486641296556385 ) ) ;
#34555=CARTESIAN_POINT ( 'NONE',  ( 0.9791128995231614951, 36.06089395152650212, 21.35297079244299567 ) ) ;
#34556=ORIENTED_EDGE ( 'NONE', *, *, #17120, .F. ) ;
#34563=LINE ( 'NONE', #53627, #52040 ) ;
#34564=AXIS2_PLACEMENT_3D ( 'NONE', #5382, #695, #24508 ) ;
#34568=CARTESIAN_POINT ( 'NONE',  ( 4.962356264823609031, -35.98698831890617100, -21.82137185415387037 ) ) ;
#34569=CARTESIAN_POINT ( 'NONE',  ( 0.9762797500689124330, 41.90547441298052433, -0.5059638413352701702 ) ) ;
#34570=AXIS2_PLACEMENT_3D ( 'NONE', #42704, #37707, #18584 ) ;
#34571=ORIENTED_EDGE ( 'NONE', *, *, #60382, .T. ) ;
#34577=DIRECTION ( 'NONE',  ( -0.07906939808003032866, -0.9443293062557420736, -0.3193590324913493372 ) ) ;
#34580=CARTESIAN_POINT ( 'NONE',  ( 1.231276596079887931, 8.892602616354244205, -40.96581977363174332 ) ) ;
#34582=CARTESIAN_POINT ( 'NONE',  ( 0.9769922540276043676, -0.9586864849378278208, -41.89764283715400239 ) ) ;
#34586=CARTESIAN_POINT ( 'NONE',  ( 1.091591847532196402, 15.78966934106792053, -38.82583332081330241 ) ) ;
#34587=CARTESIAN_POINT ( 'NONE',  ( 5.917102823773431552, -17.30871814525804808, -10.24197218409408094 ) ) ;
#34592=CARTESIAN_POINT ( 'NONE',  ( 2.528100132419517365, 10.90475753638862066, 40.53813071300465509 ) ) ;
#34596=CARTESIAN_POINT ( 'NONE',  ( 3.782625744892855302, -25.80136476166733672, 33.18927056339735060 ) ) ;
#34597=CARTESIAN_POINT ( 'NONE',  ( 0.5806925824938499181, 10.33919002968644385, 45.74192291403583965 ) ) ;
#34599=ORIENTED_EDGE ( 'NONE', *, *, #28016, .T. ) ;
#34602=CARTESIAN_POINT ( 'NONE',  ( 0.6845945791218023269, 31.98229355120883710, -34.31529425661756960 ) ) ;
#34610=ORIENTED_EDGE ( 'NONE', *, *, #49430, .F. ) ;
#34614=CIRCLE ( 'NONE', #22625, 46.67105333295396719 ) ;
#34617=EDGE_CURVE ( 'NONE', #17781, #2801, #19812, .T. ) ;
#34618=AXIS2_PLACEMENT_3D ( 'NONE', #32747, #4505, #56218 ) ;
#34619=CARTESIAN_POINT ( 'NONE',  ( 0.9790850452238881729, -41.07895617916494757, -8.297993100349147610 ) ) ;
#34623=VECTOR ( 'NONE', #57582, 999.9999999999998863 ) ;
#34627=ORIENTED_EDGE ( 'NONE', *, *, #5659, .T. ) ;
#34629=CARTESIAN_POINT ( 'NONE',  ( 3.661933894777869014, 2.831097433652313367, 46.95333909609433221 ) ) ;
#34630=CARTESIAN_POINT ( 'NONE',  ( 0.5806925824938502512, -13.37132486740698134, 44.94919391528425479 ) ) ;
#34631=CARTESIAN_POINT ( 'NONE',  ( 5.895596859100789899, 3.341829471546786667, 19.83331437242874884 ) ) ;
#34632=ORIENTED_EDGE ( 'NONE', *, *, #17695, .T. ) ;
#34646=LINE ( 'NONE', #30236, #34490 ) ;
#34652=EDGE_CURVE ( 'NONE', #37577, #45332, #14335, .T. ) ;
#34657=ORIENTED_EDGE ( 'NONE', *, *, #10768, .T. ) ;
#34661=CARTESIAN_POINT ( 'NONE',  ( 2.528190830796657185, -31.93279228743793041, 27.24978739147064744 ) ) ;
#34662=CARTESIAN_POINT ( 'NONE',  ( 0.8560838555295158248, 23.34035564869604684, -40.68907263964262455 ) ) ;
#34669=CARTESIAN_POINT ( 'NONE',  ( 5.838029081930955932, 25.39899213859815319, 39.82406629786000707 ) ) ;
#34679=CARTESIAN_POINT ( 'NONE',  ( 5.894904586330512508, -9.666977479134521545, 17.63743060878054436 ) ) ;
#34680=EDGE_CURVE ( 'NONE', #55527, #20220, #350, .T. ) ;
#34682=CARTESIAN_POINT ( 'NONE',  ( 5.910764540655178756, 14.90587032029975667, -13.50245416446839286 ) ) ;
#34688=B_SPLINE_CURVE_WITH_KNOTS ( 'NONE', 3,
 ( #20262, #21169, #59679, #11787 ),
 .UNSPECIFIED., .F., .F.,
 ( 4, 4 ),
 ( 4.443059973708341306E-17, 0.005004948556313854741 ),
 .UNSPECIFIED. ) ;
#34689=CARTESIAN_POINT ( 'NONE',  ( 4.962356264823608143, 30.91935898304044272, 28.55221248765537467 ) ) ;
#34694=CARTESIAN_POINT ( 'NONE',  ( 1.092182651088187795, -27.65225184159188387, -31.49784361716628212 ) ) ;
#34695=CARTESIAN_POINT ( 'NONE',  ( 0.5848930533535030563, -25.08041605097284332, 39.62632727237867414 ) ) ;
#34696=ORIENTED_EDGE ( 'NONE', *, *, #38941, .T. ) ;
#34700=CARTESIAN_POINT ( 'NONE',  ( 0.5806925824938494740, -34.41156632303759011, 31.86010774524702072 ) ) ;
#34706=CARTESIAN_POINT ( 'NONE',  ( 4.962356264823608143, -40.70360067759239087, 10.69824704058788711 ) ) ;
#34707=CARTESIAN_POINT ( 'NONE',  ( 0.9787464366903563251, 40.37245734402069530, 11.24271679335978469 ) ) ;
#34709=ORIENTED_EDGE ( 'NONE', *, *, #45925, .F. ) ;
#34712=VERTEX_POINT ( 'NONE', #20118 ) ;
#34718=CARTESIAN_POINT ( 'NONE',  ( 4.962356264823608143, 0.000000000000000000, 0.000000000000000000 ) ) ;
#34721=EDGE_CURVE ( 'NONE', #57622, #3838, #39754, .T. ) ;
#34724=EDGE_LOOP ( 'NONE', ( #61355, #57311, #4859, #17416 ) ) ;
#34726=EDGE_CURVE ( 'NONE', #5232, #41497, #41306, .T. ) ;
#34728=CARTESIAN_POINT ( 'NONE',  ( 0.9762797500689124330, -7.469026406146330288, 41.23758515880862774 ) ) ;
#34733=CARTESIAN_POINT ( 'NONE',  ( 0.9785694773339252972, -30.93190758888828995, -28.27635935949227530 ) ) ;
#34738=ADVANCED_FACE ( 'NONE', ( #48916 ), #33952, .F. ) ;
#34740=ORIENTED_EDGE ( 'NONE', *, *, #33987, .T. ) ;
#34751=CARTESIAN_POINT ( 'NONE',  ( 1.000433927950262536, 4.849797705185330265, 41.62809315680488709 ) ) ;
#34756=CARTESIAN_POINT ( 'NONE',  ( 0.9754292580325142348, 3.614901275221697130, 41.75236467164950227 ) ) ;
#34758=CARTESIAN_POINT ( 'NONE',  ( 0.5804410086790514622, -7.261380058783999836, -46.33348909263461479 ) ) ;
#34760=ORIENTED_EDGE ( 'NONE', *, *, #21013, .T. ) ;
#34762=CARTESIAN_POINT ( 'NONE',  ( 0.5817217712918323347, -19.32622360567856390, -42.72858569098310255 ) ) ;
#34765=CARTESIAN_POINT ( 'NONE',  ( 5.895881250540457863, -17.30746725809839859, 10.24593864505115803 ) ) ;
#34767=CARTESIAN_POINT ( 'NONE',  ( 4.962356264823608143, -29.56943756613123497, 29.94802096775367772 ) ) ;
#34769=B_SPLINE_CURVE_WITH_KNOTS ( 'NONE', 3,
 ( #43604, #19474, #57039, #37666 ),
 .UNSPECIFIED., .F., .F.,
 ( 4, 4 ),
 ( 1.734723475976807094E-18, 0.004042984057420971958 ),
 .UNSPECIFIED. ) ;
#34772=VERTEX_POINT ( 'NONE', #31050 ) ;
#34775=CARTESIAN_POINT ( 'NONE',  ( 1.092182651088183798, 15.79015195333629329, 38.82566529671880318 ) ) ;
#34779=B_SPLINE_CURVE_WITH_KNOTS ( 'NONE', 3,
 ( #4683, #27291, #42640, #61700, #47328, #23830 ),
 .UNSPECIFIED., .F., .F.,
 ( 4, 2, 4 ),
 ( 0.000000000000000000, 0.0002291459268755702348, 0.0004582918537511404696 ),
 .UNSPECIFIED. ) ;
#34780=VERTEX_POINT ( 'NONE', #50458 ) ;
#34782=VERTEX_POINT ( 'NONE', #11969 ) ;
#34785=ORIENTED_EDGE ( 'NONE', *, *, #9816, .T. ) ;
#34787=ORIENTED_EDGE ( 'NONE', *, *, #2589, .F. ) ;
#34815=EDGE_CURVE ( 'NONE', #10104, #31868, #7216, .T. ) ;
#34824=CARTESIAN_POINT ( 'NONE',  ( 0.7764139734771235979, 17.68681948199870035, -43.44210961173568109 ) ) ;
#34833=DIRECTION ( 'NONE',  ( -1.000000000000000000, -0.000000000000000000, -0.000000000000000000 ) ) ;
#34835=CARTESIAN_POINT ( 'NONE',  ( 5.895596859100789899, 20.06773179721813349, 1.346968346847024822 ) ) ;
#34837=ORIENTED_EDGE ( 'NONE', *, *, #23352, .T. ) ;
#34846=ORIENTED_EDGE ( 'NONE', *, *, #9250, .F. ) ;
#34852=ORIENTED_EDGE ( 'NONE', *, *, #60712, .F. ) ;
#34855=VERTEX_POINT ( 'NONE', #30620 ) ;
#34857=CARTESIAN_POINT ( 'NONE',  ( 0.9790724872846771065, -17.60412452180793963, -38.03196037285134423 ) ) ;
#34867=CARTESIAN_POINT ( 'NONE',  ( 4.960386119450139297, 42.96877549456522871, 8.253532405581891496 ) ) ;
#34868=B_SPLINE_CURVE_WITH_KNOTS ( 'NONE', 3,
 ( #60505, #12020, #40224, #17623 ),
 .UNSPECIFIED., .F., .F.,
 ( 4, 4 ),
 ( 2.145734436807298343E-17, 0.005004948556313821781 ),
 .UNSPECIFIED. ) ;
#34869=ORIENTED_EDGE ( 'NONE', *, *, #54120, .F. ) ;
#34875=CARTESIAN_POINT ( 'NONE',  ( 3.661933894777899212, 45.82839639926445585, -10.60137955284777256 ) ) ;
#34880=CARTESIAN_POINT ( 'NONE',  ( 5.910764540655178756, 20.06626233353476962, -1.358806252166474771 ) ) ;
#34881=DIRECTION ( 'NONE',  ( -1.000000000000000000, -0.000000000000000000, -0.000000000000000000 ) ) ;
#34890=CARTESIAN_POINT ( 'NONE',  ( 0.9769922540276048117, 15.47377581453935314, -38.94732105199923211 ) ) ;
#34895=CARTESIAN_POINT ( 'NONE',  ( 0.9789233960466710016, 9.843146567393633362, -40.73633749473739130 ) ) ;
#34902=B_SPLINE_CURVE_WITH_KNOTS ( 'NONE', 3,
 ( #29946, #20860, #10536, #43776, #5192, #53427 ),
 .UNSPECIFIED., .F., .F.,
 ( 4, 2, 4 ),
 ( 5.485677294651095664E-18, 0.0002291472222819944263, 0.0004582944445639833774 ),
 .UNSPECIFIED. ) ;
#34905=EDGE_CURVE ( 'NONE', #50801, #26111, #5870, .T. ) ;
#34906=CARTESIAN_POINT ( 'NONE',  ( 0.6845945791218034371, -34.20288208893667559, -32.10248241996619356 ) ) ;
#34915=CARTESIAN_POINT ( 'NONE',  ( 4.962356264823598373, -19.84272732133986139, 37.11471096901200895 ) ) ;
#34921=CARTESIAN_POINT ( 'NONE',  ( 4.960386119450151732, -25.57375555595621464, -35.50238712307299949 ) ) ;
#34953=CARTESIAN_POINT ( 'NONE',  ( 0.5782707292762423457, -42.18185855468838952, -20.50432058323027462 ) ) ;
#34955=CARTESIAN_POINT ( 'NONE',  ( 0.5326698147273822848, 9.797174393178825657E-16, -8.000000000000000000 ) ) ;
#34956=EDGE_CURVE ( 'NONE', #30066, #37909, #60553, .T. ) ;
#34965=CARTESIAN_POINT ( 'NONE',  ( 5.895881250540457863, -11.93421320881288850, -16.18957185026512846 ) ) ;
#34966=CARTESIAN_POINT ( 'NONE',  ( 4.962356264823608143, 0.000000000000000000, 0.000000000000000000 ) ) ;
#34967=B_SPLINE_CURVE_WITH_KNOTS ( 'NONE', 3,
 ( #58540, #29433, #10653, #61973, #43259, #30053 ),
 .UNSPECIFIED., .F., .F.,
 ( 4, 2, 4 ),
 ( 3.496446946337351263E-18, 0.0002448709889506569398, 0.0004897419779013104102 ),
 .UNSPECIFIED. ) ;
#34980=EDGE_CURVE ( 'NONE', #46743, #11571, #35183, .T. ) ;
#34994=CARTESIAN_POINT ( 'NONE',  ( 0.7764146366350236361, -29.59659202960835600, 36.38794050096938548 ) ) ;
#35002=CARTESIAN_POINT ( 'NONE',  ( 2.618530812446111078, -6.426312013671601875, -46.56639671588451534 ) ) ;
#35006=VERTEX_POINT ( 'NONE', #51269 ) ;
#35007=EDGE_CURVE ( 'NONE', #40188, #32685, #11182, .T. ) ;
#35012=LINE ( 'NONE', #25586, #36631 ) ;
#35013=CARTESIAN_POINT ( 'NONE',  ( 4.960386119450134856, 23.93873278148718597, 36.62476672265492539 ) ) ;
#35015=CARTESIAN_POINT ( 'NONE',  ( 0.9762797500689124330, -40.96497924994823592, 8.842808390834631993 ) ) ;
#35019=CARTESIAN_POINT ( 'NONE',  ( 0.6064782688330858651, -46.83443355140296660, 2.422866141161769349 ) ) ;
#35023=CARTESIAN_POINT ( 'NONE',  ( 0.5797568599927140909, 46.89167813021173004, 0.6291508591968832942 ) ) ;
#35032=VERTEX_POINT ( 'NONE', #37207 ) ;
#35033=CARTESIAN_POINT ( 'NONE',  ( 0.9788927965476041937, 4.335847588109925432, 41.68377428118113670 ) ) ;
#35034=EDGE_CURVE ( 'NONE', #47897, #6436, #10544, .T. ) ;
#35037=CARTESIAN_POINT ( 'NONE',  ( 0.9790320750461898314, 36.10202571947430528, -21.28334728121043895 ) ) ;
#35041=ADVANCED_FACE ( 'NONE', ( #36582 ), #59535, .F. ) ;
#35042=CARTESIAN_POINT ( 'NONE',  ( 4.962356264823608143, 34.94214251265138671, -23.45809613945485950 ) ) ;
#35046=EDGE_CURVE ( 'NONE', #34160, #7089, #18398, .T. ) ;
#35052=CARTESIAN_POINT ( 'NONE',  ( 0.9775691876210972353, -26.76781511548317383, -32.24620571374718736 ) ) ;
#35053=CARTESIAN_POINT ( 'NONE',  ( 0.9783242366443545279, 38.47773455156494293, 16.60718019369418386 ) ) ;
#35056=ORIENTED_EDGE ( 'NONE', *, *, #10443, .F. ) ;
#35059=EDGE_CURVE ( 'NONE', #19501, #45323, #56126, .T. ) ;
#35060=CARTESIAN_POINT ( 'NONE',  ( 3.376099380956842921, -6.821144471874572623, 11.54038005118904131 ) ) ;
#35063=CARTESIAN_POINT ( 'NONE',  ( 5.896782393890504181, -17.30187591025955030, -10.25529994022567237 ) ) ;
#35068=CARTESIAN_POINT ( 'NONE',  ( 1.231276596079887264, -0.5545928549379750550, 41.91621640586514985 ) ) ;
#35071=CARTESIAN_POINT ( 'NONE',  ( 3.376099380956838925, 12.80002687883560419, 3.983427611135065494 ) ) ;
#35090=ADVANCED_FACE ( 'NONE', ( #33739 ), #19496, .F. ) ;
#35096=VERTEX_POINT ( 'NONE', #13705 ) ;
#35101=CARTESIAN_POINT ( 'NONE',  ( 5.895881250540457863, 16.58446435569113220, 11.37906954206324173 ) ) ;
#35106=VERTEX_POINT ( 'NONE', #14942 ) ;
#35107=CARTESIAN_POINT ( 'NONE',  ( 5.896782393890504181, 16.57826022845085134, 11.38803647148080778 ) ) ;
#35115=ORIENTED_EDGE ( 'NONE', *, *, #30610, .T. ) ;
#35116=CARTESIAN_POINT ( 'NONE',  ( 0.5837157313716019313, -46.78513062885863860, -3.223137543242450054 ) ) ;
#35122=CARTESIAN_POINT ( 'NONE',  ( 0.9762797500689124330, 40.55021165774366665, -10.58324712448374605 ) ) ;
#35123=ORIENTED_EDGE ( 'NONE', *, *, #8137, .T. ) ;
#35124=CARTESIAN_POINT ( 'NONE',  ( 0.9780106845699478857, -12.11659434839023142, -40.11881588297436707 ) ) ;
#35132=EDGE_CURVE ( 'NONE', #58688, #59308, #52162, .T. ) ;
#35133=CARTESIAN_POINT ( 'NONE',  ( 4.960386119450151732, 27.88794419592712615, 33.71496749512290592 ) ) ;
#35141=CARTESIAN_POINT ( 'NONE',  ( 0.7056313189692707821, -6.968533899719071556, 46.38090317410846097 ) ) ;
#35145=CARTESIAN_POINT ( 'NONE',  ( 4.956445790444027999, 20.31112743693101663, -42.48524629068760561 ) ) ;
#35152=B_SPLINE_CURVE_WITH_KNOTS ( 'NONE', 3,
 ( #13467, #13785, #46676, #51344, #31955, #60736 ),
 .UNSPECIFIED., .F., .F.,
 ( 4, 2, 4 ),
 ( 1.738108305489988542E-18, 0.0002291459268755697198, 0.0004582918537511377049 ),
 .UNSPECIFIED. ) ;
#35163=EDGE_CURVE ( 'NONE', #52281, #43273, #15761, .T. ) ;
#35166=CARTESIAN_POINT ( 'NONE',  ( 3.376099380956838925, 6.842217874692699375, -11.52789825541945312 ) ) ;
#35171=CARTESIAN_POINT ( 'NONE',  ( 1.157643937452368599, -21.85425515765621540, 35.76861481940291299 ) ) ;
#35177=ORIENTED_EDGE ( 'NONE', *, *, #18245, .F. ) ;
#35181=CARTESIAN_POINT ( 'NONE',  ( 0.9787284016396613495, 36.15334032947335174, 21.19603693972311476 ) ) ;
#35183=B_SPLINE_CURVE_WITH_KNOTS ( 'NONE', 3,
 ( #3041, #36906, #12787, #41293, #50652, #45999 ),
 .UNSPECIFIED., .F., .F.,
 ( 4, 2, 4 ),
 ( 4.770489558936219510E-18, 0.0002291472222819939926, 0.0004582944445639832148 ),
 .UNSPECIFIED. ) ;
#35185=CARTESIAN_POINT ( 'NONE',  ( 4.956445790444018229, -10.39006634428234577, -45.93021414603951058 ) ) ;
#35188=VERTEX_POINT ( 'NONE', #52250 ) ;
#35191=CARTESIAN_POINT ( 'NONE',  ( 5.901463166500146684, 20.06674442072660369, -1.357806574543771960 ) ) ;
#35194=ORIENTED_EDGE ( 'NONE', *, *, #57065, .F. ) ;
#35197=CARTESIAN_POINT ( 'NONE',  ( 0.9788927965476027504, 14.92997836612718210, -39.15906483330202548 ) ) ;
#35199=EDGE_CURVE ( 'NONE', #50474, #36178, #21744, .T. ) ;
#35203=EDGE_CURVE ( 'NONE', #6434, #14965, #53131, .T. ) ;
#35209=DIRECTION ( 'NONE',  ( 0.07500201931887538753, -0.7028774959225082553, 0.7073456883474977808 ) ) ;
#35210=CARTESIAN_POINT ( 'NONE',  ( 0.5782707292762423457, 33.12197115878034026, 33.20649605520795689 ) ) ;
#35214=CARTESIAN_POINT ( 'NONE',  ( 0.5806925824938502512, -14.41498975133575300, -44.62544602368080859 ) ) ;
#35222=CARTESIAN_POINT ( 'NONE',  ( 0.8560838555295223751, -24.46533024579953164, 40.02274915651970133 ) ) ;
#35224=CARTESIAN_POINT ( 'NONE',  ( 4.958415959904820092, -26.53498967168899725, -36.86595010230982439 ) ) ;
#35231=EDGE_CURVE ( 'NONE', #47413, #18906, #9039, .T. ) ;
#35234=VERTEX_POINT ( 'NONE', #9655 ) ;
#35249=ORIENTED_EDGE ( 'NONE', *, *, #53113, .T. ) ;
#35256=CARTESIAN_POINT ( 'NONE',  ( 0.6845945791218034371, -20.52768236698797111, 42.17843972166340905 ) ) ;
#35260=CARTESIAN_POINT ( 'NONE',  ( 4.956445790444041322, 46.25174887658561573, -8.849507104743011610 ) ) ;
#35267=CARTESIAN_POINT ( 'NONE',  ( 5.917102823773431552, -19.93133248418637749, 2.689182674449420052 ) ) ;
#35269=CARTESIAN_POINT ( 'NONE',  ( 0.5804410086790514622, -2.113107284888617432, -46.85141011173460157 ) ) ;
#35271=DIRECTION ( 'NONE',  ( 0.000000000000000000, 0.000000000000000000, 1.000000000000000000 ) ) ;
#35280=CARTESIAN_POINT ( 'NONE',  ( 0.9785694773339237429, 41.50447357468266318, 5.806382609089985714 ) ) ;
#35292=CARTESIAN_POINT ( 'NONE',  ( 0.9762797500689124330, -7.469026406146330288, 41.23758515880862774 ) ) ;
#35293=CARTESIAN_POINT ( 'NONE',  ( 5.894904586330512508, 8.465111963867252953, 18.24476065890792142 ) ) ;
#35294=CARTESIAN_POINT ( 'NONE',  ( 0.6064515330803548210, -29.73185795686339716, 36.26776748670900474 ) ) ;
#35305=EDGE_CURVE ( 'NONE', #36038, #2801, #2305, .T. ) ;
#35315=B_SPLINE_CURVE_WITH_KNOTS ( 'NONE', 3,
 ( #29516, #15128, #39565, #10737 ),
 .UNSPECIFIED., .F., .F.,
 ( 4, 4 ),
 ( 0.000000000000000000, 0.004447772540403782497 ),
 .UNSPECIFIED. ) ;
#35317=CARTESIAN_POINT ( 'NONE',  ( 0.5804410086790514622, -25.69437916690408130, 39.23415261073905924 ) ) ;
#35319=CARTESIAN_POINT ( 'NONE',  ( 4.956445790444005794, -28.36659270909926533, -37.58822246682746737 ) ) ;
#35325=CARTESIAN_POINT ( 'NONE',  ( 0.7764139734771234869, -46.85094005902467273, 2.242740843821329211 ) ) ;
#35327=CARTESIAN_POINT ( 'NONE',  ( 4.962356264823608143, 26.83784316460287300, 32.41860225448540689 ) ) ;
#35328=DIRECTION ( 'NONE',  ( -1.000000000000000000, -0.000000000000000000, -0.000000000000000000 ) ) ;
#35333=AXIS2_PLACEMENT_3D ( 'NONE', #54443, #30652, #49769 ) ;
#35338=DIRECTION ( 'NONE',  ( 0.000000000000000000, 0.000000000000000000, 1.000000000000000000 ) ) ;
#35340=CARTESIAN_POINT ( 'NONE',  ( 0.9769922540276043676, 3.754999534460876198, 41.74004712003000606 ) ) ;
#35351=ORIENTED_EDGE ( 'NONE', *, *, #25870, .T. ) ;
#35358=CARTESIAN_POINT ( 'NONE',  ( 0.9772918015221174759, 38.41934892684628977, -16.74187814398117879 ) ) ;
#35360=ADVANCED_FACE ( 'NONE', ( #9980 ), #24173, .T. ) ;
#35364=CARTESIAN_POINT ( 'NONE',  ( 4.962356264823601926, -38.91448554252674796, -16.02805081171206680 ) ) ;
#35365=CARTESIAN_POINT ( 'NONE',  ( 3.661933894777873455, -46.43415008926496768, 7.516706089722269724 ) ) ;
#35367=CARTESIAN_POINT ( 'NONE',  ( 0.5806925824938499181, 36.46274162637902094, 29.49052111156212774 ) ) ;
#35369=CARTESIAN_POINT ( 'NONE',  ( 0.5832655196449145762, 45.16907574789987478, 12.60911491952589358 ) ) ;
#35373=CARTESIAN_POINT ( 'NONE',  ( 0.5804410086790514622, 40.62771722849963396, 23.42879520283684514 ) ) ;
#35378=CARTESIAN_POINT ( 'NONE',  ( 3.782542959838389951, -28.43539247177547935, 30.96233693332376191 ) ) ;
#35383=ORIENTED_EDGE ( 'NONE', *, *, #24907, .F. ) ;
#35384=EDGE_CURVE ( 'NONE', #36659, #30629, #24687, .T. ) ;
#35386=CARTESIAN_POINT ( 'NONE',  ( 0.5834584762367742705, -19.57482590732785255, -42.61528105868828220 ) ) ;
#35388=CARTESIAN_POINT ( 'NONE',  ( 0.5804410086790514622, 32.20888702807411619, -34.08969709850992302 ) ) ;
#35390=VERTEX_POINT ( 'NONE', #58178 ) ;
#35395=CARTESIAN_POINT ( 'NONE',  ( 4.956445790443998689, -16.41925925744477510, 44.13554095710679093 ) ) ;
#35402=ORIENTED_EDGE ( 'NONE', *, *, #33919, .T. ) ;
#35410=CARTESIAN_POINT ( 'NONE',  ( 0.8554163680231708922, -38.15570339590799165, -27.30105806512478850 ) ) ;
#35411=CARTESIAN_POINT ( 'NONE',  ( 0.8554163680231720024, -38.15570339590837534, 27.30105806512423428 ) ) ;
#35414=DIRECTION ( 'NONE',  ( -1.000000000000000000, -0.000000000000000000, -0.000000000000000000 ) ) ;
#35415=CARTESIAN_POINT ( 'NONE',  ( 0.5804410086790514622, -38.97211966759144985, -26.09010809617945270 ) ) ;
#35417=CARTESIAN_POINT ( 'NONE',  ( 0.5835871038041848813, 32.69977443625123925, -33.61486582926951883 ) ) ;
#35423=VECTOR ( 'NONE', #17326, 1000.000000000000114 ) ;
#35438=EDGE_LOOP ( 'NONE', ( #20024, #35625, #15515, #14009 ) ) ;
#35443=EDGE_CURVE ( 'NONE', #15172, #54983, #34403, .T. ) ;
#35444=CARTESIAN_POINT ( 'NONE',  ( 4.958415959904820980, 28.93810772186849078, 35.01128211448664018 ) ) ;
#35449=CARTESIAN_POINT ( 'NONE',  ( 3.661933894777875231, -23.70323884901255695, -40.62988595871659214 ) ) ;
#35453=EDGE_CURVE ( 'NONE', #44029, #20909, #20607, .T. ) ;
#35456=ORIENTED_EDGE ( 'NONE', *, *, #60517, .T. ) ;
#35470=FACE_OUTER_BOUND ( 'NONE', #49725, .T. ) ;
#35472=EDGE_LOOP ( 'NONE', ( #5083, #51763, #7770, #20292 ) ) ;
#35478=DIRECTION ( 'NONE',  ( 0.07906939808003034253, 0.9940710100007911221, 0.07463817631258570784 ) ) ;
#35495=VECTOR ( 'NONE', #40544, 1000.000000000000000 ) ;
#35507=ADVANCED_FACE ( 'NONE', ( #16217 ), #3914, .F. ) ;
#35513=VECTOR ( 'NONE', #42520, 999.9999999999998863 ) ;
#35515=ADVANCED_FACE ( 'NONE', ( #7402 ), #45232, .T. ) ;
#35520=CARTESIAN_POINT ( 'NONE',  ( 5.896278296736517710, -13.97836643676194157, -14.46140558085523509 ) ) ;
#35524=CARTESIAN_POINT ( 'NONE',  ( 0.5832655196449125778, -13.67655705356959395, -44.85740708215072914 ) ) ;
#35527=DIRECTION ( 'NONE',  ( 0.000000000000000000, 0.000000000000000000, 1.000000000000000000 ) ) ;
#35530=CARTESIAN_POINT ( 'NONE',  ( 2.528100132419516033, 38.15966356554061178, -17.49553815110665056 ) ) ;
#35542=EDGE_CURVE ( 'NONE', #51245, #50421, #54398, .T. ) ;
#35544=AXIS2_PLACEMENT_3D ( 'NONE', #56540, #130, #23355 ) ;
#35547=CARTESIAN_POINT ( 'NONE',  ( 0.5782707292762442330, -44.53844888462766249, 14.69907904118576170 ) ) ;
#35549=CARTESIAN_POINT ( 'NONE',  ( 0.5835871038041867687, -38.58555166310420503, -26.65313594598980629 ) ) ;
#35550=ORIENTED_EDGE ( 'NONE', *, *, #56374, .T. ) ;
#35553=EDGE_CURVE ( 'NONE', #54938, #32404, #7161, .T. ) ;
#35555=ADVANCED_FACE ( 'NONE', ( #22148 ), #12364, .F. ) ;
#35559=VERTEX_POINT ( 'NONE', #27457 ) ;
#35560=CARTESIAN_POINT ( 'NONE',  ( 1.231276596079881047, 29.74482033789362134, -29.53849072116746655 ) ) ;
#35568=CARTESIAN_POINT ( 'NONE',  ( 2.528100132419519142, 41.74865220873254401, 4.393610973489210814 ) ) ;
#35574=ORIENTED_EDGE ( 'NONE', *, *, #59546, .F. ) ;
#35576=CARTESIAN_POINT ( 'NONE',  ( 0.7056313189692721144, 5.532685211636314548, 46.57400603669923811 ) ) ;
#35577=ORIENTED_EDGE ( 'NONE', *, *, #54635, .F. ) ;
#35579=CARTESIAN_POINT ( 'NONE',  ( 5.901463166500146684, -19.93124146756676396, 2.695085138206950504 ) ) ;
#35581=DIRECTION ( 'NONE',  ( -0.07500201931887527651, 0.7028774959224980412, 0.7073456883475078838 ) ) ;
#35583=EDGE_CURVE ( 'NONE', #13148, #24845, #9636, .T. ) ;
#35587=CARTESIAN_POINT ( 'NONE',  ( 0.5848930533535030563, 32.47085631013385409, 33.83661586025115042 ) ) ;
#35595=EDGE_CURVE ( 'NONE', #37991, #29994, #49243, .T. ) ;
#35596=CARTESIAN_POINT ( 'NONE',  ( 0.9787464366903551038, 14.89694933529458609, 39.17160825639061983 ) ) ;
#35598=EDGE_CURVE ( 'NONE', #40951, #34089, #53009, .T. ) ;
#35599=CARTESIAN_POINT ( 'NONE',  ( 0.8560838555295223751, 16.00311602465208694, -44.09391240957481273 ) ) ;
#35601=CARTESIAN_POINT ( 'NONE',  ( 0.9754292580325150119, -34.87747760158924848, 23.23551211087558244 ) ) ;
#35604=CARTESIAN_POINT ( 'NONE',  ( 5.901463166500145796, 5.972693816097719655, -19.20533256467548711 ) ) ;
#35611=CARTESIAN_POINT ( 'NONE',  ( 0.9769922540276041456, 29.45054638516204903, -29.81605058859312152 ) ) ;
#35614=ORIENTED_EDGE ( 'NONE', *, *, #37418, .T. ) ;
#35621=CARTESIAN_POINT ( 'NONE',  ( 0.5806925824938499181, 32.20670061096218006, 34.08739940358331921 ) ) ;
#35623=( BOUNDED_SURFACE ( )  B_SPLINE_SURFACE ( 3, 1, ( 
 ( #15350, #34458 ),
 ( #53529, #10645 ),
 ( #21582, #26272 ),
 ( #45407, #16576 ) ),
 .UNSPECIFIED., .F., .F., .F. ) 
 B_SPLINE_SURFACE_WITH_KNOTS ( ( 4, 4 ),
 ( 2, 2 ),
 ( 0.000000000000000000, 1.000000000000000000 ),
 ( 0.000000000000000000, 1.000000000000000000 ),
 .UNSPECIFIED. ) 
 GEOMETRIC_REPRESENTATION_ITEM ( )  RATIONAL_B_SPLINE_SURFACE ( (
 ( 1.000000000000000000, 1.000000000000000000),
 ( 0.9952954269826590483, 0.8620686068821307169),
 ( 0.9952954269826590483, 0.8620686068821307169),
 ( 1.000000000000000000, 1.000000000000000000) ) ) 
 REPRESENTATION_ITEM ( '' )  SURFACE ( )  );
#35625=ORIENTED_EDGE ( 'NONE', *, *, #38299, .F. ) ;
#35638=CARTESIAN_POINT ( 'NONE',  ( 0.5817217712918332229, -35.08429077047930633, 31.11796097338052292 ) ) ;
#35642=CARTESIAN_POINT ( 'NONE',  ( 4.956445790443988031, 0.000000000000000000, 0.000000000000000000 ) ) ;
#35643=CARTESIAN_POINT ( 'NONE',  ( 0.8560838555295158248, 46.35895890951125153, 7.156798369940231552 ) ) ;
#35651=CARTESIAN_POINT ( 'NONE',  ( 0.9790320750461913857, 4.109333313230322027, 41.70672022903462306 ) ) ;
#35652=EDGE_LOOP ( 'NONE', ( #32313, #42857, #58008, #23909 ) ) ;
#35654=CARTESIAN_POINT ( 'NONE',  ( 0.9762797500689124330, 25.26481495167865532, 33.43671500974846822 ) ) ;
#35658=CARTESIAN_POINT ( 'NONE',  ( 5.896782393890504181, 14.92098591823879872, -13.48666994130618235 ) ) ;
#35660=CARTESIAN_POINT ( 'NONE',  ( 0.5804410086790514622, 16.34485605153927068, 43.95867983128994183 ) ) ;
#35663=EDGE_CURVE ( 'NONE', #53844, #5378, #23164, .T. ) ;
#35665=LINE ( 'NONE', #26860, #51482 ) ;
#35671=ORIENTED_EDGE ( 'NONE', *, *, #29156, .T. ) ;
#35681=DIRECTION ( 'NONE',  ( -0.07500201931887529039, -0.5251354798924672274, 0.8477071574878906057 ) ) ;
#35688=CARTESIAN_POINT ( 'NONE',  ( 4.291220156522059348, -17.85566473792906450, -43.59546116366212942 ) ) ;
#35693=CARTESIAN_POINT ( 'NONE',  ( 0.9789233960466705575, 9.587306714400842367, 40.79730722481993865 ) ) ;
#35699=( BOUNDED_SURFACE ( )  B_SPLINE_SURFACE ( 3, 1, ( 
 ( #47146, #23329 ),
 ( #28328, #36513 ),
 ( #18635, #46844 ),
 ( #47444, #46525 ) ),
 .UNSPECIFIED., .F., .F., .F. ) 
 B_SPLINE_SURFACE_WITH_KNOTS ( ( 4, 4 ),
 ( 2, 2 ),
 ( 0.000000000000000000, 1.000000000000000000 ),
 ( 0.000000000000000000, 1.000000000000000000 ),
 .UNSPECIFIED. ) 
 GEOMETRIC_REPRESENTATION_ITEM ( )  RATIONAL_B_SPLINE_SURFACE ( (
 ( 1.000000000000000000, 1.000000000000000000),
 ( 0.7282232189291693025, 0.9929344683865674037),
 ( 0.7282232189291693025, 0.9929344683865674037),
 ( 1.000000000000000000, 1.000000000000000000) ) ) 
 REPRESENTATION_ITEM ( '' )  SURFACE ( )  );
#35709=CARTESIAN_POINT ( 'NONE',  ( 4.962356264823603702, 26.83784316460332420, -32.41860225448503030 ) ) ;
#35710=ORIENTED_EDGE ( 'NONE', *, *, #10296, .T. ) ;
#35713=CARTESIAN_POINT ( 'NONE',  ( 0.8560838555295158248, 46.60258007729424889, -5.345312359545362213 ) ) ;
#35718=ORIENTED_EDGE ( 'NONE', *, *, #10222, .F. ) ;
#35723=( BOUNDED_SURFACE ( )  B_SPLINE_SURFACE ( 3, 1, ( 
 ( #52798, #53406 ),
 ( #23684, #16761 ),
 ( #35875, #7322 ),
 ( #45583, #40286 ) ),
 .UNSPECIFIED., .F., .F., .F. ) 
 B_SPLINE_SURFACE_WITH_KNOTS ( ( 4, 4 ),
 ( 2, 2 ),
 ( 0.000000000000000000, 1.000000000000000000 ),
 ( 0.000000000000000000, 1.000000000000000000 ),
 .UNSPECIFIED. ) 
 GEOMETRIC_REPRESENTATION_ITEM ( )  RATIONAL_B_SPLINE_SURFACE ( (
 ( 1.000000000000000000, 1.000000000000000000),
 ( 0.9952954269826590483, 0.8620686068821307169),
 ( 0.9952954269826590483, 0.8620686068821307169),
 ( 1.000000000000000000, 1.000000000000000000) ) ) 
 REPRESENTATION_ITEM ( '' )  SURFACE ( )  );
#35735=CARTESIAN_POINT ( 'NONE',  ( 0.9762797500689124330, -17.18051571332144434, 38.22505284509125545 ) ) ;
#35737=B_SPLINE_CURVE_WITH_KNOTS ( 'NONE', 3,
 ( #56344, #52262, #8740, #42587, #52573, #28460 ),
 .UNSPECIFIED., .F., .F.,
 ( 4, 2, 4 ),
 ( 7.023086426956682172E-18, 0.0002448709889506552593, 0.0004897419779013034713 ),
 .UNSPECIFIED. ) ;
#35743=VERTEX_POINT ( 'NONE', #798 ) ;
#35747=EDGE_CURVE ( 'NONE', #41171, #33079, #26838, .T. ) ;
#35748=VECTOR ( 'NONE', #16516, 999.9999999999998863 ) ;
#35751=CARTESIAN_POINT ( 'NONE',  ( 3.661921753702032323, 42.53630361713042163, -20.08218111723261146 ) ) ;
#35754=EDGE_CURVE ( 'NONE', #37975, #57176, #22404, .T. ) ;
#35769=CARTESIAN_POINT ( 'NONE',  ( 4.962356264823608143, 41.15374796524913847, 8.809348799718396350 ) ) ;
#35778=VERTEX_POINT ( 'NONE', #39660 ) ;
#35781=EDGE_CURVE ( 'NONE', #59710, #46145, #43436, .T. ) ;
#35790=ORIENTED_EDGE ( 'NONE', *, *, #29576, .F. ) ;
#35792=EDGE_CURVE ( 'NONE', #52112, #19096, #41849, .T. ) ;
#35794=CARTESIAN_POINT ( 'NONE',  ( 0.8560838555295158248, 11.76118766017326323, -45.40977096290972526 ) ) ;
#35795=( BOUNDED_SURFACE ( )  B_SPLINE_SURFACE ( 3, 1, ( 
 ( #49961, #17077 ),
 ( #22931, #45284 ),
 ( #56725, #26148 ),
 ( #31154, #35876 ) ),
 .UNSPECIFIED., .F., .F., .F. ) 
 B_SPLINE_SURFACE_WITH_KNOTS ( ( 4, 4 ),
 ( 2, 2 ),
 ( 0.000000000000000000, 1.000000000000000000 ),
 ( 0.000000000000000000, 1.000000000000000000 ),
 .UNSPECIFIED. ) 
 GEOMETRIC_REPRESENTATION_ITEM ( )  RATIONAL_B_SPLINE_SURFACE ( (
 ( 1.000000000000000000, 1.000000000000000000),
 ( 0.9729067724841187204, 0.9999501103223794596),
 ( 0.9729067724841187204, 0.9999501103223794596),
 ( 1.000000000000000000, 1.000000000000000000) ) ) 
 REPRESENTATION_ITEM ( '' )  SURFACE ( )  );
#35799=CARTESIAN_POINT ( 'NONE',  ( 5.910764540655178756, -19.39351348817917753, 5.328496321944423464 ) ) ;
#35806=CARTESIAN_POINT ( 'NONE',  ( 0.8560838555295158248, -46.73345513967312570, -4.044379407262746362 ) ) ;
#35807=CARTESIAN_POINT ( 'NONE',  ( 0.5782707292762423457, -14.58551739541048953, -44.57576736317388111 ) ) ;
#35820=EDGE_CURVE ( 'NONE', #31862, #60706, #19193, .T. ) ;
#35822=CARTESIAN_POINT ( 'NONE',  ( 4.962356264823602814, 6.570263404307167932, -41.57002810511882274 ) ) ;
#35823=EDGE_CURVE ( 'NONE', #46743, #58288, #21683, .T. ) ;
#35828=VECTOR ( 'NONE', #53197, 1000.000000000000114 ) ;
#35831=CARTESIAN_POINT ( 'NONE',  ( 3.376099380956838925, -10.24506893069234614, 8.645631627442240230 ) ) ;
#35832=ADVANCED_FACE ( 'NONE', ( #49332 ), #9781, .T. ) ;
#35833=CARTESIAN_POINT ( 'NONE',  ( 3.376099380956842921, -10.24506893069222002, -8.645631627442380562 ) ) ;
#35836=CARTESIAN_POINT ( 'NONE',  ( 0.9772918015221170318, -22.19949068734035436, 35.54601903129756124 ) ) ;
#35843=CONICAL_SURFACE ( 'NONE', #59832, 42.08604991992415023, 1.569615340895231137 ) ;
#35848=ORIENTED_EDGE ( 'NONE', *, *, #17850, .T. ) ;
#35862=ORIENTED_EDGE ( 'NONE', *, *, #20449, .F. ) ;
#35863=EDGE_CURVE ( 'NONE', #50427, #37103, #32072, .T. ) ;
#35869=FACE_OUTER_BOUND ( 'NONE', #14689, .T. ) ;
#35871=CARTESIAN_POINT ( 'NONE',  ( 0.8560838555295223751, 16.00311602465208694, -44.09391240957481273 ) ) ;
#35875=CARTESIAN_POINT ( 'NONE',  ( 5.895881250540457863, 5.963300346357911508, -19.20850672455900821 ) ) ;
#35876=CARTESIAN_POINT ( 'NONE',  ( 0.5804410086790514622, -35.14691939471192939, 31.05179397260356922 ) ) ;
#35877=CARTESIAN_POINT ( 'NONE',  ( 4.291220156522060236, 44.81988414002825039, -14.51092633087706574 ) ) ;
#35883=CIRCLE ( 'NONE', #24873, 47.09074272231896430 ) ;
#35884=VERTEX_POINT ( 'NONE', #46433 ) ;
#35891=CARTESIAN_POINT ( 'NONE',  ( 3.376099380956842921, -13.03750648666903089, 3.119584626537648564 ) ) ;
#35893=CARTESIAN_POINT ( 'NONE',  ( 5.895596859100789899, -9.669028665050088733, -17.63627137143583568 ) ) ;
#35895=DIRECTION ( 'NONE',  ( 0.000000000000000000, 0.000000000000000000, 1.000000000000000000 ) ) ;
#35898=CARTESIAN_POINT ( 'NONE',  ( 2.618530812446115519, 42.70834099002650674, -19.63986759318458297 ) ) ;
#35900=ORIENTED_EDGE ( 'NONE', *, *, #53573, .F. ) ;
#35907=B_SPLINE_CURVE_WITH_KNOTS ( 'NONE', 3,
 ( #19054, #52220, #5218, #37235, #43479, #23423 ),
 .UNSPECIFIED., .F., .F.,
 ( 4, 2, 4 ),
 ( 1.569810930355577320E-17, 0.0002448709889506590540, 0.0004897419779013023871 ),
 .UNSPECIFIED. ) ;
#35909=CARTESIAN_POINT ( 'NONE',  ( 0.9769922540276054779, -31.37627228715922456, 27.78238817035295938 ) ) ;
#35910=CARTESIAN_POINT ( 'NONE',  ( 0.6845945791218034371, -42.25019583682509250, 20.37958469802246597 ) ) ;
#35915=CARTESIAN_POINT ( 'NONE',  ( 5.838029081930955932, 44.61407408311357159, 15.51288019225876447 ) ) ;
#35916=ORIENTED_EDGE ( 'NONE', *, *, #24714, .T. ) ;
#35917=ORIENTED_EDGE ( 'NONE', *, *, #23972, .T. ) ;
#35927=VERTEX_POINT ( 'NONE', #18230 ) ;
#35932=LINE ( 'NONE', #16501, #19957 ) ;
#35935=B_SPLINE_CURVE_WITH_KNOTS ( 'NONE', 3,
 ( #33573, #20391, #33884, #10065, #43601, #53267, #24778, #10379, #43921, #20093, #39211, #58263, #16008, #26315, #26622, #54809, #31021, #21007, #35122 ),
 .UNSPECIFIED., .F., .F.,
 ( 4, 3, 3, 3, 3, 3, 4 ),
 ( 8.674294979774126656E-18, 0.0002732106629380573362, 0.0004098138914053730468, 0.0005464171197651428950, 0.0006830203481512527302, 0.0008196235766963571277, 0.001011968216111138342 ),
 .UNSPECIFIED. ) ;
#35940=ORIENTED_EDGE ( 'NONE', *, *, #5279, .F. ) ;
#35941=( BOUNDED_SURFACE ( )  B_SPLINE_SURFACE ( 3, 1, ( 
 ( #46420, #8476 ),
 ( #10, #19151 ),
 ( #27917, #32938 ),
 ( #37644, #23833 ) ),
 .UNSPECIFIED., .F., .F., .F. ) 
 B_SPLINE_SURFACE_WITH_KNOTS ( ( 4, 4 ),
 ( 2, 2 ),
 ( 0.000000000000000000, 1.000000000000000000 ),
 ( 0.000000000000000000, 1.000000000000000000 ),
 .UNSPECIFIED. ) 
 GEOMETRIC_REPRESENTATION_ITEM ( )  RATIONAL_B_SPLINE_SURFACE ( (
 ( 1.000000000000000000, 1.000000000000000000),
 ( 0.7282232189291693025, 0.9929344683865674037),
 ( 0.7282232189291693025, 0.9929344683865674037),
 ( 1.000000000000000000, 1.000000000000000000) ) ) 
 REPRESENTATION_ITEM ( '' )  SURFACE ( )  );
#35945=ORIENTED_EDGE ( 'NONE', *, *, #16758, .F. ) ;
#35947=ADVANCED_FACE ( 'NONE', ( #5017 ), #34314, .F. ) ;
#35953=CARTESIAN_POINT ( 'NONE',  ( 0.5806925824938499181, -20.23436166722466467, 42.30594485723624132 ) ) ;
#35964=ORIENTED_EDGE ( 'NONE', *, *, #52308, .F. ) ;
#35966=CARTESIAN_POINT ( 'NONE',  ( 0.9784957157296372277, 25.04636459167678098, 33.60078388569483820 ) ) ;
#35968=VERTEX_POINT ( 'NONE', #29155 ) ;
#35969=CARTESIAN_POINT ( 'NONE',  ( 5.838029081930955932, -32.85120734338305226, 33.93911068715524237 ) ) ;
#35972=VERTEX_POINT ( 'NONE', #33566 ) ;
#35984=CARTESIAN_POINT ( 'NONE',  ( 0.8560838555295158248, -46.14148336882297485, 8.446084690930096173 ) ) ;
#35988=CARTESIAN_POINT ( 'NONE',  ( 0.5834584762367743815, 36.69082382167502487, 29.20649647424346185 ) ) ;
#35990=CARTESIAN_POINT ( 'NONE',  ( 0.5830081025819929819, 45.30112779307347637, 12.12599913647833105 ) ) ;
#35998=CARTESIAN_POINT ( 'NONE',  ( 3.782542959838393948, -33.65309862801750285, -25.19338814311196018 ) ) ;
#36003=CARTESIAN_POINT ( 'NONE',  ( 2.528190830796657185, -28.01583037401040244, 31.26287550126642145 ) ) ;
#36004=CARTESIAN_POINT ( 'NONE',  ( 5.895881250540457863, -19.93280900245019183, 2.685294561150000092 ) ) ;
#36006=CARTESIAN_POINT ( 'NONE',  ( 1.092182651088184020, -7.740215841539130004, -41.19284213511701864 ) ) ;
#36012=CARTESIAN_POINT ( 'NONE',  ( 0.5817216825391126056, -20.15223717566626860, -42.34527469533232846 ) ) ;
#36017=CARTESIAN_POINT ( 'NONE',  ( 4.962356264823609031, -33.29728444345293781, 25.73958909062332268 ) ) ;
#36025=ORIENTED_EDGE ( 'NONE', *, *, #25464, .T. ) ;
#36034=CARTESIAN_POINT ( 'NONE',  ( 5.910764540655178756, -18.52235246776667310, -7.837327192926230701 ) ) ;
#36037=CARTESIAN_POINT ( 'NONE',  ( 2.528190830796658517, 40.79054845818019004, -9.918936063603915443 ) ) ;
#36038=VERTEX_POINT ( 'NONE', #53260 ) ;
#36051=ORIENTED_EDGE ( 'NONE', *, *, #39033, .F. ) ;
#36074=DIRECTION ( 'NONE',  ( -1.000000000000000000, -0.000000000000000000, -0.000000000000000000 ) ) ;
#36080=CARTESIAN_POINT ( 'NONE',  ( 0.5804410086790514622, -14.41595396256474615, 44.62846763227044988 ) ) ;
#36086=CARTESIAN_POINT ( 'NONE',  ( 3.376099380956842921, 0.01224625995926260230, 13.40552996569639710 ) ) ;
#36088=ORIENTED_EDGE ( 'NONE', *, *, #14479, .F. ) ;
#36123=CARTESIAN_POINT ( 'NONE',  ( 4.958415959904820092, 1.012370948441083440, 45.41122172861450679 ) ) ;
#36129=SURFACE_STYLE_USAGE ( .BOTH. , #22011 ) ;
#36135=CARTESIAN_POINT ( 'NONE',  ( 5.896782393890504181, -19.39988559968493576, 5.307591317834223332 ) ) ;
#36138=CARTESIAN_POINT ( 'NONE',  ( 0.6845945791218034371, -30.94166671083587516, 35.25648567100093800 ) ) ;
#36147=CARTESIAN_POINT ( 'NONE',  ( 0.9762797500689124330, -22.97506929404208975, 35.04955029839425151 ) ) ;
#36162=VERTEX_POINT ( 'NONE', #10370 ) ;
#36166=EDGE_CURVE ( 'NONE', #18232, #23007, #34488, .T. ) ;
#36178=VERTEX_POINT ( 'NONE', #21615 ) ;
#36179=CARTESIAN_POINT ( 'NONE',  ( 5.896782393890504181, 14.91246379622031526, -13.49609241241443947 ) ) ;
#36181=CARTESIAN_POINT ( 'NONE',  ( 0.5806925824938502512, -46.82446035038566379, -2.586943222941716858 ) ) ;
#36196=CARTESIAN_POINT ( 'NONE',  ( 4.291220156522059348, 46.92833126662976184, -4.137719400244163737 ) ) ;
#36200=CARTESIAN_POINT ( 'NONE',  ( 2.528100132419517365, -13.58805440665008923, -39.71924667052476110 ) ) ;
#36203=B_SPLINE_CURVE_WITH_KNOTS ( 'NONE', 3,
 ( #35953, #25914, #15905, #11839, #21833, #40656, #26522, #59722, #1774, #55016, #25289, #50324, #12146, #7084, #16515, #25598 ),
 .UNSPECIFIED., .F., .F.,
 ( 4, 3, 3, 3, 3, 4 ),
 ( 9.813676791237319219E-18, 0.0002732102107931888070, 0.0004098135523333875513, 0.0005464168938825055390, 0.0008195847345945404079, 0.001092771384553103747 ),
 .UNSPECIFIED. ) ;
#36204=CARTESIAN_POINT ( 'NONE',  ( 0.6064515330803633697, 40.70784744179291437, 23.28530636888421057 ) ) ;
#36210=ADVANCED_FACE ( 'NONE', ( #22239 ), #47128, .F. ) ;
#36230=ORIENTED_EDGE ( 'NONE', *, *, #35781, .T. ) ;
#36238=EDGE_CURVE ( 'NONE', #48578, #34855, #7397, .T. ) ;
#36240=CARTESIAN_POINT ( 'NONE',  ( 0.9787464366903569912, 32.99929854755155390, -25.83370450129101314 ) ) ;
#36246=B_SPLINE_CURVE_WITH_KNOTS ( 'NONE', 3,
 ( #39519, #11000, #58569, #15699 ),
 .UNSPECIFIED., .F., .F.,
 ( 4, 4 ),
 ( 0.000000000000000000, 0.004042984057420972825 ),
 .UNSPECIFIED. ) ;
#36263=CARTESIAN_POINT ( 'NONE',  ( 0.5804410086790514622, -19.24447200597919405, -42.76879877979365574 ) ) ;
#36270=ORIENTED_EDGE ( 'NONE', *, *, #12959, .T. ) ;
#36272=CARTESIAN_POINT ( 'NONE',  ( 0.9754292589017204973, -0.8180784385973481898, 41.90057534883716528 ) ) ;
#36273=CARTESIAN_POINT ( 'NONE',  ( 1.231276596079881047, 33.41651732065586344, -25.31033664684003170 ) ) ;
#36279=CARTESIAN_POINT ( 'NONE',  ( 3.376099380956842921, -13.33697911751164256, 1.354020550481185969 ) ) ;
#36292=CARTESIAN_POINT ( 'NONE',  ( 0.5806925824938499181, 45.08220210717423271, 12.91578164539256335 ) ) ;
#36304=ADVANCED_FACE ( 'NONE', ( #51646 ), #55509, .F. ) ;
#36306=EDGE_CURVE ( 'NONE', #40743, #42423, #35737, .T. ) ;
#36313=ADVANCED_FACE ( 'NONE', ( #4323 ), #44402, .F. ) ;
#36319=CARTESIAN_POINT ( 'NONE',  ( 4.958415959904818315, 40.30989464198789562, -20.93600601295462837 ) ) ;
#36321=CARTESIAN_POINT ( 'NONE',  ( 1.091591847532194182, -0.6204316382185598444, -41.90911661605549909 ) ) ;
#36325=B_SPLINE_CURVE_WITH_KNOTS ( 'NONE', 3,
 ( #50418, #7483, #26610, #45742, #161, #48720 ),
 .UNSPECIFIED., .F., .F.,
 ( 4, 2, 4 ),
 ( 7.372574772901430151E-18, 0.0002291472222819941824, 0.0004582944445639809922 ),
 .UNSPECIFIED. ) ;
#36328=B_SPLINE_CURVE_WITH_KNOTS ( 'NONE', 3,
 ( #44646, #49624, #29593, #44962, #48706, #1999 ),
 .UNSPECIFIED., .F., .F.,
 ( 4, 2, 4 ),
 ( 1.223195814675714468E-16, 0.0002448718616795907653, 0.0004897437233590592326 ),
 .UNSPECIFIED. ) ;
#36336=CARTESIAN_POINT ( 'NONE',  ( 0.5806925824938499181, 42.95845041307745760, 18.80940989108190209 ) ) ;
#36338=ADVANCED_FACE ( 'NONE', ( #46670 ), #13107, .F. ) ;
#36340=DIRECTION ( 'NONE',  ( -0.07906939808003035641, -0.8264033190538698781, -0.5574994031781644876 ) ) ;
#36348=DIRECTION ( 'NONE',  ( -1.000000000000000000, -0.000000000000000000, -0.000000000000000000 ) ) ;
#36353=VERTEX_POINT ( 'NONE', #59117 ) ;
#36362=CARTESIAN_POINT ( 'NONE',  ( 0.5806925824938494740, 36.46274162637944016, -29.49052111156159128 ) ) ;
#36365=CARTESIAN_POINT ( 'NONE',  ( 0.9754292589017233839, 9.147692918817449836, -40.89800950117612643 ) ) ;
#36367=EDGE_LOOP ( 'NONE', ( #238, #12528, #24757, #53069, #59107, #58611 ) ) ;
#36375=ORIENTED_EDGE ( 'NONE', *, *, #867, .T. ) ;
#36376=CARTESIAN_POINT ( 'NONE',  ( 0.5782707292762423457, -44.06349990951380846, 16.06687055502393946 ) ) ;
#36377=CARTESIAN_POINT ( 'NONE',  ( 2.528190830796658517, 16.21068873809912958, -38.72296097652494495 ) ) ;
#36384=CARTESIAN_POINT ( 'NONE',  ( 0.5835226383429286123, 32.73248470276266175, 33.58313445361189764 ) ) ;
#36390=CARTESIAN_POINT ( 'NONE',  ( 5.896782393890504181, -19.39652907507971236, -5.319844614046497000 ) ) ;
#36392=VERTEX_POINT ( 'NONE', #6475 ) ;
#36394=CARTESIAN_POINT ( 'NONE',  ( 0.8554163680231720024, 9.985124899324969050, -45.84215040611314862 ) ) ;
#36399=CARTESIAN_POINT ( 'NONE',  ( 0.7056313189692702270, -14.69870890607749025, -44.53870901195897858 ) ) ;
#36404=EDGE_LOOP ( 'NONE', ( #13441, #16214, #8129, #21503 ) ) ;
#36406=EDGE_LOOP ( 'NONE', ( #58179, #42271, #52876, #11734 ) ) ;
#36407=ORIENTED_EDGE ( 'NONE', *, *, #17192, .F. ) ;
#36410=VECTOR ( 'NONE', #19049, 999.9999999999998863 ) ;
#36411=VERTEX_POINT ( 'NONE', #35042 ) ;
#36412=CARTESIAN_POINT ( 'NONE',  ( 1.231276596079887264, -37.02495017545888345, 19.65781868679367150 ) ) ;
#36414=CARTESIAN_POINT ( 'NONE',  ( 2.528190830796654076, 8.550381731088631199, 41.09921055696414527 ) ) ;
#36416=CARTESIAN_POINT ( 'NONE',  ( 4.291220156522059348, 45.95810865397728406, -10.35573494518448356 ) ) ;
#36417=CARTESIAN_POINT ( 'NONE',  ( 4.291220156522059348, -46.81214323738918637, -5.292659334196264886 ) ) ;
#36433=ORIENTED_EDGE ( 'NONE', *, *, #46996, .T. ) ;
#36436=CARTESIAN_POINT ( 'NONE',  ( 4.956445790444001354, -33.12351118015997997, 33.47194433010209025 ) ) ;
#36444=EDGE_CURVE ( 'NONE', #37898, #24638, #44455, .T. ) ;
#36446=LINE ( 'NONE', #55206, #37259 ) ;
#36447=CARTESIAN_POINT ( 'NONE',  ( 0.9775691876210961251, 32.65442599162690840, 26.26827310934911353 ) ) ;
#36471=CARTESIAN_POINT ( 'NONE',  ( 1.157644175074339588, -39.31880106288546273, -14.52701478131064938 ) ) ;
#36474=CARTESIAN_POINT ( 'NONE',  ( 4.962356264823608143, 27.50309822711080443, -31.85616401533997077 ) ) ;
#36475=CARTESIAN_POINT ( 'NONE',  ( 4.962356264823602814, -25.31392337492848554, -33.62202970123303203 ) ) ;
#36482=CARTESIAN_POINT ( 'NONE',  ( 4.962356264823608143, 0.000000000000000000, 0.000000000000000000 ) ) ;
#36485=ORIENTED_EDGE ( 'NONE', *, *, #33850, .F. ) ;
#36488=CARTESIAN_POINT ( 'NONE',  ( 2.891212509700765487, 5.349982771599759140E-15, 41.99381090189422139 ) ) ;
#36490=CARTESIAN_POINT ( 'NONE',  ( 0.5848930533535030563, 4.512869149484262543, -46.67876491968475250 ) ) ;
#36494=CARTESIAN_POINT ( 'NONE',  ( 1.091591847532197734, 32.40455690483145190, 26.58389893821784256 ) ) ;
#36500=CARTESIAN_POINT ( 'NONE',  ( 0.8560838555295158248, 9.983184696770717181, 45.83349056521764453 ) ) ;
#36502=AXIS2_PLACEMENT_3D ( 'NONE', #18730, #38779, #14967 ) ;
#36503=VERTEX_POINT ( 'NONE', #17458 ) ;
#36504=CARTESIAN_POINT ( 'NONE',  ( 1.092182651088187351, -13.16162218539093764, -39.79362870977350042 ) ) ;
#36510=FACE_OUTER_BOUND ( 'NONE', #40083, .T. ) ;
#36513=CARTESIAN_POINT ( 'NONE',  ( 4.291220156522060236, -5.703517857940846092, 46.76386298574836786 ) ) ;
#36515=CARTESIAN_POINT ( 'NONE',  ( 5.910764540655177868, -18.52235246776677968, 7.837327192925977570 ) ) ;
#36520=CARTESIAN_POINT ( 'NONE',  ( 0.7764139734771270396, -25.98546517425588931, 39.04863724362736122 ) ) ;
#36534=VERTEX_POINT ( 'NONE', #31552 ) ;
#36538=EDGE_CURVE ( 'NONE', #49383, #61119, #2857, .T. ) ;
#36549=CARTESIAN_POINT ( 'NONE',  ( 0.9762797500689124330, 33.20096159360354449, -25.57383300261748360 ) ) ;
#36559=LINE ( 'NONE', #3011, #12576 ) ;
#36563=CARTESIAN_POINT ( 'NONE',  ( 0.9787464366903567692, 4.370983831000746278, -41.68007309542044680 ) ) ;
#36564=ORIENTED_EDGE ( 'NONE', *, *, #33329, .T. ) ;
#36572=EDGE_CURVE ( 'NONE', #36573, #3024, #45662, .T. ) ;
#36573=VERTEX_POINT ( 'NONE', #11858 ) ;
#36579=CARTESIAN_POINT ( 'NONE',  ( 0.5835871038041849923, -41.91697779741947016, 21.02858590662108895 ) ) ;
#36582=FACE_OUTER_BOUND ( 'NONE', #18529, .T. ) ;
#36596=CARTESIAN_POINT ( 'NONE',  ( 5.896782393890504181, 16.57826022845101122, -11.38803647148056797 ) ) ;
#36601=CARTESIAN_POINT ( 'NONE',  ( 5.901463166500146684, 17.95741941801098207, 9.058087998373544281 ) ) ;
#36602=CARTESIAN_POINT ( 'NONE',  ( 2.282816707992308736, 6.007215363275087761, 46.58766285173788191 ) ) ;
#36611=CARTESIAN_POINT ( 'NONE',  ( 0.6845945791218034371, -41.46895371680775355, -21.92561055813956372 ) ) ;
#36616=CARTESIAN_POINT ( 'NONE',  ( 4.962356264823597485, -9.332162870646813602, 41.03835198954837438 ) ) ;
#36618=CARTESIAN_POINT ( 'NONE',  ( 0.8560838555295223751, 33.26091945577352504, 33.07694168205818386 ) ) ;
#36621=CARTESIAN_POINT ( 'NONE',  ( 0.5782707292762423457, -25.84399470232749252, -39.13852694639499674 ) ) ;
#36623=LINE ( 'NONE', #18125, #2922 ) ;
#36628=EDGE_CURVE ( 'NONE', #37468, #12657, #32728, .T. ) ;
#36631=VECTOR ( 'NONE', #44722, 1000.000000000000114 ) ;
#36639=AXIS2_PLACEMENT_3D ( 'NONE', #12334, #6647, #21713 ) ;
#36644=CARTESIAN_POINT ( 'NONE',  ( 0.9762797500689124330, 28.76866969767982951, 30.47438972336447804 ) ) ;
#36646=ADVANCED_FACE ( 'NONE', ( #19315 ), #16744, .F. ) ;
#36656=CARTESIAN_POINT ( 'NONE',  ( 0.9769922540276041456, -18.04061514536692812, 37.82681271615258822 ) ) ;
#36658=ORIENTED_EDGE ( 'NONE', *, *, #54295, .F. ) ;
#36659=VERTEX_POINT ( 'NONE', #33115 ) ;
#36666=EDGE_CURVE ( 'NONE', #37717, #12846, #10311, .T. ) ;
#36672=CARTESIAN_POINT ( 'NONE',  ( 0.7764146366350267447, -44.00885459193158766, 16.22532561076629065 ) ) ;
#36677=EDGE_LOOP ( 'NONE', ( #25185, #40673, #35123, #9495 ) ) ;
#36684=AXIS2_PLACEMENT_3D ( 'NONE', #7646, #58719, #40292 ) ;
#36686=CARTESIAN_POINT ( 'NONE',  ( 0.5830081025819924267, 32.79755092742119160, 33.51943745866657309 ) ) ;
#36687=CARTESIAN_POINT ( 'NONE',  ( 2.528190830796654076, 32.18156550548854966, 26.95553705213378493 ) ) ;
#36689=CARTESIAN_POINT ( 'NONE',  ( 0.7056313189692720034, -8.631130581270838320, -46.10045801124549314 ) ) ;
#36691=CARTESIAN_POINT ( 'NONE',  ( 0.5804410086790514622, 17.36461428077188884, -43.56592731407664587 ) ) ;
#36696=ORIENTED_EDGE ( 'NONE', *, *, #30029, .F. ) ;
#36704=CARTESIAN_POINT ( 'NONE',  ( 0.9790320750461911636, -41.80925896709178602, -2.884960513567975227 ) ) ;
#36708=CARTESIAN_POINT ( 'NONE',  ( 2.618530812446111078, 43.80811722902110716, -17.04627977144998141 ) ) ;
#36709=CARTESIAN_POINT ( 'NONE',  ( 3.782542959838395280, 2.488391571546694436, 41.96481574823395988 ) ) ;
#36712=ORIENTED_EDGE ( 'NONE', *, *, #31804, .F. ) ;
#36714=CARTESIAN_POINT ( 'NONE',  ( 2.528190830796658517, -16.56543340168992628, -38.57253624493965560 ) ) ;
#36715=EDGE_CURVE ( 'NONE', #10852, #55528, #29015, .T. ) ;
#36717=DIRECTION ( 'NONE',  ( -1.000000000000000000, -0.000000000000000000, -0.000000000000000000 ) ) ;
#36721=( BOUNDED_SURFACE ( )  B_SPLINE_SURFACE ( 3, 1, ( 
 ( #11559, #15643 ),
 ( #1504, #30636 ),
 ( #34440, #10627 ),
 ( #39153, #29716 ) ),
 .UNSPECIFIED., .F., .F., .F. ) 
 B_SPLINE_SURFACE_WITH_KNOTS ( ( 4, 4 ),
 ( 2, 2 ),
 ( 0.000000000000000000, 1.000000000000000000 ),
 ( 0.000000000000000000, 1.000000000000000000 ),
 .UNSPECIFIED. ) 
 GEOMETRIC_REPRESENTATION_ITEM ( )  RATIONAL_B_SPLINE_SURFACE ( (
 ( 1.000000000000000000, 1.000000000000000000),
 ( 0.9952954269826590483, 0.8620686068821339365),
 ( 0.9952954269826590483, 0.8620686068821339365),
 ( 1.000000000000000000, 1.000000000000000000) ) ) 
 REPRESENTATION_ITEM ( '' )  SURFACE ( )  );
#36725=ORIENTED_EDGE ( 'NONE', *, *, #50413, .T. ) ;
#36726=EDGE_CURVE ( 'NONE', #16730, #7010, #34342, .T. ) ;
#36727=CARTESIAN_POINT ( 'NONE',  ( 3.782542959838401497, -35.60516656857437567, 22.34971961838993693 ) ) ;
#36730=DIRECTION ( 'NONE',  ( -0.07500201931887529039, -0.3083113411842438034, -0.9483242135447474963 ) ) ;
#36734=ADVANCED_FACE ( 'NONE', ( #24627 ), #25890, .F. ) ;
#36735=DIRECTION ( 'NONE',  ( -1.000000000000000000, -0.000000000000000000, -0.000000000000000000 ) ) ;
#36737=VERTEX_POINT ( 'NONE', #29619 ) ;
#36745=CARTESIAN_POINT ( 'NONE',  ( 0.5837800304671215690, -1.521551379193686770, -46.87133680171679373 ) ) ;
#36746=CONICAL_SURFACE ( 'NONE', #29731, 42.08604991992415023, 1.569615340895231137 ) ;
#36749=DIRECTION ( 'NONE',  ( -1.000000000000000000, -0.000000000000000000, -0.000000000000000000 ) ) ;
#36752=FACE_OUTER_BOUND ( 'NONE', #9278, .T. ) ;
#36754=CARTESIAN_POINT ( 'NONE',  ( 1.231276596079881047, -13.22565419922034557, 39.77887431816932917 ) ) ;
#36756=DIRECTION ( 'NONE',  ( 0.07500201931887538753, 0.9957672615368112767, -0.05312492776061850802 ) ) ;
#36757=CARTESIAN_POINT ( 'NONE',  ( 0.9783242366443536397, 32.72304825568722464, 26.18275392433902837 ) ) ;
#36761=CARTESIAN_POINT ( 'NONE',  ( 5.895596859100789899, -19.93390588528923857, 2.677233529021818104 ) ) ;
#36763=CARTESIAN_POINT ( 'NONE',  ( 5.895596859100789899, -7.232071727010249695, 18.76766692340490295 ) ) ;
#36766=VECTOR ( 'NONE', #19518, 1000.000000000000000 ) ;
#36772=B_SPLINE_CURVE_WITH_KNOTS ( 'NONE', 3,
 ( #26571, #31900, #6815, #25958 ),
 .UNSPECIFIED., .F., .F.,
 ( 4, 4 ),
 ( 8.673617379884035472E-19, 0.004042984057420972825 ),
 .UNSPECIFIED. ) ;
#36780=CARTESIAN_POINT ( 'NONE',  ( 1.231276596079887264, -23.26513148155214594, -34.87134107206314582 ) ) ;
#36787=CARTESIAN_POINT ( 'NONE',  ( 5.896278296736517710, -19.39678151694237229, -5.319008027667046612 ) ) ;
#36797=ORIENTED_EDGE ( 'NONE', *, *, #3371, .T. ) ;
#36798=ORIENTED_EDGE ( 'NONE', *, *, #36799, .F. ) ;
#36799=EDGE_CURVE ( 'NONE', #53953, #37569, #40599, .T. ) ;
#36805=EDGE_CURVE ( 'NONE', #6137, #26843, #55113, .T. ) ;
#36817=EDGE_CURVE ( 'NONE', #30066, #54983, #37709, .T. ) ;
#36820=B_SPLINE_CURVE_WITH_KNOTS ( 'NONE', 3,
 ( #15529, #61869, #4861, #48414 ),
 .UNSPECIFIED., .F., .F.,
 ( 4, 4 ),
 ( 0.000000000000000000, 0.005004948556313810505 ),
 .UNSPECIFIED. ) ;
#36826=CARTESIAN_POINT ( 'NONE',  ( 1.000110580585055420, -23.10262754908167793, 34.96692841958402198 ) ) ;
#36833=CARTESIAN_POINT ( 'NONE',  ( 4.956445790444018229, -10.39006634428234577, -45.93021414603951058 ) ) ;
#36840=CARTESIAN_POINT ( 'NONE',  ( 0.5806925824938502512, 17.36345040154772690, 43.56297685531322372 ) ) ;
#36843=CARTESIAN_POINT ( 'NONE',  ( 0.9780106845699478857, -31.29111759374672630, 27.87825687143571685 ) ) ;
#36846=ADVANCED_FACE ( 'NONE', ( #45913 ), #27902, .F. ) ;
#36847=CARTESIAN_POINT ( 'NONE',  ( 4.956445790444004018, -45.27177431812791042, 12.96165499572219737 ) ) ;
#36856=LINE ( 'NONE', #3291, #55492 ) ;
#36861=CARTESIAN_POINT ( 'NONE',  ( 0.9780303403264759554, 24.59793831445992041, -33.93053262289160443 ) ) ;
#36863=VECTOR ( 'NONE', #55981, 1000.000000000000114 ) ;
#36864=CARTESIAN_POINT ( 'NONE',  ( 4.962356264823598373, -24.61258717641114657, 34.13877780978559429 ) ) ;
#36866=CARTESIAN_POINT ( 'NONE',  ( 4.958415959904818315, 40.76596448693018715, 20.03347431857450545 ) ) ;
#36867=CARTESIAN_POINT ( 'NONE',  ( 5.894904586330512508, -18.51647496758831579, 7.852997315440658710 ) ) ;
#36869=CARTESIAN_POINT ( 'NONE',  ( 2.618530812446111078, -12.57566640959636217, -45.29436392701359182 ) ) ;
#36876=CARTESIAN_POINT ( 'NONE',  ( 1.231276596079887264, -31.65135013586864332, -27.48579279545554144 ) ) ;
#36879=CARTESIAN_POINT ( 'NONE',  ( 0.5797568599927116484, 46.38942897415957844, 6.873586263546419772 ) ) ;
#36885=VERTEX_POINT ( 'NONE', #45593 ) ;
#36886=CARTESIAN_POINT ( 'NONE',  ( 4.962356264823608143, 0.000000000000000000, 0.000000000000000000 ) ) ;
#36896=CARTESIAN_POINT ( 'NONE',  ( 5.910764540655177868, 14.92665574186510113, -13.47947279506912466 ) ) ;
#36902=ORIENTED_EDGE ( 'NONE', *, *, #6764, .F. ) ;
#36906=CARTESIAN_POINT ( 'NONE',  ( 1.157643937452368599, -26.42675007435921586, 32.53658179806398465 ) ) ;
#36915=CARTESIAN_POINT ( 'NONE',  ( 0.9789889208857696090, -26.98387854568887079, 32.06563887830525061 ) ) ;
#36934=CARTESIAN_POINT ( 'NONE',  ( 0.8560838555295223751, -26.00596412780120303, -39.03924517540328765 ) ) ;
#36945=ORIENTED_EDGE ( 'NONE', *, *, #18279, .F. ) ;
#36950=CIRCLE ( 'NONE', #9931, 42.08604991992415023 ) ;
#36952=ORIENTED_EDGE ( 'NONE', *, *, #15447, .T. ) ;
#36964=CARTESIAN_POINT ( 'NONE',  ( 0.5806925824938506953, -38.96949031362410665, -26.08833430941730924 ) ) ;
#36971=CIRCLE ( 'NONE', #20939, 41.88877248453276536 ) ;
#36978=CARTESIAN_POINT ( 'NONE',  ( 5.894904586330512508, 20.06808393774119281, -1.342169560605708467 ) ) ;
#36980=VERTEX_POINT ( 'NONE', #28618 ) ;
#36986=CARTESIAN_POINT ( 'NONE',  ( 3.376099380956838925, 11.76186387009564349, -6.431713763329790723 ) ) ;
#36988=EDGE_LOOP ( 'NONE', ( #10133, #2657, #10424, #55949 ) ) ;
#36989=CARTESIAN_POINT ( 'NONE',  ( 1.793499172322287949, -0.3976920648075739639, -41.94333330318345077 ) ) ;
#36993=CARTESIAN_POINT ( 'NONE',  ( 0.5837800304671242335, -41.83504527563591324, -21.19118493536846870 ) ) ;
#37005=CARTESIAN_POINT ( 'NONE',  ( 4.962356264823593932, 31.50371261889118557, 27.90612278853270922 ) ) ;
#37007=CARTESIAN_POINT ( 'NONE',  ( 1.231276596079881047, 19.39962232756238691, 37.16088568059176112 ) ) ;
#37008=CARTESIAN_POINT ( 'NONE',  ( 0.5837800304671207918, 22.57726808510225425, -41.10358011162680469 ) ) ;
#37011=DIRECTION ( 'NONE',  ( -1.000000000000000000, -0.000000000000000000, -0.000000000000000000 ) ) ;
#37016=CARTESIAN_POINT ( 'NONE',  ( 0.9787284016396619046, 20.30453793353213854, 36.66144757418319955 ) ) ;
#37018=CARTESIAN_POINT ( 'NONE',  ( 0.7056313189692740018, -45.78630481351672188, 10.16675638939457649 ) ) ;
#37021=CARTESIAN_POINT ( 'NONE',  ( 0.9789233960466698914, -41.80609487568101201, -2.930385312190553648 ) ) ;
#37033=CARTESIAN_POINT ( 'NONE',  ( 1.157643937452369487, 24.19453194249153327, -34.22903590051158318 ) ) ;
#37039=CARTESIAN_POINT ( 'NONE',  ( 3.238018933889920792, 11.38191749426270150, 7.061122185704597598 ) ) ;
#37043=CARTESIAN_POINT ( 'NONE',  ( 0.5834584762367766020, -44.24114406392340726, -15.55497222525211143 ) ) ;
#37046=CARTESIAN_POINT ( 'NONE',  ( 0.6064515330803581517, 43.44825878165435995, 17.65171790165140919 ) ) ;
#37051=CARTESIAN_POINT ( 'NONE',  ( 0.6064515330803604831, -25.83061180769639620, -39.14222566075134324 ) ) ;
#37055=CARTESIAN_POINT ( 'NONE',  ( 0.8560838555295158248, -35.39593983670192756, 30.78149244527153883 ) ) ;
#37058=CARTESIAN_POINT ( 'NONE',  ( 0.9769922540276045897, -41.84221118692512675, 2.358159891712742429 ) ) ;
#37061=DIRECTION ( 'NONE',  ( 0.000000000000000000, 0.000000000000000000, 1.000000000000000000 ) ) ;
#37065=CARTESIAN_POINT ( 'NONE',  ( 5.901463166500145796, -15.79333916981814134, 12.45344563595652509 ) ) ;
#37073=CARTESIAN_POINT ( 'NONE',  ( 5.894904586330512508, -7.227592724925899326, 18.76942501687893738 ) ) ;
#37098=CARTESIAN_POINT ( 'NONE',  ( 3.238018933889920792, 5.069615556373336496, -12.39784217024198121 ) ) ;
#37101=CARTESIAN_POINT ( 'NONE',  ( 1.157643937452369265, -2.225587402986053398, -41.85748481820694877 ) ) ;
#37102=ORIENTED_EDGE ( 'NONE', *, *, #15211, .F. ) ;
#37103=VERTEX_POINT ( 'NONE', #52730 ) ;
#37115=CARTESIAN_POINT ( 'NONE',  ( 0.5804410086790514622, 4.150428748652404742, -46.71502748642835456 ) ) ;
#37136=AXIS2_PLACEMENT_3D ( 'NONE', #9149, #8847, #23559 ) ;
#37138=CARTESIAN_POINT ( 'NONE',  ( 4.962356264823608143, -14.71877352713578269, -39.42833123173278409 ) ) ;
#37139=CARTESIAN_POINT ( 'NONE',  ( 4.960386119450139297, 1.932332837766398859, 43.71158375621307357 ) ) ;
#37140=CARTESIAN_POINT ( 'NONE',  ( 0.9780303403264763995, 41.90745447159759607, -0.3238411741276359668 ) ) ;
#37150=CARTESIAN_POINT ( 'NONE',  ( 0.5837800304671211249, -25.27226667711949304, 39.50379563004109684 ) ) ;
#37159=CARTESIAN_POINT ( 'NONE',  ( 0.8554163680231738898, -14.77070554666880753, 44.53124443315532233 ) ) ;
#37161=FACE_OUTER_BOUND ( 'NONE', #1441, .T. ) ;
#37163=CARTESIAN_POINT ( 'NONE',  ( 0.5834584762367753807, 22.37749980484480972, 41.21266178612297182 ) ) ;
#37168=CARTESIAN_POINT ( 'NONE',  ( 0.9787284016396597952, 24.70838012762134284, -33.85013959199871181 ) ) ;
#37183=CARTESIAN_POINT ( 'NONE',  ( 0.9769922540276043676, 4.634276657682153910, -41.65159102538806479 ) ) ;
#37190=( BOUNDED_SURFACE ( )  B_SPLINE_SURFACE ( 3, 1, ( 
 ( #48688, #38701 ),
 ( #57758, #34602 ),
 ( #15805, #10174 ),
 ( #29269, #43716 ) ),
 .UNSPECIFIED., .F., .F., .F. ) 
 B_SPLINE_SURFACE_WITH_KNOTS ( ( 4, 4 ),
 ( 2, 2 ),
 ( 0.000000000000000000, 1.000000000000000000 ),
 ( 0.000000000000000000, 1.000000000000000000 ),
 .UNSPECIFIED. ) 
 GEOMETRIC_REPRESENTATION_ITEM ( )  RATIONAL_B_SPLINE_SURFACE ( (
 ( 1.000000000000000000, 1.000000000000000000),
 ( 0.9952954269826590483, 0.8620686068821307169),
 ( 0.9952954269826590483, 0.8620686068821307169),
 ( 1.000000000000000000, 1.000000000000000000) ) ) 
 REPRESENTATION_ITEM ( '' )  SURFACE ( )  );
#37191=EDGE_CURVE ( 'NONE', #51445, #29061, #48356, .T. ) ;
#37202=CARTESIAN_POINT ( 'NONE',  ( 1.231276596079887931, -41.87427716283724521, -1.954912557623687652 ) ) ;
#37204=ORIENTED_EDGE ( 'NONE', *, *, #29751, .F. ) ;
#37207=CARTESIAN_POINT ( 'NONE',  ( 4.956445790444005794, -40.23882117934059011, -24.46171131046819625 ) ) ;
#37208=CARTESIAN_POINT ( 'NONE',  ( 5.896782393890504181, -19.93422257774826889, 2.674482585249640110 ) ) ;
#37213=ORIENTED_EDGE ( 'NONE', *, *, #8467, .F. ) ;
#37215=CARTESIAN_POINT ( 'NONE',  ( 0.9790724872846771065, -27.08825771237176383, 31.97751560221001554 ) ) ;
#37217=CARTESIAN_POINT ( 'NONE',  ( 0.5848930533535030563, 40.25661832390772332, -24.05572205340705594 ) ) ;
#37224=VECTOR ( 'NONE', #14353, 999.9999999999998863 ) ;
#37231=DIRECTION ( 'NONE',  ( -0.07500201931887527651, -0.8838330717251269286, 0.4617507968840091626 ) ) ;
#37234=FACE_OUTER_BOUND ( 'NONE', #48262, .T. ) ;
#37235=CARTESIAN_POINT ( 'NONE',  ( 0.7056313189692768884, 23.27565847123662124, 40.71845241027597240 ) ) ;
#37236=CARTESIAN_POINT ( 'NONE',  ( 4.956445790443998689, -10.39006634428300835, 45.93021414603936847 ) ) ;
#37238=EDGE_LOOP ( 'NONE', ( #23664, #43819, #45440, #31140 ) ) ;
#37244=ORIENTED_EDGE ( 'NONE', *, *, #51218, .F. ) ;
#37259=VECTOR ( 'NONE', #36756, 999.9999999999998863 ) ;
#37266=ADVANCED_FACE ( 'NONE', ( #51114 ), #59910, .F. ) ;
#37272=FACE_OUTER_BOUND ( 'NONE', #25904, .T. ) ;
#37276=CARTESIAN_POINT ( 'NONE',  ( 5.910764540655177868, 8.451874527002114945, 18.25012480639449564 ) ) ;
#37281=CARTESIAN_POINT ( 'NONE',  ( 1.231276596079887931, 8.892602616354244205, -40.96581977363174332 ) ) ;
#37285=ORIENTED_EDGE ( 'NONE', *, *, #47477, .T. ) ;
#37294=CARTESIAN_POINT ( 'NONE',  ( 0.5806925824938499181, 28.25565086187788921, -37.42780459384738379 ) ) ;
#37298=EDGE_CURVE ( 'NONE', #42435, #44157, #31949, .T. ) ;
#37300=CARTESIAN_POINT ( 'NONE',  ( 0.6064515330803589288, -8.500244729551798883, -46.12027943947015274 ) ) ;
#37301=VECTOR ( 'NONE', #24731, 999.9999999999997726 ) ;
#37305=ORIENTED_EDGE ( 'NONE', *, *, #39231, .T. ) ;
#37306=CARTESIAN_POINT ( 'NONE',  ( 1.231276596079887931, 5.037240371905710390, 41.61613846158375196 ) ) ;
#37307=CARTESIAN_POINT ( 'NONE',  ( 0.9762797500689124330, 19.69530149098661909, 36.99215976885973589 ) ) ;
#37311=EDGE_CURVE ( 'NONE', #35778, #43148, #43168, .T. ) ;
#37317=AXIS2_PLACEMENT_3D ( 'NONE', #34461, #29126, #52926 ) ;
#37319=CARTESIAN_POINT ( 'NONE',  ( 1.231276596079881047, 25.54232633153377208, -33.23952972879584422 ) ) ;
#37323=VERTEX_POINT ( 'NONE', #39764 ) ;
#37324=CARTESIAN_POINT ( 'NONE',  ( 5.894904586330512508, 8.465111963867505196, -18.24476065890780418 ) ) ;
#37328=ORIENTED_EDGE ( 'NONE', *, *, #15447, .F. ) ;
#37333=VERTEX_POINT ( 'NONE', #39448 ) ;
#37334=CARTESIAN_POINT ( 'NONE',  ( 5.896782393890504181, 20.06834277495334362, -1.337050913387380691 ) ) ;
#37345=ORIENTED_EDGE ( 'NONE', *, *, #20303, .T. ) ;
#37347=CARTESIAN_POINT ( 'NONE',  ( 0.5835226383429296115, 10.69419208715441272, -45.66045039362849423 ) ) ;
#37349=CARTESIAN_POINT ( 'NONE',  ( 5.896782393890504181, -17.30835043929350192, -10.24436879210333906 ) ) ;
#37353=CARTESIAN_POINT ( 'NONE',  ( 0.5837157313716041518, -1.476039657514138348, -46.87278923332241476 ) ) ;
#37356=CARTESIAN_POINT ( 'NONE',  ( 0.7056759521544992975, 45.00498525904872338, 13.20227749101629477 ) ) ;
#37357=CARTESIAN_POINT ( 'NONE',  ( 0.5782707292762442330, 46.89575936232449749, 0.7239527184646523672 ) ) ;
#37359=FACE_OUTER_BOUND ( 'NONE', #52191, .T. ) ;
#37361=AXIS2_PLACEMENT_3D ( 'NONE', #20802, #436, #10479 ) ;
#37367=CARTESIAN_POINT ( 'NONE',  ( 0.9791128995231617171, -12.41164548084656083, 40.02859591222185998 ) ) ;
#37369=CARTESIAN_POINT ( 'NONE',  ( 3.238018933889920792, 4.556392162264823575, -12.59550645394239865 ) ) ;
#37371=CARTESIAN_POINT ( 'NONE',  ( 0.7056759521544981872, 33.20631110585615176, -33.12234490277042909 ) ) ;
#37375=EDGE_CURVE ( 'NONE', #26144, #52281, #27332, .T. ) ;
#37377=CARTESIAN_POINT ( 'NONE',  ( 0.5817216825391118284, 45.10732437693867070, -12.82825942055636936 ) ) ;
#37378=DIRECTION ( 'NONE',  ( 0.000000000000000000, 0.000000000000000000, -1.000000000000000000 ) ) ;
#37384=DIRECTION ( 'NONE',  ( 1.000000000000000000, 0.000000000000000000, 0.000000000000000000 ) ) ;
#37386=EDGE_CURVE ( 'NONE', #21039, #24195, #47542, .T. ) ;
#37389=CARTESIAN_POINT ( 'NONE',  ( 0.5806925824938502512, 16.34374012233117313, -43.95571090492413191 ) ) ;
#37395=CARTESIAN_POINT ( 'NONE',  ( 0.5797568665920712627, 4.067664388277952625, -46.71915469083538142 ) ) ;
#37396=CARTESIAN_POINT ( 'NONE',  ( 3.661933894777893439, 29.39589352174664683, -36.72209973585098908 ) ) ;
#37397=ORIENTED_EDGE ( 'NONE', *, *, #14734, .T. ) ;
#37409=ORIENTED_EDGE ( 'NONE', *, *, #20822, .T. ) ;
#37410=EDGE_CURVE ( 'NONE', #32248, #47641, #25897, .T. ) ;
#37414=DIRECTION ( 'NONE',  ( -1.000000000000000000, -0.000000000000000000, -0.000000000000000000 ) ) ;
#37416=CARTESIAN_POINT ( 'NONE',  ( 0.5806925824938494740, -38.35106547415225009, 26.98922265165951018 ) ) ;
#37418=EDGE_CURVE ( 'NONE', #15516, #36162, #25629, .T. ) ;
#37420=CARTESIAN_POINT ( 'NONE',  ( 4.956445790444004018, -43.56224489968113289, 17.88487823385560205 ) ) ;
#37428=DIRECTION ( 'NONE',  ( 1.000000000000000000, -0.000000000000000000, -0.000000000000000000 ) ) ;
#37430=EDGE_CURVE ( 'NONE', #39646, #13518, #25705, .T. ) ;
#37438=CARTESIAN_POINT ( 'NONE',  ( 0.5832655196449144652, -30.10317133800721834, -35.95878555190522263 ) ) ;
#37445=ADVANCED_FACE ( 'NONE', ( #48510 ), #51480, .F. ) ;
#37453=COLOUR_RGB ( '', 0.08235294, 0.09019608, 0.10196078) ;
#37458=B_SPLINE_CURVE_WITH_KNOTS ( 'NONE', 3,
 ( #6450, #29985, #49096, #6148 ),
 .UNSPECIFIED., .F., .F.,
 ( 4, 4 ),
 ( 1.551583845779545699E-17, 0.005004948556313833924 ),
 .UNSPECIFIED. ) ;
#37468=VERTEX_POINT ( 'NONE', #16869 ) ;
#37481=VECTOR ( 'NONE', #17529, 999.9999999999998863 ) ;
#37487=CARTESIAN_POINT ( 'NONE',  ( 0.9780303403264775097, -37.54924812539149315, -18.61165168954299887 ) ) ;
#37489=CARTESIAN_POINT ( 'NONE',  ( 0.7764139734771238199, 46.35884964711795675, 7.134250507430955679 ) ) ;
#37493=VERTEX_POINT ( 'NONE', #46605 ) ;
#37497=EDGE_CURVE ( 'NONE', #37701, #6142, #52727, .T. ) ;
#37501=CARTESIAN_POINT ( 'NONE',  ( 4.956445790443988031, 0.000000000000000000, 0.000000000000000000 ) ) ;
#37502=ADVANCED_FACE ( 'NONE', ( #55048 ), #12740, .F. ) ;
#37512=CARTESIAN_POINT ( 'NONE',  ( 5.838029081930957709, -4.708022006888409550, 46.99893176377070603 ) ) ;
#37513=CARTESIAN_POINT ( 'NONE',  ( 0.5830081025819928708, -41.73161187439133357, 21.39403198902457248 ) ) ;
#37517=DIRECTION ( 'NONE',  ( -1.000000000000000000, -0.000000000000000000, -0.000000000000000000 ) ) ;
#37519=EDGE_CURVE ( 'NONE', #20804, #55162, #31106, .T. ) ;
#37526=CARTESIAN_POINT ( 'NONE',  ( 0.5806925824938499181, 43.38503874128572591, -17.80339225430652306 ) ) ;
#37527=CARTESIAN_POINT ( 'NONE',  ( 0.9789233960466703355, -27.15769414545705729, 31.91858981117664484 ) ) ;
#37545=CARTESIAN_POINT ( 'NONE',  ( 1.157644175074336923, -16.89177048331274378, -38.36235609837159899 ) ) ;
#37546=CARTESIAN_POINT ( 'NONE',  ( 4.962356264823608143, 0.000000000000000000, 0.000000000000000000 ) ) ;
#37550=EDGE_LOOP ( 'NONE', ( #21008, #41109, #28896, #43748 ) ) ;
#37557=CARTESIAN_POINT ( 'NONE',  ( 5.896782393890504181, 16.58545041924856278, 11.37756218478545911 ) ) ;
#37569=VERTEX_POINT ( 'NONE', #47216 ) ;
#37570=CARTESIAN_POINT ( 'NONE',  ( 0.9780303403264759554, -7.289770003306762725, -41.26982998140380232 ) ) ;
#37572=B_SPLINE_CURVE_WITH_KNOTS ( 'NONE', 3,
 ( #54499, #34824, #2192, #11628, #10698, #6568 ),
 .UNSPECIFIED., .F., .F.,
 ( 4, 2, 4 ),
 ( 1.187272666737178580E-16, 0.0002448718616795955358, 0.0004897437233590723514 ),
 .UNSPECIFIED. ) ;
#37574=CARTESIAN_POINT ( 'NONE',  ( 0.7764146366350235251, -39.16768488414486171, -25.80567640046461975 ) ) ;
#37577=VERTEX_POINT ( 'NONE', #8668 ) ;
#37578=CARTESIAN_POINT ( 'NONE',  ( 4.960386119450146403, -4.847629508246811270, -43.48490488460468839 ) ) ;
#37580=ADVANCED_FACE ( 'NONE', ( #43145 ), #4276, .F. ) ;
#37585=CARTESIAN_POINT ( 'NONE',  ( 3.238018933889920792, -2.498552698661791638, -13.15920692061884090 ) ) ;
#37586=EDGE_CURVE ( 'NONE', #46003, #53253, #31902, .T. ) ;
#37587=CARTESIAN_POINT ( 'NONE',  ( 0.5848930533535030563, 45.27791896734284194, -12.21405487028341241 ) ) ;
#37591=ORIENTED_EDGE ( 'NONE', *, *, #56212, .T. ) ;
#37593=CARTESIAN_POINT ( 'NONE',  ( 2.528190830796651412, 23.91659899089207642, 34.50000621538883649 ) ) ;
#37594=CARTESIAN_POINT ( 'NONE',  ( 4.256456730324547522, 0.6428818333149034503, -47.05679108708081770 ) ) ;
#37606=ORIENTED_EDGE ( 'NONE', *, *, #44810, .F. ) ;
#37608=CARTESIAN_POINT ( 'NONE',  ( 0.6064782688330886407, 28.38738766212763309, -37.32948791691164558 ) ) ;
#37611=CARTESIAN_POINT ( 'NONE',  ( 0.9783242366443554161, 28.94125691613812634, 30.31069346485841365 ) ) ;
#37613=CARTESIAN_POINT ( 'NONE',  ( 0.7764146366350260786, -8.679346565860239338, -46.09457036201614955 ) ) ;
#37614=CARTESIAN_POINT ( 'NONE',  ( 0.6064515330803591509, 37.24100359994584153, 28.50336799232513840 ) ) ;
#37623=CARTESIAN_POINT ( 'NONE',  ( 0.9785694773339250752, 19.94506828457740610, 36.85823729966229934 ) ) ;
#37633=DIRECTION ( 'NONE',  ( -0.07906939808003034253, 0.6987975377710859970, 0.7109360248941737348 ) ) ;
#37634=CARTESIAN_POINT ( 'NONE',  ( 0.5835871038041873238, -45.92888218877342865, -9.474821042704075325 ) ) ;
#37639=ORIENTED_EDGE ( 'NONE', *, *, #35453, .T. ) ;
#37644=CARTESIAN_POINT ( 'NONE',  ( 5.896782393890504181, -13.98685533979025131, 14.45316451791071266 ) ) ;
#37646=CARTESIAN_POINT ( 'NONE',  ( 0.5806925824938502512, 11.40214825760292250, 45.48860711711456872 ) ) ;
#37648=CARTESIAN_POINT ( 'NONE',  ( 5.838029081930957709, 14.01343897760509805, 45.10752250095163873 ) ) ;
#37649=EDGE_CURVE ( 'NONE', #41654, #30011, #34902, .T. ) ;
#37660=CARTESIAN_POINT ( 'NONE',  ( 0.5806925824938499181, 43.38503874128572591, -17.80339225430652306 ) ) ;
#37666=CARTESIAN_POINT ( 'NONE',  ( 1.231276596079887931, 36.49189576017872128, 20.63051901543724043 ) ) ;
#37668=CARTESIAN_POINT ( 'NONE',  ( 0.5830081025819895402, -1.840045895287395261, -46.85985771943282430 ) ) ;
#37673=CARTESIAN_POINT ( 'NONE',  ( 0.9790320750461900534, -41.82074296194507923, 2.713409414944875309 ) ) ;
#37678=B_SPLINE_CURVE_WITH_KNOTS ( 'NONE', 3,
 ( #18724, #23412, #43159, #52838 ),
 .UNSPECIFIED., .F., .F.,
 ( 4, 4 ),
 ( 0.000000000000000000, 0.005004948556313805301 ),
 .UNSPECIFIED. ) ;
#37679=CARTESIAN_POINT ( 'NONE',  ( 0.5804410086790514622, -46.82762660194602233, 2.587129429331431751 ) ) ;
#37684=CARTESIAN_POINT ( 'NONE',  ( 0.9785694773339259633, -12.62891347609833126, 39.96055492767703043 ) ) ;
#37693=CARTESIAN_POINT ( 'NONE',  ( 0.5834584762367753807, 45.27752917664024324, -12.21398136037885784 ) ) ;
#37701=VERTEX_POINT ( 'NONE', #19640 ) ;
#37707=DIRECTION ( 'NONE',  ( -1.000000000000000000, -0.000000000000000000, -0.000000000000000000 ) ) ;
#37709=CIRCLE ( 'NONE', #14718, 47.09074272231896430 ) ;
#37712=DIRECTION ( 'NONE',  ( -1.000000000000000000, -0.000000000000000000, -0.000000000000000000 ) ) ;
#37714=CARTESIAN_POINT ( 'NONE',  ( 4.956445790444029775, 29.98832127573299289, -36.30755619981957949 ) ) ;
#37717=VERTEX_POINT ( 'NONE', #20553 ) ;
#37719=EDGE_LOOP ( 'NONE', ( #6291, #55330, #21078, #8860 ) ) ;
#37723=DIRECTION ( 'NONE',  ( -1.000000000000000000, -0.000000000000000000, -0.000000000000000000 ) ) ;
#37725=CARTESIAN_POINT ( 'NONE',  ( 5.917102823773431552, -9.657882276496826179, 17.64128759430757754 ) ) ;
#37732=EDGE_LOOP ( 'NONE', ( #15307, #55050, #7565, #33328 ) ) ;
#37745=CARTESIAN_POINT ( 'NONE',  ( 5.910764540655177868, 18.99430111539255961, 6.611940986348878724 ) ) ;
#37747=VERTEX_POINT ( 'NONE', #50581 ) ;
#37749=CARTESIAN_POINT ( 'NONE',  ( 0.5804410086790514622, -7.261380058784692615, 46.33348909263450821 ) ) ;
#37758=CARTESIAN_POINT ( 'NONE',  ( 0.5806925824938502512, -20.23436166722406426, -42.30594485723652554 ) ) ;
#37765=CARTESIAN_POINT ( 'NONE',  ( 0.9785694773339252972, -1.177911127880463260, -41.89209867134238863 ) ) ;
#37766=CARTESIAN_POINT ( 'NONE',  ( 1.231276596079887264, 3.353048872156665805, -41.78556968953512296 ) ) ;
#37767=ORIENTED_EDGE ( 'NONE', *, *, #51466, .F. ) ;
#37773=CARTESIAN_POINT ( 'NONE',  ( 0.5824935313925944103, -35.02383213588255728, -31.18604430785284265 ) ) ;
#37786=FACE_OUTER_BOUND ( 'NONE', #49399, .T. ) ;
#37790=ORIENTED_EDGE ( 'NONE', *, *, #8641, .F. ) ;
#37794=ADVANCED_FACE ( 'NONE', ( #60280 ), #17121, .F. ) ;
#37797=CARTESIAN_POINT ( 'NONE',  ( 0.9762797500689124330, 24.45014227843030596, -34.03697001423921620 ) ) ;
#37801=B_SPLINE_CURVE_WITH_KNOTS ( 'NONE', 3,
 ( #58303, #36714, #55167, #44889 ),
 .UNSPECIFIED., .F., .F.,
 ( 4, 4 ),
 ( 0.000000000000000000, 0.004041751736740997747 ),
 .UNSPECIFIED. ) ;
#37802=CARTESIAN_POINT ( 'NONE',  ( 1.231276596079887264, 25.54232633153331733, 33.23952972879620660 ) ) ;
#37813=CARTESIAN_POINT ( 'NONE',  ( 0.9784957157296372277, -37.50864571392711611, -18.69316863721794419 ) ) ;
#37815=CARTESIAN_POINT ( 'NONE',  ( 5.896278296736517710, 0.6665948613552165058, 20.10180665774095132 ) ) ;
#37816=CARTESIAN_POINT ( 'NONE',  ( 0.9784957157296363395, 3.963203712989006533, -41.72081103384405054 ) ) ;
#37819=EDGE_LOOP ( 'NONE', ( #3038, #23153, #61253, #46179 ) ) ;
#37830=DIRECTION ( 'NONE',  ( 0.000000000000000000, 0.000000000000000000, 1.000000000000000000 ) ) ;
#37833=CARTESIAN_POINT ( 'NONE',  ( 1.231276596079881047, 14.27346765619277846, 39.41503383336979027 ) ) ;
#37839=CARTESIAN_POINT ( 'NONE',  ( 5.896782393890504181, -19.39988559968486115, -5.307591317834501332 ) ) ;
#37843=CARTESIAN_POINT ( 'NONE',  ( 0.6845945791218023269, -46.13320409389241661, -8.493173773402611815 ) ) ;
#37856=CARTESIAN_POINT ( 'NONE',  ( 0.8554163680231720024, 43.54276151446858734, 17.47092993535067151 ) ) ;
#37858=ORIENTED_EDGE ( 'NONE', *, *, #40400, .F. ) ;
#37863=CARTESIAN_POINT ( 'NONE',  ( 0.5837800005270554760, 46.47757879888824561, 6.250594182549330746 ) ) ;
#37865=EDGE_CURVE ( 'NONE', #61953, #58463, #16929, .T. ) ;
#37868=EDGE_CURVE ( 'NONE', #12199, #56380, #39338, .T. ) ;
#37869=EDGE_CURVE ( 'NONE', #24828, #41141, #7915, .T. ) ;
#37874=VERTEX_POINT ( 'NONE', #38680 ) ;
#37876=B_SPLINE_CURVE_WITH_KNOTS ( 'NONE', 3,
 ( #41621, #3365, #46947, #51923, #60689, #8694, #17807, #9012, #23424, #37863, #32526, #27814, #55680, #42249, #13118, #3981 ),
 .UNSPECIFIED., .F., .F.,
 ( 4, 3, 3, 3, 3, 4 ),
 ( 1.214354834101861570E-17, 0.0002732102107931890780, 0.0004098135523333805040, 0.0005464168938824999011, 0.0008195847345945434436, 0.001092771384553108301 ),
 .UNSPECIFIED. ) ;
#37877=CARTESIAN_POINT ( 'NONE',  ( 0.5837800304671211249, 43.15703759574290643, 18.34958959048216443 ) ) ;
#37880=CARTESIAN_POINT ( 'NONE',  ( 0.7764139734771222656, 37.35658946184352658, -28.36416215378391570 ) ) ;
#37898=VERTEX_POINT ( 'NONE', #49278 ) ;
#37902=CARTESIAN_POINT ( 'NONE',  ( 0.8554163680231720024, -24.47000373826209341, 40.03029340588522444 ) ) ;
#37906=CARTESIAN_POINT ( 'NONE',  ( 4.291220156522059348, -32.02897670715592682, 34.54755633034208984 ) ) ;
#37909=VERTEX_POINT ( 'NONE', #28947 ) ;
#37919=ORIENTED_EDGE ( 'NONE', *, *, #45708, .F. ) ;
#37920=CARTESIAN_POINT ( 'NONE',  ( 0.5326698147273822848, 0.000000000000000000, 8.000000000000000000 ) ) ;
#37928=CARTESIAN_POINT ( 'NONE',  ( 5.901463166500145796, 8.479222689262201129, -18.23789058324832268 ) ) ;
#37931=CARTESIAN_POINT ( 'NONE',  ( 0.9784957157296378938, 29.30143428922444926, 29.96262681385981708 ) ) ;
#37933=CARTESIAN_POINT ( 'NONE',  ( 1.231276596079881047, 19.39962232756238691, 37.16088568059176112 ) ) ;
#37945=CARTESIAN_POINT ( 'NONE',  ( 4.956445790443998689, -16.41925925744477510, 44.13554095710679093 ) ) ;
#37953=CARTESIAN_POINT ( 'NONE',  ( 0.5832655196449136881, -45.91040371394484509, -9.563995702421170364 ) ) ;
#37956=ORIENTED_EDGE ( 'NONE', *, *, #51612, .F. ) ;
#37966=EDGE_LOOP ( 'NONE', ( #43410, #8010, #52089, #5978 ) ) ;
#37967=CARTESIAN_POINT ( 'NONE',  ( 5.895596859100789899, -19.39920506799825262, -5.310275505304632659 ) ) ;
#37968=CARTESIAN_POINT ( 'NONE',  ( 5.896782393890504181, 8.460428369634295009, 18.24684188237239724 ) ) ;
#37969=CARTESIAN_POINT ( 'NONE',  ( 5.917102823773431552, -7.236410236533870943, -18.76496962268603852 ) ) ;
#37975=VERTEX_POINT ( 'NONE', #58981 ) ;
#37980=VERTEX_POINT ( 'NONE', #22025 ) ;
#37986=CARTESIAN_POINT ( 'NONE',  ( 0.5782707292762442330, 39.98024706216819624, 24.52174950030299527 ) ) ;
#37991=VERTEX_POINT ( 'NONE', #21090 ) ;
#37993=CARTESIAN_POINT ( 'NONE',  ( 5.894904586330512508, -15.78384355525776428, -12.46594138782911010 ) ) ;
#37997=B_SPLINE_CURVE_WITH_KNOTS ( 'NONE', 3,
 ( #15190, #34293, #53371, #10482, #29577, #35222 ),
 .UNSPECIFIED., .F., .F.,
 ( 4, 2, 4 ),
 ( 1.266058488688919593E-17, 0.0002448709889506549340, 0.0004897419779012971829 ),
 .UNSPECIFIED. ) ;
#37999=CARTESIAN_POINT ( 'NONE',  ( 3.661933894777871679, -26.87748316552291783, 38.60352397953695913 ) ) ;
#38003=CARTESIAN_POINT ( 'NONE',  ( 5.896782393890504181, -4.656380635072583374, -19.56640504178867346 ) ) ;
#38014=ORIENTED_EDGE ( 'NONE', *, *, #47110, .F. ) ;
#38019=ORIENTED_EDGE ( 'NONE', *, *, #25784, .T. ) ;
#38034=ORIENTED_EDGE ( 'NONE', *, *, #50693, .T. ) ;
#38041=ORIENTED_EDGE ( 'NONE', *, *, #53130, .T. ) ;
#38043=CARTESIAN_POINT ( 'NONE',  ( 0.9769922540276041456, -39.73250790563689350, 13.32889232511943511 ) ) ;
#38047=AXIS2_PLACEMENT_3D ( 'NONE', #2042, #21172, #21475 ) ;
#38055=DIRECTION ( 'NONE',  ( 0.000000000000000000, 0.000000000000000000, 1.000000000000000000 ) ) ;
#38056=CARTESIAN_POINT ( 'NONE',  ( 0.5830081025819940921, 36.63399018927692907, -29.27768428674311352 ) ) ;
#38058=VERTEX_POINT ( 'NONE', #24445 ) ;
#38059=CARTESIAN_POINT ( 'NONE',  ( 4.962356264823597485, -9.332162870646813602, 41.03835198954837438 ) ) ;
#38066=CARTESIAN_POINT ( 'NONE',  ( 4.956445790443993360, 20.31112743693043399, 42.48524629068788983 ) ) ;
#38072=FACE_OUTER_BOUND ( 'NONE', #44227, .T. ) ;
#38092=ORIENTED_EDGE ( 'NONE', *, *, #28269, .F. ) ;
#38095=CARTESIAN_POINT ( 'NONE',  ( 2.282816707992308736, -43.92595909538881926, 16.64352979263095733 ) ) ;
#38098=VERTEX_POINT ( 'NONE', #57940 ) ;
#38107=CARTESIAN_POINT ( 'NONE',  ( 0.5832655196449118007, 17.06701948983755557, -43.68011021857475384 ) ) ;
#38110=CARTESIAN_POINT ( 'NONE',  ( 5.895881250540457863, 14.91370150166942388, 13.49478377475549173 ) ) ;
#38117=CARTESIAN_POINT ( 'NONE',  ( 0.9762797500689124330, -37.62962005162893320, -18.44821075215020656 ) ) ;
#38125=CARTESIAN_POINT ( 'NONE',  ( 0.8554163680231708922, -18.91615390926475726, -42.93465493506180053 ) ) ;
#38132=ORIENTED_EDGE ( 'NONE', *, *, #44443, .T. ) ;
#38133=CARTESIAN_POINT ( 'NONE',  ( 0.8554163680231708922, 40.82560365045097228, -23.11872746688499802 ) ) ;
#38135=CARTESIAN_POINT ( 'NONE',  ( 5.896782393890504181, 0.6657210432558627877, -20.10181341000305366 ) ) ;
#38137=B_SPLINE_CURVE_WITH_KNOTS ( 'NONE', 3,
 ( #29656, #1141, #20278, #1438 ),
 .UNSPECIFIED., .F., .F.,
 ( 4, 4 ),
 ( 0.000000000000000000, 0.005004948556313796627 ),
 .UNSPECIFIED. ) ;
#38148=ORIENTED_EDGE ( 'NONE', *, *, #25673, .F. ) ;
#38150=CARTESIAN_POINT ( 'NONE',  ( 5.917102823773431552, -19.93133248418633485, -2.689182674449699384 ) ) ;
#38152=CARTESIAN_POINT ( 'NONE',  ( 5.917102823773431552, 14.92182362672981810, 13.48439459911010374 ) ) ;
#38166=EDGE_CURVE ( 'NONE', #47447, #42648, #59378, .T. ) ;
#38178=CARTESIAN_POINT ( 'NONE',  ( 0.5817217712918331118, 42.99501725333171009, 18.72600986313105409 ) ) ;
#38186=ORIENTED_EDGE ( 'NONE', *, *, #50456, .F. ) ;
#38188=DIRECTION ( 'NONE',  ( 0.000000000000000000, 0.000000000000000000, -1.000000000000000000 ) ) ;
#38192=ORIENTED_EDGE ( 'NONE', *, *, #16811, .T. ) ;
#38193=CARTESIAN_POINT ( 'NONE',  ( 0.9772918015221170318, -7.379427770854193547, -41.25385923190006565 ) ) ;
#38195=CARTESIAN_POINT ( 'NONE',  ( 3.661933894777874343, -43.78265458920037645, -17.19622987966910088 ) ) ;
#38199=CARTESIAN_POINT ( 'NONE',  ( 0.9775691876210965692, -37.57309490400189844, 18.56330380952859471 ) ) ;
#38200=ADVANCED_FACE ( 'NONE', ( #31935 ), #9978, .F. ) ;
#38201=LINE ( 'NONE', #19386, #8246 ) ;
#38209=VECTOR ( 'NONE', #20232, 1000.000000000000227 ) ;
#38212=AXIS2_PLACEMENT_3D ( 'NONE', #1672, #41404, #20813 ) ;
#38216=CARTESIAN_POINT ( 'NONE',  ( 0.9787284016396609054, 38.65591695182520482, 16.18814638994915711 ) ) ;
#38217=ORIENTED_EDGE ( 'NONE', *, *, #29823, .T. ) ;
#38220=EDGE_LOOP ( 'NONE', ( #37919, #33149, #5366, #45421 ) ) ;
#38222=CARTESIAN_POINT ( 'NONE',  ( 0.9784957157296372277, -41.02185128615600007, 8.575591760856571710 ) ) ;
#38224=DIRECTION ( 'NONE',  ( 0.07500201931887538753, -0.9970919462213602147, -0.01350362464641113522 ) ) ;
#38225=CARTESIAN_POINT ( 'NONE',  ( 1.091591847532195514, 41.90644475422998028, 0.7803070014481171546 ) ) ;
#38232=EDGE_CURVE ( 'NONE', #41264, #26843, #10108, .T. ) ;
#38238=B_SPLINE_CURVE_WITH_KNOTS ( 'NONE', 3,
 ( #50153, #28113, #17568, #51916, #31661, #7518 ),
 .UNSPECIFIED., .F., .F.,
 ( 4, 2, 4 ),
 ( 7.589415207398531038E-19, 0.0002448709889506578614, 0.0004897419779013149638 ),
 .UNSPECIFIED. ) ;
#38246=CARTESIAN_POINT ( 'NONE',  ( 5.894904586330512508, -4.661384928608805822, -19.56529842882498471 ) ) ;
#38252=CARTESIAN_POINT ( 'NONE',  ( 5.896782393890504181, 12.99025607003297722, 15.35510775321956345 ) ) ;
#38255=ORIENTED_EDGE ( 'NONE', *, *, #53516, .F. ) ;
#38263=ORIENTED_EDGE ( 'NONE', *, *, #37430, .T. ) ;
#38264=CARTESIAN_POINT ( 'NONE',  ( 2.528100132419513812, 39.10451633858129128, 15.26730429898167607 ) ) ;
#38266=CARTESIAN_POINT ( 'NONE',  ( 0.5804410086790514622, 45.37396088368707581, 11.86269470150154071 ) ) ;
#38267=CARTESIAN_POINT ( 'NONE',  ( 0.5835871038041861025, 40.27961859024754432, 24.01638563826134387 ) ) ;
#38268=ORIENTED_EDGE ( 'NONE', *, *, #38630, .F. ) ;
#38271=CARTESIAN_POINT ( 'NONE',  ( 0.5837800304671200147, 16.81232615035175115, 43.77879648407090230 ) ) ;
#38272=ORIENTED_EDGE ( 'NONE', *, *, #43119, .F. ) ;
#38276=ORIENTED_EDGE ( 'NONE', *, *, #45093, .T. ) ;
#38277=CARTESIAN_POINT ( 'NONE',  ( 0.5837800005270550319, 43.17478902026662979, -18.30772655731048459 ) ) ;
#38279=EDGE_CURVE ( 'NONE', #789, #29761, #37801, .T. ) ;
#38282=CARTESIAN_POINT ( 'NONE',  ( 0.5834584762367753807, 11.04850436512404421, -45.57594256081847561 ) ) ;
#38284=CARTESIAN_POINT ( 'NONE',  ( 0.9762797500689124330, -34.26226594605912368, -24.13341909939868657 ) ) ;
#38287=CARTESIAN_POINT ( 'NONE',  ( 0.9784957157296355623, -22.74614816786835902, -35.19866191373972697 ) ) ;
#38291=CARTESIAN_POINT ( 'NONE',  ( 0.8554163680231738898, -0.6539261334249050206, -46.91244881397520317 ) ) ;
#38295=CONICAL_SURFACE ( 'NONE', #31293, 41.88877248453276536, 0.04450589592585735277 ) ;
#38299=EDGE_CURVE ( 'NONE', #35006, #54810, #34012, .T. ) ;
#38306=CARTESIAN_POINT ( 'NONE',  ( 5.917102823773431552, -13.97547681749021464, 14.46291000371417468 ) ) ;
#38309=B_SPLINE_CURVE_WITH_KNOTS ( 'NONE', 3,
 ( #42972, #312, #9736, #56412, #47963, #4387, #9422, #5015, #38271, #23523, #61716, #19458, #38577, #33876, #13528, #32633 ),
 .UNSPECIFIED., .F., .F.,
 ( 4, 3, 3, 3, 3, 4 ),
 ( 6.939740885162003740E-18, 0.0002732102107932011126, 0.0004098135523333842987, 0.0005464168938824958896, 0.0008195847345945464794, 0.001092771384553105915 ),
 .UNSPECIFIED. ) ;
#38316=ORIENTED_EDGE ( 'NONE', *, *, #969, .T. ) ;
#38326=VERTEX_POINT ( 'NONE', #50475 ) ;
#38337=CARTESIAN_POINT ( 'NONE',  ( 0.9787464366903567692, -39.64751462911939228, 13.57971194923611868 ) ) ;
#38352=CARTESIAN_POINT ( 'NONE',  ( 0.5817217712918332229, 37.08439386095844981, -28.70509860588673590 ) ) ;
#38355=CARTESIAN_POINT ( 'NONE',  ( 2.618530812446111078, 46.37964111407201528, 7.658699584660552340 ) ) ;
#38366=CARTESIAN_POINT ( 'NONE',  ( 0.7764146366350233031, -41.45356081493326883, 21.94636118885760823 ) ) ;
#38370=DIRECTION ( 'NONE',  ( -0.07906939808003035641, 0.9968364091521051407, -0.008074879317899831543 ) ) ;
#38373=CARTESIAN_POINT ( 'NONE',  ( 0.9772918015221172539, -1.814983444719383776, -41.86935264422026393 ) ) ;
#38375=EDGE_CURVE ( 'NONE', #31128, #14818, #34779, .T. ) ;
#38385=LINE ( 'NONE', #57433, #54852 ) ;
#38391=ORIENTED_EDGE ( 'NONE', *, *, #33199, .T. ) ;
#38398=CARTESIAN_POINT ( 'NONE',  ( 4.294020221588231045, 0.6022396715791498156, 42.05358393252018345 ) ) ;
#38400=ORIENTED_EDGE ( 'NONE', *, *, #9253, .T. ) ;
#38402=ADVANCED_FACE ( 'NONE', ( #14141 ), #20882, .F. ) ;
#38405=CARTESIAN_POINT ( 'NONE',  ( 0.5835871038041883230, 46.89579726320849318, 0.1365721404356005364 ) ) ;
#38406=CARTESIAN_POINT ( 'NONE',  ( 4.960386119450151732, 23.14534831554928118, 37.13124447179546195 ) ) ;
#38407=DIRECTION ( 'NONE',  ( 0.000000000000000000, 0.000000000000000000, 1.000000000000000000 ) ) ;
#38409=ORIENTED_EDGE ( 'NONE', *, *, #6764, .T. ) ;
#38414=CARTESIAN_POINT ( 'NONE',  ( 5.895881250540457863, 0.6675221664546298062, 20.10179334700246656 ) ) ;
#38416=CARTESIAN_POINT ( 'NONE',  ( 1.231276596079887931, -7.805643096901414779, -41.18675402191659174 ) ) ;
#38419=VERTEX_POINT ( 'NONE', #33243 ) ;
#38432=CARTESIAN_POINT ( 'NONE',  ( 2.282816707992306959, 37.66448606630884655, 28.06926176030984621 ) ) ;
#38438=EDGE_LOOP ( 'NONE', ( #57541, #49811, #52070, #35790 ) ) ;
#38441=CARTESIAN_POINT ( 'NONE',  ( 5.838029081930957709, 44.62720369181010227, 15.47506862028764907 ) ) ;
#38442=LINE ( 'NONE', #43771, #934 ) ;
#38443=B_SPLINE_CURVE_WITH_KNOTS ( 'NONE', 3,
 ( #3334, #27467, #46595, #22465, #41590, #32180 ),
 .UNSPECIFIED., .F., .F.,
 ( 4, 2, 4 ),
 ( 1.084202172485504434E-19, 0.0002291459268755673075, 0.0004582918537511345065 ),
 .UNSPECIFIED. ) ;
#38448=B_SPLINE_CURVE_WITH_KNOTS ( 'NONE', 3,
 ( #7158, #17215, #31303, #44817 ),
 .UNSPECIFIED., .F., .F.,
 ( 4, 4 ),
 ( 0.002405070305343063371, 0.004447772540402989729 ),
 .UNSPECIFIED. ) ;
#38462=ORIENTED_EDGE ( 'NONE', *, *, #21824, .T. ) ;
#38473=DIRECTION ( 'NONE',  ( -0.07500201931887529039, -0.9374924185315484104, 0.3398274007403745411 ) ) ;
#38487=VERTEX_POINT ( 'NONE', #301 ) ;
#38489=CARTESIAN_POINT ( 'NONE',  ( 4.956445790443989807, 44.30493387627029733, 15.95653108789479191 ) ) ;
#38492=ORIENTED_EDGE ( 'NONE', *, *, #206, .F. ) ;
#38493=B_SPLINE_CURVE_WITH_KNOTS ( 'NONE', 3,
 ( #45188, #2538, #12589, #36399, #39873, #55461 ),
 .UNSPECIFIED., .F., .F.,
 ( 4, 2, 4 ),
 ( 7.007167689862070887E-18, 0.0002448709889506578614, 0.0004897419779013087839 ),
 .UNSPECIFIED. ) ;
#38502=CARTESIAN_POINT ( 'NONE',  ( 5.838029081930957709, -22.68231883182896880, 41.43159990350574162 ) ) ;
#38504=CARTESIAN_POINT ( 'NONE',  ( 0.5782707292762423457, -24.62356639979799411, 39.91761931105558858 ) ) ;
#38508=CARTESIAN_POINT ( 'NONE',  ( 5.896782393890504181, 8.460428369634295009, 18.24684188237239724 ) ) ;
#38512=ORIENTED_EDGE ( 'NONE', *, *, #31213, .T. ) ;
#38517=CONICAL_SURFACE ( 'NONE', #18813, 42.08604991992415023, 1.569615340895231137 ) ;
#38519=ORIENTED_EDGE ( 'NONE', *, *, #36628, .F. ) ;
#38525=EDGE_CURVE ( 'NONE', #61765, #35559, #39186, .T. ) ;
#38531=ORIENTED_EDGE ( 'NONE', *, *, #20010, .F. ) ;
#38533=FACE_OUTER_BOUND ( 'NONE', #42925, .T. ) ;
#38534=CARTESIAN_POINT ( 'NONE',  ( 0.8560838555295158248, -8.701885300216421371, 46.09392613244839509 ) ) ;
#38537=DIRECTION ( 'NONE',  ( -0.07500201931887529039, 0.6834640454944322929, -0.7261209235481894675 ) ) ;
#38540=VECTOR ( 'NONE', #7368, 1000.000000000000114 ) ;
#38551=CARTESIAN_POINT ( 'NONE',  ( 1.231276596079887931, 38.25526645152051941, -17.14092645516095104 ) ) ;
#38557=EDGE_CURVE ( 'NONE', #26909, #13226, #54829, .T. ) ;
#38573=EDGE_CURVE ( 'NONE', #53916, #49966, #5672, .T. ) ;
#38575=CARTESIAN_POINT ( 'NONE',  ( 0.5782707292762423457, -46.74268073083585762, 3.854627323459990595 ) ) ;
#38577=CARTESIAN_POINT ( 'NONE',  ( 0.5830081025819928708, 17.10943265121773749, 43.66347843147279661 ) ) ;
#38578=EDGE_LOOP ( 'NONE', ( #232, #9347, #29215, #31502 ) ) ;
#38579=EDGE_CURVE ( 'NONE', #59637, #36737, #54042, .T. ) ;
#38589=ORIENTED_EDGE ( 'NONE', *, *, #30171, .F. ) ;
#38592=CARTESIAN_POINT ( 'NONE',  ( 0.8560838555295158248, -42.27062166135473120, 20.33635607586422012 ) ) ;
#38593=CARTESIAN_POINT ( 'NONE',  ( 0.9775691876210976794, -22.23098038610267935, -35.52628914005386207 ) ) ;
#38616=ORIENTED_EDGE ( 'NONE', *, *, #39355, .T. ) ;
#38618=CARTESIAN_POINT ( 'NONE',  ( 0.9784957157296357844, -1.167710547123469222, 41.89235621292397838 ) ) ;
#38619=CARTESIAN_POINT ( 'NONE',  ( 0.5848930533535030563, 46.89605428954452293, -0.1821385726608810984 ) ) ;
#38624=ADVANCED_FACE ( 'NONE', ( #40421 ), #9590, .F. ) ;
#38628=EDGE_CURVE ( 'NONE', #44492, #13765, #38448, .T. ) ;
#38630=EDGE_CURVE ( 'NONE', #40451, #19905, #39893, .T. ) ;
#38639=CARTESIAN_POINT ( 'NONE',  ( 4.962356264823608143, 0.000000000000000000, 0.000000000000000000 ) ) ;
#38640=VERTEX_POINT ( 'NONE', #41347 ) ;
#38645=ORIENTED_EDGE ( 'NONE', *, *, #20508, .T. ) ;
#38661=CARTESIAN_POINT ( 'NONE',  ( 2.528190830796654076, -8.172783047358173292, 41.17596086813060197 ) ) ;
#38666=ORIENTED_EDGE ( 'NONE', *, *, #51983, .F. ) ;
#38667=ORIENTED_EDGE ( 'NONE', *, *, #27230, .F. ) ;
#38671=CARTESIAN_POINT ( 'NONE',  ( 5.896278296736517710, -11.93494920661379766, 16.18900759929194422 ) ) ;
#38672=EDGE_CURVE ( 'NONE', #12754, #30302, #22829, .T. ) ;
#38674=DIRECTION ( 'NONE',  ( -1.000000000000000000, -0.000000000000000000, -0.000000000000000000 ) ) ;
#38680=CARTESIAN_POINT ( 'NONE',  ( 0.8560838555295223751, 5.603718208093996012, 46.57221463840868125 ) ) ;
#38681=CARTESIAN_POINT ( 'NONE',  ( 1.157643937452368155, 3.373327138002636172, -41.78065268296760593 ) ) ;
#38696=CARTESIAN_POINT ( 'NONE',  ( 1.231276596079887264, -37.02495017545888345, 19.65781868679367150 ) ) ;
#38700=CARTESIAN_POINT ( 'NONE',  ( 5.917102823773431552, 19.70720580609864925, -4.014443593801511945 ) ) ;
#38701=CARTESIAN_POINT ( 'NONE',  ( 0.8554163680231720024, 31.95314001164609152, -34.35407277904558754 ) ) ;
#38708=EDGE_CURVE ( 'NONE', #53909, #50432, #27215, .T. ) ;
#38710=ORIENTED_EDGE ( 'NONE', *, *, #39263, .F. ) ;
#38711=B_SPLINE_CURVE_WITH_KNOTS ( 'NONE', 3,
 ( #9956, #39097, #24661, #43485 ),
 .UNSPECIFIED., .F., .F.,
 ( 4, 4 ),
 ( 0.000000000000000000, 0.004447772540403784232 ),
 .UNSPECIFIED. ) ;
#38715=EDGE_CURVE ( 'NONE', #19905, #14965, #14068, .T. ) ;
#38719=CARTESIAN_POINT ( 'NONE',  ( 4.962356264823608143, 0.000000000000000000, 0.000000000000000000 ) ) ;
#38720=VECTOR ( 'NONE', #17182, 1000.000000000000227 ) ;
#38726=CARTESIAN_POINT ( 'NONE',  ( 0.8560838555295158248, -34.16988317699912159, -32.13708010619451727 ) ) ;
#38731=CARTESIAN_POINT ( 'NONE',  ( 0.7764146366350247463, -0.6759651462121027965, 46.89971796066871690 ) ) ;
#38737=CARTESIAN_POINT ( 'NONE',  ( 0.8554163680231708922, -2.480940174720814184, 46.85136507041470821 ) ) ;
#38747=CARTESIAN_POINT ( 'NONE',  ( 1.231276596079887264, 15.85305549123172320, 38.80666698661448777 ) ) ;
#38757=ORIENTED_EDGE ( 'NONE', *, *, #982, .F. ) ;
#38760=CARTESIAN_POINT ( 'NONE',  ( 0.6064782688330870863, 3.986484645119572345, 46.72731948863529539 ) ) ;
#38763=FACE_BOUND ( 'NONE', #57494, .T. ) ;
#38766=FACE_OUTER_BOUND ( 'NONE', #935, .T. ) ;
#38771=CARTESIAN_POINT ( 'NONE',  ( 4.962356264823594820, 34.94214251265108118, 23.45809613945535332 ) ) ;
#38779=DIRECTION ( 'NONE',  ( -1.000000000000000000, -0.000000000000000000, -0.000000000000000000 ) ) ;
#38782=DIRECTION ( 'NONE',  ( -1.000000000000000000, -0.000000000000000000, -0.000000000000000000 ) ) ;
#38783=CARTESIAN_POINT ( 'NONE',  ( 5.895596859100789899, -11.92767122914705880, 16.19440774656069237 ) ) ;
#38787=CARTESIAN_POINT ( 'NONE',  ( 0.5804410086790514622, -14.41595396256411910, -44.62846763227064883 ) ) ;
#38795=CARTESIAN_POINT ( 'NONE',  ( 0.5817216825391131607, 43.35051279402986779, 17.88764916645309455 ) ) ;
#38812=CARTESIAN_POINT ( 'NONE',  ( 5.838029081930955932, -37.05692651727511588, -29.28906374820117620 ) ) ;
#38814=CARTESIAN_POINT ( 'NONE',  ( 0.9762797500689124330, 40.55021165774366665, -10.58324712448374605 ) ) ;
#38817=VERTEX_POINT ( 'NONE', #48188 ) ;
#38818=CARTESIAN_POINT ( 'NONE',  ( 0.8554163680231738898, -20.57434774096721242, 42.16517150618003740 ) ) ;
#38819=CARTESIAN_POINT ( 'NONE',  ( 0.9790724872846768845, 36.07885981586515101, -21.32254873059516243 ) ) ;
#38828=CARTESIAN_POINT ( 'NONE',  ( 0.9790724872846771065, -31.05450468904443895, -28.14165859539148684 ) ) ;
#38831=EDGE_CURVE ( 'NONE', #13574, #54025, #48724, .T. ) ;
#38836=CARTESIAN_POINT ( 'NONE',  ( 0.9783242366443547500, -41.83210916748958397, 2.531626513875353091 ) ) ;
#38840=CARTESIAN_POINT ( 'NONE',  ( 4.256459001490160432, 0.6428830997700460959, 47.05679116045861576 ) ) ;
#38848=CARTESIAN_POINT ( 'NONE',  ( 4.956445790444004018, -45.55738122058057371, -11.91902120403893761 ) ) ;
#38860=DIRECTION ( 'NONE',  ( 0.07500201931887537365, -0.2442817726706159320, 0.9667994169624807288 ) ) ;
#38863=CARTESIAN_POINT ( 'NONE',  ( 5.896782393890504181, -17.30835043929363692, 10.24436879210309925 ) ) ;
#38865=EDGE_CURVE ( 'NONE', #11980, #16218, #21226, .T. ) ;
#38886=CARTESIAN_POINT ( 'NONE',  ( 1.231276596079887264, 14.27346765619334512, -39.41503383336959132 ) ) ;
#38893=CARTESIAN_POINT ( 'NONE',  ( 2.528100132419516477, 16.21066372738161476, 38.72296683042027610 ) ) ;
#38898=VERTEX_POINT ( 'NONE', #14681 ) ;
#38906=ORIENTED_EDGE ( 'NONE', *, *, #37868, .T. ) ;
#38909=CARTESIAN_POINT ( 'NONE',  ( 2.282803330402976449, 46.71114521383905327, -4.956391859874321959 ) ) ;
#38912=CARTESIAN_POINT ( 'NONE',  ( 5.917102823773431552, 0.6806365918031147544, 20.10040924662084194 ) ) ;
#38916=CARTESIAN_POINT ( 'NONE',  ( 0.9789889208857707192, 41.52179126368472595, -5.681174904662252167 ) ) ;
#38919=CARTESIAN_POINT ( 'NONE',  ( 2.528100132419517365, -41.36196155245985295, -7.172301943233399868 ) ) ;
#38920=( BOUNDED_SURFACE ( )  B_SPLINE_SURFACE ( 3, 1, ( 
 ( #18961, #24566 ),
 ( #58055, #53358 ),
 ( #425, #15480 ),
 ( #20187, #48368 ) ),
 .UNSPECIFIED., .F., .F., .F. ) 
 B_SPLINE_SURFACE_WITH_KNOTS ( ( 4, 4 ),
 ( 2, 2 ),
 ( 0.000000000000000000, 1.000000000000000000 ),
 ( 0.000000000000000000, 1.000000000000000000 ),
 .UNSPECIFIED. ) 
 GEOMETRIC_REPRESENTATION_ITEM ( )  RATIONAL_B_SPLINE_SURFACE ( (
 ( 1.000000000000000000, 1.000000000000000000),
 ( 0.9952954269826590483, 0.8620686068821307169),
 ( 0.9952954269826590483, 0.8620686068821307169),
 ( 1.000000000000000000, 1.000000000000000000) ) ) 
 REPRESENTATION_ITEM ( '' )  SURFACE ( )  );
#38922=EDGE_CURVE ( 'NONE', #51483, #34855, #43502, .T. ) ;
#38926=CARTESIAN_POINT ( 'NONE',  ( 1.231276596079881047, 5.037240371906286818, -41.61613846158368091 ) ) ;
#38927=CARTESIAN_POINT ( 'NONE',  ( 5.838029081930955932, 13.97520979541447339, 45.11938130479041575 ) ) ;
#38930=EDGE_CURVE ( 'NONE', #33742, #60718, #55600, .T. ) ;
#38933=ORIENTED_EDGE ( 'NONE', *, *, #10768, .F. ) ;
#38938=ORIENTED_EDGE ( 'NONE', *, *, #58959, .F. ) ;
#38941=EDGE_CURVE ( 'NONE', #371, #20909, #59256, .T. ) ;
#38951=ORIENTED_EDGE ( 'NONE', *, *, #35305, .F. ) ;
#38955=CARTESIAN_POINT ( 'NONE',  ( 0.9789233960466696693, -17.52144526371232303, -38.07014161653558659 ) ) ;
#38965=DIRECTION ( 'NONE',  ( -0.07906939808003034253, 0.4861426559824175153, 0.8702949777642189355 ) ) ;
#38969=CARTESIAN_POINT ( 'NONE',  ( 4.962356264823601926, -41.65024625884322518, 6.040909239515423579 ) ) ;
#38973=CARTESIAN_POINT ( 'NONE',  ( 0.9762797500689124330, -22.97506929404208975, 35.04955029839425151 ) ) ;
#38974=DIRECTION ( 'NONE',  ( 0.000000000000000000, 0.000000000000000000, 1.000000000000000000 ) ) ;
#38975=ORIENTED_EDGE ( 'NONE', *, *, #24947, .T. ) ;
#38987=CARTESIAN_POINT ( 'NONE',  ( 0.5804410086790514622, -44.12183670707856464, -15.89916279082931005 ) ) ;
#38989=CARTESIAN_POINT ( 'NONE',  ( 2.528190830796658517, -11.27641220880940409, -40.43632851595235422 ) ) ;
#38991=EDGE_CURVE ( 'NONE', #18385, #5387, #30596, .T. ) ;
#39013=ORIENTED_EDGE ( 'NONE', *, *, #41633, .T. ) ;
#39015=CARTESIAN_POINT ( 'NONE',  ( 1.000110580585048980, 36.38996880054845207, -20.78912344152613301 ) ) ;
#39019=CARTESIAN_POINT ( 'NONE',  ( 2.528100132419517365, 40.15111052815427684, -12.25324862997623931 ) ) ;
#39024=B_SPLINE_CURVE_WITH_KNOTS ( 'NONE', 3,
 ( #16803, #60602, #17721, #51515 ),
 .UNSPECIFIED., .F., .F.,
 ( 4, 4 ),
 ( 0.000000000000000000, 0.004447772540403811120 ),
 .UNSPECIFIED. ) ;
#39030=CARTESIAN_POINT ( 'NONE',  ( 0.9772918015221183641, -41.14952526578677805, -7.940618751146248933 ) ) ;
#39032=CARTESIAN_POINT ( 'NONE',  ( 0.8560838555295223751, -13.02223058219873764, 45.06433561859954295 ) ) ;
#39033=EDGE_CURVE ( 'NONE', #56156, #33009, #29381, .T. ) ;
#39043=CARTESIAN_POINT ( 'NONE',  ( 4.962356264823608143, -9.332162870646227404, -41.03835198954849517 ) ) ;
#39044=VERTEX_POINT ( 'NONE', #42200 ) ;
#39045=CARTESIAN_POINT ( 'NONE',  ( 0.5806925824938502512, 46.40146083665138832, -6.791670970259978013 ) ) ;
#39047=CARTESIAN_POINT ( 'NONE',  ( 4.958415959904820980, 40.76596448693046426, -20.03347431857393346 ) ) ;
#39048=CARTESIAN_POINT ( 'NONE',  ( 5.895881250540457863, -11.92688455204506681, 16.19497164216380369 ) ) ;
#39052=CARTESIAN_POINT ( 'NONE',  ( 5.896782393890504181, -9.660289833039602314, 17.64100017628490136 ) ) ;
#39060=EDGE_CURVE ( 'NONE', #61765, #15970, #1738, .T. ) ;
#39062=CARTESIAN_POINT ( 'NONE',  ( 0.8554163680231738898, 17.71207986799998224, -43.44522643353823099 ) ) ;
#39064=CLOSED_SHELL ( 'NONE', ( #44378, #47250, #44862, #34514, #8484, #15713, #14170, #42687, #10257, #57707, #18995, #2090, #21718, #47115, #44709, #13110, #41676, #12184, #21504, #30982, #57484, #44555, #27127, #7405, #20799, #15204, #24083, #9992, #46732, #41266, #16322, #22569, #26329, #22636, #13300, #61090, #13750, #18910, #27574, #35515, #53455, #57847, #57544, #56935, #56832, #58594, #35360, #29125, #41847, #35832, #29139, #30812, #49669, #12620, #39643, #13306, #60406, #40554, #37266, #12803, #32874, #55147, #13220, #8461, #30448, #30975, #35090, #58650, #59356, #41677, #49883, #38624, #33904, #8989, #26097, #53822, #33418, #10835, #55443, #11820, #39506, #4995, #24671, #4812, #26967, #39075, #31056, #33373, #10843, #53111, #11119, #58491, #37445, #36734, #39286, #11079, #42018, #8244, #26616, #32116, #41506, #46143, #35507, #54353, #26026, #25047, #7179, #42895, #27456, #5088, #59527, #12598, #567, #48573, #18292, #39819, #36646, #43736, #46406, #35947, #1428, #30301, #28277, #57919, #40297, #56744, #57820, #46434, #1211, #2896, #13730, #39815, #1375, #39322, #38402, #59167, #61752, #17427, #48173, #41051, #9386, #36304, #61882, #16404, #56008, #43049, #15360, #2542, #54231, #28632, #42080, #48584, #38200, #4058, #11822, #12295, #10476, #28375, #11157, #17161, #17274, #59831, #19777, #58533, #5012, #54551, #3362, #22084, #9068, #33881, #37502, #40564, #8472, #31982, #25824, #11115, #54450, #34738, #49317, #7346, #56696, #17553, #37580, #24409, #30060, #9108, #53672, #60400, #1576, #56144, #36210, #1981, #8881, #57267, #50328, #20442, #59388, #51554, #41745, #51479, #42100, #48723, #533, #24863, #26261, #15948, #23784, #50756, #339, #1533, #35041, #9080, #16069, #29128, #3227, #36313, #13880, #6828, #35555, #34109, #27084, #45493, #9154, #48434, #31476, #7373, #15335, #51187, #14885, #51602, #5268, #43984, #60721, #48523, #43244, #56443, #17900, #31273, #5846, #39363, #20316, #16946, #58176, #30755, #60444, #55823, #10130, #23606, #14799, #11654, #60592, #45837, #54511, #40131, #12056, #5461, #2234, #47835, #8767, #7176, #1198, #57234, #57852, #2152, #16056, #27790, #43506, #42310, #36846, #27253, #1463, #33758, #13179, #43104, #24323, #37794, #58929, #2600, #3522, #59633, #8841, #8336, #48116, #4508, #36338, #23415, #52204, #45887, #11838, #57054, #57212, #51475, #31915 ) ) ;
#39068=CARTESIAN_POINT ( 'NONE',  ( 0.8554163680231816613, 46.90810212776801791, -0.9140174411379278219 ) ) ;
#39072=FACE_OUTER_BOUND ( 'NONE', #36677, .T. ) ;
#39075=ADVANCED_FACE ( 'NONE', ( #17440 ), #29172, .F. ) ;
#39077=CARTESIAN_POINT ( 'NONE',  ( 1.231276596079887264, 32.36747132271594296, -26.63876069172940930 ) ) ;
#39094=( BOUNDED_SURFACE ( )  B_SPLINE_SURFACE ( 3, 1, ( 
 ( #1581, #20409 ),
 ( #1900, #44858 ),
 ( #54196, #58912 ),
 ( #29487, #39858 ) ),
 .UNSPECIFIED., .F., .F., .F. ) 
 B_SPLINE_SURFACE_WITH_KNOTS ( ( 4, 4 ),
 ( 2, 2 ),
 ( 0.000000000000000000, 1.000000000000000000 ),
 ( 0.000000000000000000, 1.000000000000000000 ),
 .UNSPECIFIED. ) 
 GEOMETRIC_REPRESENTATION_ITEM ( )  RATIONAL_B_SPLINE_SURFACE ( (
 ( 1.000000000000000000, 1.000000000000000000),
 ( 0.7282232189291694135, 0.9929344683865672927),
 ( 0.7282232189291694135, 0.9929344683865672927),
 ( 1.000000000000000000, 1.000000000000000000) ) ) 
 REPRESENTATION_ITEM ( '' )  SURFACE ( )  );
#39095=B_SPLINE_CURVE_WITH_KNOTS ( 'NONE', 3,
 ( #31227, #20600, #7394, #21211, #35023, #2705 ),
 .UNSPECIFIED., .F., .F.,
 ( 4, 2, 4 ),
 ( 1.205235924680983448E-16, 0.0002448718616795927169, 0.0004897437233590649789 ),
 .UNSPECIFIED. ) ;
#39096=ORIENTED_EDGE ( 'NONE', *, *, #43935, .T. ) ;
#39097=CARTESIAN_POINT ( 'NONE',  ( 3.661933894777863685, 44.83346409145190137, 14.23346979875768170 ) ) ;
#39101=CARTESIAN_POINT ( 'NONE',  ( 0.5806925824938499181, 42.95845041307745760, 18.80940989108190209 ) ) ;
#39104=( BOUNDED_SURFACE ( )  B_SPLINE_SURFACE ( 3, 1, ( 
 ( #16765, #58712 ),
 ( #11141, #35877 ),
 ( #21762, #25841 ),
 ( #25223, #7016 ) ),
 .UNSPECIFIED., .F., .F., .F. ) 
 B_SPLINE_SURFACE_WITH_KNOTS ( ( 4, 4 ),
 ( 2, 2 ),
 ( 0.000000000000000000, 1.000000000000000000 ),
 ( 0.000000000000000000, 1.000000000000000000 ),
 .UNSPECIFIED. ) 
 GEOMETRIC_REPRESENTATION_ITEM ( )  RATIONAL_B_SPLINE_SURFACE ( (
 ( 1.000000000000000000, 1.000000000000000000),
 ( 0.7282232189291693025, 0.9929344683865674037),
 ( 0.7282232189291693025, 0.9929344683865674037),
 ( 1.000000000000000000, 1.000000000000000000) ) ) 
 REPRESENTATION_ITEM ( '' )  SURFACE ( )  );
#39111=ORIENTED_EDGE ( 'NONE', *, *, #50030, .T. ) ;
#39114=CARTESIAN_POINT ( 'NONE',  ( 0.9790724872846766624, 40.40890317131761833, 11.11106450672177814 ) ) ;
#39116=B_SPLINE_CURVE_WITH_KNOTS ( 'NONE', 3,
 ( #52674, #49451, #11566, #52987, #57663, #59147, #2127, #43316, #20956, #14796, #21263, #35693, #26260, #25645, #6819, #5049, #25963, #25340, #45097 ),
 .UNSPECIFIED., .F., .F.,
 ( 4, 3, 3, 3, 3, 3, 4 ),
 ( 1.214354834101861570E-17, 0.0002732106629380600467, 0.0004098138914053718000, 0.0005464171197651384497, 0.0006830203481512496944, 0.0008196235766963560435, 0.001011968216111135523 ),
 .UNSPECIFIED. ) ;
#39118=CARTESIAN_POINT ( 'NONE',  ( 3.661921753702005677, -46.43414857639643856, -7.516712700321615870 ) ) ;
#39122=ORIENTED_EDGE ( 'NONE', *, *, #47061, .F. ) ;
#39125=CARTESIAN_POINT ( 'NONE',  ( 4.291220156522060236, 0.5803847665930184085, 47.10681639453469671 ) ) ;
#39127=CARTESIAN_POINT ( 'NONE',  ( 5.917102823773431552, 19.71063251686268458, 3.997584750438410328 ) ) ;
#39128=ORIENTED_EDGE ( 'NONE', *, *, #47930, .T. ) ;
#39133=B_SPLINE_CURVE_WITH_KNOTS ( 'NONE', 3,
 ( #20914, #59111, #45986, #40063 ),
 .UNSPECIFIED., .F., .F.,
 ( 4, 4 ),
 ( 4.336808689942017736E-19, 0.004041751736740999482 ),
 .UNSPECIFIED. ) ;
#39136=ORIENTED_EDGE ( 'NONE', *, *, #14108, .F. ) ;
#39145=CARTESIAN_POINT ( 'NONE',  ( 3.782542959838395280, -21.14749290209289967, -36.33209871934869994 ) ) ;
#39150=CARTESIAN_POINT ( 'NONE',  ( 4.962356264823608143, 0.000000000000000000, 0.000000000000000000 ) ) ;
#39153=CARTESIAN_POINT ( 'NONE',  ( 5.896782393890504181, -13.98685533979004347, -14.45316451791091161 ) ) ;
#39158=CARTESIAN_POINT ( 'NONE',  ( 3.238018933889920792, 11.38191749426280097, -7.061122185704434173 ) ) ;
#39165=DIRECTION ( 'NONE',  ( -0.07500201931887527651, 0.8647811570515492319, 0.4965161100172628683 ) ) ;
#39169=CARTESIAN_POINT ( 'NONE',  ( 5.917102823773431552, 12.97825203069038835, 15.36407147469780554 ) ) ;
#39174=CARTESIAN_POINT ( 'NONE',  ( 5.917102823773431552, 10.82912387347634464, -16.94756012482760354 ) ) ;
#39177=EDGE_CURVE ( 'NONE', #35968, #4749, #3957, .T. ) ;
#39178=CARTESIAN_POINT ( 'NONE',  ( 4.956445790444026223, 7.299064093731650438, -46.52162629890785439 ) ) ;
#39179=ORIENTED_EDGE ( 'NONE', *, *, #9250, .T. ) ;
#39186=LINE ( 'NONE', #48551, #9731 ) ;
#39192=CARTESIAN_POINT ( 'NONE',  ( 5.895596859100789899, 16.58392706178506160, 11.37987462241481929 ) ) ;
#39194=VECTOR ( 'NONE', #28051, 1000.000000000000000 ) ;
#39206=CARTESIAN_POINT ( 'NONE',  ( 0.5835226383429314989, -46.80316998458874167, -2.950551463651092998 ) ) ;
#39211=CARTESIAN_POINT ( 'NONE',  ( 0.9790320750461911636, 40.44225345157877882, -10.98914320138077905 ) ) ;
#39222=CARTESIAN_POINT ( 'NONE',  ( 0.9790724872846782167, 41.54009254446635424, -5.545802140234084021 ) ) ;
#39224=CARTESIAN_POINT ( 'NONE',  ( 4.291220156522059348, -42.97446925027733755, 19.30243481954189022 ) ) ;
#39231=EDGE_CURVE ( 'NONE', #46648, #59248, #56335, .T. ) ;
#39238=CARTESIAN_POINT ( 'NONE',  ( 4.962356264823601926, -42.08379584346671720, 0.4355746408606013254 ) ) ;
#39241=CARTESIAN_POINT ( 'NONE',  ( 0.9769922540276050338, -1.841908291151032273, 41.86811351055972352 ) ) ;
#39247=ORIENTED_EDGE ( 'NONE', *, *, #31122, .F. ) ;
#39255=ORIENTED_EDGE ( 'NONE', *, *, #10222, .T. ) ;
#39260=CARTESIAN_POINT ( 'NONE',  ( 2.282803330402960906, 36.03600629612929396, 30.13143139119534197 ) ) ;
#39263=EDGE_CURVE ( 'NONE', #4666, #3997, #61545, .T. ) ;
#39266=CARTESIAN_POINT ( 'NONE',  ( 1.091591847532195070, -37.05036493332335823, -19.59666934107434244 ) ) ;
#39276=ORIENTED_EDGE ( 'NONE', *, *, #3713, .F. ) ;
#39286=ADVANCED_FACE ( 'NONE', ( #44657 ), #11627, .F. ) ;
#39288=CARTESIAN_POINT ( 'NONE',  ( 4.960386119450145515, 6.813122688534734905, -43.22057176742709572 ) ) ;
#39299=FACE_OUTER_BOUND ( 'NONE', #30923, .T. ) ;
#39303=CARTESIAN_POINT ( 'NONE',  ( 0.7764139734771241530, 45.46540455849966378, -11.52985078996363910 ) ) ;
#39308=ORIENTED_EDGE ( 'NONE', *, *, #56953, .F. ) ;
#39319=ORIENTED_EDGE ( 'NONE', *, *, #13321, .F. ) ;
#39322=ADVANCED_FACE ( 'NONE', ( #10825 ), #22410, .F. ) ;
#39334=EDGE_CURVE ( 'NONE', #13574, #22672, #12990, .T. ) ;
#39338=B_SPLINE_CURVE_WITH_KNOTS ( 'NONE', 3,
 ( #51502, #38373, #27400, #3575, #22707, #60907, #8591, #27718, #46847, #3888, #42158, #18334, #61515, #37765, #56822, #13951, #15473, #34582, #24870 ),
 .UNSPECIFIED., .F., .F.,
 ( 4, 3, 3, 3, 3, 3, 4 ),
 ( 9.107943584450270299E-18, 0.0002732106629380616730, 0.0004098138914053771668, 0.0005464171197651476655, 0.0006830203481512577175, 0.0008196235766963648256, 0.001011968216111140727 ),
 .UNSPECIFIED. ) ;
#39343=DIRECTION ( 'NONE',  ( 0.07906939808003032866, -0.2389416749771389459, 0.9678093336222693965 ) ) ;
#39347=CARTESIAN_POINT ( 'NONE',  ( 4.960386119450149955, 39.26151414358990621, -19.31243050019935126 ) ) ;
#39349=ORIENTED_EDGE ( 'NONE', *, *, #34467, .T. ) ;
#39353=CARTESIAN_POINT ( 'NONE',  ( 0.8560838555295158248, -2.480523550131575661, 46.84250032821661591 ) ) ;
#39355=EDGE_CURVE ( 'NONE', #48936, #18068, #24963, .T. ) ;
#39360=DIRECTION ( 'NONE',  ( 0.07906939808003035641, 0.9443293062557466255, -0.3193590324913357370 ) ) ;
#39363=ADVANCED_FACE ( 'NONE', ( #61486 ), #59163, .F. ) ;
#39365=CARTESIAN_POINT ( 'NONE',  ( 0.8560838555295223751, -18.91252766612315739, 42.92655508376904550 ) ) ;
#39369=ORIENTED_EDGE ( 'NONE', *, *, #14589, .T. ) ;
#39371=CARTESIAN_POINT ( 'NONE',  ( 0.9791128995231621612, 41.53542872017264642, 5.580823888783615239 ) ) ;
#39372=( BOUNDED_SURFACE ( )  B_SPLINE_SURFACE ( 3, 1, ( 
 ( #4167, #42429 ),
 ( #56797, #33030 ),
 ( #5929, #15379 ),
 ( #58559, #34482 ) ),
 .UNSPECIFIED., .F., .F., .F. ) 
 B_SPLINE_SURFACE_WITH_KNOTS ( ( 4, 4 ),
 ( 2, 2 ),
 ( 0.000000000000000000, 1.000000000000000000 ),
 ( 0.000000000000000000, 1.000000000000000000 ),
 .UNSPECIFIED. ) 
 GEOMETRIC_REPRESENTATION_ITEM ( )  RATIONAL_B_SPLINE_SURFACE ( (
 ( 1.000000000000000000, 1.000000000000000000),
 ( 0.9729067724841187204, 0.9999501103223794596),
 ( 0.9729067724841187204, 0.9999501103223794596),
 ( 1.000000000000000000, 1.000000000000000000) ) ) 
 REPRESENTATION_ITEM ( '' )  SURFACE ( )  );
#39373=CARTESIAN_POINT ( 'NONE',  ( 0.5837800005270556980, 27.81773451563321231, -37.75458786769539898 ) ) ;
#39374=ORIENTED_EDGE ( 'NONE', *, *, #22012, .T. ) ;
#39382=CARTESIAN_POINT ( 'NONE',  ( 5.896782393890504181, -13.97772289704291460, 14.46199673252260354 ) ) ;
#39388=CARTESIAN_POINT ( 'NONE',  ( 0.9790850452238870627, 29.09817565893450819, -30.16013102731797346 ) ) ;
#39394=CARTESIAN_POINT ( 'NONE',  ( 5.895596859100789899, -9.669028665050335647, 17.63627137143570067 ) ) ;
#39396=CARTESIAN_POINT ( 'NONE',  ( 1.091591847532195958, -41.22213727214368362, 7.582505500979439539 ) ) ;
#39399=CARTESIAN_POINT ( 'NONE',  ( 5.895596859100789899, 5.955534046174260965, 19.21092911436994299 ) ) ;
#39408=ORIENTED_EDGE ( 'NONE', *, *, #969, .F. ) ;
#39409=CARTESIAN_POINT ( 'NONE',  ( 0.5806925824938499181, 17.36345040154836994, -43.56297685531297503 ) ) ;
#39411=EDGE_CURVE ( 'NONE', #13765, #30850, #24165, .T. ) ;
#39413=CARTESIAN_POINT ( 'NONE',  ( 1.231276596079881047, 5.037240371906286818, -41.61613846158368091 ) ) ;
#39414=CARTESIAN_POINT ( 'NONE',  ( 4.956445790444027111, 14.46717203539434671, -44.81337951368921324 ) ) ;
#39416=LINE ( 'NONE', #49400, #58508 ) ;
#39418=CARTESIAN_POINT ( 'NONE',  ( 5.895596859100789899, 18.99884588797230478, 6.600911917119146821 ) ) ;
#39421=B_SPLINE_CURVE_WITH_KNOTS ( 'NONE', 3,
 ( #61309, #46323, #13418, #17497 ),
 .UNSPECIFIED., .F., .F.,
 ( 4, 4 ),
 ( 0.000000000000000000, 0.005004948556313593665 ),
 .UNSPECIFIED. ) ;
#39425=CARTESIAN_POINT ( 'NONE',  ( 5.910764540655178756, -7.242942773736176676, -18.76275615269638308 ) ) ;
#39430=CARTESIAN_POINT ( 'NONE',  ( 0.9762797500689124330, -11.93232144563832975, 40.17392798947675914 ) ) ;
#39434=CARTESIAN_POINT ( 'NONE',  ( 5.901463166500146684, 19.71248269111027440, 3.991979019648623783 ) ) ;
#39440=ORIENTED_EDGE ( 'NONE', *, *, #17240, .F. ) ;
#39441=CARTESIAN_POINT ( 'NONE',  ( 0.9790320750461900534, -31.02392677839150181, -28.17539883996666106 ) ) ;
#39445=CARTESIAN_POINT ( 'NONE',  ( 0.9785694773339246311, -26.88704742894960731, -32.14688299459353260 ) ) ;
#39447=ORIENTED_EDGE ( 'NONE', *, *, #59231, .F. ) ;
#39448=CARTESIAN_POINT ( 'NONE',  ( 4.956445790443998689, 1.033212179477464909, 47.07940656732852602 ) ) ;
#39450=CARTESIAN_POINT ( 'NONE',  ( 4.962356264823608143, 0.000000000000000000, 0.000000000000000000 ) ) ;
#39451=CARTESIAN_POINT ( 'NONE',  ( 0.6845945791218034371, -0.7015599581307697674, -46.90324439033072679 ) ) ;
#39452=CARTESIAN_POINT ( 'NONE',  ( 0.5806925824938511393, -42.09901922557415332, -20.66143612114853312 ) ) ;
#39459=EDGE_CURVE ( 'NONE', #46746, #41690, #52562, .T. ) ;
#39460=CARTESIAN_POINT ( 'NONE',  ( 4.962356264823608143, -10.17958088187436871, 40.83640203215416165 ) ) ;
#39475=FACE_OUTER_BOUND ( 'NONE', #41795, .T. ) ;
#39479=B_SPLINE_CURVE_WITH_KNOTS ( 'NONE', 3,
 ( #51045, #41379, #60434, #50740, #21948, #1336, #12871, #15781, #15468, #30164, #41085, #34895, #7508, #24866, #60141, #17250, #7829, #44006, #32898 ),
 .UNSPECIFIED., .F., .F.,
 ( 4, 3, 3, 3, 3, 3, 4 ),
 ( 1.040890552917501732E-17, 0.0002732106629380605888, 0.0004098138914053724505, 0.0005464171197651409434, 0.0006830203481512540312, 0.0008196235766963588625, 0.001011968216111140510 ),
 .UNSPECIFIED. ) ;
#39480=EDGE_CURVE ( 'NONE', #61, #40810, #25725, .T. ) ;
#39482=ORIENTED_EDGE ( 'NONE', *, *, #39734, .F. ) ;
#39484=AXIS2_PLACEMENT_3D ( 'NONE', #61144, #32672, #42691 ) ;
#39500=CARTESIAN_POINT ( 'NONE',  ( 0.5782707292762442330, -38.25309408463849081, -27.13737545635934012 ) ) ;
#39504=CARTESIAN_POINT ( 'NONE',  ( 5.895596859100789899, 16.57987064389762111, 11.38578379577399069 ) ) ;
#39506=ADVANCED_FACE ( 'NONE', ( #2790 ), #40012, .F. ) ;
#39508=CARTESIAN_POINT ( 'NONE',  ( 0.5797568599927140909, -34.35528703333429235, -31.92083271984328618 ) ) ;
#39512=EDGE_CURVE ( 'NONE', #45872, #22599, #8612, .T. ) ;
#39516=ORIENTED_EDGE ( 'NONE', *, *, #27468, .T. ) ;
#39519=CARTESIAN_POINT ( 'NONE',  ( 4.962356264823609031, -3.779019546646985361, -41.91604238389410853 ) ) ;
#39523=CARTESIAN_POINT ( 'NONE',  ( 2.528100132419517365, -36.90587533319831692, 20.00525292323244386 ) ) ;
#39526=ORIENTED_EDGE ( 'NONE', *, *, #45787, .F. ) ;
#39532=EDGE_CURVE ( 'NONE', #3838, #13148, #6614, .T. ) ;
#39541=B_SPLINE_CURVE_WITH_KNOTS ( 'NONE', 3,
 ( #57587, #48525, #15341, #18807, #14723, #5285, #48232, #42932, #24727, #14416, #4348, #43547, #591, #19125, #20046, #43242, #52600, #34447, #42966 ),
 .UNSPECIFIED., .F., .F.,
 ( 4, 3, 3, 3, 3, 3, 4 ),
 ( 3.469446951953614189E-18, 0.0002732106629380643293, 0.0004098138914053842683, 0.0005464171197651466897, 0.0006830203481512559828, 0.0008196235766963655845, 0.001011968216111143546 ),
 .UNSPECIFIED. ) ;
#39542=DIRECTION ( 'NONE',  ( 1.000000000000000000, 0.000000000000000000, 0.000000000000000000 ) ) ;
#39543=CARTESIAN_POINT ( 'NONE',  ( 0.8554163680231720024, -46.86440027434175448, -2.221139355847800090 ) ) ;
#39548=CARTESIAN_POINT ( 'NONE',  ( 0.9754292589017243831, 38.35198883237011813, -16.89533721169931724 ) ) ;
#39554=EDGE_LOOP ( 'NONE', ( #44879, #34537, #12071, #9664 ) ) ;
#39565=CARTESIAN_POINT ( 'NONE',  ( 2.282803330402960018, 26.79503163932819376, 38.58138394231581714 ) ) ;
#39568=CARTESIAN_POINT ( 'NONE',  ( 1.000433927950263868, -21.99288785380132083, 35.67536350905153597 ) ) ;
#39573=ORIENTED_EDGE ( 'NONE', *, *, #34721, .F. ) ;
#39574=CARTESIAN_POINT ( 'NONE',  ( 5.896782393890504181, -9.660289833039353624, -17.64100017628503991 ) ) ;
#39577=CARTESIAN_POINT ( 'NONE',  ( 5.910764540655178756, -4.647344284407041393, 19.56791837603970308 ) ) ;
#39589=CARTESIAN_POINT ( 'NONE',  ( 5.917102823773431552, 20.06644099299511552, -1.351911212464495415 ) ) ;
#39591=VECTOR ( 'NONE', #12664, 999.9999999999998863 ) ;
#39596=CARTESIAN_POINT ( 'NONE',  ( 0.9775691876210985676, 15.41418421489670365, -38.97097168379585952 ) ) ;
#39609=CARTESIAN_POINT ( 'NONE',  ( 5.895881250540457863, -13.97904524590137854, -14.46077368681714326 ) ) ;
#39616=CARTESIAN_POINT ( 'NONE',  ( 5.895596859100789899, -19.93295055289972950, -2.684337063064522244 ) ) ;
#39621=CARTESIAN_POINT ( 'NONE',  ( 4.291220156522059348, -46.54716543045785215, 7.262946213162170039 ) ) ;
#39623=EDGE_LOOP ( 'NONE', ( #6941, #47403, #5325, #34610 ) ) ;
#39626=CARTESIAN_POINT ( 'NONE',  ( 4.956445790443991584, 39.12691469763999663, 26.20348443209871903 ) ) ;
#39627=DIRECTION ( 'NONE',  ( -1.000000000000000000, -0.000000000000000000, -0.000000000000000000 ) ) ;
#39630=ORIENTED_EDGE ( 'NONE', *, *, #8939, .T. ) ;
#39640=CARTESIAN_POINT ( 'NONE',  ( 0.9780106845699476636, -41.00520688714551198, -8.654724409120960971 ) ) ;
#39643=ADVANCED_FACE ( 'NONE', ( #23765, #23154 ), #3706, .F. ) ;
#39646=VERTEX_POINT ( 'NONE', #41655 ) ;
#39649=CARTESIAN_POINT ( 'NONE',  ( 1.231276596079887264, -30.51591784428387655, 28.74118176309011830 ) ) ;
#39654=CARTESIAN_POINT ( 'NONE',  ( 3.661921753702001237, 18.64961689156368507, 43.18359542270576412 ) ) ;
#39656=EDGE_CURVE ( 'NONE', #57391, #2702, #53288, .T. ) ;
#39658=CARTESIAN_POINT ( 'NONE',  ( 0.5835871038041883230, 46.49557224142410661, -6.115244463143569398 ) ) ;
#39660=CARTESIAN_POINT ( 'NONE',  ( 0.9762797500689124330, -40.96497924994810091, -8.842808390835211085 ) ) ;
#39661=CARTESIAN_POINT ( 'NONE',  ( 0.6845945791218023269, -42.25019583682482249, -20.37958469802306638 ) ) ;
#39672=B_SPLINE_CURVE_WITH_KNOTS ( 'NONE', 3,
 ( #10897, #35638, #50023, #11833, #24990, #30287, #34395, #53467, #59095, #44130, #58775, #1158, #16206, #58468, #15595, #34700 ),
 .UNSPECIFIED., .F., .F.,
 ( 4, 3, 3, 3, 3, 4 ),
 ( 3.469446951953614189E-18, 0.0002732102107932004621, 0.0004098135523333870092, 0.0005464168938825021780, 0.0008195847345945489731, 0.001092771384553111336 ),
 .UNSPECIFIED. ) ;
#39674=CARTESIAN_POINT ( 'NONE',  ( 5.896782393890504181, -7.222780579330736472, 18.77118876312459150 ) ) ;
#39676=CARTESIAN_POINT ( 'NONE',  ( 0.5804410086790514622, 16.34485605153989951, -43.95867983128970735 ) ) ;
#39679=CARTESIAN_POINT ( 'NONE',  ( 5.838029081930955932, 47.13000430274632890, -3.134924652369159404 ) ) ;
#39681=CARTESIAN_POINT ( 'NONE',  ( 0.9788927965476035276, 41.55338940985792107, 5.445405511482348970 ) ) ;
#39682=CARTESIAN_POINT ( 'NONE',  ( 0.5835226383429273911, 27.67095686594207038, -37.86239058312538930 ) ) ;
#39687=CARTESIAN_POINT ( 'NONE',  ( 4.956445790444005794, -33.12351118015950391, -33.47194433010255921 ) ) ;
#39695=CARTESIAN_POINT ( 'NONE',  ( 0.8554163680231816613, 28.56078411578431187, 37.22213163970302929 ) ) ;
#39697=EDGE_CURVE ( 'NONE', #35927, #33554, #51854, .T. ) ;
#39702=ORIENTED_EDGE ( 'NONE', *, *, #27073, .F. ) ;
#39704=B_SPLINE_CURVE_WITH_KNOTS ( 'NONE', 3,
 ( #31709, #2871, #27309, #50494, #60195, #3480 ),
 .UNSPECIFIED., .F., .F.,
 ( 4, 2, 4 ),
 ( 1.191143508120180971E-16, 0.0002448718616795919037, 0.0004897437233590647620 ),
 .UNSPECIFIED. ) ;
#39706=CARTESIAN_POINT ( 'NONE',  ( 4.958415959904820092, -41.61824873627301002, -18.19684934125545439 ) ) ;
#39714=CARTESIAN_POINT ( 'NONE',  ( 4.962356264823608143, 0.000000000000000000, 0.000000000000000000 ) ) ;
#39717=VERTEX_POINT ( 'NONE', #4619 ) ;
#39721=ORIENTED_EDGE ( 'NONE', *, *, #52398, .T. ) ;
#39723=ORIENTED_EDGE ( 'NONE', *, *, #2966, .F. ) ;
#39731=CARTESIAN_POINT ( 'NONE',  ( 3.661933894777871679, -31.78301468154000275, 34.67666568031975771 ) ) ;
#39734=EDGE_CURVE ( 'NONE', #61015, #30313, #24237, .T. ) ;
#39735=VERTEX_POINT ( 'NONE', #33804 ) ;
#39738=ORIENTED_EDGE ( 'NONE', *, *, #47185, .T. ) ;
#39744=CARTESIAN_POINT ( 'NONE',  ( 0.9788927965476033055, 35.98586392618627627, -21.47915757467643516 ) ) ;
#39748=ORIENTED_EDGE ( 'NONE', *, *, #54275, .F. ) ;
#39750=DIRECTION ( 'NONE',  ( -0.07906939808003035641, 0.3658060745126643365, 0.9273262350095013984 ) ) ;
#39754=B_SPLINE_CURVE_WITH_KNOTS ( 'NONE', 3,
 ( #5661, #49526, #26043, #11642 ),
 .UNSPECIFIED., .F., .F.,
 ( 4, 4 ),
 ( 7.589415207398531038E-19, 0.004446298630425091040 ),
 .UNSPECIFIED. ) ;
#39761=CARTESIAN_POINT ( 'NONE',  ( 0.9762797500689124330, -27.44172181261391330, -31.67454323498310842 ) ) ;
#39762=CARTESIAN_POINT ( 'NONE',  ( 0.9789233960466703355, 38.53168644443766766, 16.48168275935076821 ) ) ;
#39764=CARTESIAN_POINT ( 'NONE',  ( 0.5326698147273788431, 5.141974873329280286E-15, 41.88877248453276536 ) ) ;
#39766=EDGE_CURVE ( 'NONE', #14707, #26754, #9252, .T. ) ;
#39768=CARTESIAN_POINT ( 'NONE',  ( 5.895596859100789899, -2.016778947467960048, -20.01151633159111043 ) ) ;
#39773=CARTESIAN_POINT ( 'NONE',  ( 5.895881250540457863, -17.30282815192068924, -10.25377099185475060 ) ) ;
#39777=EDGE_CURVE ( 'NONE', #61467, #44269, #46698, .T. ) ;
#39781=( GEOMETRIC_REPRESENTATION_CONTEXT ( 3 ) GLOBAL_UNCERTAINTY_ASSIGNED_CONTEXT ( ( #14202 ) ) GLOBAL_UNIT_ASSIGNED_CONTEXT ( ( #17870, #56669, #51665 ) ) REPRESENTATION_CONTEXT ( 'NONE', 'WORKASPACE' ) );
#39794=CARTESIAN_POINT ( 'NONE',  ( 1.157644175074336923, 24.19453189427239437, 34.22903594751417700 ) ) ;
#39809=CARTESIAN_POINT ( 'NONE',  ( 1.231276596079881047, -26.41281459480337546, -32.55211200826465756 ) ) ;
#39815=ADVANCED_FACE ( 'NONE', ( #11216 ), #44508, .F. ) ;
#39816=ORIENTED_EDGE ( 'NONE', *, *, #32914, .T. ) ;
#39819=ADVANCED_FACE ( 'NONE', ( #14691 ), #56786, .F. ) ;
#39825=B_SPLINE_CURVE_WITH_KNOTS ( 'NONE', 3,
 ( #31787, #22075, #60261, #42432 ),
 .UNSPECIFIED., .F., .F.,
 ( 4, 4 ),
 ( 1.734723475976807094E-17, 0.005004948556313830454 ),
 .UNSPECIFIED. ) ;
#39829=ORIENTED_EDGE ( 'NONE', *, *, #42375, .T. ) ;
#39839=CARTESIAN_POINT ( 'NONE',  ( 0.9790850452238869517, -12.46487240820922793, -40.01205176081654713 ) ) ;
#39847=CARTESIAN_POINT ( 'NONE',  ( 0.9788927965476039716, 41.51561430229724436, -5.726288652754957020 ) ) ;
#39851=CARTESIAN_POINT ( 'NONE',  ( 1.000433927950267421, 20.71612682160601082, 36.43159023655132955 ) ) ;
#39858=CARTESIAN_POINT ( 'NONE',  ( 5.838029081930957709, 42.14833990873939484, -21.32094043634769776 ) ) ;
#39861=CARTESIAN_POINT ( 'NONE',  ( 4.958415959904820092, -39.33684062738397103, 22.71160327406307644 ) ) ;
#39867=CARTESIAN_POINT ( 'NONE',  ( 4.962356264823602814, -33.29728444345256122, -25.73958909062380229 ) ) ;
#39870=VERTEX_POINT ( 'NONE', #2092 ) ;
#39873=CARTESIAN_POINT ( 'NONE',  ( 0.7764146366350230810, -14.74570993613317427, -44.52644733356332551 ) ) ;
#39876=ORIENTED_EDGE ( 'NONE', *, *, #36666, .T. ) ;
#39878=ORIENTED_EDGE ( 'NONE', *, *, #24223, .F. ) ;
#39893=B_SPLINE_CURVE_WITH_KNOTS ( 'NONE', 3,
 ( #6529, #26287, #11592, #2150 ),
 .UNSPECIFIED., .F., .F.,
 ( 4, 4 ),
 ( 6.992893892674702526E-18, 0.004042984057420969356 ),
 .UNSPECIFIED. ) ;
#39895=CARTESIAN_POINT ( 'NONE',  ( 0.8554163680231738898, 11.76336166872350475, -45.41837508500966436 ) ) ;
#39900=CARTESIAN_POINT ( 'NONE',  ( 0.6845945791218023269, -14.72268806499601901, -44.53817437721004069 ) ) ;
#39904=CARTESIAN_POINT ( 'NONE',  ( 5.838029081930957709, -47.23414715677122899, 0.02001313068585724997 ) ) ;
#39908=VERTEX_POINT ( 'NONE', #50638 ) ;
#39916=EDGE_CURVE ( 'NONE', #43148, #38326, #39133, .T. ) ;
#39929=CARTESIAN_POINT ( 'NONE',  ( 5.896782393890504181, 14.92098591823861220, 13.48666994130638663 ) ) ;
#39930=CARTESIAN_POINT ( 'NONE',  ( 0.8554163680231720024, -34.17638377241251391, 32.14312158693672217 ) ) ;
#39942=EDGE_CURVE ( 'NONE', #24195, #26516, #40697, .T. ) ;
#39945=ORIENTED_EDGE ( 'NONE', *, *, #46886, .T. ) ;
#39948=DIRECTION ( 'NONE',  ( 0.000000000000000000, 0.000000000000000000, 1.000000000000000000 ) ) ;
#39952=EDGE_LOOP ( 'NONE', ( #10857, #14364, #33128, #24297 ) ) ;
#39953=( BOUNDED_SURFACE ( )  B_SPLINE_SURFACE ( 3, 1, ( 
 ( #9420, #48801 ),
 ( #48486, #33258 ),
 ( #61713, #13526 ),
 ( #3783, #32631 ) ),
 .UNSPECIFIED., .F., .F., .F. ) 
 B_SPLINE_SURFACE_WITH_KNOTS ( ( 4, 4 ),
 ( 2, 2 ),
 ( 0.000000000000000000, 1.000000000000000000 ),
 ( 0.000000000000000000, 1.000000000000000000 ),
 .UNSPECIFIED. ) 
 GEOMETRIC_REPRESENTATION_ITEM ( )  RATIONAL_B_SPLINE_SURFACE ( (
 ( 1.000000000000000000, 1.000000000000000000),
 ( 0.9952954269826590483, 0.8620686068821307169),
 ( 0.9952954269826590483, 0.8620686068821307169),
 ( 1.000000000000000000, 1.000000000000000000) ) ) 
 REPRESENTATION_ITEM ( '' )  SURFACE ( )  );
#39955=VECTOR ( 'NONE', #8433, 1000.000000000000000 ) ;
#39961=CARTESIAN_POINT ( 'NONE',  ( 0.5782707292762423457, 5.414380361654348661, 46.58777563918405917 ) ) ;
#39968=ORIENTED_EDGE ( 'NONE', *, *, #38166, .F. ) ;
#39969=CARTESIAN_POINT ( 'NONE',  ( 4.962356264823608143, 34.44911810793244200, 24.17630781256866612 ) ) ;
#39972=ORIENTED_EDGE ( 'NONE', *, *, #37375, .T. ) ;
#39976=CARTESIAN_POINT ( 'NONE',  ( 3.782625744892851749, 41.85823871763314230, 3.889210145086195336 ) ) ;
#39978=CARTESIAN_POINT ( 'NONE',  ( 0.5837800304671220131, -13.93760103191574196, 44.77700983378232280 ) ) ;
#39979=CARTESIAN_POINT ( 'NONE',  ( 2.282816707992324723, 46.36091564783490071, -7.560586399367689836 ) ) ;
#39980=CARTESIAN_POINT ( 'NONE',  ( 4.960386119450148179, -26.33153931528526925, 34.94404816216813714 ) ) ;
#39983=CARTESIAN_POINT ( 'NONE',  ( 5.838029081930957709, -28.00222738077776796, 38.03866874468847215 ) ) ;
#39988=FACE_OUTER_BOUND ( 'NONE', #24498, .T. ) ;
#40000=CARTESIAN_POINT ( 'NONE',  ( 0.9788927965476018622, 15.19445284419454012, 39.05720439813027411 ) ) ;
#40001=ORIENTED_EDGE ( 'NONE', *, *, #61664, .F. ) ;
#40011=CARTESIAN_POINT ( 'NONE',  ( 4.958415959904821868, 37.73202888843214708, 25.28829669600464669 ) ) ;
#40012=( BOUNDED_SURFACE ( )  B_SPLINE_SURFACE ( 3, 1, ( 
 ( #60409, #50712 ),
 ( #60119, #55408 ),
 ( #40137, #6860 ),
 ( #17527, #8117 ) ),
 .UNSPECIFIED., .F., .F., .F. ) 
 B_SPLINE_SURFACE_WITH_KNOTS ( ( 4, 4 ),
 ( 2, 2 ),
 ( 0.000000000000000000, 1.000000000000000000 ),
 ( 0.000000000000000000, 1.000000000000000000 ),
 .UNSPECIFIED. ) 
 GEOMETRIC_REPRESENTATION_ITEM ( )  RATIONAL_B_SPLINE_SURFACE ( (
 ( 1.000000000000000000, 1.000000000000000000),
 ( 0.7282232189291693025, 0.9929344683865674037),
 ( 0.7282232189291693025, 0.9929344683865674037),
 ( 1.000000000000000000, 1.000000000000000000) ) ) 
 REPRESENTATION_ITEM ( '' )  SURFACE ( )  );
#40017=ORIENTED_EDGE ( 'NONE', *, *, #21075, .F. ) ;
#40019=AXIS2_PLACEMENT_3D ( 'NONE', #39150, #43855, #33823 ) ;
#40030=ORIENTED_EDGE ( 'NONE', *, *, #49512, .T. ) ;
#40031=CARTESIAN_POINT ( 'NONE',  ( 1.231276596079887264, 29.74482033789320568, 29.53849072116790353 ) ) ;
#40033=DIRECTION ( 'NONE',  ( 0.000000000000000000, 0.000000000000000000, 1.000000000000000000 ) ) ;
#40036=CARTESIAN_POINT ( 'NONE',  ( 1.000433927950263424, -27.55767315202177414, -31.57520115690769913 ) ) ;
#40038=B_SPLINE_CURVE_WITH_KNOTS ( 'NONE', 3,
 ( #19469, #23533, #48277, #8821 ),
 .UNSPECIFIED., .F., .F.,
 ( 4, 4 ),
 ( 0.000000000000000000, 0.004447772540403792906 ),
 .UNSPECIFIED. ) ;
#40045=VECTOR ( 'NONE', #61567, 1000.000000000000000 ) ;
#40049=CARTESIAN_POINT ( 'NONE',  ( 2.282803330402963571, -31.31874722888088058, 35.00904139605154342 ) ) ;
#40056=CARTESIAN_POINT ( 'NONE',  ( 0.7764146366350229700, -18.93147413529521828, 42.91433048218058843 ) ) ;
#40063=CARTESIAN_POINT ( 'NONE',  ( 4.962356264823603702, -40.70360067759225586, -10.69824704058845022 ) ) ;
#40066=CARTESIAN_POINT ( 'NONE',  ( 5.896782393890504181, 19.71107130340470448, 3.999969368646206558 ) ) ;
#40072=VERTEX_POINT ( 'NONE', #28386 ) ;
#40081=CARTESIAN_POINT ( 'NONE',  ( 1.091591847532196624, -40.91128483460986587, -9.111847460162190160 ) ) ;
#40083=EDGE_LOOP ( 'NONE', ( #2912, #11623, #11502, #50657 ) ) ;
#40087=CARTESIAN_POINT ( 'NONE',  ( 0.5837799406558229487, 45.25381588408496469, 12.30185748196357487 ) ) ;
#40091=CARTESIAN_POINT ( 'NONE',  ( 0.8554163680231720024, 40.82560365045065964, 23.11872746688557712 ) ) ;
#40095=B_SPLINE_CURVE_WITH_KNOTS ( 'NONE', 3,
 ( #9337, #57861, #5238, #4609 ),
 .UNSPECIFIED., .F., .F.,
 ( 4, 4 ),
 ( 0.000000000000000000, 0.004447772540403798977 ),
 .UNSPECIFIED. ) ;
#40103=VECTOR ( 'NONE', #37633, 1000.000000000000114 ) ;
#40104=ORIENTED_EDGE ( 'NONE', *, *, #16476, .T. ) ;
#40105=CARTESIAN_POINT ( 'NONE',  ( 2.282816707992305183, 33.58715780361674774, 32.83899811326333662 ) ) ;
#40108=CARTESIAN_POINT ( 'NONE',  ( 0.5832655196449147983, -19.53343502719934222, -42.63425968644826725 ) ) ;
#40110=CARTESIAN_POINT ( 'NONE',  ( 5.895596859100789899, -13.97974974393973291, 14.46010996878324129 ) ) ;
#40111=DIRECTION ( 'NONE',  ( 0.000000000000000000, 0.000000000000000000, 1.000000000000000000 ) ) ;
#40118=CARTESIAN_POINT ( 'NONE',  ( 4.962356264823602814, -36.43094049105359744, -21.07183363638911189 ) ) ;
#40119=EDGE_LOOP ( 'NONE', ( #14452, #24016, #36230, #46108 ) ) ;
#40120=EDGE_CURVE ( 'NONE', #34089, #41352, #5458, .T. ) ;
#40129=ORIENTED_EDGE ( 'NONE', *, *, #33052, .T. ) ;
#40131=ADVANCED_FACE ( 'NONE', ( #4869 ), #61178, .F. ) ;
#40132=CARTESIAN_POINT ( 'NONE',  ( 0.9790850452238872847, 20.09612553610694974, -36.77612090338274697 ) ) ;
#40137=CARTESIAN_POINT ( 'NONE',  ( 5.901463166500145796, -15.77541139567702544, -12.47614786854420643 ) ) ;
#40142=CARTESIAN_POINT ( 'NONE',  ( 4.958415959904821868, -11.02103540056480924, -44.06518730837458264 ) ) ;
#40143=VERTEX_POINT ( 'NONE', #33728 ) ;
#40147=CARTESIAN_POINT ( 'NONE',  ( 1.231276596079887264, -21.83837404314831332, 35.78214904347716185 ) ) ;
#40150=CARTESIAN_POINT ( 'NONE',  ( 2.282816707992310512, -46.76237757432279807, 4.447135033303774243 ) ) ;
#40153=CARTESIAN_POINT ( 'NONE',  ( 0.9769922540276041456, -11.99378815008531696, -40.15570446271611615 ) ) ;
#40157=EDGE_CURVE ( 'NONE', #43273, #8104, #59281, .T. ) ;
#40163=EDGE_CURVE ( 'NONE', #50298, #5968, #8460, .T. ) ;
#40165=CARTESIAN_POINT ( 'NONE',  ( 2.528100132419516477, -39.24302147699968657, 14.90768405849201983 ) ) ;
#40188=VERTEX_POINT ( 'NONE', #59972 ) ;
#40190=ORIENTED_EDGE ( 'NONE', *, *, #52100, .F. ) ;
#40196=CARTESIAN_POINT ( 'NONE',  ( 0.9780303403264768436, -17.93405777852207095, -37.87755516122598465 ) ) ;
#40198=EDGE_CURVE ( 'NONE', #15929, #16052, #47668, .T. ) ;
#40206=B_SPLINE_CURVE_WITH_KNOTS ( 'NONE', 3,
 ( #19789, #29470, #963, #15705, #53272, #20099 ),
 .UNSPECIFIED., .F., .F.,
 ( 4, 2, 4 ),
 ( 1.223756431218073065E-16, 0.0002448718616795922832, 0.0004897437233590622684 ),
 .UNSPECIFIED. ) ;
#40210=ORIENTED_EDGE ( 'NONE', *, *, #47047, .F. ) ;
#40220=CARTESIAN_POINT ( 'NONE',  ( 3.661921753702022109, -3.452423898254273205, -46.91174578994899491 ) ) ;
#40221=CARTESIAN_POINT ( 'NONE',  ( 5.896782393890504181, -20.11283288166117345, -0.006352352428112362746 ) ) ;
#40224=CARTESIAN_POINT ( 'NONE',  ( 4.960386119450149955, 12.51307094103702511, 41.92683532413238368 ) ) ;
#40242=CARTESIAN_POINT ( 'NONE',  ( 0.5837800304671216800, -13.85068106606779281, -44.80397266075372897 ) ) ;
#40244=CARTESIAN_POINT ( 'NONE',  ( 0.9775691876210965692, -22.86778163026855992, 35.11977039076914053 ) ) ;
#40254=VERTEX_POINT ( 'NONE', #21456 ) ;
#40256=CARTESIAN_POINT ( 'NONE',  ( 0.9762797500689124330, -22.97506929404158171, -35.04955029839458547 ) ) ;
#40263=CARTESIAN_POINT ( 'NONE',  ( 0.5830082357119573677, -38.50772913779835704, -26.76540363208243534 ) ) ;
#40268=CARTESIAN_POINT ( 'NONE',  ( 5.838029081930957709, -45.55059156558392175, 12.49834653777350724 ) ) ;
#40271=B_SPLINE_CURVE_WITH_KNOTS ( 'NONE', 3,
 ( #16889, #36003, #35378, #54436 ),
 .UNSPECIFIED., .F., .F.,
 ( 4, 4 ),
 ( 0.000000000000000000, 0.004041751736740996012 ),
 .UNSPECIFIED. ) ;
#40285=CARTESIAN_POINT ( 'NONE',  ( 3.782625744892852193, 40.96637710780765218, 9.433665817480269666 ) ) ;
#40286=CARTESIAN_POINT ( 'NONE',  ( 0.5804410086790514622, -13.37224000219898734, 44.95223074752782111 ) ) ;
#40291=ORIENTED_EDGE ( 'NONE', *, *, #24541, .T. ) ;
#40292=DIRECTION ( 'NONE',  ( 0.000000000000000000, 0.000000000000000000, 1.000000000000000000 ) ) ;
#40293=EDGE_CURVE ( 'NONE', #12657, #37577, #17361, .T. ) ;
#40294=ORIENTED_EDGE ( 'NONE', *, *, #31573, .F. ) ;
#40295=CARTESIAN_POINT ( 'NONE',  ( 1.157643937452369709, -13.20506546943684079, -39.78226389413553221 ) ) ;
#40296=DIRECTION ( 'NONE',  ( -1.000000000000000000, -0.000000000000000000, -0.000000000000000000 ) ) ;
#40297=ADVANCED_FACE ( 'NONE', ( #11447 ), #3540, .F. ) ;
#40306=CARTESIAN_POINT ( 'NONE',  ( 3.661921753702030546, 44.83346572263544516, -14.23346321635423628 ) ) ;
#40313=CARTESIAN_POINT ( 'NONE',  ( 5.901463166500145796, 19.70672075163017922, 4.020326797401583718 ) ) ;
#40319=CARTESIAN_POINT ( 'NONE',  ( 5.896782393890504181, -18.51439742298330771, -7.857682542699298445 ) ) ;
#40323=CARTESIAN_POINT ( 'NONE',  ( 4.962356264823608143, 0.000000000000000000, 0.000000000000000000 ) ) ;
#40327=CARTESIAN_POINT ( 'NONE',  ( 5.910764540655178756, 3.360528482494880897, 19.82947520201943092 ) ) ;
#40330=ORIENTED_EDGE ( 'NONE', *, *, #33850, .T. ) ;
#40337=CARTESIAN_POINT ( 'NONE',  ( 5.894904586330512508, 10.82137050184791427, -16.95368256525344464 ) ) ;
#40345=VERTEX_POINT ( 'NONE', #8901 ) ;
#40347=CARTESIAN_POINT ( 'NONE',  ( 4.956445790443495092, 1.033212179477288384, -47.07940656732829865 ) ) ;
#40373=CARTESIAN_POINT ( 'NONE',  ( 0.9788927965476033055, 38.52767114616671051, -16.49106329757458766 ) ) ;
#40377=ORIENTED_EDGE ( 'NONE', *, *, #24223, .T. ) ;
#40380=ORIENTED_EDGE ( 'NONE', *, *, #14451, .T. ) ;
#40383=CARTESIAN_POINT ( 'NONE',  ( 0.5837800005270553649, 45.22975938364896820, 12.38967815316459564 ) ) ;
#40389=EDGE_CURVE ( 'NONE', #40072, #39717, #41697, .T. ) ;
#40393=CARTESIAN_POINT ( 'NONE',  ( 5.901463166500146684, 3.331057597888285482, -19.83486641296551056 ) ) ;
#40396=CARTESIAN_POINT ( 'NONE',  ( 1.231276596079887264, 14.27346765619334512, -39.41503383336959132 ) ) ;
#40400=EDGE_CURVE ( 'NONE', #54983, #26937, #21125, .T. ) ;
#40420=EDGE_LOOP ( 'NONE', ( #8027, #33266, #59207, #19540 ) ) ;
#40421=FACE_OUTER_BOUND ( 'NONE', #52382, .T. ) ;
#40424=B_SPLINE_CURVE_WITH_KNOTS ( 'NONE', 3,
 ( #61211, #4493, #55580, #42452 ),
 .UNSPECIFIED., .F., .F.,
 ( 4, 4 ),
 ( 0.000000000000000000, 0.004447772540403798110 ),
 .UNSPECIFIED. ) ;
#40426=CARTESIAN_POINT ( 'NONE',  ( 0.9769922540276034795, 20.52688070952990884, -36.53736065211683126 ) ) ;
#40427=EDGE_CURVE ( 'NONE', #45184, #22660, #48048, .T. ) ;
#40428=CARTESIAN_POINT ( 'NONE',  ( 5.896278296736517710, 16.58497454171988039, -11.37829508603494588 ) ) ;
#40429=VERTEX_POINT ( 'NONE', #19549 ) ;
#40430=ORIENTED_EDGE ( 'NONE', *, *, #35034, .T. ) ;
#40433=CARTESIAN_POINT ( 'NONE',  ( 3.238018933889920792, -5.387504234938370828, 12.26304572633462975 ) ) ;
#40438=EDGE_CURVE ( 'NONE', #5400, #61383, #48752, .T. ) ;
#40451=VERTEX_POINT ( 'NONE', #34568 ) ;
#40455=CARTESIAN_POINT ( 'NONE',  ( 0.5804410086790514622, -13.37224000219835673, -44.95223074752801296 ) ) ;
#40456=( GEOMETRIC_REPRESENTATION_CONTEXT ( 3 ) GLOBAL_UNCERTAINTY_ASSIGNED_CONTEXT ( ( #32375 ) ) GLOBAL_UNIT_ASSIGNED_CONTEXT ( ( #25774, #54560, #26389 ) ) REPRESENTATION_CONTEXT ( 'NONE', 'WORKASPACE' ) );
#40457=B_SPLINE_CURVE_WITH_KNOTS ( 'NONE', 3,
 ( #42665, #15086, #47663, #4709 ),
 .UNSPECIFIED., .F., .F.,
 ( 4, 4 ),
 ( 0.000000000000000000, 0.005004948556313801832 ),
 .UNSPECIFIED. ) ;
#40473=CARTESIAN_POINT ( 'NONE',  ( 5.896278296736517710, 20.06757494133106690, 1.348857141599983489 ) ) ;
#40481=DIRECTION ( 'NONE',  ( 0.07906939808003035641, 0.02523889567980490412, 0.9965495614529794599 ) ) ;
#40482=ORIENTED_EDGE ( 'NONE', *, *, #3713, .T. ) ;
#40488=ORIENTED_EDGE ( 'NONE', *, *, #30370, .F. ) ;
#40498=ORIENTED_EDGE ( 'NONE', *, *, #36817, .F. ) ;
#40499=CARTESIAN_POINT ( 'NONE',  ( 3.238018933889920792, -4.230209958195113806, 12.70876925895028897 ) ) ;
#40503=VERTEX_POINT ( 'NONE', #38973 ) ;
#40504=B_SPLINE_CURVE_WITH_KNOTS ( 'NONE', 3,
 ( #39761, #44464, #25021, #20326, #44162, #54108, #20627, #573, #58499, #30016, #15934, #1491, #1191, #39445, #15629, #11231, #35052, #19707, #33816 ),
 .UNSPECIFIED., .F., .F.,
 ( 4, 3, 3, 3, 3, 3, 4 ),
 ( 9.813676791237319219E-18, 0.0002732106629380643835, 0.0004098138914053805820, 0.0005464171197651613264, 0.0006830203481512775584, 0.0008196235766963826065, 0.001011968216111132053 ),
 .UNSPECIFIED. ) ;
#40505=FACE_OUTER_BOUND ( 'NONE', #698, .T. ) ;
#40507=CARTESIAN_POINT ( 'NONE',  ( 0.9789233960466710016, 35.99109370129050234, 21.47039592129751284 ) ) ;
#40512=EDGE_CURVE ( 'NONE', #5770, #25596, #15146, .T. ) ;
#40519=CARTESIAN_POINT ( 'NONE',  ( 0.9762797500689124330, -34.26226594605947895, 24.13341909939818564 ) ) ;
#40522=ORIENTED_EDGE ( 'NONE', *, *, #34726, .F. ) ;
#40523=CARTESIAN_POINT ( 'NONE',  ( 0.5806925824938502512, 22.05663578530182889, -41.38510819338409163 ) ) ;
#40530=CARTESIAN_POINT ( 'NONE',  ( 0.7056759521545020730, -24.52215593799390447, -39.98015379247183887 ) ) ;
#40534=CARTESIAN_POINT ( 'NONE',  ( 0.8554163680231720024, 33.26717477998049333, 33.08323677136276331 ) ) ;
#40544=DIRECTION ( 'NONE',  ( 0.07500201931887538753, -0.4673421949333655956, -0.8808893062882278135 ) ) ;
#40549=CARTESIAN_POINT ( 'NONE',  ( 5.894904586330512508, 17.95060305802250511, 9.072224750024437512 ) ) ;
#40554=ADVANCED_FACE ( 'NONE', ( #11070 ), #33219, .F. ) ;
#40564=ADVANCED_FACE ( 'NONE', ( #44913 ), #16370, .F. ) ;
#40567=CARTESIAN_POINT ( 'NONE',  ( 0.5837157313716032636, -38.61143574556265179, -26.61567382668169301 ) ) ;
#40568=ORIENTED_EDGE ( 'NONE', *, *, #40198, .T. ) ;
#40574=VERTEX_POINT ( 'NONE', #12015 ) ;
#40578=VERTEX_POINT ( 'NONE', #40519 ) ;
#40585=ORIENTED_EDGE ( 'NONE', *, *, #14789, .T. ) ;
#40586=CARTESIAN_POINT ( 'NONE',  ( 1.231276596079887931, 40.64579686208652731, 10.25650859035686757 ) ) ;
#40588=FACE_OUTER_BOUND ( 'NONE', #42634, .T. ) ;
#40599=LINE ( 'NONE', #31477, #21674 ) ;
#40602=CARTESIAN_POINT ( 'NONE',  ( 1.157644175074337811, -23.24616985789975132, 34.88004963323383834 ) ) ;
#40603=CARTESIAN_POINT ( 'NONE',  ( 0.5837157313716030416, -46.79729193653216868, 3.041468557951020557 ) ) ;
#40620=EDGE_CURVE ( 'NONE', #33924, #58761, #3141, .T. ) ;
#40628=DIRECTION ( 'NONE',  ( 0.07906939808003035641, 0.8933371237230053330, -0.4423763258421154476 ) ) ;
#40635=DIRECTION ( 'NONE',  ( 0.000000000000000000, 0.000000000000000000, 1.000000000000000000 ) ) ;
#40639=( BOUNDED_SURFACE ( )  B_SPLINE_SURFACE ( 3, 1, ( 
 ( #49886, #25447 ),
 ( #31088, #39900 ),
 ( #30146, #35807 ),
 ( #50191, #16072 ) ),
 .UNSPECIFIED., .F., .F., .F. ) 
 B_SPLINE_SURFACE_WITH_KNOTS ( ( 4, 4 ),
 ( 2, 2 ),
 ( 0.000000000000000000, 1.000000000000000000 ),
 ( 0.000000000000000000, 1.000000000000000000 ),
 .UNSPECIFIED. ) 
 GEOMETRIC_REPRESENTATION_ITEM ( )  RATIONAL_B_SPLINE_SURFACE ( (
 ( 1.000000000000000000, 1.000000000000000000),
 ( 0.9952954269826590483, 0.8620686068821307169),
 ( 0.9952954269826590483, 0.8620686068821307169),
 ( 1.000000000000000000, 1.000000000000000000) ) ) 
 REPRESENTATION_ITEM ( '' )  SURFACE ( )  );
#40656=CARTESIAN_POINT ( 'NONE',  ( 0.5834584762367743815, -19.90520019176333477, 42.46197115465809446 ) ) ;
#40663=CARTESIAN_POINT ( 'NONE',  ( 5.895881250540457863, 8.470336106973904933, 18.24228844863481314 ) ) ;
#40673=ORIENTED_EDGE ( 'NONE', *, *, #9060, .F. ) ;
#40676=CARTESIAN_POINT ( 'NONE',  ( 0.9762797500689124330, -0.8945891712305065191, 41.89897964629235361 ) ) ;
#40680=LINE ( 'NONE', #2418, #32517 ) ;
#40686=VERTEX_POINT ( 'NONE', #3490 ) ;
#40687=VECTOR ( 'NONE', #60763, 1000.000000000000227 ) ;
#40690=ORIENTED_EDGE ( 'NONE', *, *, #4241, .F. ) ;
#40692=CARTESIAN_POINT ( 'NONE',  ( 0.5835871038041856584, 36.71915229544869419, 29.17084687843575708 ) ) ;
#40693=CARTESIAN_POINT ( 'NONE',  ( 5.896782393890504181, -2.019528367549316084, -20.01118667272572793 ) ) ;
#40697=B_SPLINE_CURVE_WITH_KNOTS ( 'NONE', 3,
 ( #49726, #60339, #7095, #31237 ),
 .UNSPECIFIED., .F., .F.,
 ( 4, 4 ),
 ( 0.000000000000000000, 0.005004948556313814842 ),
 .UNSPECIFIED. ) ;
#40702=EDGE_CURVE ( 'NONE', #48102, #20804, #1685, .T. ) ;
#40707=EDGE_CURVE ( 'NONE', #15442, #25145, #60715, .T. ) ;
#40708=CARTESIAN_POINT ( 'NONE',  ( 5.895596859100789899, -17.30333226730972385, -10.25294473112801619 ) ) ;
#40715=CARTESIAN_POINT ( 'NONE',  ( 0.5835871038041854364, -19.61618793221725454, -42.59623955127298700 ) ) ;
#40721=VECTOR ( 'NONE', #52860, 1000.000000000000000 ) ;
#40728=ORIENTED_EDGE ( 'NONE', *, *, #38557, .F. ) ;
#40729=AXIS2_PLACEMENT_3D ( 'NONE', #23887, #37384, #41788 ) ;
#40732=B_SPLINE_CURVE_WITH_KNOTS ( 'NONE', 3,
 ( #4894, #57504, #52207, #33751 ),
 .UNSPECIFIED., .F., .F.,
 ( 4, 4 ),
 ( 0.000000000000000000, 0.004447772540403782497 ),
 .UNSPECIFIED. ) ;
#40736=CARTESIAN_POINT ( 'NONE',  ( 1.091591847532197956, 35.65871381344827995, 22.02759905496810333 ) ) ;
#40740=B_SPLINE_CURVE_WITH_KNOTS ( 'NONE', 3,
 ( #37202, #8052, #32808, #7414, #56270, #8659 ),
 .UNSPECIFIED., .F., .F.,
 ( 4, 2, 4 ),
 ( 7.410741937918042371E-18, 0.0002291472222819936674, 0.0004582944445639799622 ),
 .UNSPECIFIED. ) ;
#40743=VERTEX_POINT ( 'NONE', #5636 ) ;
#40758=( BOUNDED_SURFACE ( )  B_SPLINE_SURFACE ( 3, 1, ( 
 ( #57035, #5025 ),
 ( #51725, #14771 ),
 ( #42983, #29161 ),
 ( #23236, #43287 ) ),
 .UNSPECIFIED., .F., .F., .F. ) 
 B_SPLINE_SURFACE_WITH_KNOTS ( ( 4, 4 ),
 ( 2, 2 ),
 ( 0.000000000000000000, 1.000000000000000000 ),
 ( 0.000000000000000000, 1.000000000000000000 ),
 .UNSPECIFIED. ) 
 GEOMETRIC_REPRESENTATION_ITEM ( )  RATIONAL_B_SPLINE_SURFACE ( (
 ( 1.000000000000000000, 1.000000000000000000),
 ( 0.7282232189291693025, 0.9929344683865674037),
 ( 0.7282232189291693025, 0.9929344683865674037),
 ( 1.000000000000000000, 1.000000000000000000) ) ) 
 REPRESENTATION_ITEM ( '' )  SURFACE ( )  );
#40761=CARTESIAN_POINT ( 'NONE',  ( 1.231276596079887264, 40.19859528295904738, -11.88905834349085922 ) ) ;
#40766=AXIS2_PLACEMENT_3D ( 'NONE', #22221, #12522, #31613 ) ;
#40770=VECTOR ( 'NONE', #61944, 1000.000000000000000 ) ;
#40783=CARTESIAN_POINT ( 'NONE',  ( 0.9762797500689124330, 29.49606728235512776, 29.77090526101756751 ) ) ;
#40784=EDGE_CURVE ( 'NONE', #48962, #44981, #33796, .T. ) ;
#40789=EDGE_CURVE ( 'NONE', #37980, #44953, #40457, .T. ) ;
#40810=VERTEX_POINT ( 'NONE', #20098 ) ;
#40823=CARTESIAN_POINT ( 'NONE',  ( 0.5806925824938502512, -44.47729014209954101, -14.86583411581937320 ) ) ;
#40824=CARTESIAN_POINT ( 'NONE',  ( 0.5835871038041838821, -30.38152644921350998, 35.72390381127519277 ) ) ;
#40828=ORIENTED_EDGE ( 'NONE', *, *, #57434, .F. ) ;
#40840=( BOUNDED_SURFACE ( )  B_SPLINE_SURFACE ( 3, 1, ( 
 ( #24430, #57924 ),
 ( #6217, #19747 ),
 ( #25359, #19141 ),
 ( #38252, #57298 ) ),
 .UNSPECIFIED., .F., .F., .F. ) 
 B_SPLINE_SURFACE_WITH_KNOTS ( ( 4, 4 ),
 ( 2, 2 ),
 ( 0.000000000000000000, 1.000000000000000000 ),
 ( 0.000000000000000000, 1.000000000000000000 ),
 .UNSPECIFIED. ) 
 GEOMETRIC_REPRESENTATION_ITEM ( )  RATIONAL_B_SPLINE_SURFACE ( (
 ( 1.000000000000000000, 1.000000000000000000),
 ( 0.9952954269826590483, 0.8620686068821339365),
 ( 0.9952954269826590483, 0.8620686068821339365),
 ( 1.000000000000000000, 1.000000000000000000) ) ) 
 REPRESENTATION_ITEM ( '' )  SURFACE ( )  );
#40844=CARTESIAN_POINT ( 'NONE',  ( 0.9762797500689124330, -31.41867615533366376, -27.73430319715951242 ) ) ;
#40852=CARTESIAN_POINT ( 'NONE',  ( 0.9785694773339252972, 32.75148539916909129, 26.14719124232438574 ) ) ;
#40855=DIRECTION ( 'NONE',  ( 0.000000000000000000, 0.000000000000000000, 1.000000000000000000 ) ) ;
#40859=DIRECTION ( 'NONE',  ( 0.07500201931887537365, 0.9798016564750019475, -0.1853737065145253660 ) ) ;
#40860=DIRECTION ( 'NONE',  ( 0.07906939808003032866, -0.9890184005629941710, 0.1248624588700636417 ) ) ;
#40864=ORIENTED_EDGE ( 'NONE', *, *, #10963, .F. ) ;
#40867=FACE_OUTER_BOUND ( 'NONE', #56491, .T. ) ;
#40878=AXIS2_PLACEMENT_3D ( 'NONE', #54338, #22950, #27637 ) ;
#40880=CARTESIAN_POINT ( 'NONE',  ( 0.7056313189692662302, 17.64074258352390601, 43.45748318827730117 ) ) ;
#40885=B_SPLINE_CURVE_WITH_KNOTS ( 'NONE', 3,
 ( #49934, #60236, #6991, #41484 ),
 .UNSPECIFIED., .F., .F.,
 ( 4, 4 ),
 ( 4.046035655711835948E-17, 0.005004948556313840863 ),
 .UNSPECIFIED. ) ;
#40887=ORIENTED_EDGE ( 'NONE', *, *, #61924, .T. ) ;
#40888=ORIENTED_EDGE ( 'NONE', *, *, #59619, .T. ) ;
#40889=CARTESIAN_POINT ( 'NONE',  ( 5.895596859100789899, 8.462961974658517406, 18.24572437114984780 ) ) ;
#40895=CARTESIAN_POINT ( 'NONE',  ( 0.5804410086790514622, 28.25755288515069807, 37.43034272883843983 ) ) ;
#40898=ORIENTED_EDGE ( 'NONE', *, *, #44863, .F. ) ;
#40899=CARTESIAN_POINT ( 'NONE',  ( 0.5830081025819946472, -13.63296368238104250, 44.87064001791286216 ) ) ;
#40906=CARTESIAN_POINT ( 'NONE',  ( 5.901463166500146684, 10.81005692193087420, -16.96055835417133295 ) ) ;
#40910=AXIS2_PLACEMENT_3D ( 'NONE', #21954, #36074, #41695 ) ;
#40913=EDGE_CURVE ( 'NONE', #29096, #61317, #42875, .T. ) ;
#40915=CARTESIAN_POINT ( 'NONE',  ( 4.962356264823608143, -14.71877352713578269, -39.42833123173278409 ) ) ;
#40917=CARTESIAN_POINT ( 'NONE',  ( 0.5835226383429271690, -46.77883816727116795, 3.314026895820559204 ) ) ;
#40920=FACE_OUTER_BOUND ( 'NONE', #15135, .T. ) ;
#40927=CARTESIAN_POINT ( 'NONE',  ( 0.9762797500689124330, -34.83496347773955648, 23.29914386174426255 ) ) ;
#40930=CARTESIAN_POINT ( 'NONE',  ( 0.9788927965476029724, -30.98642140960746616, 28.21663163557970222 ) ) ;
#40934=CARTESIAN_POINT ( 'NONE',  ( 0.9789233960466705575, -7.100278355974616318, 41.30281799223896400 ) ) ;
#40944=CARTESIAN_POINT ( 'NONE',  ( 0.5832655196449125778, -8.024559735822561990, 46.20434637585024262 ) ) ;
#40945=CARTESIAN_POINT ( 'NONE',  ( 0.9762797500689124330, -1.905951756780080775, -41.86516610604251554 ) ) ;
#40946=EDGE_CURVE ( 'NONE', #46145, #4231, #27006, .T. ) ;
#40947=ORIENTED_EDGE ( 'NONE', *, *, #32084, .T. ) ;
#40949=CARTESIAN_POINT ( 'NONE',  ( 2.618530812446111078, -35.79257080906894828, 30.47324505325918409 ) ) ;
#40951=VERTEX_POINT ( 'NONE', #10575 ) ;
#40960=CARTESIAN_POINT ( 'NONE',  ( 5.895596859100789899, 10.81936814621394127, -16.95492424427719413 ) ) ;
#40961=ORIENTED_EDGE ( 'NONE', *, *, #7778, .F. ) ;
#40962=FACE_OUTER_BOUND ( 'NONE', #22067, .T. ) ;
#40965=ORIENTED_EDGE ( 'NONE', *, *, #12064, .T. ) ;
#40971=CARTESIAN_POINT ( 'NONE',  ( 0.6064515330803574855, 45.03781699277671180, -13.07399619711731731 ) ) ;
#40974=CARTESIAN_POINT ( 'NONE',  ( 0.8554163680231720024, 36.24698750680840931, -29.78861141095861598 ) ) ;
#40976=EDGE_CURVE ( 'NONE', #4099, #56285, #47988, .T. ) ;
#40985=CARTESIAN_POINT ( 'NONE',  ( 0.9790850452238870627, 24.90012728558320276, 33.70936059056818124 ) ) ;
#40994=B_SPLINE_CURVE_WITH_KNOTS ( 'NONE', 3,
 ( #23260, #45, #42387, #61440 ),
 .UNSPECIFIED., .F., .F.,
 ( 4, 4 ),
 ( 0.000000000000000000, 0.004041751736740989073 ),
 .UNSPECIFIED. ) ;
#40995=ORIENTED_EDGE ( 'NONE', *, *, #28272, .T. ) ;
#40998=DIRECTION ( 'NONE',  ( -0.07500201931887529039, -0.9939633762263326844, 0.08007186658771524301 ) ) ;
#41003=ORIENTED_EDGE ( 'NONE', *, *, #34905, .F. ) ;
#41005=CARTESIAN_POINT ( 'NONE',  ( 5.910764540655177868, 5.943959005784828165, 19.21381247453801322 ) ) ;
#41014=CARTESIAN_POINT ( 'NONE',  ( 4.956445790444035104, 38.51510088324747016, -27.09474218539284252 ) ) ;
#41024=CARTESIAN_POINT ( 'NONE',  ( 0.5804410086790514622, -38.35366574782020876, 26.99103880105171882 ) ) ;
#41032=FACE_OUTER_BOUND ( 'NONE', #25881, .T. ) ;
#41033=ORIENTED_EDGE ( 'NONE', *, *, #21003, .T. ) ;
#41034=CARTESIAN_POINT ( 'NONE',  ( 1.231276596079887264, -34.07446381689716475, 24.41736444846234733 ) ) ;
#41035=LINE ( 'NONE', #60095, #13961 ) ;
#41036=CARTESIAN_POINT ( 'NONE',  ( 4.956445790444027111, 14.46717203539434671, -44.81337951368921324 ) ) ;
#41037=ORIENTED_EDGE ( 'NONE', *, *, #5580, .F. ) ;
#41038=CARTESIAN_POINT ( 'NONE',  ( 3.376099380956838925, -10.78512648832971799, -7.961747940169664695 ) ) ;
#41041=VECTOR ( 'NONE', #57428, 1000.000000000000114 ) ;
#41042=CARTESIAN_POINT ( 'NONE',  ( 5.895596859100789899, 20.06821053248683029, 1.339816866691926567 ) ) ;
#41051=ADVANCED_FACE ( 'NONE', ( #21822 ), #12009, .F. ) ;
#41053=CARTESIAN_POINT ( 'NONE',  ( 0.6845945791218023269, -38.17654861005544831, 27.25724962166981058 ) ) ;
#41054=B_SPLINE_CURVE_WITH_KNOTS ( 'NONE', 3,
 ( #47086, #32362, #18568, #52062, #28262, #37693, #349, #43318, #9774, #8529, #56450, #18266, #18891, #13883, #37377, #28879 ),
 .UNSPECIFIED., .F., .F.,
 ( 4, 3, 3, 3, 3, 4 ),
 ( 6.939740885162003740E-18, 0.0002732102107931858796, 0.0004098135523333801787, 0.0005464168938824975159, 0.0008195847345945385647, 0.001092771384553108084 ),
 .UNSPECIFIED. ) ;
#41062=EDGE_CURVE ( 'NONE', #14203, #49966, #3792, .T. ) ;
#41063=CARTESIAN_POINT ( 'NONE',  ( 5.896782393890504181, 19.00205529748295774, -6.591508275759957236 ) ) ;
#41070=ORIENTED_EDGE ( 'NONE', *, *, #34385, .F. ) ;
#41074=CARTESIAN_POINT ( 'NONE',  ( 0.5837157313716013762, -44.33100354085927819, 15.29703202070088253 ) ) ;
#41077=CARTESIAN_POINT ( 'NONE',  ( 0.9762797500689124330, 9.222352665238926051, -40.88120590813907285 ) ) ;
#41084=CARTESIAN_POINT ( 'NONE',  ( 0.5797568665920724840, -44.09074206032379806, 15.97597487391192850 ) ) ;
#41085=CARTESIAN_POINT ( 'NONE',  ( 0.9790320750461918298, 9.798880805960621387, -40.74701298859544352 ) ) ;
#41089=CARTESIAN_POINT ( 'NONE',  ( 0.9754292589017206083, 41.60825678442307662, 5.008036966395961187 ) ) ;
#41092=AXIS2_PLACEMENT_3D ( 'NONE', #44244, #48910, #49521 ) ;
#41094=CARTESIAN_POINT ( 'NONE',  ( 1.511340767998295531, -0.4710343482720885655, 46.93530765796581505 ) ) ;
#41095=CARTESIAN_POINT ( 'NONE',  ( 0.5817216825391109403, 32.92749829871815592, 33.39183744562994605 ) ) ;
#41097=B_SPLINE_CURVE_WITH_KNOTS ( 'NONE', 3,
 ( #60675, #50666, #22181, #31577 ),
 .UNSPECIFIED., .F., .F.,
 ( 4, 4 ),
 ( 1.084202172485504434E-19, 0.004446298630425057213 ),
 .UNSPECIFIED. ) ;
#41100=CARTESIAN_POINT ( 'NONE',  ( 4.960386119450151732, 42.78128882304991976, 9.175935446107084559 ) ) ;
#41103=CARTESIAN_POINT ( 'NONE',  ( 0.6845945791218023269, 10.02997083121021582, -45.82364243312635921 ) ) ;
#41109=ORIENTED_EDGE ( 'NONE', *, *, #29408, .F. ) ;
#41110=DIRECTION ( 'NONE',  ( -1.000000000000000000, -0.000000000000000000, -0.000000000000000000 ) ) ;
#41122=AXIS2_PLACEMENT_3D ( 'NONE', #12911, #36717, #31381 ) ;
#41133=ORIENTED_EDGE ( 'NONE', *, *, #17076, .F. ) ;
#41136=ORIENTED_EDGE ( 'NONE', *, *, #9060, .T. ) ;
#41141=VERTEX_POINT ( 'NONE', #42714 ) ;
#41147=CARTESIAN_POINT ( 'NONE',  ( 0.5824935313925958535, 4.331522541955116878, -46.69556820001628950 ) ) ;
#41150=CARTESIAN_POINT ( 'NONE',  ( 2.618530812446115519, 36.00211569111162646, -30.22539420689188105 ) ) ;
#41151=LINE ( 'NONE', #2587, #57201 ) ;
#41157=CARTESIAN_POINT ( 'NONE',  ( 0.9790724872846766624, -22.58437671703066130, 35.30270723733094940 ) ) ;
#41160=B_SPLINE_CURVE_WITH_KNOTS ( 'NONE', 3,
 ( #4724, #28870, #32663, #3504 ),
 .UNSPECIFIED., .F., .F.,
 ( 4, 4 ),
 ( 2.276824562219559311E-18, 0.004446298630425058948 ),
 .UNSPECIFIED. ) ;
#41167=CARTESIAN_POINT ( 'NONE',  ( 0.9754292589017249382, -11.85895077972789124, 40.19568077914918547 ) ) ;
#41171=VERTEX_POINT ( 'NONE', #52388 ) ;
#41173=EDGE_CURVE ( 'NONE', #59625, #17743, #18912, .T. ) ;
#41176=ORIENTED_EDGE ( 'NONE', *, *, #56476, .F. ) ;
#41179=DIRECTION ( 'NONE',  ( 0.000000000000000000, 0.000000000000000000, 1.000000000000000000 ) ) ;
#41180=CARTESIAN_POINT ( 'NONE',  ( 0.5837800005270554760, -38.66303329572635761, -26.54063139820414108 ) ) ;
#41183=CARTESIAN_POINT ( 'NONE',  ( 4.962356264823608143, 1.841560470688809792, -42.04574000888963781 ) ) ;
#41186=EDGE_CURVE ( 'NONE', #5328, #51700, #19217, .T. ) ;
#41188=CARTESIAN_POINT ( 'NONE',  ( 0.6064782688330881966, 10.17905733607075724, 45.77904802601024414 ) ) ;
#41191=DIRECTION ( 'NONE',  ( 0.07906939808003035641, 0.1578407582592837588, 0.9842938206244089550 ) ) ;
#41209=CARTESIAN_POINT ( 'NONE',  ( 4.962356264823608143, 0.000000000000000000, 0.000000000000000000 ) ) ;
#41210=CARTESIAN_POINT ( 'NONE',  ( 0.9754292580325127915, 20.64935461952654805, -36.46822755085641177 ) ) ;
#41212=EDGE_CURVE ( 'NONE', #5378, #59500, #44235, .T. ) ;
#41215=CARTESIAN_POINT ( 'NONE',  ( 0.5824935313925933000, -46.76557014396445311, 3.495658187492202362 ) ) ;
#41227=CARTESIAN_POINT ( 'NONE',  ( 0.5806925824938494740, -35.14454992382308518, -31.04968555389040219 ) ) ;
#41229=CARTESIAN_POINT ( 'NONE',  ( 0.9762797500689124330, -31.41867615533404390, 27.73430319715907544 ) ) ;
#41231=CARTESIAN_POINT ( 'NONE',  ( 0.5804410086790514622, -42.10186154173687356, 20.66284362269178132 ) ) ;
#41232=CARTESIAN_POINT ( 'NONE',  ( 3.376099380956842921, -10.78512648832982634, 7.961747940169504822 ) ) ;
#41235=CARTESIAN_POINT ( 'NONE',  ( 3.782542959838396168, -14.09167658397165468, 39.60634424494784156 ) ) ;
#41237=ORIENTED_EDGE ( 'NONE', *, *, #9809, .F. ) ;
#41240=CARTESIAN_POINT ( 'NONE',  ( 3.238018933889920792, -11.19612451184702273, 7.352162150202567581 ) ) ;
#41243=LINE ( 'NONE', #60303, #38540 ) ;
#41246=VECTOR ( 'NONE', #31278, 1000.000000000000114 ) ;
#41248=ORIENTED_EDGE ( 'NONE', *, *, #52038, .F. ) ;
#41253=B_SPLINE_CURVE_WITH_KNOTS ( 'NONE', 3,
 ( #33642, #390, #33033, #88 ),
 .UNSPECIFIED., .F., .F.,
 ( 4, 4 ),
 ( 5.485677294651096434E-18, 0.004042984057420971958 ),
 .UNSPECIFIED. ) ;
#41264=VERTEX_POINT ( 'NONE', #43654 ) ;
#41266=ADVANCED_FACE ( 'NONE', ( #17740 ), #18699, .T. ) ;
#41267=CARTESIAN_POINT ( 'NONE',  ( 5.901463166500145796, -9.678444301826402807, 17.63081354439098547 ) ) ;
#41270=ORIENTED_EDGE ( 'NONE', *, *, #14237, .F. ) ;
#41275=CARTESIAN_POINT ( 'NONE',  ( 0.5804410086790514622, 17.36461428077125291, 43.56592731407689456 ) ) ;
#41285=CARTESIAN_POINT ( 'NONE',  ( 5.894904586330512508, -18.51647496758820921, -7.852997315440910064 ) ) ;
#41291=CIRCLE ( 'NONE', #19284, 42.08604991992415023 ) ;
#41293=CARTESIAN_POINT ( 'NONE',  ( 1.000433927950261204, -26.55171663538948224, 32.42568459364935762 ) ) ;
#41300=CARTESIAN_POINT ( 'NONE',  ( 0.7056759521545006297, 39.91793999877379662, 24.62329984732515697 ) ) ;
#41301=VERTEX_POINT ( 'NONE', #19839 ) ;
#41304=CARTESIAN_POINT ( 'NONE',  ( 0.8560838555295223751, -42.27062166135446120, -20.33635607586480631 ) ) ;
#41306=B_SPLINE_CURVE_WITH_KNOTS ( 'NONE', 3,
 ( #39238, #10715, #21341, #24804 ),
 .UNSPECIFIED., .F., .F.,
 ( 4, 4 ),
 ( 0.000000000000000000, 0.005004948556313794893 ),
 .UNSPECIFIED. ) ;
#41309=CARTESIAN_POINT ( 'NONE',  ( 3.661933894777896104, 38.05324307217590274, -27.65107333615731378 ) ) ;
#41321=CARTESIAN_POINT ( 'NONE',  ( 1.000110580585052311, -41.19582803197042864, 7.702028014245381193 ) ) ;
#41329=CARTESIAN_POINT ( 'NONE',  ( 3.782542959838389063, 30.43994881966847288, -28.99391952207450274 ) ) ;
#41330=DIRECTION ( 'NONE',  ( 0.000000000000000000, 0.000000000000000000, 1.000000000000000000 ) ) ;
#41332=ORIENTED_EDGE ( 'NONE', *, *, #2633, .F. ) ;
#41334=CARTESIAN_POINT ( 'NONE',  ( 1.157643937452369487, -41.23316700651808020, -7.538448992156369322 ) ) ;
#41336=CARTESIAN_POINT ( 'NONE',  ( 5.895596859100789899, -19.39920506799825262, -5.310275505304632659 ) ) ;
#41338=ORIENTED_EDGE ( 'NONE', *, *, #55714, .T. ) ;
#41347=CARTESIAN_POINT ( 'NONE',  ( 0.5806925824938499181, -46.82446035038572063, 2.586943222941027631 ) ) ;
#41350=ORIENTED_EDGE ( 'NONE', *, *, #59562, .F. ) ;
#41352=VERTEX_POINT ( 'NONE', #11053 ) ;
#41362=CARTESIAN_POINT ( 'NONE',  ( 0.9791128995231621612, -17.63619210405237681, 38.01712985372675746 ) ) ;
#41372=FACE_OUTER_BOUND ( 'NONE', #17500, .T. ) ;
#41373=( BOUNDED_SURFACE ( )  B_SPLINE_SURFACE ( 3, 1, ( 
 ( #37968, #2313 ),
 ( #56100, #31142 ),
 ( #46733, #21440 ),
 ( #40889, #23220 ) ),
 .UNSPECIFIED., .F., .F., .F. ) 
 B_SPLINE_SURFACE_WITH_KNOTS ( ( 4, 4 ),
 ( 2, 2 ),
 ( 0.000000000000000000, 1.000000000000000000 ),
 ( 0.000000000000000000, 1.000000000000000000 ),
 .UNSPECIFIED. ) 
 GEOMETRIC_REPRESENTATION_ITEM ( )  RATIONAL_B_SPLINE_SURFACE ( (
 ( 1.000000000000000000, 1.000000000000000000),
 ( 0.9952954269826590483, 0.8620686068821307169),
 ( 0.9952954269826590483, 0.8620686068821307169),
 ( 1.000000000000000000, 1.000000000000000000) ) ) 
 REPRESENTATION_ITEM ( '' )  SURFACE ( )  );
#41375=LINE ( 'NONE', #27255, #39955 ) ;
#41379=CARTESIAN_POINT ( 'NONE',  ( 0.9772918015221174759, 9.311194862264514427, -40.86121028539926670 ) ) ;
#41390=CARTESIAN_POINT ( 'NONE',  ( 5.895881250540457863, -18.51513737938366333, -7.856040314996530327 ) ) ;
#41392=CARTESIAN_POINT ( 'NONE',  ( 0.7056759521544971880, -38.18414334534395493, -27.23453737626569549 ) ) ;
#41399=VERTEX_POINT ( 'NONE', #10740 ) ;
#41400=B_SPLINE_CURVE_WITH_KNOTS ( 'NONE', 3,
 ( #53619, #25760, #34247, #20758, #20446, #30138 ),
 .UNSPECIFIED., .F., .F.,
 ( 4, 2, 4 ),
 ( 1.738108305489988542E-18, 0.0002291459268755712919, 0.0004582918537511408491 ),
 .UNSPECIFIED. ) ;
#41401=EDGE_CURVE ( 'NONE', #59818, #59625, #5989, .T. ) ;
#41404=DIRECTION ( 'NONE',  ( -1.000000000000000000, -0.000000000000000000, -0.000000000000000000 ) ) ;
#41413=CARTESIAN_POINT ( 'NONE',  ( 0.5817216825391117174, 16.42910366609513417, -43.92401968099184018 ) ) ;
#41421=ORIENTED_EDGE ( 'NONE', *, *, #25203, .T. ) ;
#41435=VECTOR ( 'NONE', #47194, 1000.000000000000000 ) ;
#41440=EDGE_CURVE ( 'NONE', #25211, #4627, #20439, .T. ) ;
#41446=CARTESIAN_POINT ( 'NONE',  ( 3.661933894777873455, -36.12137754761139519, 30.13100146053178108 ) ) ;
#41461=CONICAL_SURFACE ( 'NONE', #14446, 41.88877248453276536, 0.04450589592585735277 ) ;
#41465=( BOUNDED_SURFACE ( )  B_SPLINE_SURFACE ( 3, 1, ( 
 ( #55066, #21262 ),
 ( #40393, #59455 ),
 ( #16563, #54754 ),
 ( #12193, #55994 ) ),
 .UNSPECIFIED., .F., .F., .F. ) 
 B_SPLINE_SURFACE_WITH_KNOTS ( ( 4, 4 ),
 ( 2, 2 ),
 ( 0.000000000000000000, 1.000000000000000000 ),
 ( 0.000000000000000000, 1.000000000000000000 ),
 .UNSPECIFIED. ) 
 GEOMETRIC_REPRESENTATION_ITEM ( )  RATIONAL_B_SPLINE_SURFACE ( (
 ( 1.000000000000000000, 1.000000000000000000),
 ( 0.7282232189291694135, 0.9929344683865672927),
 ( 0.7282232189291694135, 0.9929344683865672927),
 ( 1.000000000000000000, 1.000000000000000000) ) ) 
 REPRESENTATION_ITEM ( '' )  SURFACE ( )  );
#41467=VECTOR ( 'NONE', #55106, 1000.000000000000114 ) ;
#41468=EDGE_CURVE ( 'NONE', #60467, #53953, #42658, .T. ) ;
#41469=LINE ( 'NONE', #2598, #58273 ) ;
#41472=VERTEX_POINT ( 'NONE', #35794 ) ;
#41476=EDGE_CURVE ( 'NONE', #40143, #8823, #7445, .T. ) ;
#41477=ORIENTED_EDGE ( 'NONE', *, *, #23563, .T. ) ;
#41484=CARTESIAN_POINT ( 'NONE',  ( 4.962356264823609031, -35.98698831890617100, -21.82137185415387037 ) ) ;
#41497=VERTEX_POINT ( 'NONE', #45501 ) ;
#41500=CARTESIAN_POINT ( 'NONE',  ( 3.238018933889920792, 2.836920992588588764, 13.09043053720782268 ) ) ;
#41501=CARTESIAN_POINT ( 'NONE',  ( 0.5830082357119545922, -38.81693288260808572, 26.31497209813148785 ) ) ;
#41506=ADVANCED_FACE ( 'NONE', ( #31384 ), #54396, .F. ) ;
#41507=B_SPLINE_CURVE_WITH_KNOTS ( 'NONE', 3,
 ( #54671, #59999, #11800, #49995 ),
 .UNSPECIFIED., .F., .F.,
 ( 4, 4 ),
 ( 0.000000000000000000, 0.005004948556313800097 ),
 .UNSPECIFIED. ) ;
#41526=CARTESIAN_POINT ( 'NONE',  ( 5.896782393890504181, -4.668739246792056541, -19.56345983519980081 ) ) ;
#41534=CARTESIAN_POINT ( 'NONE',  ( 0.8554163680231816613, -46.15020320557298561, -8.447734441620468715 ) ) ;
#41543=VERTEX_POINT ( 'NONE', #8181 ) ;
#41544=ORIENTED_EDGE ( 'NONE', *, *, #8623, .T. ) ;
#41549=ORIENTED_EDGE ( 'NONE', *, *, #59468, .F. ) ;
#41556=CARTESIAN_POINT ( 'NONE',  ( 0.9762797500689124330, 25.26481495167912783, -33.43671500974812716 ) ) ;
#41568=ORIENTED_EDGE ( 'NONE', *, *, #21557, .F. ) ;
#41570=CARTESIAN_POINT ( 'NONE',  ( 5.838029081930955932, 19.90064824094183749, -42.83724148148685629 ) ) ;
#41577=VERTEX_POINT ( 'NONE', #36412 ) ;
#41579=( BOUNDED_SURFACE ( )  B_SPLINE_SURFACE ( 3, 1, ( 
 ( #17402, #21796 ),
 ( #7356, #26482 ),
 ( #40313, #7047 ),
 ( #2980, #41534 ) ),
 .UNSPECIFIED., .F., .F., .F. ) 
 B_SPLINE_SURFACE_WITH_KNOTS ( ( 4, 4 ),
 ( 2, 2 ),
 ( 0.000000000000000000, 1.000000000000000000 ),
 ( 0.000000000000000000, 1.000000000000000000 ),
 .UNSPECIFIED. ) 
 GEOMETRIC_REPRESENTATION_ITEM ( )  RATIONAL_B_SPLINE_SURFACE ( (
 ( 1.000000000000000000, 1.000000000000000000),
 ( 0.7282232189291693025, 0.9929344683865674037),
 ( 0.7282232189291693025, 0.9929344683865674037),
 ( 1.000000000000000000, 1.000000000000000000) ) ) 
 REPRESENTATION_ITEM ( '' )  SURFACE ( )  );
#41584=CARTESIAN_POINT ( 'NONE',  ( 0.9789233960466692253, 24.75338403626521355, 33.81725455422888871 ) ) ;
#41586=ORIENTED_EDGE ( 'NONE', *, *, #56427, .T. ) ;
#41590=CARTESIAN_POINT ( 'NONE',  ( 1.157644175074339365, 29.72797329618415318, -29.55080166730750335 ) ) ;
#41594=CARTESIAN_POINT ( 'NONE',  ( 4.958415959904820092, 7.056061540672502908, 44.87110372340845288 ) ) ;
#41601=ORIENTED_EDGE ( 'NONE', *, *, #46559, .T. ) ;
#41614=EDGE_CURVE ( 'NONE', #15708, #50474, #28430, .T. ) ;
#41619=FACE_OUTER_BOUND ( 'NONE', #47696, .T. ) ;
#41621=CARTESIAN_POINT ( 'NONE',  ( 0.5806925824938490299, 46.40146083665128174, 6.791670970260652140 ) ) ;
#41633=EDGE_CURVE ( 'NONE', #21594, #24966, #30744, .T. ) ;
#41636=ORIENTED_EDGE ( 'NONE', *, *, #6746, .F. ) ;
#41645=CARTESIAN_POINT ( 'NONE',  ( 0.5806925824938499181, -7.260877859416734026, -46.33035738103254175 ) ) ;
#41652=( BOUNDED_SURFACE ( )  B_SPLINE_SURFACE ( 3, 1, ( 
 ( #2819, #41691 ),
 ( #21952, #60146 ),
 ( #17255, #36376 ),
 ( #22260, #7834 ) ),
 .UNSPECIFIED., .F., .F., .F. ) 
 B_SPLINE_SURFACE_WITH_KNOTS ( ( 4, 4 ),
 ( 2, 2 ),
 ( 0.000000000000000000, 1.000000000000000000 ),
 ( 0.000000000000000000, 1.000000000000000000 ),
 .UNSPECIFIED. ) 
 GEOMETRIC_REPRESENTATION_ITEM ( )  RATIONAL_B_SPLINE_SURFACE ( (
 ( 1.000000000000000000, 1.000000000000000000),
 ( 0.9952954269826590483, 0.8620686068821307169),
 ( 0.9952954269826590483, 0.8620686068821307169),
 ( 1.000000000000000000, 1.000000000000000000) ) ) 
 REPRESENTATION_ITEM ( '' )  SURFACE ( )  );
#41653=ORIENTED_EDGE ( 'NONE', *, *, #52076, .T. ) ;
#41654=VERTEX_POINT ( 'NONE', #38886 ) ;
#41655=CARTESIAN_POINT ( 'NONE',  ( 4.956445790443989807, 44.30493387627029733, 15.95653108789479191 ) ) ;
#41658=CARTESIAN_POINT ( 'NONE',  ( 2.282803330402959574, 39.73060135428402617, 25.05945377465257451 ) ) ;
#41675=CARTESIAN_POINT ( 'NONE',  ( 5.895596859100789899, -2.009647457886758914, -20.01223376606161963 ) ) ;
#41676=ADVANCED_FACE ( 'NONE', ( #52320 ), #42764, .T. ) ;
#41677=ADVANCED_FACE ( 'NONE', ( #29145 ), #57147, .F. ) ;
#41683=CARTESIAN_POINT ( 'NONE',  ( 1.092182651088186462, -16.93161368780761578, 38.34164370979851100 ) ) ;
#41685=CARTESIAN_POINT ( 'NONE',  ( 0.5824936645240087474, -41.69005659875550407, -21.47504039187983693 ) ) ;
#41687=FILL_AREA_STYLE_COLOUR ( '', #59718 ) ;
#41689=EDGE_CURVE ( 'NONE', #5387, #54885, #58259, .T. ) ;
#41690=VERTEX_POINT ( 'NONE', #42645 ) ;
#41691=CARTESIAN_POINT ( 'NONE',  ( 0.8554163680231720024, -44.01281378489805007, 16.25046755781837504 ) ) ;
#41692=CARTESIAN_POINT ( 'NONE',  ( 0.5797568599927140909, 28.32170417884941926, -37.37788625747514715 ) ) ;
#41695=DIRECTION ( 'NONE',  ( 0.000000000000000000, 0.000000000000000000, 1.000000000000000000 ) ) ;
#41697=CIRCLE ( 'NONE', #45670, 8.000000000000000000 ) ;
#41698=CARTESIAN_POINT ( 'NONE',  ( 0.9789889208857700531, 29.20362932482186480, 30.05799281889552788 ) ) ;
#41702=CARTESIAN_POINT ( 'NONE',  ( 3.376099380956842921, 3.553490516825148049, 12.92598502161057006 ) ) ;
#41703=B_SPLINE_CURVE_WITH_KNOTS ( 'NONE', 3,
 ( #16647, #55759, #41100, #35769 ),
 .UNSPECIFIED., .F., .F.,
 ( 4, 4 ),
 ( 7.152448122690996019E-18, 0.005004948556313816577 ),
 .UNSPECIFIED. ) ;
#41704=CARTESIAN_POINT ( 'NONE',  ( 0.8554163680231738898, 31.95314001164559770, 34.35407277904604229 ) ) ;
#41718=CARTESIAN_POINT ( 'NONE',  ( 4.962356264823603702, -4.645793755590432283, -41.82884409403234116 ) ) ;
#41738=CARTESIAN_POINT ( 'NONE',  ( 0.5824936645240096356, -44.18041932528780080, -15.72668837619807825 ) ) ;
#41742=DIRECTION ( 'NONE',  ( -0.07500201931887529039, -0.6334382584229031332, 0.7701497710603116831 ) ) ;
#41744=DIRECTION ( 'NONE',  ( -1.000000000000000000, -0.000000000000000000, -0.000000000000000000 ) ) ;
#41745=ADVANCED_FACE ( 'NONE', ( #20075 ), #14016, .F. ) ;
#41756=( BOUNDED_SURFACE ( )  B_SPLINE_SURFACE ( 3, 1, ( 
 ( #23717, #9298 ),
 ( #19038, #52515 ),
 ( #27483, #46613 ),
 ( #38152, #46931 ) ),
 .UNSPECIFIED., .F., .F., .F. ) 
 B_SPLINE_SURFACE_WITH_KNOTS ( ( 4, 4 ),
 ( 2, 2 ),
 ( 0.000000000000000000, 1.000000000000000000 ),
 ( 0.000000000000000000, 1.000000000000000000 ),
 .UNSPECIFIED. ) 
 GEOMETRIC_REPRESENTATION_ITEM ( )  RATIONAL_B_SPLINE_SURFACE ( (
 ( 1.000000000000000000, 1.000000000000000000),
 ( 0.7282232189291694135, 0.9929344683865672927),
 ( 0.7282232189291694135, 0.9929344683865672927),
 ( 1.000000000000000000, 1.000000000000000000) ) ) 
 REPRESENTATION_ITEM ( '' )  SURFACE ( )  );
#41757=ORIENTED_EDGE ( 'NONE', *, *, #21299, .F. ) ;
#41764=VECTOR ( 'NONE', #46678, 1000.000000000000227 ) ;
#41765=DIRECTION ( 'NONE',  ( -1.000000000000000000, 0.000000000000000000, 0.000000000000000000 ) ) ;
#41767=CARTESIAN_POINT ( 'NONE',  ( 0.5817216825391114954, 4.240840028299648345, -46.70385667224744708 ) ) ;
#41770=CARTESIAN_POINT ( 'NONE',  ( 0.5817216825391126056, 40.11545677781317920, -24.28960847183133609 ) ) ;
#41772=CARTESIAN_POINT ( 'NONE',  ( 4.962356264823602814, -36.43094049105359744, -21.07183363638911189 ) ) ;
#41773=CARTESIAN_POINT ( 'NONE',  ( 0.8554163680231720024, 42.82911630180360163, -19.15391004255791430 ) ) ;
#41776=LINE ( 'NONE', #23877, #11748 ) ;
#41777=B_SPLINE_CURVE_WITH_KNOTS ( 'NONE', 3,
 ( #53690, #10819, #48710, #1382 ),
 .UNSPECIFIED., .F., .F.,
 ( 4, 4 ),
 ( 1.301042606982605321E-18, 0.004041751736740996012 ),
 .UNSPECIFIED. ) ;
#41785=EDGE_LOOP ( 'NONE', ( #28741, #14282, #55537, #59375 ) ) ;
#41788=DIRECTION ( 'NONE',  ( 0.000000000000000000, 0.000000000000000000, -1.000000000000000000 ) ) ;
#41795=EDGE_LOOP ( 'NONE', ( #9565, #20079, #38217, #28439 ) ) ;
#41798=CARTESIAN_POINT ( 'NONE',  ( 5.895596859100789899, -19.39731145114843613, -5.317188324634858354 ) ) ;
#41808=VERTEX_POINT ( 'NONE', #44821 ) ;
#41809=ORIENTED_EDGE ( 'NONE', *, *, #22218, .F. ) ;
#41810=CARTESIAN_POINT ( 'NONE',  ( 0.7764139734771244861, 10.00418665513137384, 45.82528472662399111 ) ) ;
#41813=CARTESIAN_POINT ( 'NONE',  ( 4.962356264823608143, 23.01169039590672938, -35.23773124060741679 ) ) ;
#41820=EDGE_CURVE ( 'NONE', #30940, #6137, #55267, .T. ) ;
#41827=DIRECTION ( 'NONE',  ( -0.07906939808003032866, -0.9752531043637164831, 0.2064689146486601845 ) ) ;
#41836=( BOUNDED_SURFACE ( )  B_SPLINE_SURFACE ( 3, 1, ( 
 ( #13801, #14413 ),
 ( #9691, #57583 ),
 ( #61068, #32591 ),
 ( #52284, #47009 ) ),
 .UNSPECIFIED., .F., .F., .F. ) 
 B_SPLINE_SURFACE_WITH_KNOTS ( ( 4, 4 ),
 ( 2, 2 ),
 ( 0.000000000000000000, 1.000000000000000000 ),
 ( 0.000000000000000000, 1.000000000000000000 ),
 .UNSPECIFIED. ) 
 GEOMETRIC_REPRESENTATION_ITEM ( )  RATIONAL_B_SPLINE_SURFACE ( (
 ( 1.000000000000000000, 1.000000000000000000),
 ( 0.9952954269826590483, 0.8620686068821307169),
 ( 0.9952954269826590483, 0.8620686068821307169),
 ( 1.000000000000000000, 1.000000000000000000) ) ) 
 REPRESENTATION_ITEM ( '' )  SURFACE ( )  );
#41837=CARTESIAN_POINT ( 'NONE',  ( 0.5830081025819910945, -46.77220438400303237, 3.404839415199392150 ) ) ;
#41840=CARTESIAN_POINT ( 'NONE',  ( 4.956445790443991584, 38.51510088324707226, 27.09474218539341450 ) ) ;
#41841=CARTESIAN_POINT ( 'NONE',  ( 0.9775691876210983455, 41.90693278755279749, 0.3777477061777904099 ) ) ;
#41845=CARTESIAN_POINT ( 'NONE',  ( 0.5797568599927122035, -25.76189090885626598, 39.18609811490797767 ) ) ;
#41847=ADVANCED_FACE ( 'NONE', ( #59179 ), #27761, .T. ) ;
#41849=B_SPLINE_CURVE_WITH_KNOTS ( 'NONE', 3,
 ( #160, #58711, #19618, #34333 ),
 .UNSPECIFIED., .F., .F.,
 ( 4, 4 ),
 ( 6.582812753581314488E-17, 0.005004948556313859077 ),
 .UNSPECIFIED. ) ;
#41854=CARTESIAN_POINT ( 'NONE',  ( 0.5830082357119559244, -25.46372197616247490, 39.38059037214954827 ) ) ;
#41855=CARTESIAN_POINT ( 'NONE',  ( 5.838029081930955932, -40.63013578422354755, -24.08852681897500503 ) ) ;
#41861=CARTESIAN_POINT ( 'NONE',  ( 0.5804410086790514622, -25.69437916690351642, -39.23415261073943583 ) ) ;
#41863=CARTESIAN_POINT ( 'NONE',  ( 4.962356264823608143, 0.000000000000000000, 0.000000000000000000 ) ) ;
#41865=CARTESIAN_POINT ( 'NONE',  ( 0.5824936645240086364, 22.21727860259796472, 41.29928220362735658 ) ) ;
#41869=ORIENTED_EDGE ( 'NONE', *, *, #36166, .T. ) ;
#41871=CARTESIAN_POINT ( 'NONE',  ( 0.9789889208857696090, 24.78187179627650139, -33.79635673138873386 ) ) ;
#41875=CARTESIAN_POINT ( 'NONE',  ( 0.9769922540276034795, 33.16186414041638386, -25.62464286226623145 ) ) ;
#41877=B_SPLINE_CURVE_WITH_KNOTS ( 'NONE', 3,
 ( #23867, #29481, #48291, #19486 ),
 .UNSPECIFIED., .F., .F.,
 ( 4, 4 ),
 ( 4.336808689942017736E-19, 0.004446298630425048540 ),
 .UNSPECIFIED. ) ;
#41893=CARTESIAN_POINT ( 'NONE',  ( 1.231276596079881047, -31.65135013586901991, 27.48579279545509380 ) ) ;
#41899=ORIENTED_EDGE ( 'NONE', *, *, #59954, .T. ) ;
#41906=EDGE_CURVE ( 'NONE', #2801, #36534, #24665, .T. ) ;
#41907=CARTESIAN_POINT ( 'NONE',  ( 5.910764540655178756, 0.6565643306764937792, -20.10149650520693143 ) ) ;
#41912=CARTESIAN_POINT ( 'NONE',  ( 2.618530812446115519, -26.46994001812951680, -38.84673814665556080 ) ) ;
#41921=CARTESIAN_POINT ( 'NONE',  ( 0.9790320750461900534, -27.12300087535202309, 31.94808219686815676 ) ) ;
#41922=FACE_OUTER_BOUND ( 'NONE', #58381, .T. ) ;
#41936=CARTESIAN_POINT ( 'NONE',  ( 5.894904586330512508, -17.30581086051407169, -10.24882054295791001 ) ) ;
#41940=B_SPLINE_CURVE_WITH_KNOTS ( 'NONE', 3,
 ( #47906, #10302, #5262, #4958 ),
 .UNSPECIFIED., .F., .F.,
 ( 4, 4 ),
 ( 1.551583845779545699E-17, 0.005004948556313822648 ),
 .UNSPECIFIED. ) ;
#41949=EDGE_CURVE ( 'NONE', #29740, #6434, #16919, .T. ) ;
#41950=CARTESIAN_POINT ( 'NONE',  ( 2.618530812446115519, -2.977833924573772606, -46.91331681213615923 ) ) ;
#41954=( BOUNDED_SURFACE ( )  B_SPLINE_SURFACE ( 3, 1, ( 
 ( #1015, #58629 ),
 ( #21063, #16065 ),
 ( #6304, #43663 ),
 ( #48634, #6001 ) ),
 .UNSPECIFIED., .F., .F., .F. ) 
 B_SPLINE_SURFACE_WITH_KNOTS ( ( 4, 4 ),
 ( 2, 2 ),
 ( 0.000000000000000000, 1.000000000000000000 ),
 ( 0.000000000000000000, 1.000000000000000000 ),
 .UNSPECIFIED. ) 
 GEOMETRIC_REPRESENTATION_ITEM ( )  RATIONAL_B_SPLINE_SURFACE ( (
 ( 1.000000000000000000, 1.000000000000000000),
 ( 0.9952954269826590483, 0.8620686068821339365),
 ( 0.9952954269826590483, 0.8620686068821339365),
 ( 1.000000000000000000, 1.000000000000000000) ) ) 
 REPRESENTATION_ITEM ( '' )  SURFACE ( )  );
#41959=VECTOR ( 'NONE', #30205, 1000.000000000000114 ) ;
#41963=CARTESIAN_POINT ( 'NONE',  ( 0.8560838555295223751, 43.53454501559562573, 17.46757637357886850 ) ) ;
#41966=CARTESIAN_POINT ( 'NONE',  ( 5.896782393890504181, 12.98055409426303441, 15.36331026452057813 ) ) ;
#41967=VERTEX_POINT ( 'NONE', #31932 ) ;
#41983=CARTESIAN_POINT ( 'NONE',  ( 5.896782393890504181, 12.98055409426324580, -15.36331026452040049 ) ) ;
#42012=DIRECTION ( 'NONE',  ( 0.07906939808003035641, -0.6871887087747612366, -0.7221632148065547652 ) ) ;
#42015=B_SPLINE_CURVE_WITH_KNOTS ( 'NONE', 3,
 ( #834, #197, #53442, #10551, #15566, #29648, #44102, #39388, #58439, #52215, #9310, #28411, #58748, #59688, #59998, #11799, #30876, #35611, #54979 ),
 .UNSPECIFIED., .F., .F.,
 ( 4, 3, 3, 3, 3, 3, 4 ),
 ( 9.813676791237319219E-18, 0.0002732106629380591793, 0.0004098138914053713121, 0.0005464171197651385582, 0.0006830203481512525134, 0.0008196235766963584288, 0.001011968216111141378 ),
 .UNSPECIFIED. ) ;
#42018=ADVANCED_FACE ( 'NONE', ( #8112 ), #20403, .F. ) ;
#42022=CARTESIAN_POINT ( 'NONE',  ( 4.962356264823608143, 0.000000000000000000, 0.000000000000000000 ) ) ;
#42032=CARTESIAN_POINT ( 'NONE',  ( 0.5806925824938506953, -46.06186276235258958, -8.804950948515241294 ) ) ;
#42033=EDGE_CURVE ( 'NONE', #37323, #10433, #14072, .T. ) ;
#42042=VERTEX_POINT ( 'NONE', #14686 ) ;
#42043=CARTESIAN_POINT ( 'NONE',  ( 1.000433927950262758, 24.32662655438078048, -34.12673318875604878 ) ) ;
#42050=FACE_OUTER_BOUND ( 'NONE', #56030, .T. ) ;
#42052=CARTESIAN_POINT ( 'NONE',  ( 0.5837800005270546988, -44.30121660599532873, -15.38302525092088224 ) ) ;
#42060=EDGE_CURVE ( 'NONE', #50622, #31128, #2116, .T. ) ;
#42066=CARTESIAN_POINT ( 'NONE',  ( 0.5824935313925946323, 5.056376536285211110, 46.62264721545897572 ) ) ;
#42069=CARTESIAN_POINT ( 'NONE',  ( 0.5817217712918332229, -1.111903975787065235, -46.88281799931615268 ) ) ;
#42080=ADVANCED_FACE ( 'NONE', ( #42275 ), #14375, .F. ) ;
#42083=CARTESIAN_POINT ( 'NONE',  ( 0.9784957157296367836, -12.19398871309499022, 40.09538248049621245 ) ) ;
#42086=CARTESIAN_POINT ( 'NONE',  ( 0.8560838555295158248, 33.26091945577399400, -33.07694168205770069 ) ) ;
#42094=ORIENTED_EDGE ( 'NONE', *, *, #30280, .F. ) ;
#42097=CARTESIAN_POINT ( 'NONE',  ( 0.8560838555295158248, -39.18289055412748922, 25.78902716088759206 ) ) ;
#42100=ADVANCED_FACE ( 'NONE', ( #57866 ), #52772, .F. ) ;
#42101=ORIENTED_EDGE ( 'NONE', *, *, #59546, .T. ) ;
#42112=CARTESIAN_POINT ( 'NONE',  ( 0.5326698147273788431, 0.000000000000000000, 0.000000000000000000 ) ) ;
#42113=CARTESIAN_POINT ( 'NONE',  ( 2.282803330402973785, 28.91046258521398116, -37.02272357034160422 ) ) ;
#42117=ORIENTED_EDGE ( 'NONE', *, *, #30370, .T. ) ;
#42124=EDGE_CURVE ( 'NONE', #2726, #40574, #15606, .T. ) ;
#42131=CARTESIAN_POINT ( 'NONE',  ( 3.238018933889920792, -1.956241471237834872, -13.25068344176488822 ) ) ;
#42136=ORIENTED_EDGE ( 'NONE', *, *, #58185, .F. ) ;
#42137=CARTESIAN_POINT ( 'NONE',  ( 4.960386119450151732, -40.46376651419630832, 16.64692356433904052 ) ) ;
#42146=ORIENTED_EDGE ( 'NONE', *, *, #14704, .F. ) ;
#42149=CARTESIAN_POINT ( 'NONE',  ( 4.956445790444006683, -23.10347171912805564, -41.03373788315033721 ) ) ;
#42158=CARTESIAN_POINT ( 'NONE',  ( 0.9790320750461913857, -1.314454984195479570, -41.88805725546019687 ) ) ;
#42166=CARTESIAN_POINT ( 'NONE',  ( 3.661933894777866350, 20.93652954769201813, 42.12235624285840885 ) ) ;
#42168=CARTESIAN_POINT ( 'NONE',  ( 0.5806925824938502512, -24.77160101449099727, 39.81946942793729249 ) ) ;
#42181=EDGE_CURVE ( 'NONE', #42423, #17824, #16338, .T. ) ;
#42188=CARTESIAN_POINT ( 'NONE',  ( 0.9789889208857682767, 32.83019349609273974, -26.04828771822593936 ) ) ;
#42196=CARTESIAN_POINT ( 'NONE',  ( 2.282803330402968012, -33.94297585900464043, -32.47108401781518694 ) ) ;
#42197=EDGE_CURVE ( 'NONE', #40188, #25455, #10356, .T. ) ;
#42200=CARTESIAN_POINT ( 'NONE',  ( 4.962356264823608143, 23.01169039590672938, -35.23773124060741679 ) ) ;
#42205=ORIENTED_EDGE ( 'NONE', *, *, #10072, .F. ) ;
#42210=VERTEX_POINT ( 'NONE', #21215 ) ;
#42214=CARTESIAN_POINT ( 'NONE',  ( 4.960386119450151732, -43.29863790797077883, -6.297969513007882547 ) ) ;
#42219=CARTESIAN_POINT ( 'NONE',  ( 1.231276596079881047, -26.41281459480337546, -32.55211200826465756 ) ) ;
#42220=VERTEX_POINT ( 'NONE', #50329 ) ;
#42229=ORIENTED_EDGE ( 'NONE', *, *, #44103, .T. ) ;
#42231=FACE_OUTER_BOUND ( 'NONE', #38578, .T. ) ;
#42234=CARTESIAN_POINT ( 'NONE',  ( 5.894904586330512508, -17.30581086051421025, 10.24882054295766842 ) ) ;
#42237=AXIS2_PLACEMENT_3D ( 'NONE', #31863, #7723, #35338 ) ;
#42240=CIRCLE ( 'NONE', #9202, 47.09074272231896430 ) ;
#42248=DIRECTION ( 'NONE',  ( -1.000000000000000000, -0.000000000000000000, -0.000000000000000000 ) ) ;
#42249=CARTESIAN_POINT ( 'NONE',  ( 0.5824935313925957425, 46.52475397494940523, 5.889435000427824640 ) ) ;
#42271=ORIENTED_EDGE ( 'NONE', *, *, #33136, .F. ) ;
#42272=CARTESIAN_POINT ( 'NONE',  ( 0.5837800005270550319, -7.800213544018094858, -46.24274999726447533 ) ) ;
#42274=EDGE_LOOP ( 'NONE', ( #29963, #57699, #5440, #58577 ) ) ;
#42275=FACE_OUTER_BOUND ( 'NONE', #57721, .T. ) ;
#42281=CARTESIAN_POINT ( 'NONE',  ( 0.9762797500689124330, 28.76866969768027715, -30.47438972336406238 ) ) ;
#42284=CARTESIAN_POINT ( 'NONE',  ( 2.528100132419516033, 41.42605997219556002, -6.792299596759092672 ) ) ;
#42287=CARTESIAN_POINT ( 'NONE',  ( 5.894904586330512508, -19.39796360309183498, 5.314924281188501354 ) ) ;
#42301=CARTESIAN_POINT ( 'NONE',  ( 0.9790320750461924959, -41.08593480789065211, 8.263358488166169025 ) ) ;
#42305=FILL_AREA_STYLE ('',( #41687 ) ) ;
#42307=ORIENTED_EDGE ( 'NONE', *, *, #35553, .F. ) ;
#42309=CARTESIAN_POINT ( 'NONE',  ( 3.376099380956842921, 11.29282810595550934, -7.223601387217343905 ) ) ;
#42310=ADVANCED_FACE ( 'NONE', ( #2402 ), #52397, .F. ) ;
#42316=CARTESIAN_POINT ( 'NONE',  ( 0.5837157313716024865, 22.61716662562863789, -41.08163625527314622 ) ) ;
#42324=CARTESIAN_POINT ( 'NONE',  ( 0.9790320750461907195, 20.06511352880068344, 36.79304759894904464 ) ) ;
#42336=DIRECTION ( 'NONE',  ( 0.000000000000000000, 0.000000000000000000, 1.000000000000000000 ) ) ;
#42338=FACE_OUTER_BOUND ( 'NONE', #49816, .T. ) ;
#42339=ORIENTED_EDGE ( 'NONE', *, *, #33765, .T. ) ;
#42343=ORIENTED_EDGE ( 'NONE', *, *, #15164, .F. ) ;
#42353=CARTESIAN_POINT ( 'NONE',  ( 1.231276596079887264, 15.85305549123172320, 38.80666698661448777 ) ) ;
#42360=CARTESIAN_POINT ( 'NONE',  ( 0.5835871038041853254, 43.22792673488614668, -18.18188117618243282 ) ) ;
#42373=CARTESIAN_POINT ( 'NONE',  ( 2.528190830796658961, -41.78722795036133419, -4.010201538270607990 ) ) ;
#42375=EDGE_CURVE ( 'NONE', #32617, #38098, #43328, .T. ) ;
#42382=CARTESIAN_POINT ( 'NONE',  ( 0.5824936645240085253, 40.53382933285173095, -23.58488623367848191 ) ) ;
#42387=CARTESIAN_POINT ( 'NONE',  ( 3.782542959838393948, -24.05480172452273635, 34.47614200270191986 ) ) ;
#42389=( BOUNDED_SURFACE ( )  B_SPLINE_SURFACE ( 3, 1, ( 
 ( #32287, #36691 ),
 ( #46393, #3437 ),
 ( #15654, #47929 ),
 ( #28806, #43243 ) ),
 .UNSPECIFIED., .F., .F., .F. ) 
 B_SPLINE_SURFACE_WITH_KNOTS ( ( 4, 4 ),
 ( 2, 2 ),
 ( 0.000000000000000000, 1.000000000000000000 ),
 ( 0.000000000000000000, 1.000000000000000000 ),
 .UNSPECIFIED. ) 
 GEOMETRIC_REPRESENTATION_ITEM ( )  RATIONAL_B_SPLINE_SURFACE ( (
 ( 1.000000000000000000, 1.000000000000000000),
 ( 0.9952954269826590483, 0.8620686068821339365),
 ( 0.9952954269826590483, 0.8620686068821339365),
 ( 1.000000000000000000, 1.000000000000000000) ) ) 
 REPRESENTATION_ITEM ( '' )  SURFACE ( )  );
#42391=CARTESIAN_POINT ( 'NONE',  ( 0.5804410086790514622, 11.40290849443536025, -45.49168638029294698 ) ) ;
#42400=VERTEX_POINT ( 'NONE', #13684 ) ;
#42404=EDGE_CURVE ( 'NONE', #57082, #57756, #59705, .T. ) ;
#42405=ORIENTED_EDGE ( 'NONE', *, *, #6674, .F. ) ;
#42409=EDGE_LOOP ( 'NONE', ( #8231, #3768, #4872, #32551, #12515, #7230 ) ) ;
#42410=DIRECTION ( 'NONE',  ( 0.000000000000000000, 0.000000000000000000, 1.000000000000000000 ) ) ;
#42416=CARTESIAN_POINT ( 'NONE',  ( 5.910764540655178756, -4.677486889029723649, -19.56073502893278260 ) ) ;
#42420=ORIENTED_EDGE ( 'NONE', *, *, #13321, .T. ) ;
#42421=CARTESIAN_POINT ( 'NONE',  ( 0.9790724872846782167, -39.60305385475923856, 13.70887797591368340 ) ) ;
#42423=VERTEX_POINT ( 'NONE', #53405 ) ;
#42424=LINE ( 'NONE', #23598, #16585 ) ;
#42429=CARTESIAN_POINT ( 'NONE',  ( 0.5804410086790514622, -38.97211966759145696, -26.09010809617946336 ) ) ;
#42430=VERTEX_POINT ( 'NONE', #29607 ) ;
#42431=CARTESIAN_POINT ( 'NONE',  ( 0.5806925824938511393, -45.84420715090610798, 9.875780123533177246 ) ) ;
#42432=CARTESIAN_POINT ( 'NONE',  ( 4.962356264823608143, 34.94214251265138671, -23.45809613945485950 ) ) ;
#42435=VERTEX_POINT ( 'NONE', #54014 ) ;
#42445=CARTESIAN_POINT ( 'NONE',  ( 4.962356264823602814, 22.27740539909316198, -35.70648129607287302 ) ) ;
#42451=CARTESIAN_POINT ( 'NONE',  ( 5.917102823773431552, 12.99138957749402401, 15.35296436840526368 ) ) ;
#42452=CARTESIAN_POINT ( 'NONE',  ( 0.8560838555295167129, -41.44626783305055540, -21.96769712083564841 ) ) ;
#42461=B_SPLINE_CURVE_WITH_KNOTS ( 'NONE', 3,
 ( #25847, #54638, #45909, #2956, #59345, #7973 ),
 .UNSPECIFIED., .F., .F.,
 ( 4, 2, 4 ),
 ( 1.168977108780794757E-16, 0.0002448718616795901690, 0.0004897437233590634610 ),
 .UNSPECIFIED. ) ;
#42464=AXIS2_PLACEMENT_3D ( 'NONE', #6016, #34881, #38974 ) ;
#42468=EDGE_CURVE ( 'NONE', #25211, #35968, #44773, .T. ) ;
#42469=CARTESIAN_POINT ( 'NONE',  ( 4.962356264823608143, -4.645793755591040686, 41.82884409403227011 ) ) ;
#42470=EDGE_CURVE ( 'NONE', #49719, #13205, #34327, .T. ) ;
#42476=CARTESIAN_POINT ( 'NONE',  ( 5.917102823773431552, 5.950457534746081301, -19.21150106521938383 ) ) ;
#42490=CARTESIAN_POINT ( 'NONE',  ( 4.962356264823608143, -4.645793755591040686, 41.82884409403227011 ) ) ;
#42491=SHAPE_REPRESENTATION ( 'straight bevel gear(output)_iso_ISO - Straight bevel gear 2M 47GT 48PT 20PA 5FW ---47O25H120MD16.0N', ( #14677 ), #18740 ) ;
#42493=CARTESIAN_POINT ( 'NONE',  ( 5.917102823773431552, 5.966888710896498083, 19.20640406644403342 ) ) ;
#42497=EDGE_LOOP ( 'NONE', ( #8727, #26198, #30356, #58373 ) ) ;
#42498=CARTESIAN_POINT ( 'NONE',  ( 0.9785694773339252972, -37.30335551955128182, -19.09960922889875690 ) ) ;
#42502=CONICAL_SURFACE ( 'NONE', #19463, 42.08604991992415023, 1.569615340895231137 ) ;
#42510=CARTESIAN_POINT ( 'NONE',  ( 0.8560838555295223751, 11.76118766017263972, 45.40977096290989579 ) ) ;
#42511=ORIENTED_EDGE ( 'NONE', *, *, #34032, .F. ) ;
#42513=CARTESIAN_POINT ( 'NONE',  ( 0.5824935313925941882, 28.11019129984335763, 37.53738565936699700 ) ) ;
#42520=DIRECTION ( 'NONE',  ( -0.07500201931887529039, -0.04681388819014925540, -0.9960839106072396643 ) ) ;
#42526=EDGE_CURVE ( 'NONE', #47205, #4749, #2635, .T. ) ;
#42527=CARTESIAN_POINT ( 'NONE',  ( 0.5806925824938499181, -42.09901922557445175, 20.66143612114793626 ) ) ;
#42530=ORIENTED_EDGE ( 'NONE', *, *, #20453, .T. ) ;
#42532=CARTESIAN_POINT ( 'NONE',  ( 0.8554163680231708922, -24.47000373826151787, -40.03029340588557972 ) ) ;
#42542=CARTESIAN_POINT ( 'NONE',  ( 0.5806925824938499181, 32.20670061096218006, 34.08739940358331921 ) ) ;
#42545=VECTOR ( 'NONE', #12275, 1000.000000000000227 ) ;
#42551=B_SPLINE_CURVE_WITH_KNOTS ( 'NONE', 3,
 ( #18612, #46505, #60884, #52409, #18310, #47126 ),
 .UNSPECIFIED., .F., .F.,
 ( 4, 2, 4 ),
 ( 1.222726755474739050E-16, 0.0002448718616795939637, 0.0004897437233590656294 ),
 .UNSPECIFIED. ) ;
#42557=CARTESIAN_POINT ( 'NONE',  ( 1.000433927950263424, -41.19597236030789134, -7.701333582022964919 ) ) ;
#42559=CARTESIAN_POINT ( 'NONE',  ( 0.5837157313716024865, 43.13919761750232595, 18.39148423863895587 ) ) ;
#42568=VERTEX_POINT ( 'NONE', #25839 ) ;
#42580=CARTESIAN_POINT ( 'NONE',  ( 1.000433927950262980, 28.65822030437768575, -30.57981501969232951 ) ) ;
#42581=CARTESIAN_POINT ( 'NONE',  ( 0.9762797500689124330, -37.17323042682988188, 19.35137526946117958 ) ) ;
#42583=CARTESIAN_POINT ( 'NONE',  ( 5.896782393890504181, 10.82771479451295349, -16.94953330350713117 ) ) ;
#42587=CARTESIAN_POINT ( 'NONE',  ( 0.7056313189692701160, -46.12214899551614877, -8.514459230800694556 ) ) ;
#42592=EDGE_CURVE ( 'NONE', #44953, #41472, #20127, .T. ) ;
#42605=CARTESIAN_POINT ( 'NONE',  ( 0.5834584762367748256, -41.77312704313945346, -21.31295019585331829 ) ) ;
#42614=EDGE_CURVE ( 'NONE', #30244, #42659, #8910, .T. ) ;
#42615=CARTESIAN_POINT ( 'NONE',  ( 0.5804410086790514622, -45.84731009780852418, -9.876437042313485293 ) ) ;
#42618=CARTESIAN_POINT ( 'NONE',  ( 0.5837799406558221715, 22.45748484441089943, -41.16922301963273867 ) ) ;
#42627=CARTESIAN_POINT ( 'NONE',  ( 5.896278296736517710, 19.71091930359941102, -4.000829891581988207 ) ) ;
#42633=CARTESIAN_POINT ( 'NONE',  ( 0.5824936645240084143, -45.88238142230681404, -9.697693233870870344 ) ) ;
#42634=EDGE_LOOP ( 'NONE', ( #61866, #8318, #16239, #78 ) ) ;
#42635=CONICAL_SURFACE ( 'NONE', #30626, 42.08604991992415023, 1.569615340895231137 ) ;
#42640=CARTESIAN_POINT ( 'NONE',  ( 1.000110580585050757, -6.321169275951049826, -41.43018587644367301 ) ) ;
#42645=CARTESIAN_POINT ( 'NONE',  ( 0.8560838555295158248, 43.53454501559585310, -17.46757637357826454 ) ) ;
#42647=FACE_OUTER_BOUND ( 'NONE', #60709, .T. ) ;
#42648=VERTEX_POINT ( 'NONE', #27380 ) ;
#42651=LINE ( 'NONE', #14153, #50247 ) ;
#42658=B_SPLINE_CURVE_WITH_KNOTS ( 'NONE', 3,
 ( #1932, #35171, #21058, #39568, #31076, #16671 ),
 .UNSPECIFIED., .F., .F.,
 ( 4, 2, 4 ),
 ( 4.770489558936219510E-18, 0.0002291472222819929626, 0.0004582944445639811548 ),
 .UNSPECIFIED. ) ;
#42659=VERTEX_POINT ( 'NONE', #32715 ) ;
#42663=CARTESIAN_POINT ( 'NONE',  ( 0.9775691876210967912, -34.33603183980574869, -24.02853775172010486 ) ) ;
#42665=CARTESIAN_POINT ( 'NONE',  ( 4.962356264823603702, 12.05238263218972072, -40.32338863178092225 ) ) ;
#42667=EDGE_CURVE ( 'NONE', #45332, #61929, #42551, .T. ) ;
#42684=CARTESIAN_POINT ( 'NONE',  ( 0.5837799406558231707, 40.30297663972491762, -23.97735647553728455 ) ) ;
#42687=ADVANCED_FACE ( 'NONE', ( #32405 ), #53843, .T. ) ;
#42690=CARTESIAN_POINT ( 'NONE',  ( 0.5804410086790514622, 16.34485605153991017, -43.95867983128970735 ) ) ;
#42691=DIRECTION ( 'NONE',  ( 0.000000000000000000, 0.000000000000000000, 1.000000000000000000 ) ) ;
#42693=LINE ( 'NONE', #61754, #14334 ) ;
#42694=ORIENTED_EDGE ( 'NONE', *, *, #35595, .F. ) ;
#42698=ORIENTED_EDGE ( 'NONE', *, *, #21351, .T. ) ;
#42700=CARTESIAN_POINT ( 'NONE',  ( 0.5782707292762442330, 36.35509350284729635, 29.63179930592889733 ) ) ;
#42701=ORIENTED_EDGE ( 'NONE', *, *, #17018, .T. ) ;
#42702=VERTEX_POINT ( 'NONE', #42431 ) ;
#42703=B_SPLINE_CURVE_WITH_KNOTS ( 'NONE', 3,
 ( #51505, #3892, #18639, #4500, #8922, #28950 ),
 .UNSPECIFIED., .F., .F.,
 ( 4, 2, 4 ),
 ( 8.787390050835121380E-18, 0.0002448709889506569398, 0.0004897419779013041218 ),
 .UNSPECIFIED. ) ;
#42704=CARTESIAN_POINT ( 'NONE',  ( 4.956445790443988031, 0.000000000000000000, 0.000000000000000000 ) ) ;
#42714=CARTESIAN_POINT ( 'NONE',  ( 4.962356264823603702, -10.17958088187380739, -40.83640203215431086 ) ) ;
#42722=CARTESIAN_POINT ( 'NONE',  ( 0.9780106845699496620, -39.69153635952322645, 13.45039731294514773 ) ) ;
#42723=ORIENTED_EDGE ( 'NONE', *, *, #27468, .F. ) ;
#42726=DIRECTION ( 'NONE',  ( 0.07500201931887538753, -0.3709639164044654658, 0.9256135639801049697 ) ) ;
#42727=ORIENTED_EDGE ( 'NONE', *, *, #39942, .F. ) ;
#42728=CARTESIAN_POINT ( 'NONE',  ( 0.8560838555295158248, -8.701885300216421371, 46.09392613244839509 ) ) ;
#42740=CARTESIAN_POINT ( 'NONE',  ( 0.8554163680231738898, 46.36773742900842166, 7.158100224665124856 ) ) ;
#42744=EDGE_LOOP ( 'NONE', ( #32941, #11671, #895, #49599 ) ) ;
#42749=CARTESIAN_POINT ( 'NONE',  ( 5.896782393890504181, -9.671431223050909409, -17.63489452692610371 ) ) ;
#42764=CONICAL_SURFACE ( 'NONE', #29723, 42.08604991992415023, 1.569615340895231137 ) ;
#42774=CARTESIAN_POINT ( 'NONE',  ( 4.956445790444005794, -36.61936279692559992, -29.60676136437043127 ) ) ;
#42780=CARTESIAN_POINT ( 'NONE',  ( 0.5848930533535030563, -25.38746244141776387, -39.43031616882066714 ) ) ;
#42781=CARTESIAN_POINT ( 'NONE',  ( 3.238018933889920792, -8.855909537851550439, 10.04889837868026703 ) ) ;
#42806=ORIENTED_EDGE ( 'NONE', *, *, #4999, .T. ) ;
#42809=EDGE_CURVE ( 'NONE', #22425, #19824, #31994, .T. ) ;
#42821=ORIENTED_EDGE ( 'NONE', *, *, #43305, .F. ) ;
#42833=DIRECTION ( 'NONE',  ( -1.000000000000000000, -0.000000000000000000, -0.000000000000000000 ) ) ;
#42834=CARTESIAN_POINT ( 'NONE',  ( 5.910764540655178756, -19.40170003828495027, -5.298610581423855770 ) ) ;
#42842=CARTESIAN_POINT ( 'NONE',  ( 0.9762797500689124330, 24.45014227843030596, -34.03697001423921620 ) ) ;
#42848=DIRECTION ( 'NONE',  ( -1.000000000000000000, -0.000000000000000000, -0.000000000000000000 ) ) ;
#42852=EDGE_CURVE ( 'NONE', #50622, #50432, #61649, .T. ) ;
#42857=ORIENTED_EDGE ( 'NONE', *, *, #43789, .T. ) ;
#42875=LINE ( 'NONE', #23746, #40721 ) ;
#42879=CIRCLE ( 'NONE', #12875, 47.09074272231896430 ) ;
#42888=FACE_OUTER_BOUND ( 'NONE', #7094, .T. ) ;
#42889=CARTESIAN_POINT ( 'NONE',  ( 0.5824935313925951874, -8.159134433442462253, -46.18080447925144938 ) ) ;
#42893=ORIENTED_EDGE ( 'NONE', *, *, #21351, .F. ) ;
#42894=CARTESIAN_POINT ( 'NONE',  ( 3.238018933889920792, 10.33920672294401122, 8.515180368487932583 ) ) ;
#42895=ADVANCED_FACE ( 'NONE', ( #42905 ), #20153, .F. ) ;
#42896=ORIENTED_EDGE ( 'NONE', *, *, #52076, .F. ) ;
#42899=CARTESIAN_POINT ( 'NONE',  ( 0.9783242366443538618, -37.52440672474880756, 18.66154843956287479 ) ) ;
#42905=FACE_OUTER_BOUND ( 'NONE', #36988, .T. ) ;
#42912=LINE ( 'NONE', #24087, #788 ) ;
#42918=CARTESIAN_POINT ( 'NONE',  ( 0.9790850452238877288, -41.05878386289116833, 8.397237519778984804 ) ) ;
#42925=EDGE_LOOP ( 'NONE', ( #42136, #60109, #48468, #48305 ) ) ;
#42931=CARTESIAN_POINT ( 'NONE',  ( 3.376099380956838925, -6.821144471874409199, -11.54038005118914434 ) ) ;
#42932=CARTESIAN_POINT ( 'NONE',  ( 0.9790850452238869517, -34.52257324172052222, 23.75982464230828128 ) ) ;
#42942=CARTESIAN_POINT ( 'NONE',  ( 0.6064515330803631477, 42.89337338949368927, -18.96029681483289053 ) ) ;
#42945=FACE_OUTER_BOUND ( 'NONE', #2131, .T. ) ;
#42950=CIRCLE ( 'NONE', #15935, 42.08604991992415023 ) ;
#42956=VECTOR ( 'NONE', #51902, 1000.000000000000114 ) ;
#42958=CARTESIAN_POINT ( 'NONE',  ( 1.231276596079881935, 10.53918392497884149, -40.57341954055061706 ) ) ;
#42965=CARTESIAN_POINT ( 'NONE',  ( 4.962356264823608143, 0.000000000000000000, 0.000000000000000000 ) ) ;
#42966=CARTESIAN_POINT ( 'NONE',  ( 0.9762797500689124330, -34.83496347773955648, 23.29914386174426255 ) ) ;
#42971=CARTESIAN_POINT ( 'NONE',  ( 0.5848930533535030563, -41.93775812029581829, 20.98803292905553874 ) ) ;
#42972=CARTESIAN_POINT ( 'NONE',  ( 0.5806925824938499181, 16.34374012233052653, 43.95571090492437349 ) ) ;
#42978=ORIENTED_EDGE ( 'NONE', *, *, #30614, .F. ) ;
#42979=CARTESIAN_POINT ( 'NONE',  ( 0.7056313189692724475, 46.36312287336356519, -7.085864900416160239 ) ) ;
#42983=CARTESIAN_POINT ( 'NONE',  ( 5.901463166500145796, 12.99631574414091517, -15.34971163961172458 ) ) ;
#42984=CARTESIAN_POINT ( 'NONE',  ( 0.5830081025819934260, 10.60549139512680483, -45.68101998259383123 ) ) ;
#42986=CARTESIAN_POINT ( 'NONE',  ( 0.5834584762367756028, 4.512861497189343041, 46.67836833181272027 ) ) ;
#42993=CARTESIAN_POINT ( 'NONE',  ( 0.5804410086790514622, 36.46521478791908066, 29.49250688439903101 ) ) ;
#42995=CARTESIAN_POINT ( 'NONE',  ( 0.6845945791218034371, -25.96635969083060402, 39.06602981005814001 ) ) ;
#43004=CARTESIAN_POINT ( 'NONE',  ( 2.618530812446115519, 12.26263843375515172, 45.38011114840057303 ) ) ;
#43010=CARTESIAN_POINT ( 'NONE',  ( 5.895881250540457863, -4.658141670565439263, 19.56602662231764356 ) ) ;
#43017=EDGE_LOOP ( 'NONE', ( #16484, #39702, #48996, #45575 ) ) ;
#43026=VECTOR ( 'NONE', #27297, 1000.000000000000114 ) ;
#43032=CARTESIAN_POINT ( 'NONE',  ( 4.956445790443991584, 30.81386304088947625, 35.60960396630300551 ) ) ;
#43039=CARTESIAN_POINT ( 'NONE',  ( 5.901463166500146684, -9.653076390470776147, 17.64471554149775301 ) ) ;
#43041=ORIENTED_EDGE ( 'NONE', *, *, #36306, .F. ) ;
#43046=CARTESIAN_POINT ( 'NONE',  ( 4.956445790443988031, 0.000000000000000000, 0.000000000000000000 ) ) ;
#43049=ADVANCED_FACE ( 'NONE', ( #54720 ), #3655, .F. ) ;
#43053=CARTESIAN_POINT ( 'NONE',  ( 0.5817216825391112733, 36.52003817910519246, -29.41975124986882406 ) ) ;
#43058=ORIENTED_EDGE ( 'NONE', *, *, #38865, .F. ) ;
#43061=LINE ( 'NONE', #100, #16819 ) ;
#43065=CARTESIAN_POINT ( 'NONE',  ( 5.901463166500146684, 12.99631574414070023, 15.34971163961190399 ) ) ;
#43068=FACE_OUTER_BOUND ( 'NONE', #6150, .T. ) ;
#43069=B_SPLINE_CURVE_WITH_KNOTS ( 'NONE', 3,
 ( #5584, #25337, #43864, #34751, #6816, #15339 ),
 .UNSPECIFIED., .F., .F.,
 ( 4, 2, 4 ),
 ( 6.805474077711127748E-18, 0.0002291472222819938571, 0.0004582944445639809379 ),
 .UNSPECIFIED. ) ;
#43075=CARTESIAN_POINT ( 'NONE',  ( 0.7056759521544978542, -45.78629854946090916, -10.16679370581612041 ) ) ;
#43088=VERTEX_POINT ( 'NONE', #3034 ) ;
#43090=VECTOR ( 'NONE', #57129, 1000.000000000000114 ) ;
#43097=CARTESIAN_POINT ( 'NONE',  ( 0.8554163680231708922, 45.48289776771382265, -11.51136324522475540 ) ) ;
#43104=ADVANCED_FACE ( 'NONE', ( #31550 ), #5651, .F. ) ;
#43119=EDGE_CURVE ( 'NONE', #19259, #1466, #12588, .T. ) ;
#43135=CARTESIAN_POINT ( 'NONE',  ( 1.157644175074335813, -30.52765897203332912, -28.72393275939801782 ) ) ;
#43136=CARTESIAN_POINT ( 'NONE',  ( 5.895596859100789899, 14.91436009500240445, 13.49407448360528861 ) ) ;
#43145=FACE_OUTER_BOUND ( 'NONE', #7526, .T. ) ;
#43148=VERTEX_POINT ( 'NONE', #28389 ) ;
#43149=EDGE_CURVE ( 'NONE', #26123, #8407, #58805, .T. ) ;
#43157=EDGE_CURVE ( 'NONE', #5597, #2574, #45893, .T. ) ;
#43159=CARTESIAN_POINT ( 'NONE',  ( 4.958415959904821868, -31.21198115812957852, 33.00024524162211037 ) ) ;
#43168=B_SPLINE_CURVE_WITH_KNOTS ( 'NONE', 3,
 ( #893, #44767, #30627, #40081, #58503, #20032 ),
 .UNSPECIFIED., .F., .F.,
 ( 4, 2, 4 ),
 ( 3.476216610979977084E-18, 0.0002291459268755725929, 0.0004582918537511417164 ),
 .UNSPECIFIED. ) ;
#43175=EDGE_CURVE ( 'NONE', #29061, #32533, #43211, .T. ) ;
#43186=B_SPLINE_CURVE_WITH_KNOTS ( 'NONE', 3,
 ( #48350, #58033, #15154, #34262, #31405, #30457 ),
 .UNSPECIFIED., .F., .F.,
 ( 4, 2, 4 ),
 ( 1.154609648881453222E-16, 0.0002448718616795960779, 0.0004897437233590766882 ),
 .UNSPECIFIED. ) ;
#43192=CARTESIAN_POINT ( 'NONE',  ( 0.9780106845699476636, 40.33556544546049594, 11.37424312428799844 ) ) ;
#43203=CARTESIAN_POINT ( 'NONE',  ( 2.618530812446111078, -21.05599821100593161, 42.02822537933662517 ) ) ;
#43211=B_SPLINE_CURVE_WITH_KNOTS ( 'NONE', 3,
 ( #51882, #8980, #33420, #28088 ),
 .UNSPECIFIED., .F., .F.,
 ( 4, 4 ),
 ( 6.206335383118182794E-17, 0.005004948556313865149 ),
 .UNSPECIFIED. ) ;
#43214=VECTOR ( 'NONE', #53378, 1000.000000000000114 ) ;
#43216=CARTESIAN_POINT ( 'NONE',  ( 1.231276596079881047, 24.17959027891106416, 34.24360064248583768 ) ) ;
#43219=CARTESIAN_POINT ( 'NONE',  ( 0.9788927965476016402, 38.63831210738078425, 16.23014017574742951 ) ) ;
#43224=CARTESIAN_POINT ( 'NONE',  ( 0.9790724872846795490, -41.07690974463345412, 8.307989877984264027 ) ) ;
#43227=CARTESIAN_POINT ( 'NONE',  ( 0.5834584762367727162, 4.875245331832543272, -46.64191218172384623 ) ) ;
#43235=CARTESIAN_POINT ( 'NONE',  ( 2.528190830796658517, 10.90478310419556962, -40.53812824494315947 ) ) ;
#43240=CARTESIAN_POINT ( 'NONE',  ( 1.231276596079881935, -41.76121777166937221, -3.643825084341031584 ) ) ;
#43242=CARTESIAN_POINT ( 'NONE',  ( 0.9780106845699472196, -34.72773020588816451, 23.45881499996284347 ) ) ;
#43243=CARTESIAN_POINT ( 'NONE',  ( 0.8554163680231708922, 17.71207986799998579, -43.44522643353822389 ) ) ;
#43244=ADVANCED_FACE ( 'NONE', ( #39988 ), #10084, .F. ) ;
#43249=CARTESIAN_POINT ( 'NONE',  ( 5.901463166500145796, 12.97422524546404965, 15.36838799681346046 ) ) ;
#43253=CARTESIAN_POINT ( 'NONE',  ( 3.376099380956838925, 11.29282810595541164, 7.223601387217505554 ) ) ;
#43254=B_SPLINE_CURVE_WITH_KNOTS ( 'NONE', 3,
 ( #32198, #51905, #8675, #27484 ),
 .UNSPECIFIED., .F., .F.,
 ( 4, 4 ),
 ( 2.602085213965210642E-18, 0.004042984057420976295 ),
 .UNSPECIFIED. ) ;
#43259=CARTESIAN_POINT ( 'NONE',  ( 0.7764146366350199724, -35.37865071303732378, -30.79596641435480109 ) ) ;
#43261=CARTESIAN_POINT ( 'NONE',  ( 1.157644175074338699, 25.52398871922472878, -33.24948533947659968 ) ) ;
#43266=CARTESIAN_POINT ( 'NONE',  ( 4.958415959904816539, 45.35203410338237973, 2.529220533737273069 ) ) ;
#43273=VERTEX_POINT ( 'NONE', #58113 ) ;
#43278=CARTESIAN_POINT ( 'NONE',  ( 0.5804410086790514622, 46.40460073163220756, 6.792119168064950863 ) ) ;
#43281=VERTEX_POINT ( 'NONE', #38747 ) ;
#43287=CARTESIAN_POINT ( 'NONE',  ( 0.8554163680231816613, -29.58718577084439261, 36.41159034254562243 ) ) ;
#43293=CARTESIAN_POINT ( 'NONE',  ( 0.9780303403264757334, -22.82262494000252673, -35.14921626783534947 ) ) ;
#43297=B_SPLINE_CURVE_WITH_KNOTS ( 'NONE', 3,
 ( #60074, #45693, #49751, #2742 ),
 .UNSPECIFIED., .F., .F.,
 ( 4, 4 ),
 ( 7.152448122690996019E-18, 0.005004948556313815709 ),
 .UNSPECIFIED. ) ;
#43298=CIRCLE ( 'NONE', #23292, 42.08604991992415023 ) ;
#43305=EDGE_CURVE ( 'NONE', #37493, #10852, #14684, .T. ) ;
#43312=B_SPLINE_CURVE_WITH_KNOTS ( 'NONE', 3,
 ( #54501, #12256, #26332, #58907 ),
 .UNSPECIFIED., .F., .F.,
 ( 4, 4 ),
 ( 3.878959614448863476E-18, 0.004042984057420974560 ),
 .UNSPECIFIED. ) ;
#43313=CARTESIAN_POINT ( 'NONE',  ( 0.5797568665920711517, 33.05098768062517678, 33.26946831461290088 ) ) ;
#43316=CARTESIAN_POINT ( 'NONE',  ( 0.9790850452238870627, 9.764526516524007604, 40.75526165013907587 ) ) ;
#43318=CARTESIAN_POINT ( 'NONE',  ( 0.5837157313716030416, 45.25373608634124878, -12.30188740843450468 ) ) ;
#43321=EDGE_CURVE ( 'NONE', #34160, #42435, #49062, .T. ) ;
#43322=CARTESIAN_POINT ( 'NONE',  ( 4.956445790444002242, -40.23882117934093827, 24.46171131046763136 ) ) ;
#43326=CARTESIAN_POINT ( 'NONE',  ( 3.238018933889920792, -0.1726436309642142564, 13.39319553147569231 ) ) ;
#43328=B_SPLINE_CURVE_WITH_KNOTS ( 'NONE', 3,
 ( #32793, #52486, #8333, #46581, #56570, #41893 ),
 .UNSPECIFIED., .F., .F.,
 ( 4, 2, 4 ),
 ( 3.476216610979977084E-18, 0.0002291459268755738398, 0.0004582918537511442101 ),
 .UNSPECIFIED. ) ;
#43329=B_SPLINE_CURVE_WITH_KNOTS ( 'NONE', 3,
 ( #28992, #9259, #57460, #14293 ),
 .UNSPECIFIED., .F., .F.,
 ( 4, 4 ),
 ( 0.000000000000000000, 0.005004948556313808770 ),
 .UNSPECIFIED. ) ;
#43331=ORIENTED_EDGE ( 'NONE', *, *, #44762, .T. ) ;
#43337=DIRECTION ( 'NONE',  ( 0.07500201931887538753, -0.7741482765856521064, -0.6285452592753808521 ) ) ;
#43338=ORIENTED_EDGE ( 'NONE', *, *, #17192, .T. ) ;
#43345=EDGE_CURVE ( 'NONE', #9401, #34772, #17694, .T. ) ;
#43347=ORIENTED_EDGE ( 'NONE', *, *, #19402, .T. ) ;
#43348=CARTESIAN_POINT ( 'NONE',  ( 3.238018933889920792, 10.68005193312860790, -8.083562523623408325 ) ) ;
#43358=CARTESIAN_POINT ( 'NONE',  ( 0.7056313189692733356, -30.91979901656658214, -35.26633908889165525 ) ) ;
#43361=FACE_OUTER_BOUND ( 'NONE', #44232, .T. ) ;
#43369=CARTESIAN_POINT ( 'NONE',  ( 5.895881250540457863, -9.669871309366996570, -17.63579514704630213 ) ) ;
#43376=CARTESIAN_POINT ( 'NONE',  ( 0.5804410086790514622, -30.69452151258693462, -35.45935984995688983 ) ) ;
#43381=CARTESIAN_POINT ( 'NONE',  ( 4.962356264823608143, 0.000000000000000000, 0.000000000000000000 ) ) ;
#43395=CARTESIAN_POINT ( 'NONE',  ( 4.962356264823608143, -40.70360067759239087, 10.69824704058788711 ) ) ;
#43400=ORIENTED_EDGE ( 'NONE', *, *, #31188, .T. ) ;
#43402=CARTESIAN_POINT ( 'NONE',  ( 5.910764540655178756, 19.70610972188039511, -4.021253299454559560 ) ) ;
#43405=EDGE_CURVE ( 'NONE', #60737, #26144, #31888, .T. ) ;
#43406=ORIENTED_EDGE ( 'NONE', *, *, #59757, .F. ) ;
#43407=CARTESIAN_POINT ( 'NONE',  ( 4.962356264823608143, 12.88441948660223169, -40.06528837230067097 ) ) ;
#43410=ORIENTED_EDGE ( 'NONE', *, *, #30971, .F. ) ;
#43415=CARTESIAN_POINT ( 'NONE',  ( 0.5837800005270551429, 16.85475894598384627, -43.76245376478063065 ) ) ;
#43418=CARTESIAN_POINT ( 'NONE',  ( 4.956445790443991584, 35.28522167764473494, 31.18479086508529363 ) ) ;
#43422=EDGE_LOOP ( 'NONE', ( #2601, #40190, #28383, #38666 ) ) ;
#43423=CARTESIAN_POINT ( 'NONE',  ( 4.956445790444027999, 20.31112743693101663, -42.48524629068760561 ) ) ;
#43425=B_SPLINE_CURVE_WITH_KNOTS ( 'NONE', 3,
 ( #42774, #61828, #47770, #32210 ),
 .UNSPECIFIED., .F., .F.,
 ( 4, 4 ),
 ( 4.443059973708341306E-17, 0.005004948556313842598 ),
 .UNSPECIFIED. ) ;
#43436=LINE ( 'NONE', #44067, #38209 ) ;
#43437=CARTESIAN_POINT ( 'NONE',  ( 5.896278296736517710, -11.92612757635576237, 16.19550742171637836 ) ) ;
#43438=ORIENTED_EDGE ( 'NONE', *, *, #58669, .T. ) ;
#43446=CARTESIAN_POINT ( 'NONE',  ( 5.895596859100789899, 14.91916793517901496, 13.48875870250535058 ) ) ;
#43450=CARTESIAN_POINT ( 'NONE',  ( 3.661921753702001237, -18.07631870279536557, 43.42669485453627232 ) ) ;
#43453=ORIENTED_EDGE ( 'NONE', *, *, #46774, .T. ) ;
#43457=CARTESIAN_POINT ( 'NONE',  ( 0.5806925824938499181, 4.150136846022649095, 46.71186922510005957 ) ) ;
#43458=ORIENTED_EDGE ( 'NONE', *, *, #30706, .T. ) ;
#43470=CARTESIAN_POINT ( 'NONE',  ( 0.9780303403264770656, -6.651109705658430293, 41.37755856836385249 ) ) ;
#43473=ORIENTED_EDGE ( 'NONE', *, *, #33129, .T. ) ;
#43479=CARTESIAN_POINT ( 'NONE',  ( 0.7764146366350278550, 23.31927532629819666, 40.69707448853623788 ) ) ;
#43485=CARTESIAN_POINT ( 'NONE',  ( 0.8560838555295158248, 44.99141268455571208, 13.27198623905747432 ) ) ;
#43493=( BOUNDED_SURFACE ( )  B_SPLINE_SURFACE ( 3, 1, ( 
 ( #51522, #56537 ),
 ( #33077, #27739 ),
 ( #46869, #3909 ),
 ( #52148, #18980 ) ),
 .UNSPECIFIED., .F., .F., .F. ) 
 B_SPLINE_SURFACE_WITH_KNOTS ( ( 4, 4 ),
 ( 2, 2 ),
 ( 0.000000000000000000, 1.000000000000000000 ),
 ( 0.000000000000000000, 1.000000000000000000 ),
 .UNSPECIFIED. ) 
 GEOMETRIC_REPRESENTATION_ITEM ( )  RATIONAL_B_SPLINE_SURFACE ( (
 ( 1.000000000000000000, 1.000000000000000000),
 ( 0.7282232189291693025, 0.9929344683865674037),
 ( 0.7282232189291693025, 0.9929344683865674037),
 ( 1.000000000000000000, 1.000000000000000000) ) ) 
 REPRESENTATION_ITEM ( '' )  SURFACE ( )  );
#43502=LINE ( 'NONE', #52554, #21717 ) ;
#43506=ADVANCED_FACE ( 'NONE', ( #46836 ), #3289, .F. ) ;
#43514=CARTESIAN_POINT ( 'NONE',  ( 5.910764540655178756, 8.451874527002367188, -18.25012480639438195 ) ) ;
#43516=DIRECTION ( 'NONE',  ( -0.07906939808003035641, -0.8860534191553621763, 0.4567902896191575191 ) ) ;
#43518=CARTESIAN_POINT ( 'NONE',  ( 5.895881250540457863, -4.658141670565172809, -19.56602662231770395 ) ) ;
#43547=CARTESIAN_POINT ( 'NONE',  ( 0.9789233960466705575, -34.62550353117659085, 23.60955806542803614 ) ) ;
#43548=CARTESIAN_POINT ( 'NONE',  ( 4.956445790444027111, 8.365049606152357597, -46.34181691762039179 ) ) ;
#43550=AXIS2_PLACEMENT_3D ( 'NONE', #5747, #10487, #39948 ) ;
#43552=CARTESIAN_POINT ( 'NONE',  ( 3.782542959838402830, -39.11335357675642399, -15.40725236296878542 ) ) ;
#43558=CARTESIAN_POINT ( 'NONE',  ( 4.956445790444027111, 8.365049606152357597, -46.34181691762039179 ) ) ;
#43559=CARTESIAN_POINT ( 'NONE',  ( 0.5804410086790514622, -44.12183670707880623, 15.89916279082866168 ) ) ;
#43598=DIRECTION ( 'NONE',  ( 0.000000000000000000, 0.000000000000000000, 1.000000000000000000 ) ) ;
#43601=CARTESIAN_POINT ( 'NONE',  ( 0.9787284016396619046, 40.36974178881868625, -11.25255290291651633 ) ) ;
#43604=CARTESIAN_POINT ( 'NONE',  ( 4.962356264823608143, 37.36413190407361640, 19.36897635181929545 ) ) ;
#43605=CARTESIAN_POINT ( 'NONE',  ( 4.956445790444002242, -43.14021684453514638, 18.88014143872134554 ) ) ;
#43612=DIRECTION ( 'NONE',  ( -0.07500201931887527651, 0.1132404149163036555, 0.9907327114452587624 ) ) ;
#43617=B_SPLINE_CURVE_WITH_KNOTS ( 'NONE', 3,
 ( #31389, #59571, #7244, #26374 ),
 .UNSPECIFIED., .F., .F.,
 ( 4, 4 ),
 ( 0.000000000000000000, 0.004447772540403816324 ),
 .UNSPECIFIED. ) ;
#43629=CIRCLE ( 'NONE', #18621, 42.08604991992415023 ) ;
#43632=CARTESIAN_POINT ( 'NONE',  ( 0.9789889208857696090, -1.304255160821619519, 41.88834941266890155 ) ) ;
#43633=CARTESIAN_POINT ( 'NONE',  ( 1.092182651088184020, 38.27635607255189854, -17.07869287297789285 ) ) ;
#43638=FACE_OUTER_BOUND ( 'NONE', #2628, .T. ) ;
#43640=ORIENTED_EDGE ( 'NONE', *, *, #34680, .T. ) ;
#43642=ORIENTED_EDGE ( 'NONE', *, *, #42526, .T. ) ;
#43649=CARTESIAN_POINT ( 'NONE',  ( 1.231276596079887264, -2.246340108599748309, -41.85965512441022440 ) ) ;
#43654=CARTESIAN_POINT ( 'NONE',  ( 0.8560838555295158248, 23.34035564869604684, -40.68907263964262455 ) ) ;
#43659=EDGE_CURVE ( 'NONE', #35390, #36038, #11075, .T. ) ;
#43662=VERTEX_POINT ( 'NONE', #24232 ) ;
#43663=CARTESIAN_POINT ( 'NONE',  ( 0.6845945791218034371, 16.04817208170904408, 44.07791616614603925 ) ) ;
#43664=DIRECTION ( 'NONE',  ( 0.000000000000000000, 0.000000000000000000, 1.000000000000000000 ) ) ;
#43666=DIRECTION ( 'NONE',  ( -0.07906939808003035641, -0.2876259487683229810, 0.9544733332484380828 ) ) ;
#43667=EDGE_CURVE ( 'NONE', #59068, #28949, #11679, .T. ) ;
#43673=CARTESIAN_POINT ( 'NONE',  ( 0.8554163680231738898, -24.47000373826152853, -40.03029340588557972 ) ) ;
#43676=CARTESIAN_POINT ( 'NONE',  ( 5.838029081930957709, 46.29164171884931989, 9.388768030290695066 ) ) ;
#43679=CARTESIAN_POINT ( 'NONE',  ( 1.231276596079887264, 41.91134057782999633, -0.8463462572780159343 ) ) ;
#43680=CONICAL_SURFACE ( 'NONE', #5572, 42.08604991992415023, 1.569615340895231137 ) ;
#43682=EDGE_LOOP ( 'NONE', ( #21813, #24378, #13074, #7869 ) ) ;
#43688=CARTESIAN_POINT ( 'NONE',  ( 4.962356264823608143, 0.000000000000000000, 0.000000000000000000 ) ) ;
#43689=CARTESIAN_POINT ( 'NONE',  ( 5.838029081930957709, -28.03445132514680793, -38.01492597718551991 ) ) ;
#43710=CARTESIAN_POINT ( 'NONE',  ( 0.9754292589017248272, -37.13786011588246794, 19.41923821648057569 ) ) ;
#43715=CARTESIAN_POINT ( 'NONE',  ( 3.376099380956842921, -12.16518930220319561, -5.631745100200117093 ) ) ;
#43716=CARTESIAN_POINT ( 'NONE',  ( 0.5804410086790514622, 32.20888702807410908, -34.08969709850992302 ) ) ;
#43729=CARTESIAN_POINT ( 'NONE',  ( 0.9762797500689124330, 36.31338395866797697, 20.92039508843128814 ) ) ;
#43730=CARTESIAN_POINT ( 'NONE',  ( 0.5824935313925958535, 46.89462116659080237, -0.3642563599602811064 ) ) ;
#43736=ADVANCED_FACE ( 'NONE', ( #55503 ), #24525, .F. ) ;
#43741=CARTESIAN_POINT ( 'NONE',  ( 1.231276596079881047, -41.87427716283725943, 1.954912557623087022 ) ) ;
#43744=CARTESIAN_POINT ( 'NONE',  ( 0.6845945791218023269, -2.432797934429159703, -46.84536278997295256 ) ) ;
#43747=CARTESIAN_POINT ( 'NONE',  ( 5.895881250540457863, 3.340873024792334167, 19.83346286054243279 ) ) ;
#43748=ORIENTED_EDGE ( 'NONE', *, *, #43321, .F. ) ;
#43760=EDGE_CURVE ( 'NONE', #9945, #57622, #46874, .T. ) ;
#43761=STYLED_ITEM ( 'NONE', ( #50742 ), #32490 ) ;
#43767=CARTESIAN_POINT ( 'NONE',  ( 0.5848930533535030563, -34.65838163711107711, -31.59224057714044775 ) ) ;
#43771=CARTESIAN_POINT ( 'NONE',  ( 3.238018933889920792, 10.68005193312848888, 8.083562523623562868 ) ) ;
#43774=FACE_OUTER_BOUND ( 'NONE', #28014, .T. ) ;
#43776=CARTESIAN_POINT ( 'NONE',  ( 1.000433927950263424, 14.44615545540195356, -39.34116508456767747 ) ) ;
#43777=( BOUNDED_SURFACE ( )  B_SPLINE_SURFACE ( 3, 1, ( 
 ( #5036, #57046 ),
 ( #19481, #52659 ),
 ( #52046, #42995 ),
 ( #4108, #9139 ) ),
 .UNSPECIFIED., .F., .F., .F. ) 
 B_SPLINE_SURFACE_WITH_KNOTS ( ( 4, 4 ),
 ( 2, 2 ),
 ( 0.000000000000000000, 1.000000000000000000 ),
 ( 0.000000000000000000, 1.000000000000000000 ),
 .UNSPECIFIED. ) 
 GEOMETRIC_REPRESENTATION_ITEM ( )  RATIONAL_B_SPLINE_SURFACE ( (
 ( 1.000000000000000000, 1.000000000000000000),
 ( 0.9952954269826590483, 0.8620686068821339365),
 ( 0.9952954269826590483, 0.8620686068821339365),
 ( 1.000000000000000000, 1.000000000000000000) ) ) 
 REPRESENTATION_ITEM ( '' )  SURFACE ( )  );
#43786=CARTESIAN_POINT ( 'NONE',  ( 4.956445790444011124, -16.41925925744418180, -44.13554095710700409 ) ) ;
#43789=EDGE_CURVE ( 'NONE', #48040, #48449, #34868, .T. ) ;
#43796=CARTESIAN_POINT ( 'NONE',  ( 0.5806925824938499181, 46.89268439822727430, 0.5463627657667635695 ) ) ;
#43804=CARTESIAN_POINT ( 'NONE',  ( 0.5848930533535030563, -14.06811673146470909, -44.73657534967826876 ) ) ;
#43808=CARTESIAN_POINT ( 'NONE',  ( 1.231276596079887264, -11.60895935156443848, 40.28037777618019533 ) ) ;
#43815=EDGE_CURVE ( 'NONE', #10282, #37103, #7579, .T. ) ;
#43816=ORIENTED_EDGE ( 'NONE', *, *, #14610, .T. ) ;
#43819=ORIENTED_EDGE ( 'NONE', *, *, #61432, .F. ) ;
#43821=CARTESIAN_POINT ( 'NONE',  ( 0.8554163680231738898, 46.90810212776802501, 0.9140174411379243802 ) ) ;
#43826=CARTESIAN_POINT ( 'NONE',  ( 2.618530812446115519, -35.79257080906851485, -30.47324505325967792 ) ) ;
#43829=DIRECTION ( 'NONE',  ( 0.000000000000000000, 0.000000000000000000, 1.000000000000000000 ) ) ;
#43834=CARTESIAN_POINT ( 'NONE',  ( 0.7056313189692720034, -46.84548992230426023, -2.291008052550091101 ) ) ;
#43840=EDGE_CURVE ( 'NONE', #48016, #41399, #59471, .T. ) ;
#43842=ORIENTED_EDGE ( 'NONE', *, *, #56835, .F. ) ;
#43848=CARTESIAN_POINT ( 'NONE',  ( 0.9769922540276054779, 38.40851559224979184, 16.76655853435725163 ) ) ;
#43850=CARTESIAN_POINT ( 'NONE',  ( 0.8554163680231720024, 28.56078411578431542, 37.22213163970302219 ) ) ;
#43855=DIRECTION ( 'NONE',  ( -1.000000000000000000, -0.000000000000000000, -0.000000000000000000 ) ) ;
#43858=DIRECTION ( 'NONE',  ( 0.000000000000000000, 0.000000000000000000, 1.000000000000000000 ) ) ;
#43859=( BOUNDED_SURFACE ( )  B_SPLINE_SURFACE ( 3, 1, ( 
 ( #6033, #40534 ),
 ( #35520, #15175 ),
 ( #39609, #35210 ),
 ( #30789, #30473 ) ),
 .UNSPECIFIED., .F., .F., .F. ) 
 B_SPLINE_SURFACE_WITH_KNOTS ( ( 4, 4 ),
 ( 2, 2 ),
 ( 0.000000000000000000, 1.000000000000000000 ),
 ( 0.000000000000000000, 1.000000000000000000 ),
 .UNSPECIFIED. ) 
 GEOMETRIC_REPRESENTATION_ITEM ( )  RATIONAL_B_SPLINE_SURFACE ( (
 ( 1.000000000000000000, 1.000000000000000000),
 ( 0.9952954269826590483, 0.8620686068821307169),
 ( 0.9952954269826590483, 0.8620686068821307169),
 ( 1.000000000000000000, 1.000000000000000000) ) ) 
 REPRESENTATION_ITEM ( '' )  SURFACE ( )  );
#43864=CARTESIAN_POINT ( 'NONE',  ( 1.092182651088185796, 4.971552582430809331, 41.61784292058406720 ) ) ;
#43874=CARTESIAN_POINT ( 'NONE',  ( 4.956445790443988031, 0.000000000000000000, 0.000000000000000000 ) ) ;
#43883=ORIENTED_EDGE ( 'NONE', *, *, #31991, .T. ) ;
#43888=ORIENTED_EDGE ( 'NONE', *, *, #65, .F. ) ;
#43902=EDGE_CURVE ( 'NONE', #32533, #24195, #15921, .T. ) ;
#43904=CARTESIAN_POINT ( 'NONE',  ( 0.5824936645240090805, 40.16258313460651408, 24.21167270132587390 ) ) ;
#43909=CIRCLE ( 'NONE', #40910, 47.09074272231896430 ) ;
#43910=CARTESIAN_POINT ( 'NONE',  ( 0.8560838555295158248, -34.16988317699912159, -32.13708010619451727 ) ) ;
#43912=ORIENTED_EDGE ( 'NONE', *, *, #1765, .F. ) ;
#43918=ORIENTED_EDGE ( 'NONE', *, *, #38279, .T. ) ;
#43921=CARTESIAN_POINT ( 'NONE',  ( 0.9791128995231621612, 40.41828153704135218, -11.07700103090292387 ) ) ;
#43923=CARTESIAN_POINT ( 'NONE',  ( 0.9791128995231614951, -12.42139118001737508, -40.02557276790864194 ) ) ;
#43924=CARTESIAN_POINT ( 'NONE',  ( 4.958415959904820092, -41.61824873627326582, 18.19684934125486819 ) ) ;
#43927=ORIENTED_EDGE ( 'NONE', *, *, #31292, .F. ) ;
#43935=EDGE_CURVE ( 'NONE', #48550, #59818, #32655, .T. ) ;
#43943=CARTESIAN_POINT ( 'NONE',  ( 4.956445790444003130, -40.78973928653796577, 23.53157918788916803 ) ) ;
#43951=CARTESIAN_POINT ( 'NONE',  ( 0.8560838555295158248, -39.18289055412748922, 25.78902716088759206 ) ) ;
#43952=CARTESIAN_POINT ( 'NONE',  ( 0.9780106845699476636, -1.713796700228813918, 41.87354949518520186 ) ) ;
#43956=CARTESIAN_POINT ( 'NONE',  ( 0.6845945791218034371, 36.27071225238031360, 29.74629310383012992 ) ) ;
#43957=ORIENTED_EDGE ( 'NONE', *, *, #10884, .F. ) ;
#43961=ORIENTED_EDGE ( 'NONE', *, *, #1107, .F. ) ;
#43964=ORIENTED_EDGE ( 'NONE', *, *, #35203, .T. ) ;
#43967=ORIENTED_EDGE ( 'NONE', *, *, #29204, .F. ) ;
#43972=CARTESIAN_POINT ( 'NONE',  ( 1.000110580585050979, -34.17542785014344275, -24.25814531310138733 ) ) ;
#43976=ORIENTED_EDGE ( 'NONE', *, *, #6565, .F. ) ;
#43984=ADVANCED_FACE ( 'NONE', ( #47984 ), #30937, .F. ) ;
#43987=FACE_OUTER_BOUND ( 'NONE', #6292, .T. ) ;
#43993=CARTESIAN_POINT ( 'NONE',  ( 0.8560838555295158248, 45.47430759461114747, -11.50913475776619599 ) ) ;
#43995=CARTESIAN_POINT ( 'NONE',  ( 1.157644175074338699, 33.40146148540439697, -25.32478323931382391 ) ) ;
#43998=ORIENTED_EDGE ( 'NONE', *, *, #39512, .T. ) ;
#44001=CARTESIAN_POINT ( 'NONE',  ( 0.9784957157296370056, 14.84483425312139282, -39.19137600276013700 ) ) ;
#44006=CARTESIAN_POINT ( 'NONE',  ( 0.9769922540276050338, 10.14454102355774801, -40.66226558502955868 ) ) ;
#44011=ORIENTED_EDGE ( 'NONE', *, *, #32914, .F. ) ;
#44013=CARTESIAN_POINT ( 'NONE',  ( 4.956445790444035104, 38.51510088324747016, -27.09474218539284252 ) ) ;
#44017=B_SPLINE_CURVE_WITH_KNOTS ( 'NONE', 3,
 ( #51999, #17897, #18821, #8458 ),
 .UNSPECIFIED., .F., .F.,
 ( 4, 4 ),
 ( 0.000000000000000000, 0.005004948556313804434 ),
 .UNSPECIFIED. ) ;
#44018=CARTESIAN_POINT ( 'NONE',  ( 4.956445790444029775, 29.98832127573299289, -36.30755619981957949 ) ) ;
#44025=DIRECTION ( 'NONE',  ( 0.07906939808003035641, -0.9868658484044052770, -0.1408681210931520544 ) ) ;
#44029=VERTEX_POINT ( 'NONE', #16626 ) ;
#44031=DIRECTION ( 'NONE',  ( -0.07500201931887526263, 0.9863955245047982823, -0.1462824881350971995 ) ) ;
#44042=EDGE_CURVE ( 'NONE', #38817, #3786, #1886, .T. ) ;
#44059=ORIENTED_EDGE ( 'NONE', *, *, #27073, .T. ) ;
#44061=CARTESIAN_POINT ( 'NONE',  ( 5.895596859100789899, 0.6684898708301673098, 20.10177366565161705 ) ) ;
#44063=CARTESIAN_POINT ( 'NONE',  ( 3.238018933889920792, 3.371911215444676646, -12.96293589904738575 ) ) ;
#44067=CARTESIAN_POINT ( 'NONE',  ( 3.376099380956838925, -6.056959685666334359, 11.95916481190387870 ) ) ;
#44072=ORIENTED_EDGE ( 'NONE', *, *, #3308, .F. ) ;
#44078=CARTESIAN_POINT ( 'NONE',  ( 3.376099380956838925, 12.15487954915001900, 5.653962042472672422 ) ) ;
#44087=CARTESIAN_POINT ( 'NONE',  ( 0.9790724872846782167, 41.52931421318174188, 5.625946228348769118 ) ) ;
#44098=CARTESIAN_POINT ( 'NONE',  ( 5.896782393890504181, -9.660289833039353624, -17.64100017628503991 ) ) ;
#44101=EDGE_CURVE ( 'NONE', #42435, #16773, #25708, .T. ) ;
#44102=CARTESIAN_POINT ( 'NONE',  ( 0.9789889208857696090, 29.06536874308044816, -30.19170809793860144 ) ) ;
#44103=EDGE_CURVE ( 'NONE', #47280, #41171, #9324, .T. ) ;
#44118=CARTESIAN_POINT ( 'NONE',  ( 3.238018933889920792, -3.704930136113204320, -12.87171259212126628 ) ) ;
#44124=CARTESIAN_POINT ( 'NONE',  ( 0.5837800005270555870, -25.23393936835100959, -39.52826283301821775 ) ) ;
#44129=( BOUNDED_SURFACE ( )  B_SPLINE_SURFACE ( 3, 1, ( 
 ( #61835, #41861 ),
 ( #56841, #42780 ),
 ( #8610, #33075 ),
 ( #51215, #8298 ) ),
 .UNSPECIFIED., .F., .F., .F. ) 
 B_SPLINE_SURFACE_WITH_KNOTS ( ( 4, 4 ),
 ( 2, 2 ),
 ( 0.000000000000000000, 1.000000000000000000 ),
 ( 0.000000000000000000, 1.000000000000000000 ),
 .UNSPECIFIED. ) 
 GEOMETRIC_REPRESENTATION_ITEM ( )  RATIONAL_B_SPLINE_SURFACE ( (
 ( 1.000000000000000000, 1.000000000000000000),
 ( 0.9729067724841187204, 0.9999501103223794596),
 ( 0.9729067724841187204, 0.9999501103223794596),
 ( 1.000000000000000000, 1.000000000000000000) ) ) 
 REPRESENTATION_ITEM ( '' )  SURFACE ( )  );
#44130=CARTESIAN_POINT ( 'NONE',  ( 0.5837800005270556980, -34.78049932281108170, 31.45714744692725517 ) ) ;
#44133=CARTESIAN_POINT ( 'NONE',  ( 4.962356264823608143, -40.47344704301786322, -11.53844366967987334 ) ) ;
#44134=CARTESIAN_POINT ( 'NONE',  ( 2.282816707992306071, 43.74200569621534385, 17.12115370178745266 ) ) ;
#44135=CARTESIAN_POINT ( 'NONE',  ( 0.9785694773339252972, 40.36023435788206370, 11.28658000864342092 ) ) ;
#44138=CARTESIAN_POINT ( 'NONE',  ( 4.291220156522060236, -37.58001468972601344, 28.41005971879809167 ) ) ;
#44140=ORIENTED_EDGE ( 'NONE', *, *, #52398, .F. ) ;
#44148=( BOUNDED_SURFACE ( )  B_SPLINE_SURFACE ( 3, 1, ( 
 ( #35107, #44518 ),
 ( #53860, #45134 ),
 ( #24764, #10988 ),
 ( #39504, #35415 ) ),
 .UNSPECIFIED., .F., .F., .F. ) 
 B_SPLINE_SURFACE_WITH_KNOTS ( ( 4, 4 ),
 ( 2, 2 ),
 ( 0.000000000000000000, 1.000000000000000000 ),
 ( 0.000000000000000000, 1.000000000000000000 ),
 .UNSPECIFIED. ) 
 GEOMETRIC_REPRESENTATION_ITEM ( )  RATIONAL_B_SPLINE_SURFACE ( (
 ( 1.000000000000000000, 1.000000000000000000),
 ( 0.9952954269826590483, 0.8620686068821307169),
 ( 0.9952954269826590483, 0.8620686068821307169),
 ( 1.000000000000000000, 1.000000000000000000) ) ) 
 REPRESENTATION_ITEM ( '' )  SURFACE ( )  );
#44155=CARTESIAN_POINT ( 'NONE',  ( 5.894904586330512508, -7.229884331608547043, -18.76854242111528137 ) ) ;
#44157=VERTEX_POINT ( 'NONE', #16017 ) ;
#44162=CARTESIAN_POINT ( 'NONE',  ( 0.9787284016396606834, -27.20011616372034524, -31.88243528353739720 ) ) ;
#44163=CARTESIAN_POINT ( 'NONE',  ( 0.9791128995231600518, 38.58521266320476428, 16.35600189476109634 ) ) ;
#44165=CARTESIAN_POINT ( 'NONE',  ( 5.896278296736517710, -11.92612757635554033, -16.19550742171654534 ) ) ;
#44177=CARTESIAN_POINT ( 'NONE',  ( 5.895881250540457863, 17.95317081027908657, -9.067046898811309319 ) ) ;
#44184=ORIENTED_EDGE ( 'NONE', *, *, #50336, .F. ) ;
#44188=CARTESIAN_POINT ( 'NONE',  ( 4.291220156522060236, -32.02897670715545075, -34.54755633034253748 ) ) ;
#44194=CARTESIAN_POINT ( 'NONE',  ( 1.231276596079881047, 38.25526645152027072, 17.14092645516147684 ) ) ;
#44197=DIRECTION ( 'NONE',  ( 1.000000000000000000, 0.000000000000000000, 0.000000000000000000 ) ) ;
#44202=ORIENTED_EDGE ( 'NONE', *, *, #30280, .T. ) ;
#44208=ORIENTED_EDGE ( 'NONE', *, *, #58152, .T. ) ;
#44209=CARTESIAN_POINT ( 'NONE',  ( 0.9791128995231609400, 20.13607257681962892, -36.75426526849933850 ) ) ;
#44211=EDGE_CURVE ( 'NONE', #49641, #15442, #7886, .T. ) ;
#44221=CARTESIAN_POINT ( 'NONE',  ( 4.956445790444004018, -46.73954499432468879, 5.740468958468036398 ) ) ;
#44227=EDGE_LOOP ( 'NONE', ( #26169, #30452, #16741, #40430 ) ) ;
#44228=CARTESIAN_POINT ( 'NONE',  ( 0.9787284016396597952, -12.59522306292760163, -39.97119406427494681 ) ) ;
#44232=EDGE_LOOP ( 'NONE', ( #5288, #15056, #21905, #24919 ) ) ;
#44235=B_SPLINE_CURVE_WITH_KNOTS ( 'NONE', 3,
 ( #32696, #12430, #56778, #43032 ),
 .UNSPECIFIED., .F., .F.,
 ( 4, 4 ),
 ( 0.000000000000000000, 0.005004948556313791423 ),
 .UNSPECIFIED. ) ;
#44240=DIRECTION ( 'NONE',  ( -1.000000000000000000, -0.000000000000000000, -0.000000000000000000 ) ) ;
#44242=EDGE_CURVE ( 'NONE', #54938, #39717, #41375, .T. ) ;
#44244=CARTESIAN_POINT ( 'NONE',  ( 4.962356264823608143, 0.000000000000000000, 0.000000000000000000 ) ) ;
#44246=DIRECTION ( 'NONE',  ( 1.000000000000000000, -0.000000000000000000, -0.000000000000000000 ) ) ;
#44255=CARTESIAN_POINT ( 'NONE',  ( 0.9772918015221172539, -0.9856339699200908910, 41.89708082227232211 ) ) ;
#44257=VERTEX_POINT ( 'NONE', #17551 ) ;
#44269=VERTEX_POINT ( 'NONE', #49702 ) ;
#44271=B_SPLINE_CURVE_WITH_KNOTS ( 'NONE', 3,
 ( #43558, #28816, #284, #48536 ),
 .UNSPECIFIED., .F., .F.,
 ( 4, 4 ),
 ( 1.058181320345852328E-16, 0.005004948556313925864 ),
 .UNSPECIFIED. ) ;
#44275=LINE ( 'NONE', #15754, #8977 ) ;
#44278=CARTESIAN_POINT ( 'NONE',  ( 0.5804410086790514622, 23.01644811389207135, 40.86273324284501030 ) ) ;
#44281=CARTESIAN_POINT ( 'NONE',  ( 0.9790724872846775506, 36.03764935392171509, 21.39212563129806810 ) ) ;
#44287=EDGE_CURVE ( 'NONE', #29776, #50801, #5644, .T. ) ;
#44288=VECTOR ( 'NONE', #1622, 999.9999999999998863 ) ;
#44291=ORIENTED_EDGE ( 'NONE', *, *, #13610, .F. ) ;
#44295=CARTESIAN_POINT ( 'NONE',  ( 0.9762797500689124330, 41.46413394121043439, -6.086902470967093137 ) ) ;
#44299=CARTESIAN_POINT ( 'NONE',  ( 0.9784957157296381158, -39.66552991218980395, -13.52696543122457662 ) ) ;
#44301=CARTESIAN_POINT ( 'NONE',  ( 0.9783242366443558602, 15.31217352658830855, -39.01117573334813216 ) ) ;
#44316=CARTESIAN_POINT ( 'NONE',  ( 0.8560838555295158248, 17.70877843982841782, -43.43698884880027578 ) ) ;
#44339=ORIENTED_EDGE ( 'NONE', *, *, #12175, .T. ) ;
#44341=( BOUNDED_SURFACE ( )  B_SPLINE_SURFACE ( 3, 1, ( 
 ( #53496, #58199 ),
 ( #53797, #53199 ),
 ( #48212, #15323 ),
 ( #10614, #24394 ) ),
 .UNSPECIFIED., .F., .F., .F. ) 
 B_SPLINE_SURFACE_WITH_KNOTS ( ( 4, 4 ),
 ( 2, 2 ),
 ( 0.000000000000000000, 1.000000000000000000 ),
 ( 0.000000000000000000, 1.000000000000000000 ),
 .UNSPECIFIED. ) 
 GEOMETRIC_REPRESENTATION_ITEM ( )  RATIONAL_B_SPLINE_SURFACE ( (
 ( 1.000000000000000000, 1.000000000000000000),
 ( 0.7282232189291693025, 0.9929344683865674037),
 ( 0.7282232189291693025, 0.9929344683865674037),
 ( 1.000000000000000000, 1.000000000000000000) ) ) 
 REPRESENTATION_ITEM ( '' )  SURFACE ( )  );
#44344=CARTESIAN_POINT ( 'NONE',  ( 0.9754292589017198312, -41.18084051786591715, -7.775978468165505753 ) ) ;
#44349=VECTOR ( 'NONE', #48610, 999.9999999999998863 ) ;
#44351=ORIENTED_EDGE ( 'NONE', *, *, #42033, .F. ) ;
#44371=VERTEX_POINT ( 'NONE', #49387 ) ;
#44375=EDGE_LOOP ( 'NONE', ( #25934, #16346, #53837, #10357 ) ) ;
#44378=ADVANCED_FACE ( 'NONE', ( #30899 ), #20286, .F. ) ;
#44385=CARTESIAN_POINT ( 'NONE',  ( 5.895881250540457863, -7.232970327322216342, 18.76730726162859142 ) ) ;
#44386=B_SPLINE_CURVE_WITH_KNOTS ( 'NONE', 3,
 ( #30656, #2766, #36319, #16264 ),
 .UNSPECIFIED., .F., .F.,
 ( 4, 4 ),
 ( 0.000000000000000000, 0.005004948556313800964 ),
 .UNSPECIFIED. ) ;
#44402=( BOUNDED_SURFACE ( )  B_SPLINE_SURFACE ( 3, 1, ( 
 ( #47900, #19094 ),
 ( #37276, #61955 ),
 ( #27855, #241 ),
 ( #38508, #14697 ) ),
 .UNSPECIFIED., .F., .F., .F. ) 
 B_SPLINE_SURFACE_WITH_KNOTS ( ( 4, 4 ),
 ( 2, 2 ),
 ( 0.000000000000000000, 1.000000000000000000 ),
 ( 0.000000000000000000, 1.000000000000000000 ),
 .UNSPECIFIED. ) 
 GEOMETRIC_REPRESENTATION_ITEM ( )  RATIONAL_B_SPLINE_SURFACE ( (
 ( 1.000000000000000000, 1.000000000000000000),
 ( 0.7282232189291693025, 0.9929344683865674037),
 ( 0.7282232189291693025, 0.9929344683865674037),
 ( 1.000000000000000000, 1.000000000000000000) ) ) 
 REPRESENTATION_ITEM ( '' )  SURFACE ( )  );
#44404=CARTESIAN_POINT ( 'NONE',  ( 5.894904586330512508, 8.467339502218703018, 18.24372697164177026 ) ) ;
#44411=EDGE_CURVE ( 'NONE', #36353, #10343, #1891, .T. ) ;
#44414=CARTESIAN_POINT ( 'NONE',  ( 0.8560838555295158248, 31.94705745926175311, 34.34761059777461867 ) ) ;
#44420=CARTESIAN_POINT ( 'NONE',  ( 3.376099380956842921, -12.50537924370754261, 4.829479641029207571 ) ) ;
#44433=ORIENTED_EDGE ( 'NONE', *, *, #9749, .T. ) ;
#44434=CARTESIAN_POINT ( 'NONE',  ( 5.917102823773431552, -17.29995091781572114, -10.25677416602847281 ) ) ;
#44435=CARTESIAN_POINT ( 'NONE',  ( 4.956445790444002242, -32.34643101787113295, 34.22347806032784234 ) ) ;
#44441=CARTESIAN_POINT ( 'NONE',  ( 5.917102823773431552, 14.91028373222390080, 13.49715366572972286 ) ) ;
#44443=EDGE_CURVE ( 'NONE', #49823, #26123, #35932, .T. ) ;
#44448=CARTESIAN_POINT ( 'NONE',  ( 1.092182651088182688, -31.60377597355978097, -27.53111927719848140 ) ) ;
#44455=LINE ( 'NONE', #1482, #50636 ) ;
#44457=EDGE_LOOP ( 'NONE', ( #6859, #6302, #23222, #35574 ) ) ;
#44458=B_SPLINE_CURVE_WITH_KNOTS ( 'NONE', 3,
 ( #38771, #10867, #40011, #510 ),
 .UNSPECIFIED., .F., .F.,
 ( 4, 4 ),
 ( 0.000000000000000000, 0.005004948556313794893 ),
 .UNSPECIFIED. ) ;
#44464=CARTESIAN_POINT ( 'NONE',  ( 0.9772918015221170318, -27.37292454379962692, -31.73420642886996745 ) ) ;
#44465=CARTESIAN_POINT ( 'NONE',  ( 0.9775691876210972353, 38.43414426860777411, 16.70779049814292705 ) ) ;
#44466=ORIENTED_EDGE ( 'NONE', *, *, #20822, .F. ) ;
#44467=CARTESIAN_POINT ( 'NONE',  ( 4.958415959904818315, -42.01301765298939017, -17.26587100357933124 ) ) ;
#44469=CARTESIAN_POINT ( 'NONE',  ( 0.5830082357119558134, 36.63400490284909239, 29.27766588572876927 ) ) ;
#44478=CARTESIAN_POINT ( 'NONE',  ( 5.896782393890504181, 8.471952691971054605, 18.24149403045202078 ) ) ;
#44480=CARTESIAN_POINT ( 'NONE',  ( 3.661921753702006566, -37.68385958972724126, 28.15240398715106096 ) ) ;
#44491=FACE_OUTER_BOUND ( 'NONE', #31369, .T. ) ;
#44492=VERTEX_POINT ( 'NONE', #55307 ) ;
#44496=ORIENTED_EDGE ( 'NONE', *, *, #40789, .F. ) ;
#44508=( BOUNDED_SURFACE ( )  B_SPLINE_SURFACE ( 3, 1, ( 
 ( #58484, #38818 ),
 ( #24075, #43203 ),
 ( #43514, #233 ),
 ( #19384, #38502 ) ),
 .UNSPECIFIED., .F., .F., .F. ) 
 B_SPLINE_SURFACE_WITH_KNOTS ( ( 4, 4 ),
 ( 2, 2 ),
 ( 0.000000000000000000, 1.000000000000000000 ),
 ( 0.000000000000000000, 1.000000000000000000 ),
 .UNSPECIFIED. ) 
 GEOMETRIC_REPRESENTATION_ITEM ( )  RATIONAL_B_SPLINE_SURFACE ( (
 ( 1.000000000000000000, 1.000000000000000000),
 ( 0.7282232189291694135, 0.9929344683865672927),
 ( 0.7282232189291694135, 0.9929344683865672927),
 ( 1.000000000000000000, 1.000000000000000000) ) ) 
 REPRESENTATION_ITEM ( '' )  SURFACE ( )  );
#44514=B_SPLINE_CURVE_WITH_KNOTS ( 'NONE', 3,
 ( #58832, #31901, #27192, #55992, #46625, #50373 ),
 .UNSPECIFIED., .F., .F.,
 ( 4, 2, 4 ),
 ( 0.000000000000000000, 0.0002291459268755701806, 0.0004582918537511403612 ),
 .UNSPECIFIED. ) ;
#44518=CARTESIAN_POINT ( 'NONE',  ( 0.8554163680231720024, -39.19027442586699550, -25.79395013442211848 ) ) ;
#44521=VECTOR ( 'NONE', #54283, 999.9999999999998863 ) ;
#44528=CIRCLE ( 'NONE', #27450, 42.08604991992415023 ) ;
#44544=CARTESIAN_POINT ( 'NONE',  ( 0.9791128995231621612, 41.53406868334494817, -5.590936670482719251 ) ) ;
#44546=CARTESIAN_POINT ( 'NONE',  ( 0.8554163680231738898, -42.27859581856526461, 20.34025095032544073 ) ) ;
#44555=ADVANCED_FACE ( 'NONE', ( #60015 ), #3906, .T. ) ;
#44558=EDGE_LOOP ( 'NONE', ( #29614, #31119, #55115, #56347 ) ) ;
#44561=CARTESIAN_POINT ( 'NONE',  ( 5.894904586330512508, -20.11291651039286066, 0.001227847351200775502 ) ) ;
#44562=ORIENTED_EDGE ( 'NONE', *, *, #16524, .T. ) ;
#44567=ORIENTED_EDGE ( 'NONE', *, *, #7905, .T. ) ;
#44570=CARTESIAN_POINT ( 'NONE',  ( 3.376099380956842921, 6.842217874692535062, 11.52789825541954727 ) ) ;
#44581=EDGE_CURVE ( 'NONE', #5328, #42400, #51149, .T. ) ;
#44585=CARTESIAN_POINT ( 'NONE',  ( 5.901463166500146684, -4.648441909663684868, 19.56808263865213604 ) ) ;
#44588=EDGE_CURVE ( 'NONE', #25309, #1809, #28747, .T. ) ;
#44599=CIRCLE ( 'NONE', #25570, 42.08604991992415023 ) ;
#44601=EDGE_LOOP ( 'NONE', ( #11341, #29748, #46353, #49116 ) ) ;
#44608=CARTESIAN_POINT ( 'NONE',  ( 3.238018933889920792, -12.74072440564274977, -4.132969149063681513 ) ) ;
#44615=CARTESIAN_POINT ( 'NONE',  ( 0.5782707292762442330, -34.29472224813873282, -31.99388034656996282 ) ) ;
#44624=EDGE_LOOP ( 'NONE', ( #58123, #36051, #55229, #20183 ) ) ;
#44630=VERTEX_POINT ( 'NONE', #37802 ) ;
#44638=DIRECTION ( 'NONE',  ( -1.000000000000000000, -0.000000000000000000, -0.000000000000000000 ) ) ;
#44646=CARTESIAN_POINT ( 'NONE',  ( 0.8560838555295158248, -29.58154842764465542, -36.40473632241614155 ) ) ;
#44647=LINE ( 'NONE', #59018, #55961 ) ;
#44652=CARTESIAN_POINT ( 'NONE',  ( 0.8560838555295158248, 27.08392101972004440, 38.29926965725714894 ) ) ;
#44657=FACE_OUTER_BOUND ( 'NONE', #43422, .T. ) ;
#44659=EDGE_CURVE ( 'NONE', #45260, #4680, #27196, .T. ) ;
#44673=ORIENTED_EDGE ( 'NONE', *, *, #45925, .T. ) ;
#44674=CARTESIAN_POINT ( 'NONE',  ( 5.895596859100789899, 0.6684898708301673098, 20.10177366565161705 ) ) ;
#44675=CARTESIAN_POINT ( 'NONE',  ( 0.8554163680231708922, 27.08908797599144336, 38.30648490452777821 ) ) ;
#44683=CARTESIAN_POINT ( 'NONE',  ( 4.958415959904816539, 28.93810772186895619, -35.01128211448620675 ) ) ;
#44685=CARTESIAN_POINT ( 'NONE',  ( 0.9780106845699483298, 41.49170912070719908, 5.896551593775888556 ) ) ;
#44696=CARTESIAN_POINT ( 'NONE',  ( 0.8560838555295223751, -14.76796170096679894, -44.52280473286144513 ) ) ;
#44698=CARTESIAN_POINT ( 'NONE',  ( 3.238018933889920792, -10.11627964985454575, -8.778859744499381890 ) ) ;
#44702=EDGE_CURVE ( 'NONE', #36162, #22620, #50378, .T. ) ;
#44704=EDGE_LOOP ( 'NONE', ( #23377, #39369, #59704, #47104 ) ) ;
#44709=ADVANCED_FACE ( 'NONE', ( #16124 ), #20917, .T. ) ;
#44714=ORIENTED_EDGE ( 'NONE', *, *, #60835, .F. ) ;
#44717=EDGE_CURVE ( 'NONE', #56156, #22549, #54299, .T. ) ;
#44722=DIRECTION ( 'NONE',  ( 0.07500201931887537365, 0.3083113411842569040, -0.9483242135447431664 ) ) ;
#44726=CARTESIAN_POINT ( 'NONE',  ( 0.5806925824938502512, 32.20670061096268455, -34.08739940358283604 ) ) ;
#44746=ORIENTED_EDGE ( 'NONE', *, *, #56835, .T. ) ;
#44753=CARTESIAN_POINT ( 'NONE',  ( 0.5848930533535030563, 16.68483824254223791, 43.82795061610521969 ) ) ;
#44762=EDGE_CURVE ( 'NONE', #50474, #61383, #36950, .T. ) ;
#44767=CARTESIAN_POINT ( 'NONE',  ( 0.9754292580325143458, -40.94879473734659570, -8.917604861321258625 ) ) ;
#44772=CARTESIAN_POINT ( 'NONE',  ( 0.5817217712918331118, 45.10732654355952320, 12.82825187237387610 ) ) ;
#44773=B_SPLINE_CURVE_WITH_KNOTS ( 'NONE', 3,
 ( #29920, #1391, #57790, #5476, #20531, #58709, #20838, #14924, #39978, #34030, #53102, #31463, #40899, #55560, #21448, #21140 ),
 .UNSPECIFIED., .F., .F.,
 ( 4, 3, 3, 3, 3, 4 ),
 ( 1.551621725782133898E-17, 0.0002732102107931891864, 0.0004098135523333867381, 0.0005464168938825064064, 0.0008195847345945496236, 0.001092771384553108734 ),
 .UNSPECIFIED. ) ;
#44775=CARTESIAN_POINT ( 'NONE',  ( 0.8560838555295223751, 39.88643293834682879, -24.68694597426934223 ) ) ;
#44784=CIRCLE ( 'NONE', #46790, 47.09074272231896430 ) ;
#44796=EDGE_CURVE ( 'NONE', #22554, #4396, #48176, .T. ) ;
#44800=CARTESIAN_POINT ( 'NONE',  ( 0.5848930533535030563, 32.47085631013434437, -33.83661586025067436 ) ) ;
#44801=CARTESIAN_POINT ( 'NONE',  ( 1.231276596079881935, 35.62927148397020005, 22.08691432816306133 ) ) ;
#44809=CARTESIAN_POINT ( 'NONE',  ( 4.956445790443989807, 42.27038699792205279, 20.75457619864928205 ) ) ;
#44810=EDGE_CURVE ( 'NONE', #59514, #59308, #16002, .T. ) ;
#44813=CARTESIAN_POINT ( 'NONE',  ( 0.9754292580325127915, -26.60990431517644339, -32.37654180484936006 ) ) ;
#44817=CARTESIAN_POINT ( 'NONE',  ( 0.8560838555295158248, -0.6537497281619772949, -46.90357604036880446 ) ) ;
#44821=CARTESIAN_POINT ( 'NONE',  ( 0.9762797500689124330, -34.83496347773955648, 23.29914386174426255 ) ) ;
#44826=B_SPLINE_CURVE_WITH_KNOTS ( 'NONE', 3,
 ( #45397, #51291, #61001, #18108 ),
 .UNSPECIFIED., .F., .F.,
 ( 4, 4 ),
 ( 4.336808689942017736E-19, 0.004041751736740985604 ),
 .UNSPECIFIED. ) ;
#44830=CARTESIAN_POINT ( 'NONE',  ( 4.956445790444005794, -40.23882117934059011, -24.46171131046819625 ) ) ;
#44836=DIRECTION ( 'NONE',  ( -1.000000000000000000, -0.000000000000000000, -0.000000000000000000 ) ) ;
#44840=CARTESIAN_POINT ( 'NONE',  ( 0.5835871038041848813, -44.34580925781567373, 15.25397175069270261 ) ) ;
#44853=CARTESIAN_POINT ( 'NONE',  ( 4.962356264823608143, 26.83784316460287300, 32.41860225448540689 ) ) ;
#44858=CARTESIAN_POINT ( 'NONE',  ( 2.618530812446111078, 41.14519205294217130, -22.73323470438608851 ) ) ;
#44861=LINE ( 'NONE', #26040, #16695 ) ;
#44862=ADVANCED_FACE ( 'NONE', ( #19437 ), #5947, .T. ) ;
#44863=EDGE_CURVE ( 'NONE', #26211, #24826, #30969, .T. ) ;
#44871=DIRECTION ( 'NONE',  ( 0.000000000000000000, 0.000000000000000000, 1.000000000000000000 ) ) ;
#44873=EDGE_CURVE ( 'NONE', #43281, #37898, #21199, .T. ) ;
#44877=B_SPLINE_CURVE_WITH_KNOTS ( 'NONE', 3,
 ( #15246, #25548, #44683, #53426 ),
 .UNSPECIFIED., .F., .F.,
 ( 4, 4 ),
 ( 0.000000000000000000, 0.005004948556313815709 ),
 .UNSPECIFIED. ) ;
#44878=DIRECTION ( 'NONE',  ( -1.000000000000000000, -0.000000000000000000, -0.000000000000000000 ) ) ;
#44879=ORIENTED_EDGE ( 'NONE', *, *, #28016, .F. ) ;
#44888=ORIENTED_EDGE ( 'NONE', *, *, #4139, .T. ) ;
#44889=CARTESIAN_POINT ( 'NONE',  ( 4.962356264823602814, -15.53171314616136200, -39.11523340858015274 ) ) ;
#44896=B_SPLINE_CURVE_WITH_KNOTS ( 'NONE', 3,
 ( #1231, #30057, #6220, #54778 ),
 .UNSPECIFIED., .F., .F.,
 ( 4, 4 ),
 ( 0.000000000000000000, 0.005004948556313797495 ),
 .UNSPECIFIED. ) ;
#44913=FACE_OUTER_BOUND ( 'NONE', #56705, .T. ) ;
#44919=CARTESIAN_POINT ( 'NONE',  ( 0.8560838555295223751, -20.57050347530454104, -42.15717282805163535 ) ) ;
#44920=CARTESIAN_POINT ( 'NONE',  ( 4.956445790444026223, 7.299064093731650438, -46.52162629890785439 ) ) ;
#44924=CARTESIAN_POINT ( 'NONE',  ( 5.895596859100789899, 12.98270243688433645, -15.36156309259591701 ) ) ;
#44928=CARTESIAN_POINT ( 'NONE',  ( 1.000110580585051867, 15.67476820051338571, -38.86797042079857079 ) ) ;
#44936=B_SPLINE_CURVE_WITH_KNOTS ( 'NONE', 3,
 ( #52513, #4575, #23715, #1122, #53725, #35599 ),
 .UNSPECIFIED., .F., .F.,
 ( 4, 2, 4 ),
 ( 7.007167689862070887E-18, 0.0002448709889506569398, 0.0004897419779013069407 ),
 .UNSPECIFIED. ) ;
#44940=VERTEX_POINT ( 'NONE', #52619 ) ;
#44943=CARTESIAN_POINT ( 'NONE',  ( 0.5804410086790514622, -8.338934868871049844, 46.15172821366630984 ) ) ;
#44946=VERTEX_POINT ( 'NONE', #1531 ) ;
#44948=CARTESIAN_POINT ( 'NONE',  ( 0.9754292589017239390, -23.03905100505517822, -35.00756483507158379 ) ) ;
#44953=VERTEX_POINT ( 'NONE', #5910 ) ;
#44957=CARTESIAN_POINT ( 'NONE',  ( 1.231276596079887931, 36.49189576017872128, 20.63051901543724043 ) ) ;
#44958=CARTESIAN_POINT ( 'NONE',  ( 4.962356264823593044, 27.50309822711036034, 31.85616401534038644 ) ) ;
#44960=EDGE_CURVE ( 'NONE', #34245, #19440, #48857, .T. ) ;
#44961=CARTESIAN_POINT ( 'NONE',  ( 0.9787464366903565471, -41.03323141156885612, -8.521027685385261563 ) ) ;
#44962=CARTESIAN_POINT ( 'NONE',  ( 0.6064782688330873084, -29.73181431155118659, -36.26780478829964238 ) ) ;
#44966=CARTESIAN_POINT ( 'NONE',  ( 0.5797568599927143129, 27.30868314757112003, 38.12428534958486637 ) ) ;
#44972=CARTESIAN_POINT ( 'NONE',  ( 0.8554163680231708922, -20.57434774096721952, 42.16517150618003029 ) ) ;
#44975=ORIENTED_EDGE ( 'NONE', *, *, #6004, .T. ) ;
#44980=EDGE_CURVE ( 'NONE', #50421, #59514, #32417, .T. ) ;
#44981=VERTEX_POINT ( 'NONE', #35713 ) ;
#44985=CARTESIAN_POINT ( 'NONE',  ( 4.958415959904816539, 13.93965400761555706, 43.23066041561943962 ) ) ;
#44993=CARTESIAN_POINT ( 'NONE',  ( 1.231276596079881047, -23.26513148155264332, 34.87134107206281186 ) ) ;
#44999=DIRECTION ( 'NONE',  ( 0.07500201931887538753, -0.3457612750068233542, -0.9353201792989109808 ) ) ;
#45016=CARTESIAN_POINT ( 'NONE',  ( 3.376099380956842921, 13.39763462305342401, -0.4601848967830201032 ) ) ;
#45018=ORIENTED_EDGE ( 'NONE', *, *, #42060, .T. ) ;
#45020=VECTOR ( 'NONE', #35681, 999.9999999999998863 ) ;
#45026=CARTESIAN_POINT ( 'NONE',  ( 3.376099380956842921, -9.001307264897979721, -9.934024922203580132 ) ) ;
#45040=ORIENTED_EDGE ( 'NONE', *, *, #39060, .F. ) ;
#45042=CARTESIAN_POINT ( 'NONE',  ( 3.376099380956842921, -13.39845304004336413, -0.4357060543759550542 ) ) ;
#45043=ORIENTED_EDGE ( 'NONE', *, *, #1472, .F. ) ;
#45056=DIRECTION ( 'NONE',  ( -0.07500201931887527651, 0.9580968512853041963, -0.2764509371575298857 ) ) ;
#45057=AXIS2_PLACEMENT_3D ( 'NONE', #21045, #41110, #30738 ) ;
#45062=CARTESIAN_POINT ( 'NONE',  ( 0.9787464366903551038, 24.71660722148015310, 33.84410318429993936 ) ) ;
#45077=LINE ( 'NONE', #21546, #33962 ) ;
#45078=CARTESIAN_POINT ( 'NONE',  ( 0.9790724872846759963, 38.56739429505658734, 16.39790557574631436 ) ) ;
#45080=EDGE_CURVE ( 'NONE', #35096, #42568, #51881, .T. ) ;
#45082=CARTESIAN_POINT ( 'NONE',  ( 5.901463166500145796, 5.945065151443557738, 19.21390305705033441 ) ) ;
#45083=VERTEX_POINT ( 'NONE', #59168 ) ;
#45085=FACE_OUTER_BOUND ( 'NONE', #30128, .T. ) ;
#45086=LINE ( 'NONE', #35060, #45020 ) ;
#45092=CARTESIAN_POINT ( 'NONE',  ( 5.917102823773431552, 8.473612197389305933, 18.23972626932754082 ) ) ;
#45093=EDGE_CURVE ( 'NONE', #47712, #8823, #20671, .T. ) ;
#45094=CARTESIAN_POINT ( 'NONE',  ( 4.956445790443988031, 0.000000000000000000, 0.000000000000000000 ) ) ;
#45097=CARTESIAN_POINT ( 'NONE',  ( 0.9762797500689124330, 9.222352665238359393, 40.88120590813919364 ) ) ;
#45098=DIRECTION ( 'NONE',  ( -1.000000000000000000, -0.000000000000000000, -0.000000000000000000 ) ) ;
#45117=CARTESIAN_POINT ( 'NONE',  ( 4.956445790444004018, -40.78973928653763181, -23.53157918788973291 ) ) ;
#45119=CARTESIAN_POINT ( 'NONE',  ( 1.157644175074336035, -26.42675002938718976, -32.53658184818230836 ) ) ;
#45128=CARTESIAN_POINT ( 'NONE',  ( 0.9790320750461898314, 20.21589195895753832, -36.71041875062102378 ) ) ;
#45129=B_SPLINE_CURVE_WITH_KNOTS ( 'NONE', 3,
 ( #8744, #28780, #19098, #28163 ),
 .UNSPECIFIED., .F., .F.,
 ( 4, 4 ),
 ( 0.000000000000000000, 0.005004948556313813107 ),
 .UNSPECIFIED. ) ;
#45133=DIRECTION ( 'NONE',  ( 0.000000000000000000, 0.000000000000000000, 1.000000000000000000 ) ) ;
#45134=CARTESIAN_POINT ( 'NONE',  ( 0.6845945791218023269, -39.15688516782633855, -25.82914757919060378 ) ) ;
#45137=CARTESIAN_POINT ( 'NONE',  ( 4.962356264823603702, -10.17958088187380739, -40.83640203215431086 ) ) ;
#45140=DIRECTION ( 'NONE',  ( -0.07906939808003035641, -0.6497517485244272972, -0.7560229464617532757 ) ) ;
#45143=CARTESIAN_POINT ( 'NONE',  ( 2.528100132419517365, -21.55886359172174949, 36.02039948786813284 ) ) ;
#45144=EDGE_CURVE ( 'NONE', #49823, #25214, #45928, .T. ) ;
#45151=CARTESIAN_POINT ( 'NONE',  ( 1.231276596079887264, 35.62927148397050559, -22.08691432816256395 ) ) ;
#45152=CARTESIAN_POINT ( 'NONE',  ( 4.962356264823608143, 0.000000000000000000, 0.000000000000000000 ) ) ;
#45157=ORIENTED_EDGE ( 'NONE', *, *, #14457, .F. ) ;
#45176=B_SPLINE_CURVE_WITH_KNOTS ( 'NONE', 3,
 ( #34268, #25155, #53955, #44001, #53343, #35197, #11378, #10454, #29546, #5712, #24861, #58337, #53637, #30462, #44301, #1331, #39596, #34890, #30159 ),
 .UNSPECIFIED., .F., .F.,
 ( 4, 3, 3, 3, 3, 3, 4 ),
 ( 8.674294979774128197E-18, 0.0002732106629380666061, 0.0004098138914053808530, 0.0005464171197651462560, 0.0006830203481512559828, 0.0008196235766963627656, 0.001011968216111142679 ),
 .UNSPECIFIED. ) ;
#45179=ORIENTED_EDGE ( 'NONE', *, *, #41614, .F. ) ;
#45184=VERTEX_POINT ( 'NONE', #52236 ) ;
#45188=CARTESIAN_POINT ( 'NONE',  ( 0.5806925824938502512, -14.41498975133575300, -44.62544602368080859 ) ) ;
#45205=CARTESIAN_POINT ( 'NONE',  ( 0.5804410086790514622, 46.40460073163232124, -6.792119168064288282 ) ) ;
#45210=CARTESIAN_POINT ( 'NONE',  ( 0.9762797500689124330, 35.79768877047958853, 21.79105926469807741 ) ) ;
#45220=CARTESIAN_POINT ( 'NONE',  ( 5.917102823773431552, -2.004558746498583677, 20.01178308606152356 ) ) ;
#45231=CARTESIAN_POINT ( 'NONE',  ( 4.958415959904820092, 42.74072562871883463, 15.37642112304467190 ) ) ;
#45232=CONICAL_SURFACE ( 'NONE', #58194, 42.08604991992415023, 1.569615340895231137 ) ;
#45240=CARTESIAN_POINT ( 'NONE',  ( 4.958415959904818315, 37.15973263041131958, -26.12198737958080130 ) ) ;
#45247=CARTESIAN_POINT ( 'NONE',  ( 3.376099380956838925, 6.035099650301207319, 11.97021118623232105 ) ) ;
#45256=ORIENTED_EDGE ( 'NONE', *, *, #54707, .F. ) ;
#45258=FACE_OUTER_BOUND ( 'NONE', #55159, .T. ) ;
#45260=VERTEX_POINT ( 'NONE', #39409 ) ;
#45263=CARTESIAN_POINT ( 'NONE',  ( 1.091591847532193960, -37.75421764082017262, 18.20379194798224276 ) ) ;
#45277=LINE ( 'NONE', #41500, #4606 ) ;
#45284=CARTESIAN_POINT ( 'NONE',  ( 0.5848930533535030563, -34.65838163711151765, 31.59224057713996103 ) ) ;
#45304=CARTESIAN_POINT ( 'NONE',  ( 0.9769922540276043676, 14.64910982633380421, 39.26493520155273131 ) ) ;
#45311=CARTESIAN_POINT ( 'NONE',  ( 0.5830082357119558134, -34.59666430896329103, -31.65916697626838783 ) ) ;
#45312=CARTESIAN_POINT ( 'NONE',  ( 5.896782393890504181, -11.92541098582135994, 16.19600752337635541 ) ) ;
#45322=LINE ( 'NONE', #45016, #28350 ) ;
#45323=VERTEX_POINT ( 'NONE', #35015 ) ;
#45328=B_SPLINE_CURVE_WITH_KNOTS ( 'NONE', 3,
 ( #13695, #32484, #19858, #27463 ),
 .UNSPECIFIED., .F., .F.,
 ( 4, 4 ),
 ( 0.000000000000000000, 0.004447772540403782497 ),
 .UNSPECIFIED. ) ;
#45330=DIRECTION ( 'NONE',  ( -0.07500201931887529039, -0.6540624036680577902, -0.7527131387228827020 ) ) ;
#45332=VERTEX_POINT ( 'NONE', #50318 ) ;
#45343=CARTESIAN_POINT ( 'NONE',  ( 3.661933894777872567, -28.90718021623337819, -37.10803278129762361 ) ) ;
#45345=ORIENTED_EDGE ( 'NONE', *, *, #16051, .T. ) ;
#45349=CARTESIAN_POINT ( 'NONE',  ( 5.910764540655177868, -17.29668172820417027, -10.26284754161198087 ) ) ;
#45357=DIRECTION ( 'NONE',  ( 0.07906939808003037029, -0.5978040102392425670, 0.7977332860230550438 ) ) ;
#45359=EDGE_LOOP ( 'NONE', ( #47883, #44714, #45043, #7180 ) ) ;
#45366=ORIENTED_EDGE ( 'NONE', *, *, #60511, .T. ) ;
#45367=CARTESIAN_POINT ( 'NONE',  ( 2.618530812446115519, -33.90288491188699993, 32.56257336037101169 ) ) ;
#45370=CARTESIAN_POINT ( 'NONE',  ( 5.895596859100789899, -7.225383168024946734, -18.77024297359278293 ) ) ;
#45378=CARTESIAN_POINT ( 'NONE',  ( 0.5848930533535030563, -30.13830825645530354, 35.92986860296647933 ) ) ;
#45380=ORIENTED_EDGE ( 'NONE', *, *, #21703, .F. ) ;
#45385=CARTESIAN_POINT ( 'NONE',  ( 0.5832655196449136881, 36.66244123469611083, 29.24210296277925281 ) ) ;
#45386=CARTESIAN_POINT ( 'NONE',  ( 5.910764540655178756, 16.57257352145957086, -11.39522028505724904 ) ) ;
#45387=EDGE_CURVE ( 'NONE', #14444, #30313, #30907, .T. ) ;
#45393=CARTESIAN_POINT ( 'NONE',  ( 1.231276596079881935, -34.07446381689681658, -24.41736444846283405 ) ) ;
#45397=CARTESIAN_POINT ( 'NONE',  ( 1.231276596079881935, 35.62927148397020005, 22.08691432816306133 ) ) ;
#45401=CARTESIAN_POINT ( 'NONE',  ( 1.000433927950264756, 38.83647759869904803, 15.75267232499282244 ) ) ;
#45407=CARTESIAN_POINT ( 'NONE',  ( 5.895596859100789899, -19.93295055289972950, -2.684337063064522244 ) ) ;
#45412=CIRCLE ( 'NONE', #53377, 47.09074272231896430 ) ;
#45420=CARTESIAN_POINT ( 'NONE',  ( 5.838029081930955932, -10.93035914537670905, -45.95206531926502436 ) ) ;
#45421=ORIENTED_EDGE ( 'NONE', *, *, #14435, .F. ) ;
#45424=CARTESIAN_POINT ( 'NONE',  ( 0.9762797500689124330, 35.79768877047958853, 21.79105926469807741 ) ) ;
#45426=ORIENTED_EDGE ( 'NONE', *, *, #53932, .F. ) ;
#45428=CARTESIAN_POINT ( 'NONE',  ( 5.910764540655178756, -9.679148173056805859, -17.62995544841716367 ) ) ;
#45432=VERTEX_POINT ( 'NONE', #44726 ) ;
#45438=CARTESIAN_POINT ( 'NONE',  ( 2.618530812446115519, -43.92476656374616084, 16.74340680741547160 ) ) ;
#45440=ORIENTED_EDGE ( 'NONE', *, *, #2554, .T. ) ;
#45445=ORIENTED_EDGE ( 'NONE', *, *, #15908, .T. ) ;
#45450=CARTESIAN_POINT ( 'NONE',  ( 4.956445790443991584, 29.98832127573247774, 36.30755619981999871 ) ) ;
#45453=CARTESIAN_POINT ( 'NONE',  ( 1.231276596079887931, 8.892602616354244205, -40.96581977363174332 ) ) ;
#45456=ORIENTED_EDGE ( 'NONE', *, *, #52188, .T. ) ;
#45462=VECTOR ( 'NONE', #41827, 999.9999999999998863 ) ;
#45469=CARTESIAN_POINT ( 'NONE',  ( 0.9762797500689124330, 14.58899758184696971, -39.28722355604386252 ) ) ;
#45470=CARTESIAN_POINT ( 'NONE',  ( 0.8560838555295158248, -38.14845555156047396, -27.29593693413630362 ) ) ;
#45474=CARTESIAN_POINT ( 'NONE',  ( 2.618530812446115519, 45.68928551531443105, 11.05513357215908599 ) ) ;
#45493=ADVANCED_FACE ( 'NONE', ( #31848 ), #46150, .F. ) ;
#45501=CARTESIAN_POINT ( 'NONE',  ( 4.956445790444004018, -47.08764048036452721, 0.5405220916596411573 ) ) ;
#45502=( BOUNDED_SURFACE ( )  B_SPLINE_SURFACE ( 3, 1, ( 
 ( #25529, #11761 ),
 ( #50264, #39661 ),
 ( #21145, #34953 ),
 ( #15531, #45585 ) ),
 .UNSPECIFIED., .F., .F., .F. ) 
 B_SPLINE_SURFACE_WITH_KNOTS ( ( 4, 4 ),
 ( 2, 2 ),
 ( 0.000000000000000000, 1.000000000000000000 ),
 ( 0.000000000000000000, 1.000000000000000000 ),
 .UNSPECIFIED. ) 
 GEOMETRIC_REPRESENTATION_ITEM ( )  RATIONAL_B_SPLINE_SURFACE ( (
 ( 1.000000000000000000, 1.000000000000000000),
 ( 0.9952954269826590483, 0.8620686068821307169),
 ( 0.9952954269826590483, 0.8620686068821307169),
 ( 1.000000000000000000, 1.000000000000000000) ) ) 
 REPRESENTATION_ITEM ( '' )  SURFACE ( )  );
#45506=ORIENTED_EDGE ( 'NONE', *, *, #35747, .T. ) ;
#45510=CARTESIAN_POINT ( 'NONE',  ( 0.5817217712918331118, -30.62363249491660966, 35.51658889624201265 ) ) ;
#45512=ORIENTED_EDGE ( 'NONE', *, *, #40163, .F. ) ;
#45523=CARTESIAN_POINT ( 'NONE',  ( 0.5782707292762423457, -0.8434722838406086831, 46.89376193284147121 ) ) ;
#45533=CARTESIAN_POINT ( 'NONE',  ( 0.5806925824938494740, 46.54710689580857519, 5.708695295225819422 ) ) ;
#45536=CARTESIAN_POINT ( 'NONE',  ( 0.9762797500689124330, -6.471194619075845367, 41.40589843715202534 ) ) ;
#45542=CARTESIAN_POINT ( 'NONE',  ( 0.9762797500689124330, -22.12212327108638377, 35.59405072711678741 ) ) ;
#45547=CARTESIAN_POINT ( 'NONE',  ( 5.895596859100789899, 17.95274561709302930, 9.067916410093047830 ) ) ;
#45550=CARTESIAN_POINT ( 'NONE',  ( 1.157643937452369265, -11.62785187674113097, 40.27152015168191213 ) ) ;
#45570=EDGE_LOOP ( 'NONE', ( #15058, #21535, #44746, #15227 ) ) ;
#45574=AXIS2_PLACEMENT_3D ( 'NONE', #49309, #44638, #30499 ) ;
#45575=ORIENTED_EDGE ( 'NONE', *, *, #25500, .F. ) ;
#45578=CARTESIAN_POINT ( 'NONE',  ( 2.282816707992318506, 15.64995451397235904, -44.28968153101309468 ) ) ;
#45581=ORIENTED_EDGE ( 'NONE', *, *, #17535, .F. ) ;
#45583=CARTESIAN_POINT ( 'NONE',  ( 5.895596859100789899, 5.962379729972213660, -19.20880556328539512 ) ) ;
#45584=CARTESIAN_POINT ( 'NONE',  ( 4.956445790443988031, 0.000000000000000000, 0.000000000000000000 ) ) ;
#45585=CARTESIAN_POINT ( 'NONE',  ( 0.5804410086790514622, -42.10186154173658224, -20.66284362269237462 ) ) ;
#45593=CARTESIAN_POINT ( 'NONE',  ( 4.962356264823608143, 7.429277797797782412, -41.42513040734446861 ) ) ;
#45595=CARTESIAN_POINT ( 'NONE',  ( 5.895596859100789899, -13.97974974393952508, -14.46010996878344201 ) ) ;
#45598=CARTESIAN_POINT ( 'NONE',  ( 0.8554163680231720024, 16.00619315955243849, -44.10223637924629259 ) ) ;
#45606=CARTESIAN_POINT ( 'NONE',  ( 0.7764139734771250412, -46.73184009015370322, -4.021889194790254862 ) ) ;
#45612=PRODUCT_CONTEXT ( 'NONE', #57535, 'mechanical' ) ;
#45614=CARTESIAN_POINT ( 'NONE',  ( 5.838029081930955932, 7.876159563729716595, -46.57285871276948797 ) ) ;
#45618=EDGE_LOOP ( 'NONE', ( #35671, #54065, #862, #55344 ) ) ;
#45621=CARTESIAN_POINT ( 'NONE',  ( 0.5837800005270551429, -7.800150850987738416, 46.24276057226276748 ) ) ;
#45624=VECTOR ( 'NONE', #55362, 999.9999999999998863 ) ;
#45627=CARTESIAN_POINT ( 'NONE',  ( 5.901463166500146684, 14.90686821212722357, -13.50196839156822648 ) ) ;
#45642=ORIENTED_EDGE ( 'NONE', *, *, #28496, .T. ) ;
#45658=ORIENTED_EDGE ( 'NONE', *, *, #44762, .F. ) ;
#45662=CIRCLE ( 'NONE', #31655, 42.08604991992415023 ) ;
#45665=CARTESIAN_POINT ( 'NONE',  ( 0.9772918015221165877, 25.19218625365867581, 33.49164981770307747 ) ) ;
#45670=AXIS2_PLACEMENT_3D ( 'NONE', #9206, #37428, #27387 ) ;
#45671=CARTESIAN_POINT ( 'NONE',  ( 0.5817216825391123836, -41.64824101621195496, 21.55594981583921310 ) ) ;
#45677=CARTESIAN_POINT ( 'NONE',  ( 0.9785694773339250752, 38.66954382086642994, -16.15554970902462983 ) ) ;
#45687=B_SPLINE_CURVE_WITH_KNOTS ( 'NONE', 3,
 ( #319, #52644, #34187, #42979, #53264, #9741 ),
 .UNSPECIFIED., .F., .F.,
 ( 4, 2, 4 ),
 ( 9.660965348001701796E-18, 0.0002448709889506563977, 0.0004897419779013031460 ),
 .UNSPECIFIED. ) ;
#45693=CARTESIAN_POINT ( 'NONE',  ( 4.958415959904820092, 44.61026793747956276, -8.551488079212832716 ) ) ;
#45694=CARTESIAN_POINT ( 'NONE',  ( 2.282803330402974673, 37.66448333203771170, -28.06926437916816397 ) ) ;
#45696=CARTESIAN_POINT ( 'NONE',  ( 0.5806925824938499181, 10.33919002968644385, 45.74192291403583965 ) ) ;
#45707=B_SPLINE_CURVE_WITH_KNOTS ( 'NONE', 3,
 ( #58430, #48746, #25250, #10539 ),
 .UNSPECIFIED., .F., .F.,
 ( 4, 4 ),
 ( 0.000000000000000000, 0.005004948556313818311 ),
 .UNSPECIFIED. ) ;
#45708=EDGE_CURVE ( 'NONE', #19210, #42430, #44647, .T. ) ;
#45709=VECTOR ( 'NONE', #39360, 999.9999999999998863 ) ;
#45736=ORIENTED_EDGE ( 'NONE', *, *, #8681, .F. ) ;
#45739=ORIENTED_EDGE ( 'NONE', *, *, #14953, .T. ) ;
#45742=CARTESIAN_POINT ( 'NONE',  ( 1.000433927950262980, -37.69758855726165336, -18.31148531988220896 ) ) ;
#45753=CARTESIAN_POINT ( 'NONE',  ( 0.8560838555295223751, 36.24009790160352651, -29.78301761346427767 ) ) ;
#45767=CARTESIAN_POINT ( 'NONE',  ( 0.6845945791218034371, -13.06825445484017933, -45.05138450944092199 ) ) ;
#45769=EDGE_CURVE ( 'NONE', #38058, #51214, #9967, .T. ) ;
#45782=( BOUNDED_SURFACE ( )  B_SPLINE_SURFACE ( 3, 1, ( 
 ( #29305, #9576 ),
 ( #58404, #5170 ),
 ( #19617, #24929 ),
 ( #19009, #38737 ) ),
 .UNSPECIFIED., .F., .F., .F. ) 
 B_SPLINE_SURFACE_WITH_KNOTS ( ( 4, 4 ),
 ( 2, 2 ),
 ( 0.000000000000000000, 1.000000000000000000 ),
 ( 0.000000000000000000, 1.000000000000000000 ),
 .UNSPECIFIED. ) 
 GEOMETRIC_REPRESENTATION_ITEM ( )  RATIONAL_B_SPLINE_SURFACE ( (
 ( 1.000000000000000000, 1.000000000000000000),
 ( 0.9952954269826590483, 0.8620686068821339365),
 ( 0.9952954269826590483, 0.8620686068821339365),
 ( 1.000000000000000000, 1.000000000000000000) ) ) 
 REPRESENTATION_ITEM ( '' )  SURFACE ( )  );
#45786=B_SPLINE_CURVE_WITH_KNOTS ( 'NONE', 3,
 ( #42542, #4279, #17260, #7208, #21336, #3137, #61605, #13725, #16642, #32837, #26037, #36384, #36686, #2827, #41095, #55447 ),
 .UNSPECIFIED., .F., .F.,
 ( 4, 3, 3, 3, 3, 4 ),
 ( 0.000000000000000000, 0.0002732102107931896201, 0.0004098135523333825097, 0.0005464168938825025032, 0.0008195847345945498404, 0.001092771384553103313 ),
 .UNSPECIFIED. ) ;
#45787=EDGE_CURVE ( 'NONE', #13848, #45995, #49540, .T. ) ;
#45791=ORIENTED_EDGE ( 'NONE', *, *, #52043, .F. ) ;
#45792=CARTESIAN_POINT ( 'NONE',  ( 0.5806925824938499181, -46.06186276235273169, 8.804950948514585818 ) ) ;
#45800=LINE ( 'NONE', #20736, #6611 ) ;
#45801=EDGE_LOOP ( 'NONE', ( #39723, #7662, #39319, #37606 ) ) ;
#45816=CARTESIAN_POINT ( 'NONE',  ( 5.838029081930955932, 19.86434078293957839, 42.85408992630882352 ) ) ;
#45818=ORIENTED_EDGE ( 'NONE', *, *, #61838, .T. ) ;
#45824=ORIENTED_EDGE ( 'NONE', *, *, #46331, .F. ) ;
#45835=FILL_AREA_STYLE ('',( #20773 ) ) ;
#45837=ADVANCED_FACE ( 'NONE', ( #53015 ), #22896, .F. ) ;
#45838=ORIENTED_EDGE ( 'NONE', *, *, #31167, .F. ) ;
#45840=CARTESIAN_POINT ( 'NONE',  ( 0.9790320750461907195, -39.56154820336092826, -13.82826946133685730 ) ) ;
#45846=CARTESIAN_POINT ( 'NONE',  ( 0.5817217712918327788, 5.146885071079491780, -46.61270779598062575 ) ) ;
#45847=CARTESIAN_POINT ( 'NONE',  ( 3.782542959838397056, -3.127173655629709614, 41.92205431898710799 ) ) ;
#45861=EDGE_CURVE ( 'NONE', #19824, #7010, #48775, .T. ) ;
#45863=CARTESIAN_POINT ( 'NONE',  ( 4.956445790444018229, -10.39006634428234577, -45.93021414603951058 ) ) ;
#45872=VERTEX_POINT ( 'NONE', #49874 ) ;
#45873=ORIENTED_EDGE ( 'NONE', *, *, #40620, .T. ) ;
#45874=DIRECTION ( 'NONE',  ( -1.000000000000000000, -0.000000000000000000, -0.000000000000000000 ) ) ;
#45878=ORIENTED_EDGE ( 'NONE', *, *, #38630, .T. ) ;
#45881=CARTESIAN_POINT ( 'NONE',  ( 5.901463166500145796, -11.94204572599471348, 16.18349202795515041 ) ) ;
#45887=ADVANCED_FACE ( 'NONE', ( #6933 ), #56901, .F. ) ;
#45893=CIRCLE ( 'NONE', #6847, 47.09074272231896430 ) ;
#45903=B_SPLINE_CURVE_WITH_KNOTS ( 'NONE', 3,
 ( #15240, #57808, #11154, #48429 ),
 .UNSPECIFIED., .F., .F.,
 ( 4, 4 ),
 ( 0.000000000000000000, 0.004447772540403803314 ),
 .UNSPECIFIED. ) ;
#45907=CARTESIAN_POINT ( 'NONE',  ( 0.5804410086790514622, -29.86002002114409493, 36.16488706179337953 ) ) ;
#45909=CARTESIAN_POINT ( 'NONE',  ( 0.7056759521545049596, -41.47345344194140182, -21.90208868387004060 ) ) ;
#45913=FACE_OUTER_BOUND ( 'NONE', #47855, .T. ) ;
#45919=CARTESIAN_POINT ( 'NONE',  ( 0.5837800304671220131, -46.79431954288349260, 3.086906331265775183 ) ) ;
#45920=CARTESIAN_POINT ( 'NONE',  ( 0.7764146366350288542, 40.80384778211000452, 23.13193636173942380 ) ) ;
#45925=EDGE_CURVE ( 'NONE', #12199, #37991, #44275, .T. ) ;
#45928=B_SPLINE_CURVE_WITH_KNOTS ( 'NONE', 3,
 ( #32231, #37880, #55698, #17511, #46643, #3996 ),
 .UNSPECIFIED., .F., .F.,
 ( 4, 2, 4 ),
 ( 1.180110611199200660E-16, 0.0002448718616795917953, 0.0004897437233590655210 ),
 .UNSPECIFIED. ) ;
#45931=CARTESIAN_POINT ( 'NONE',  ( 0.9762797500689124330, -18.09842611962814019, 37.79909730639167265 ) ) ;
#45944=ORIENTED_EDGE ( 'NONE', *, *, #18279, .T. ) ;
#45951=CARTESIAN_POINT ( 'NONE',  ( 2.891212509699203626, -1.730266096895115631E-16, -41.99381090189411481 ) ) ;
#45958=DIRECTION ( 'NONE',  ( 0.000000000000000000, 0.000000000000000000, 1.000000000000000000 ) ) ;
#45959=ORIENTED_EDGE ( 'NONE', *, *, #49940, .T. ) ;
#45979=CARTESIAN_POINT ( 'NONE',  ( 0.8554163680231720024, 17.71207986799936052, 43.44522643353847968 ) ) ;
#45984=CARTESIAN_POINT ( 'NONE',  ( 0.9754292589017199422, -39.77696748547529637, -13.19546606053464011 ) ) ;
#45985=ORIENTED_EDGE ( 'NONE', *, *, #49989, .T. ) ;
#45986=CARTESIAN_POINT ( 'NONE',  ( 3.782542959838391727, -40.81794997429708616, -10.05648115855390934 ) ) ;
#45995=VERTEX_POINT ( 'NONE', #16059 ) ;
#45997=ORIENTED_EDGE ( 'NONE', *, *, #24049, .T. ) ;
#45999=CARTESIAN_POINT ( 'NONE',  ( 0.9762797500689124330, -26.66896101499594707, 32.32787193067817810 ) ) ;
#46000=CARTESIAN_POINT ( 'NONE',  ( 0.9762797500689124330, 38.77779312671053447, -15.89363222827765831 ) ) ;
#46001=CARTESIAN_POINT ( 'NONE',  ( 5.838029081930955932, 46.29164171884946910, -9.388768030290036037 ) ) ;
#46003=VERTEX_POINT ( 'NONE', #11353 ) ;
#46006=EDGE_CURVE ( 'NONE', #5500, #15172, #13743, .T. ) ;
#46007=CARTESIAN_POINT ( 'NONE',  ( 0.6064782688330877525, 39.98346752738379450, 24.50830004111699623 ) ) ;
#46009=ORIENTED_EDGE ( 'NONE', *, *, #5616, .T. ) ;
#46013=CARTESIAN_POINT ( 'NONE',  ( 0.6064515330803585957, -42.17222881740492824, -20.51432310873376963 ) ) ;
#46014=CARTESIAN_POINT ( 'NONE',  ( 0.5806925824938502512, 45.37089516811273882, 11.86188155343358197 ) ) ;
#46020=CARTESIAN_POINT ( 'NONE',  ( 4.956445790444035104, 35.28522167764516837, -31.18479086508480691 ) ) ;
#46023=EDGE_CURVE ( 'NONE', #25242, #26909, #31386, .T. ) ;
#46028=CARTESIAN_POINT ( 'NONE',  ( 1.231276596079887931, -7.805643096901414779, -41.18675402191659174 ) ) ;
#46029=CARTESIAN_POINT ( 'NONE',  ( 0.9762797500689124330, -41.16654106227479559, 7.851158013551082782 ) ) ;
#46030=VERTEX_POINT ( 'NONE', #31696 ) ;
#46033=CARTESIAN_POINT ( 'NONE',  ( 4.291220156522059348, 26.18147253908299632, 39.16528428329022660 ) ) ;
#46037=CARTESIAN_POINT ( 'NONE',  ( 5.901463166500145796, 0.6576072425839265545, 20.10187610784470635 ) ) ;
#46039=CARTESIAN_POINT ( 'NONE',  ( 5.895881250540457863, -19.39944854657655782, -5.309338725023076577 ) ) ;
#46040=ORIENTED_EDGE ( 'NONE', *, *, #42181, .F. ) ;
#46054=ORIENTED_EDGE ( 'NONE', *, *, #37386, .F. ) ;
#46069=EDGE_LOOP ( 'NONE', ( #54533, #11432, #9721, #167 ) ) ;
#46072=CARTESIAN_POINT ( 'NONE',  ( 0.5837800304671216800, -44.31613230802797432, 15.34007005971153603 ) ) ;
#46074=DIRECTION ( 'NONE',  ( -1.000000000000000000, -0.000000000000000000, -0.000000000000000000 ) ) ;
#46075=CARTESIAN_POINT ( 'NONE',  ( 4.956445790443998689, -17.42806872899825521, 43.74700527484080936 ) ) ;
#46082=CARTESIAN_POINT ( 'NONE',  ( 0.5806925824938502512, -44.11884900496080775, 15.89809815106926116 ) ) ;
#46086=CARTESIAN_POINT ( 'NONE',  ( 3.238018933889920792, -5.886379020808539586, -12.03154330877955402 ) ) ;
#46092=CARTESIAN_POINT ( 'NONE',  ( 5.894904586330512508, 19.71013252676734240, -4.005007845049880721 ) ) ;
#46093=CARTESIAN_POINT ( 'NONE',  ( 0.5806925824938499181, 40.06810415365472977, 24.36738377166168235 ) ) ;
#46106=CARTESIAN_POINT ( 'NONE',  ( 0.9772918015221176979, -41.84074903630183684, -2.385073548527663956 ) ) ;
#46108=ORIENTED_EDGE ( 'NONE', *, *, #33129, .F. ) ;
#46114=CARTESIAN_POINT ( 'NONE',  ( 5.895881250540457863, -2.008683229082083521, 20.01231803898552286 ) ) ;
#46116=ORIENTED_EDGE ( 'NONE', *, *, #11042, .F. ) ;
#46129=CARTESIAN_POINT ( 'NONE',  ( 0.5830081025819919827, -30.06820310196314594, 35.98798683729531689 ) ) ;
#46143=ADVANCED_FACE ( 'NONE', ( #42647 ), #29285, .F. ) ;
#46145=VERTEX_POINT ( 'NONE', #27922 ) ;
#46147=CARTESIAN_POINT ( 'NONE',  ( 0.9785694773339257413, -39.51624465101048855, -13.95714205688820364 ) ) ;
#46148=CARTESIAN_POINT ( 'NONE',  ( 0.9780303403264770656, -41.79223983423273836, 3.122227255190472395 ) ) ;
#46150=( BOUNDED_SURFACE ( )  B_SPLINE_SURFACE ( 3, 1, ( 
 ( #23367, #56246 ),
 ( #32459, #36869 ),
 ( #27438, #50618 ),
 ( #42493, #61250 ) ),
 .UNSPECIFIED., .F., .F., .F. ) 
 B_SPLINE_SURFACE_WITH_KNOTS ( ( 4, 4 ),
 ( 2, 2 ),
 ( 0.000000000000000000, 1.000000000000000000 ),
 ( 0.000000000000000000, 1.000000000000000000 ),
 .UNSPECIFIED. ) 
 GEOMETRIC_REPRESENTATION_ITEM ( )  RATIONAL_B_SPLINE_SURFACE ( (
 ( 1.000000000000000000, 1.000000000000000000),
 ( 0.7282232189291694135, 0.9929344683865672927),
 ( 0.7282232189291694135, 0.9929344683865672927),
 ( 1.000000000000000000, 1.000000000000000000) ) ) 
 REPRESENTATION_ITEM ( '' )  SURFACE ( )  );
#46157=CARTESIAN_POINT ( 'NONE',  ( 0.9762797500689124330, 35.79768877047989406, -21.79105926469756938 ) ) ;
#46171=CARTESIAN_POINT ( 'NONE',  ( 5.896782393890504181, 3.339090646272911300, -19.83372281075806853 ) ) ;
#46176=DIRECTION ( 'NONE',  ( -0.07500201931887526263, 0.2180102369365608250, -0.9730602415518555537 ) ) ;
#46179=ORIENTED_EDGE ( 'NONE', *, *, #42809, .F. ) ;
#46193=CARTESIAN_POINT ( 'NONE',  ( 0.8560838555295223751, 46.89922841446243496, -0.9138972643637069959 ) ) ;
#46197=CARTESIAN_POINT ( 'NONE',  ( 0.5797568599927139799, -20.30903442135246806, 42.27018369422267341 ) ) ;
#46203=AXIS2_PLACEMENT_3D ( 'NONE', #9288, #23705, #61583 ) ;
#46205=AXIS2_PLACEMENT_3D ( 'NONE', #61915, #38782, #48163 ) ;
#46208=CARTESIAN_POINT ( 'NONE',  ( 1.231276596079887931, -35.03243822710496858, -23.02183839058345072 ) ) ;
#46209=CARTESIAN_POINT ( 'NONE',  ( 4.962356264823601926, -38.57439820587641321, 16.83007429920694875 ) ) ;
#46214=CARTESIAN_POINT ( 'NONE',  ( 0.9762797500689124330, -41.77809974471944088, 3.303810967046753255 ) ) ;
#46221=CARTESIAN_POINT ( 'NONE',  ( 0.5817217712918324457, -46.81948268753178155, 2.677871333780827090 ) ) ;
#46235=SHAPE_DEFINITION_REPRESENTATION ( #46838, #42491 ) ;
#46236=CARTESIAN_POINT ( 'NONE',  ( 0.5782707292762442330, -42.18185855468866663, 20.50432058322967777 ) ) ;
#46240=ORIENTED_EDGE ( 'NONE', *, *, #40946, .T. ) ;
#46242=CARTESIAN_POINT ( 'NONE',  ( 1.091591847532195514, 3.418266415782475587, 41.77408820867997008 ) ) ;
#46247=LINE ( 'NONE', #17730, #39194 ) ;
#46260=EDGE_CURVE ( 'NONE', #14125, #3786, #18834, .T. ) ;
#46261=CARTESIAN_POINT ( 'NONE',  ( 0.5848930533535030563, 43.24595201260145672, -18.14003078584298478 ) ) ;
#46282=DIRECTION ( 'NONE',  ( 0.000000000000000000, 0.000000000000000000, 1.000000000000000000 ) ) ;
#46285=CARTESIAN_POINT ( 'NONE',  ( 0.9790724872846768845, 24.82680137436399903, 33.76336984809620390 ) ) ;
#46288=VERTEX_POINT ( 'NONE', #3321 ) ;
#46309=CARTESIAN_POINT ( 'NONE',  ( 4.291220156522059348, -41.03139692541890327, -23.14764488353881688 ) ) ;
#46310=CARTESIAN_POINT ( 'NONE',  ( 5.896782393890504181, -2.019528367549592307, 20.01118667272569951 ) ) ;
#46318=CARTESIAN_POINT ( 'NONE',  ( 0.5806925824938494740, -34.41156632303759011, 31.86010774524702072 ) ) ;
#46323=CARTESIAN_POINT ( 'NONE',  ( 4.960386119450146403, 0.9915941002490832323, -43.74303608361785223 ) ) ;
#46325=VERTEX_POINT ( 'NONE', #32794 ) ;
#46331=EDGE_CURVE ( 'NONE', #12531, #10350, #55633, .T. ) ;
#46346=ORIENTED_EDGE ( 'NONE', *, *, #26212, .F. ) ;
#46348=DIRECTION ( 'NONE',  ( -0.07500201931887527651, 0.7908860163360004192, 0.6073499866323063268 ) ) ;
#46353=ORIENTED_EDGE ( 'NONE', *, *, #33329, .F. ) ;
#46354=ORIENTED_EDGE ( 'NONE', *, *, #10176, .T. ) ;
#46356=CARTESIAN_POINT ( 'NONE',  ( 1.091591847532194182, -7.739709431952981333, 41.19291066269509116 ) ) ;
#46358=CARTESIAN_POINT ( 'NONE',  ( 4.291220156522060236, -43.75057291092651468, 17.47215977695375244 ) ) ;
#46360=EDGE_LOOP ( 'NONE', ( #13210, #34337, #24245, #52511 ) ) ;
#46363=CARTESIAN_POINT ( 'NONE',  ( 0.6064515330803588178, -34.30059540857045164, 31.98129907703317087 ) ) ;
#46365=B_SPLINE_CURVE_WITH_KNOTS ( 'NONE', 3,
 ( #56773, #37395, #28583, #23284, #51455, #56467 ),
 .UNSPECIFIED., .F., .F.,
 ( 4, 2, 4 ),
 ( 8.787390050835121380E-18, 0.0002448709889506573735, 0.0004897419779013059650 ),
 .UNSPECIFIED. ) ;
#46366=ORIENTED_EDGE ( 'NONE', *, *, #42060, .F. ) ;
#46368=CARTESIAN_POINT ( 'NONE',  ( 2.528190830796654964, 28.30160364192409972, 31.00440883888025922 ) ) ;
#46369=CARTESIAN_POINT ( 'NONE',  ( 0.5806925824938502512, -44.11884900496080775, 15.89809815106926116 ) ) ;
#46373=CARTESIAN_POINT ( 'NONE',  ( 0.5848930533535030563, 4.875316827622536486, 46.64230234688099586 ) ) ;
#46375=CARTESIAN_POINT ( 'NONE',  ( 1.231276596079881047, -0.5545928549373742023, -41.91621640586514985 ) ) ;
#46393=CARTESIAN_POINT ( 'NONE',  ( 5.895881250540457863, -7.224475463584143498, 18.77057899704672295 ) ) ;
#46399=CARTESIAN_POINT ( 'NONE',  ( 0.9762797500689124330, 20.58271139965489738, 36.50584578699993443 ) ) ;
#46401=CARTESIAN_POINT ( 'NONE',  ( 0.7764146366350267447, -45.77880931614775051, 10.21474871276577012 ) ) ;
#46402=ORIENTED_EDGE ( 'NONE', *, *, #60357, .T. ) ;
#46406=ADVANCED_FACE ( 'NONE', ( #10207 ), #45782, .F. ) ;
#46410=EDGE_CURVE ( 'NONE', #55732, #13148, #36820, .T. ) ;
#46411=CARTESIAN_POINT ( 'NONE',  ( 4.962356264823608143, 0.000000000000000000, 0.000000000000000000 ) ) ;
#46419=ORIENTED_EDGE ( 'NONE', *, *, #18216, .F. ) ;
#46420=CARTESIAN_POINT ( 'NONE',  ( 5.917102823773431552, -13.98784315367467812, 14.45095020958616416 ) ) ;
#46424=CARTESIAN_POINT ( 'NONE',  ( 5.901463166500145796, -7.215136289071087283, -18.77390952014966530 ) ) ;
#46431=CARTESIAN_POINT ( 'NONE',  ( 0.5824936645240088584, -30.55462678129038068, 35.57601665864742557 ) ) ;
#46433=CARTESIAN_POINT ( 'NONE',  ( 1.231276596079887264, -34.07446381689716475, 24.41736444846234733 ) ) ;
#46434=ADVANCED_FACE ( 'NONE', ( #33719 ), #35723, .F. ) ;
#46441=CARTESIAN_POINT ( 'NONE',  ( 0.5817216825391131607, 10.42801594297066892, -45.72189230227252921 ) ) ;
#46448=ORIENTED_EDGE ( 'NONE', *, *, #46886, .F. ) ;
#46452=FACE_OUTER_BOUND ( 'NONE', #52400, .T. ) ;
#46453=CARTESIAN_POINT ( 'NONE',  ( 5.895596859100789899, 20.06773179721815126, -1.346968346846738385 ) ) ;
#46459=DIRECTION ( 'NONE',  ( 0.07500201931887538753, 0.04681388819016350789, -0.9960839106072389981 ) ) ;
#46468=AXIS2_PLACEMENT_3D ( 'NONE', #58407, #32251, #8735 ) ;
#46475=CARTESIAN_POINT ( 'NONE',  ( 5.901463166500146684, -2.027578129542785046, -20.01016734735710756 ) ) ;
#46476=ORIENTED_EDGE ( 'NONE', *, *, #46704, .T. ) ;
#46477=EDGE_LOOP ( 'NONE', ( #6202, #39408, #10522, #12837 ) ) ;
#46498=CARTESIAN_POINT ( 'NONE',  ( 0.5806925824938499181, -44.47729014209976128, 14.86583411581871772 ) ) ;
#46499=CARTESIAN_POINT ( 'NONE',  ( 0.6064782688330843108, -20.38304199076106471, 42.23583840320495852 ) ) ;
#46505=CARTESIAN_POINT ( 'NONE',  ( 0.7764139734771242640, 16.02283686154742881, 44.08298050058667172 ) ) ;
#46523=CARTESIAN_POINT ( 'NONE',  ( 0.8560838555295223751, 40.81790744942443183, 23.11430867518979326 ) ) ;
#46525=CARTESIAN_POINT ( 'NONE',  ( 0.8554163680231816613, -6.900908941297196009, 46.40671211038057464 ) ) ;
#46526=CARTESIAN_POINT ( 'NONE',  ( 0.9762797500689124330, 41.90547441298052433, 0.5059638413352746111 ) ) ;
#46527=CARTESIAN_POINT ( 'NONE',  ( 0.8560838555295158248, 11.76118766017326323, -45.40977096290972526 ) ) ;
#46535=CARTESIAN_POINT ( 'NONE',  ( 4.956445790443993360, 20.31112743693043399, 42.48524629068788983 ) ) ;
#46536=FACE_OUTER_BOUND ( 'NONE', #25073, .T. ) ;
#46540=B_SPLINE_CURVE_WITH_KNOTS ( 'NONE', 3,
 ( #31120, #45550, #17041, #22042, #41167, #17340 ),
 .UNSPECIFIED., .F., .F.,
 ( 4, 2, 4 ),
 ( 4.872882708070265673E-18, 0.0002291472222819940739, 0.0004582944445639832690 ),
 .UNSPECIFIED. ) ;
#46542=CARTESIAN_POINT ( 'NONE',  ( 0.5806925824938511393, 10.33919002968708689, -45.74192291403568333 ) ) ;
#46552=CARTESIAN_POINT ( 'NONE',  ( 0.5817216825391118284, 22.93558720760018943, 40.90469156038248144 ) ) ;
#46553=CARTESIAN_POINT ( 'NONE',  ( 0.5837157313716020424, -45.97435446094988265, 9.251799580674125778 ) ) ;
#46558=CARTESIAN_POINT ( 'NONE',  ( 0.9790850452238870627, 24.81859480363789672, -33.76943414148414746 ) ) ;
#46559=EDGE_CURVE ( 'NONE', #31240, #5597, #21818, .T. ) ;
#46562=CARTESIAN_POINT ( 'NONE',  ( 0.9791128995231611620, 32.88674391329360702, -25.97690337641515157 ) ) ;
#46563=EDGE_CURVE ( 'NONE', #18906, #17743, #5363, .T. ) ;
#46573=ORIENTED_EDGE ( 'NONE', *, *, #47536, .T. ) ;
#46580=EDGE_LOOP ( 'NONE', ( #13310, #40898, #26846, #15698 ) ) ;
#46581=CARTESIAN_POINT ( 'NONE',  ( 1.091591847532199511, -31.60342101358676459, 27.53148690488443862 ) ) ;
#46595=CARTESIAN_POINT ( 'NONE',  ( 1.000110580585049203, 29.60461236713370070, -29.66453116709677573 ) ) ;
#46605=CARTESIAN_POINT ( 'NONE',  ( 1.231276596079887264, -13.22565419921979313, -39.77887431816952102 ) ) ;
#46606=EDGE_CURVE ( 'NONE', #10512, #36411, #39825, .T. ) ;
#46613=CARTESIAN_POINT ( 'NONE',  ( 4.291220156522059348, -33.45801620160708012, -33.16549636532965195 ) ) ;
#46625=CARTESIAN_POINT ( 'NONE',  ( 1.157644175074336035, 8.912044513555821723, 40.95824383524741563 ) ) ;
#46626=CARTESIAN_POINT ( 'NONE',  ( 3.376099380956842921, -11.75009321188415967, 6.453192476914109577 ) ) ;
#46641=EDGE_LOOP ( 'NONE', ( #50710, #59540, #40888, #53952 ) ) ;
#46642=B_SPLINE_CURVE_WITH_KNOTS ( 'NONE', 3,
 ( #32489, #55966, #17774, #13700, #51263, #61274, #36579, #18392, #12782, #18083, #13085, #51565, #37513, #21852, #45671, #60055 ),
 .UNSPECIFIED., .F., .F.,
 ( 4, 3, 3, 3, 3, 4 ),
 ( 9.813676791237319219E-18, 0.0002732102107931869096, 0.0004098135523333678730, 0.0005464168938824852644, 0.0008195847345945424679, 0.001092771384553108951 ),
 .UNSPECIFIED. ) ;
#46643=CARTESIAN_POINT ( 'NONE',  ( 0.5797568599927116484, 37.19047634640187994, -28.56735510681254553 ) ) ;
#46648=VERTEX_POINT ( 'NONE', #23009 ) ;
#46653=CARTESIAN_POINT ( 'NONE',  ( 0.5804410086790514622, -30.69452151258693817, -35.45935984995687562 ) ) ;
#46657=ORIENTED_EDGE ( 'NONE', *, *, #35792, .T. ) ;
#46661=ORIENTED_EDGE ( 'NONE', *, *, #16032, .T. ) ;
#46663=CARTESIAN_POINT ( 'NONE',  ( 1.157644175074335813, -7.784786351351509204, 41.18736914325793919 ) ) ;
#46670=FACE_OUTER_BOUND ( 'NONE', #60000, .T. ) ;
#46676=CARTESIAN_POINT ( 'NONE',  ( 1.000110580585049425, 40.24174505028877036, 11.70553023487029698 ) ) ;
#46678=DIRECTION ( 'NONE',  ( 0.07500201931887538753, -0.2180102369365475579, -0.9730602415518585513 ) ) ;
#46683=CARTESIAN_POINT ( 'NONE',  ( 0.9775691876210993447, -41.14243135631965487, 7.977095403749041580 ) ) ;
#46687=SURFACE_STYLE_FILL_AREA ( #42305 ) ;
#46690=DIRECTION ( 'NONE',  ( -0.07906939808003035641, -0.4269277467251155200, -0.9008222518141286717 ) ) ;
#46695=EDGE_CURVE ( 'NONE', #58067, #38817, #41253, .T. ) ;
#46698=CIRCLE ( 'NONE', #11676, 42.08604991992415023 ) ;
#46703=CARTESIAN_POINT ( 'NONE',  ( 0.7764146366350282991, 37.35658959738729834, 28.36416202396149799 ) ) ;
#46704=EDGE_CURVE ( 'NONE', #53253, #22549, #50985, .T. ) ;
#46713=CARTESIAN_POINT ( 'NONE',  ( 0.8560838555295158248, -2.480523550131575661, 46.84250032821661591 ) ) ;
#46732=ADVANCED_FACE ( 'NONE', ( #43987 ), #18741, .T. ) ;
#46733=CARTESIAN_POINT ( 'NONE',  ( 5.895881250540457863, 8.462078741123132630, 18.24612027219301780 ) ) ;
#46740=CARTESIAN_POINT ( 'NONE',  ( 0.5837800304671209028, -44.28628010941674376, -15.42604052405472359 ) ) ;
#46743=VERTEX_POINT ( 'NONE', #15145 ) ;
#46744=DIRECTION ( 'NONE',  ( 0.000000000000000000, 0.000000000000000000, 1.000000000000000000 ) ) ;
#46746=VERTEX_POINT ( 'NONE', #52410 ) ;
#46750=CARTESIAN_POINT ( 'NONE',  ( 0.8560838555295223751, -26.00596412780120303, -39.03924517540328765 ) ) ;
#46753=CARTESIAN_POINT ( 'NONE',  ( 5.895596859100789899, -17.30698493747174993, -10.24677781483592121 ) ) ;
#46757=CIRCLE ( 'NONE', #59737, 47.09074272231896430 ) ;
#46762=B_SPLINE_CURVE_WITH_KNOTS ( 'NONE', 3,
 ( #27316, #51107, #61121, #13231 ),
 .UNSPECIFIED., .F., .F.,
 ( 4, 4 ),
 ( 0.000000000000000000, 0.005004948556313818311 ),
 .UNSPECIFIED. ) ;
#46768=CARTESIAN_POINT ( 'NONE',  ( 1.231276596079881047, 41.91134057782998212, 0.8463462572780127147 ) ) ;
#46774=EDGE_CURVE ( 'NONE', #44981, #57082, #30787, .T. ) ;
#46790=AXIS2_PLACEMENT_3D ( 'NONE', #17304, #8493, #32329 ) ;
#46794=ORIENTED_EDGE ( 'NONE', *, *, #4241, .T. ) ;
#46798=LINE ( 'NONE', #17347, #14096 ) ;
#46810=CARTESIAN_POINT ( 'NONE',  ( 1.231276596079881047, -16.87422718933157739, -38.37365278131454005 ) ) ;
#46811=CARTESIAN_POINT ( 'NONE',  ( 3.782625744892853525, 2.488346184749487211, -41.96482142652158842 ) ) ;
#46814=CARTESIAN_POINT ( 'NONE',  ( 3.661933894777873455, -45.68403645958177606, -11.20713958649829500 ) ) ;
#46823=CARTESIAN_POINT ( 'NONE',  ( 0.5817216825391127166, -38.40350717126904101, 26.91478383999664814 ) ) ;
#46824=FACE_BOUND ( 'NONE', #48419, .T. ) ;
#46826=DIRECTION ( 'NONE',  ( 0.000000000000000000, 0.000000000000000000, 1.000000000000000000 ) ) ;
#46830=CARTESIAN_POINT ( 'NONE',  ( 0.9754292580325127915, -22.05710644602384107, -35.63441485604581516 ) ) ;
#46831=CARTESIAN_POINT ( 'NONE',  ( 1.231276596079881047, -37.78837162824498819, 18.14705873423338289 ) ) ;
#46836=FACE_OUTER_BOUND ( 'NONE', #44601, .T. ) ;
#46838=PRODUCT_DEFINITION_SHAPE ( 'NONE', 'NONE',  #61968 ) ;
#46841=CARTESIAN_POINT ( 'NONE',  ( 0.5830082357119563685, -46.80869808478055916, 2.859688540068253459 ) ) ;
#46843=DIRECTION ( 'NONE',  ( -1.000000000000000000, -0.000000000000000000, -0.000000000000000000 ) ) ;
#46844=CARTESIAN_POINT ( 'NONE',  ( 2.618530812446115519, -6.426312013672279555, 46.56639671588441587 ) ) ;
#46847=CARTESIAN_POINT ( 'NONE',  ( 0.9791128995231623833, -1.405476621873006371, -41.88510558314887788 ) ) ;
#46849=VERTEX_POINT ( 'NONE', #35185 ) ;
#46852=CARTESIAN_POINT ( 'NONE',  ( 0.8560838555295158248, -26.00596412780176081, 39.03924517540291106 ) ) ;
#46855=B_SPLINE_CURVE_WITH_KNOTS ( 'NONE', 3,
 ( #36616, #8087, #18112, #37236 ),
 .UNSPECIFIED., .F., .F.,
 ( 4, 4 ),
 ( 0.000000000000000000, 0.005004948556313805301 ),
 .UNSPECIFIED. ) ;
#46859=CARTESIAN_POINT ( 'NONE',  ( 0.5837157313716042628, -25.31061043140172728, 39.47923584837779032 ) ) ;
#46868=CARTESIAN_POINT ( 'NONE',  ( 5.838029081930957709, -16.95764376597208667, 44.08518318051211793 ) ) ;
#46869=CARTESIAN_POINT ( 'NONE',  ( 5.901463166500145796, 17.95741941801110642, -9.058087998373295591 ) ) ;
#46871=ORIENTED_EDGE ( 'NONE', *, *, #3196, .T. ) ;
#46873=CARTESIAN_POINT ( 'NONE',  ( 0.5832655196449144652, -46.00108932644737081, 9.117837668742486912 ) ) ;
#46874=B_SPLINE_CURVE_WITH_KNOTS ( 'NONE', 3,
 ( #40523, #31722, #54886, #17015, #54254, #59588 ),
 .UNSPECIFIED., .F., .F.,
 ( 4, 2, 4 ),
 ( 1.264432626340127662E-17, 0.0002448709889506591082, 0.0004897419779013056397 ),
 .UNSPECIFIED. ) ;
#46877=ORIENTED_EDGE ( 'NONE', *, *, #54010, .T. ) ;
#46886=EDGE_CURVE ( 'NONE', #29827, #34780, #54619, .T. ) ;
#46888=ORIENTED_EDGE ( 'NONE', *, *, #50754, .F. ) ;
#46897=ORIENTED_EDGE ( 'NONE', *, *, #33447, .T. ) ;
#46902=CARTESIAN_POINT ( 'NONE',  ( 0.5806925824938502512, -2.112975627976310111, -46.84824112321764744 ) ) ;
#46912=CARTESIAN_POINT ( 'NONE',  ( 0.8560838555295223751, 37.37287335782406217, 28.34856559090382078 ) ) ;
#46918=LINE ( 'NONE', #8352, #35513 ) ;
#46928=EDGE_CURVE ( 'NONE', #55527, #33684, #39704, .T. ) ;
#46929=DIRECTION ( 'NONE',  ( 0.000000000000000000, 0.000000000000000000, 1.000000000000000000 ) ) ;
#46931=CARTESIAN_POINT ( 'NONE',  ( 5.838029081930957709, -32.85120734338257620, -33.93911068715571133 ) ) ;
#46935=EDGE_CURVE ( 'NONE', #26853, #42210, #44784, .T. ) ;
#46946=CARTESIAN_POINT ( 'NONE',  ( 0.9754292580325130135, -17.11069898979941328, -38.25639092994113355 ) ) ;
#46947=CARTESIAN_POINT ( 'NONE',  ( 0.5824936645240084143, 46.42765496787452406, 6.611432010109767887 ) ) ;
#46949=ORIENTED_EDGE ( 'NONE', *, *, #13038, .T. ) ;
#46952=CARTESIAN_POINT ( 'NONE',  ( 2.528190830796657629, 30.04139741748772252, -29.32181060844588316 ) ) ;
#46963=DIRECTION ( 'NONE',  ( 0.000000000000000000, 0.000000000000000000, 1.000000000000000000 ) ) ;
#46964=ORIENTED_EDGE ( 'NONE', *, *, #55081, .F. ) ;
#46968=CARTESIAN_POINT ( 'NONE',  ( 0.5817217712918332229, -7.350851069864205556, -46.31630320477930951 ) ) ;
#46976=EDGE_LOOP ( 'NONE', ( #5063, #48788, #57812, #23116 ) ) ;
#46979=CARTESIAN_POINT ( 'NONE',  ( 0.9754292589017173887, 28.71299572461916583, -30.52689541065851486 ) ) ;
#46981=CONICAL_SURFACE ( 'NONE', #5914, 42.08604991992415023, 1.569615340895231137 ) ;
#46992=CARTESIAN_POINT ( 'NONE',  ( 4.962356264823591268, 23.01169039590626753, 35.23773124060775785 ) ) ;
#46996=EDGE_CURVE ( 'NONE', #16356, #43088, #56717, .T. ) ;
#46998=CARTESIAN_POINT ( 'NONE',  ( 2.891212509699203626, -1.730266096895115631E-16, -41.99381090189411481 ) ) ;
#47009=CARTESIAN_POINT ( 'NONE',  ( 0.5804410086790514622, -7.261380058784682845, 46.33348909263450111 ) ) ;
#47017=CARTESIAN_POINT ( 'NONE',  ( 5.917102823773431552, -13.98784315367447029, -14.45095020958636667 ) ) ;
#47019=DIRECTION ( 'NONE',  ( 0.000000000000000000, 0.000000000000000000, 1.000000000000000000 ) ) ;
#47021=CARTESIAN_POINT ( 'NONE',  ( 1.231276596079881047, 40.19859528295886975, 11.88905834349143653 ) ) ;
#47028=CARTESIAN_POINT ( 'NONE',  ( 0.5806925824938499181, -45.84420715090598009, -9.875780123533834498 ) ) ;
#47029=CARTESIAN_POINT ( 'NONE',  ( 4.962356264823603702, 26.83784316460332420, -32.41860225448503030 ) ) ;
#47037=EDGE_CURVE ( 'NONE', #53844, #44630, #21696, .T. ) ;
#47042=CARTESIAN_POINT ( 'NONE',  ( 5.894904586330512508, -19.39861238634053819, -5.312555839344970998 ) ) ;
#47047=EDGE_CURVE ( 'NONE', #57756, #31240, #45687, .T. ) ;
#47049=CARTESIAN_POINT ( 'NONE',  ( 5.901463166500145796, 19.71248269111032414, -3.991979019648351112 ) ) ;
#47050=CARTESIAN_POINT ( 'NONE',  ( 5.895596859100789899, 17.95274561709314654, -9.067916410092799140 ) ) ;
#47056=EDGE_LOOP ( 'NONE', ( #31061, #13206, #1662, #17723 ) ) ;
#47059=CIRCLE ( 'NONE', #45057, 47.09074272231896430 ) ;
#47061=EDGE_CURVE ( 'NONE', #29140, #31868, #11271, .T. ) ;
#47066=CARTESIAN_POINT ( 'NONE',  ( 2.282803330402965347, -35.70555387398805181, 30.52229234524697432 ) ) ;
#47067=LINE ( 'NONE', #57041, #58419 ) ;
#47071=CARTESIAN_POINT ( 'NONE',  ( 0.9789889208857693870, -41.80852869865788080, 2.895138355220653548 ) ) ;
#47072=CARTESIAN_POINT ( 'NONE',  ( 4.962356264823601926, -41.76635909427990612, -5.177532797579353918 ) ) ;
#47075=CARTESIAN_POINT ( 'NONE',  ( 5.895881250540457863, 20.06765451668685785, -1.347933161250387535 ) ) ;
#47076=CARTESIAN_POINT ( 'NONE',  ( 0.9762797500689124330, -12.89881610234976961, 39.87411852747928265 ) ) ;
#47077=DIRECTION ( 'NONE',  ( 0.000000000000000000, 0.000000000000000000, 1.000000000000000000 ) ) ;
#47078=CARTESIAN_POINT ( 'NONE',  ( 0.9790724872846777727, -12.45512225568080567, 40.01506140914315779 ) ) ;
#47086=CARTESIAN_POINT ( 'NONE',  ( 0.5806925824938499181, 45.37089516811292356, -11.86188155343291584 ) ) ;
#47104=ORIENTED_EDGE ( 'NONE', *, *, #11042, .T. ) ;
#47110=EDGE_CURVE ( 'NONE', #22672, #60467, #9045, .T. ) ;
#47115=ADVANCED_FACE ( 'NONE', ( #6552 ), #57736, .T. ) ;
#47124=PLANE ( 'NONE',  #48388 ) ;
#47126=CARTESIAN_POINT ( 'NONE',  ( 0.5806925824938499181, 16.34374012233052653, 43.95571090492437349 ) ) ;
#47128=( BOUNDED_SURFACE ( )  B_SPLINE_SURFACE ( 3, 1, ( 
 ( #12856, #2797 ),
 ( #31320, #59501 ),
 ( #32257, #22546 ),
 ( #60417, #12541 ) ),
 .UNSPECIFIED., .F., .F., .F. ) 
 B_SPLINE_SURFACE_WITH_KNOTS ( ( 4, 4 ),
 ( 2, 2 ),
 ( 0.000000000000000000, 1.000000000000000000 ),
 ( 0.000000000000000000, 1.000000000000000000 ),
 .UNSPECIFIED. ) 
 GEOMETRIC_REPRESENTATION_ITEM ( )  RATIONAL_B_SPLINE_SURFACE ( (
 ( 1.000000000000000000, 1.000000000000000000),
 ( 0.7282232189291693025, 0.9929344683865674037),
 ( 0.7282232189291693025, 0.9929344683865674037),
 ( 1.000000000000000000, 1.000000000000000000) ) ) 
 REPRESENTATION_ITEM ( '' )  SURFACE ( )  );
#47138=CARTESIAN_POINT ( 'NONE',  ( 0.6845945791218034371, 21.77999332122215037, 41.54561844095550782 ) ) ;
#47140=B_SPLINE_CURVE_WITH_KNOTS ( 'NONE', 3,
 ( #12242, #26942, #31327, #16619, #6876, #50431, #44840, #41074, #46072, #3117, #22246, #52268, #55731, #8133, #60424, #46369 ),
 .UNSPECIFIED., .F., .F.,
 ( 4, 3, 3, 3, 3, 4 ),
 ( 8.674294979774126656E-18, 0.0002732102107931889696, 0.0004098135523333802871, 0.0005464168938824911191, 0.0008195847345945437689, 0.001092771384553109385 ),
 .UNSPECIFIED. ) ;
#47143=( BOUNDED_SURFACE ( )  B_SPLINE_SURFACE ( 3, 1, ( 
 ( #35063, #40091 ),
 ( #21255, #53511 ),
 ( #39773, #6497 ),
 ( #25638, #35373 ) ),
 .UNSPECIFIED., .F., .F., .F. ) 
 B_SPLINE_SURFACE_WITH_KNOTS ( ( 4, 4 ),
 ( 2, 2 ),
 ( 0.000000000000000000, 1.000000000000000000 ),
 ( 0.000000000000000000, 1.000000000000000000 ),
 .UNSPECIFIED. ) 
 GEOMETRIC_REPRESENTATION_ITEM ( )  RATIONAL_B_SPLINE_SURFACE ( (
 ( 1.000000000000000000, 1.000000000000000000),
 ( 0.9952954269826590483, 0.8620686068821307169),
 ( 0.9952954269826590483, 0.8620686068821307169),
 ( 1.000000000000000000, 1.000000000000000000) ) ) 
 REPRESENTATION_ITEM ( '' )  SURFACE ( )  );
#47146=CARTESIAN_POINT ( 'NONE',  ( 5.917102823773431552, 3.353685953999792968, -19.83034312798663024 ) ) ;
#47149=B_SPLINE_CURVE_WITH_KNOTS ( 'NONE', 3,
 ( #57614, #57014, #43266, #299 ),
 .UNSPECIFIED., .F., .F.,
 ( 4, 4 ),
 ( 0.000000000000000000, 0.005004948556313799229 ),
 .UNSPECIFIED. ) ;
#47161=CARTESIAN_POINT ( 'NONE',  ( 2.282803330402963571, -44.78788971279550424, 14.16127969257910912 ) ) ;
#47164=EDGE_LOOP ( 'NONE', ( #43976, #39573, #46888, #14399 ) ) ;
#47175=CARTESIAN_POINT ( 'NONE',  ( 0.9788927965476029724, 24.74514878889634062, -33.82327932130707637 ) ) ;
#47179=CARTESIAN_POINT ( 'NONE',  ( 4.962356264823601926, -41.76635909427990612, -5.177532797579353918 ) ) ;
#47183=EDGE_CURVE ( 'NONE', #42042, #61015, #25456, .T. ) ;
#47185=EDGE_CURVE ( 'NONE', #4962, #17422, #12070, .T. ) ;
#47191=FACE_OUTER_BOUND ( 'NONE', #47164, .T. ) ;
#47193=CARTESIAN_POINT ( 'NONE',  ( 0.9785694773339257413, 4.416269084231816855, -41.67531611266228708 ) ) ;
#47194=DIRECTION ( 'NONE',  ( 0.9990097760809873995, 0.000000000000000000, -0.04449120468829072944 ) ) ;
#47199=VERTEX_POINT ( 'NONE', #1560 ) ;
#47205=VERTEX_POINT ( 'NONE', #43808 ) ;
#47207=CARTESIAN_POINT ( 'NONE',  ( 3.782542959838397501, 13.48688832728106846, 39.81634961475020162 ) ) ;
#47214=CARTESIAN_POINT ( 'NONE',  ( 0.7056759521544957448, 36.27980703839233456, 29.72413884999874156 ) ) ;
#47215=ORIENTED_EDGE ( 'NONE', *, *, #6926, .T. ) ;
#47216=CARTESIAN_POINT ( 'NONE',  ( 0.5806925824938502512, -24.77160101449099727, 39.81946942793729249 ) ) ;
#47233=CARTESIAN_POINT ( 'NONE',  ( 0.5804410086790514622, 43.38796872094602008, 17.80460676694675826 ) ) ;
#47243=CARTESIAN_POINT ( 'NONE',  ( 0.8554163680231738898, 27.08908797599145046, 38.30648490452777821 ) ) ;
#47250=ADVANCED_FACE ( 'NONE', ( #52227 ), #48777, .T. ) ;
#47256=CARTESIAN_POINT ( 'NONE',  ( 4.958415959904820092, 29.71032706691326908, -34.35841118852379594 ) ) ;
#47264=CARTESIAN_POINT ( 'NONE',  ( 0.9784957157296357844, -7.200058621843461459, -41.28549639806200844 ) ) ;
#47268=CIRCLE ( 'NONE', #31251, 47.09074272231896430 ) ;
#47275=ORIENTED_EDGE ( 'NONE', *, *, #22362, .T. ) ;
#47280=VERTEX_POINT ( 'NONE', #24050 ) ;
#47293=ORIENTED_EDGE ( 'NONE', *, *, #12396, .T. ) ;
#47296=CARTESIAN_POINT ( 'NONE',  ( 3.661933894777869902, -9.674350085358240037, 46.03301114827903717 ) ) ;
#47304=CARTESIAN_POINT ( 'NONE',  ( 0.5835871038041858805, 22.65703148838214176, -41.05963196420492523 ) ) ;
#47306=( BOUNDED_SURFACE ( )  B_SPLINE_SURFACE ( 3, 1, ( 
 ( #3153, #23498 ),
 ( #42627, #32605 ),
 ( #28195, #32924 ),
 ( #61688, #28497 ) ),
 .UNSPECIFIED., .F., .F., .F. ) 
 B_SPLINE_SURFACE_WITH_KNOTS ( ( 4, 4 ),
 ( 2, 2 ),
 ( 0.000000000000000000, 1.000000000000000000 ),
 ( 0.000000000000000000, 1.000000000000000000 ),
 .UNSPECIFIED. ) 
 GEOMETRIC_REPRESENTATION_ITEM ( )  RATIONAL_B_SPLINE_SURFACE ( (
 ( 1.000000000000000000, 1.000000000000000000),
 ( 0.9952954269826590483, 0.8620686068821307169),
 ( 0.9952954269826590483, 0.8620686068821307169),
 ( 1.000000000000000000, 1.000000000000000000) ) ) 
 REPRESENTATION_ITEM ( '' )  SURFACE ( )  );
#47308=CARTESIAN_POINT ( 'NONE',  ( 4.291220156522059348, 31.16808953869599463, 35.32618280841457192 ) ) ;
#47317=B_SPLINE_CURVE_WITH_KNOTS ( 'NONE', 3,
 ( #20104, #20711, #15404, #39851, #16021, #25714 ),
 .UNSPECIFIED., .F., .F.,
 ( 4, 2, 4 ),
 ( 7.757919228897728493E-18, 0.0002291472222819924205, 0.0004582944445639770890 ),
 .UNSPECIFIED. ) ;
#47321=CARTESIAN_POINT ( 'NONE',  ( 0.9762797500689124330, 24.45014227842982635, 34.03697001423955726 ) ) ;
#47325=ORIENTED_EDGE ( 'NONE', *, *, #42852, .F. ) ;
#47328=CARTESIAN_POINT ( 'NONE',  ( 1.157644175074337367, -6.156433857109804286, -41.46203803049500181 ) ) ;
#47336=CARTESIAN_POINT ( 'NONE',  ( 5.896782393890504181, -7.234636363571307349, -18.76662259344776018 ) ) ;
#47339=CARTESIAN_POINT ( 'NONE',  ( 4.291220156522060236, -45.68901888636798247, 11.48488356522638654 ) ) ;
#47353=CARTESIAN_POINT ( 'NONE',  ( 0.9780106845699469975, -34.37272748497746733, -23.97596404107485668 ) ) ;
#47355=CARTESIAN_POINT ( 'NONE',  ( 0.8560838555295158248, 46.60258007729424889, -5.345312359545362213 ) ) ;
#47357=EDGE_LOOP ( 'NONE', ( #61286, #50308, #57025, #43058 ) ) ;
#47359=CARTESIAN_POINT ( 'NONE',  ( 5.895596859100789899, -20.11288567981415909, 0.003583743010676890273 ) ) ;
#47362=CARTESIAN_POINT ( 'NONE',  ( 5.896278296736517710, 20.06757494133108466, -1.348857141599696829 ) ) ;
#47366=CARTESIAN_POINT ( 'NONE',  ( 0.5837157313716030416, 40.39573142367531489, -23.82062019193272917 ) ) ;
#47367=DIRECTION ( 'NONE',  ( -0.07906939808003035641, 0.3507354328807477106, -0.9331305837926522351 ) ) ;
#47370=CARTESIAN_POINT ( 'NONE',  ( 0.5804410086790514622, 42.96136033320072301, -18.81067170986420223 ) ) ;
#47376=EDGE_CURVE ( 'NONE', #42648, #5378, #7466, .T. ) ;
#47377=CARTESIAN_POINT ( 'NONE',  ( 2.282816707992307848, -6.514472263567006927, 46.51944343535488002 ) ) ;
#47386=CARTESIAN_POINT ( 'NONE',  ( 2.618530812446111078, 3.301668998265828048, 46.89163860459656519 ) ) ;
#47392=ORIENTED_EDGE ( 'NONE', *, *, #31753, .T. ) ;
#47399=CARTESIAN_POINT ( 'NONE',  ( 0.8554163680231816613, 27.08908797599198337, -38.30648490452740162 ) ) ;
#47403=ORIENTED_EDGE ( 'NONE', *, *, #61810, .F. ) ;
#47405=CARTESIAN_POINT ( 'NONE',  ( 4.962356264823608143, 37.36413190407361640, 19.36897635181929545 ) ) ;
#47413=VERTEX_POINT ( 'NONE', #17239 ) ;
#47416=ORIENTED_EDGE ( 'NONE', *, *, #15789, .F. ) ;
#47426=CARTESIAN_POINT ( 'NONE',  ( 0.5804410086790514622, -46.06497594411315077, 8.805557513506689915 ) ) ;
#47431=VERTEX_POINT ( 'NONE', #31019 ) ;
#47435=CARTESIAN_POINT ( 'NONE',  ( 2.282816707992308736, -31.31875043000178493, -35.00903937429915658 ) ) ;
#47436=CARTESIAN_POINT ( 'NONE',  ( 0.6064515330803547100, -41.53117911960045916, 21.78291754960180526 ) ) ;
#47438=CARTESIAN_POINT ( 'NONE',  ( 0.6064515330803561532, -20.38298978299800623, -42.23586229193488606 ) ) ;
#47444=CARTESIAN_POINT ( 'NONE',  ( 5.896782393890504181, 3.351618377817360273, -19.83160964539916549 ) ) ;
#47445=CARTESIAN_POINT ( 'NONE',  ( 0.9780106845699487739, 41.90743226373805896, 0.3136359603809434904 ) ) ;
#47447=VERTEX_POINT ( 'NONE', #50127 ) ;
#47453=CARTESIAN_POINT ( 'NONE',  ( 4.958415959904820092, 24.86570830293467438, -38.01184689561937802 ) ) ;
#47454=DIRECTION ( 'NONE',  ( -1.000000000000000000, -0.000000000000000000, -0.000000000000000000 ) ) ;
#47477=EDGE_CURVE ( 'NONE', #9430, #42648, #42912, .T. ) ;
#47478=B_SPLINE_CURVE_WITH_KNOTS ( 'NONE', 3,
 ( #37945, #52295, #28493, #33534 ),
 .UNSPECIFIED., .F., .F.,
 ( 4, 4 ),
 ( 0.000000000000000000, 0.004447772540403792038 ),
 .UNSPECIFIED. ) ;
#47479=CARTESIAN_POINT ( 'NONE',  ( 3.238018933889920792, 2.836920992588773061, -13.09043053720778715 ) ) ;
#47481=CARTESIAN_POINT ( 'NONE',  ( 0.5830082357119540371, 46.89517470974700331, 0.2731737188040911923 ) ) ;
#47482=CARTESIAN_POINT ( 'NONE',  ( 4.956445790444004018, -46.73954499432459642, -5.740468958468717631 ) ) ;
#47493=CARTESIAN_POINT ( 'NONE',  ( 0.5806925824938494740, -1.020860314013172454, 46.88475452172951918 ) ) ;
#47494=CARTESIAN_POINT ( 'NONE',  ( 0.8560838555295223751, -13.02223058219873764, 45.06433561859954295 ) ) ;
#47502=( BOUNDED_SURFACE ( )  B_SPLINE_SURFACE ( 3, 1, ( 
 ( #58026, #47426 ),
 ( #29228, #52412 ),
 ( #28610, #34256 ),
 ( #47736, #48045 ) ),
 .UNSPECIFIED., .F., .F., .F. ) 
 B_SPLINE_SURFACE_WITH_KNOTS ( ( 4, 4 ),
 ( 2, 2 ),
 ( 0.000000000000000000, 1.000000000000000000 ),
 ( 0.000000000000000000, 1.000000000000000000 ),
 .UNSPECIFIED. ) 
 GEOMETRIC_REPRESENTATION_ITEM ( )  RATIONAL_B_SPLINE_SURFACE ( (
 ( 1.000000000000000000, 1.000000000000000000),
 ( 0.9952954269826590483, 0.8620686068821339365),
 ( 0.9952954269826590483, 0.8620686068821339365),
 ( 1.000000000000000000, 1.000000000000000000) ) ) 
 REPRESENTATION_ITEM ( '' )  SURFACE ( )  );
#47506=ORIENTED_EDGE ( 'NONE', *, *, #39033, .T. ) ;
#47510=CARTESIAN_POINT ( 'NONE',  ( 1.231276596079881047, -30.51591784428347154, -28.74118176309054107 ) ) ;
#47511=CARTESIAN_POINT ( 'NONE',  ( 0.5848930533535030563, -34.90273318373162681, -31.32207366527313397 ) ) ;
#47513=ORIENTED_EDGE ( 'NONE', *, *, #52427, .T. ) ;
#47521=CARTESIAN_POINT ( 'NONE',  ( 0.8560838555295158248, -42.27062166135473120, 20.33635607586422012 ) ) ;
#47522=CARTESIAN_POINT ( 'NONE',  ( 0.5848930533535030563, 36.91687493861158487, -28.92088219875856581 ) ) ;
#47523=VERTEX_POINT ( 'NONE', #37281 ) ;
#47528=B_SPLINE_CURVE_WITH_KNOTS ( 'NONE', 3,
 ( #20771, #11687, #40220, #20459 ),
 .UNSPECIFIED., .F., .F.,
 ( 4, 4 ),
 ( 5.421010862427522170E-19, 0.004446298630425085836 ),
 .UNSPECIFIED. ) ;
#47536=EDGE_CURVE ( 'NONE', #37747, #14203, #29119, .T. ) ;
#47542=B_SPLINE_CURVE_WITH_KNOTS ( 'NONE', 3,
 ( #59129, #11234, #39145, #6801 ),
 .UNSPECIFIED., .F., .F.,
 ( 4, 4 ),
 ( 4.336808689942017736E-19, 0.004041751736740997747 ),
 .UNSPECIFIED. ) ;
#47558=B_SPLINE_CURVE_WITH_KNOTS ( 'NONE', 3,
 ( #56442, #12954, #51128, #41772 ),
 .UNSPECIFIED., .F., .F.,
 ( 4, 4 ),
 ( 4.336808689942017736E-19, 0.004041751736740994277 ),
 .UNSPECIFIED. ) ;
#47559=CARTESIAN_POINT ( 'NONE',  ( 0.5806925824938502512, 43.38503874128546300, 17.80339225430713057 ) ) ;
#47561=ORIENTED_EDGE ( 'NONE', *, *, #19611, .T. ) ;
#47562=B_SPLINE_CURVE_WITH_KNOTS ( 'NONE', 3,
 ( #34689, #1443, #58762, #40031 ),
 .UNSPECIFIED., .F., .F.,
 ( 4, 4 ),
 ( 0.000000000000000000, 0.004042984057420972825 ),
 .UNSPECIFIED. ) ;
#47567=ORIENTED_EDGE ( 'NONE', *, *, #28990, .F. ) ;
#47570=CARTESIAN_POINT ( 'NONE',  ( 0.5837157313716019313, -7.710401042972349295, -46.25782938420864099 ) ) ;
#47579=ORIENTED_EDGE ( 'NONE', *, *, #15484, .F. ) ;
#47580=CARTESIAN_POINT ( 'NONE',  ( -4.467299999999999827, 0.000000000000000000, 0.000000000000000000 ) ) ;
#47581=CARTESIAN_POINT ( 'NONE',  ( 0.9791128995231604959, -37.40198472735112034, 18.90579204109574363 ) ) ;
#47604=ORIENTED_EDGE ( 'NONE', *, *, #15506, .T. ) ;
#47606=DIRECTION ( 'NONE',  ( -1.000000000000000000, -0.000000000000000000, -0.000000000000000000 ) ) ;
#47608=CARTESIAN_POINT ( 'NONE',  ( 4.956445790443998689, -10.39006634428300835, 45.93021414603936847 ) ) ;
#47609=B_SPLINE_CURVE_WITH_KNOTS ( 'NONE', 3,
 ( #43679, #24229, #33960, #20165, #10449, #34569 ),
 .UNSPECIFIED., .F., .F.,
 ( 4, 2, 4 ),
 ( 6.892149644104416487E-18, 0.0002291472222819936403, 0.0004582944445639803958 ),
 .UNSPECIFIED. ) ;
#47615=FACE_OUTER_BOUND ( 'NONE', #38438, .T. ) ;
#47619=AXIS2_PLACEMENT_3D ( 'NONE', #51855, #24598, #38407 ) ;
#47620=CARTESIAN_POINT ( 'NONE',  ( 0.9790850452238867296, 20.18493756421641905, 36.72745057571902549 ) ) ;
#47622=CARTESIAN_POINT ( 'NONE',  ( 0.5806925824938499181, -2.112975627976999782, 46.84824112321762613 ) ) ;
#47623=ORIENTED_EDGE ( 'NONE', *, *, #41476, .F. ) ;
#47626=CARTESIAN_POINT ( 'NONE',  ( 4.956445790444029775, 25.79263028817611314, -39.39896284113449809 ) ) ;
#47633=ORIENTED_EDGE ( 'NONE', *, *, #58189, .T. ) ;
#47641=VERTEX_POINT ( 'NONE', #15320 ) ;
#47642=CARTESIAN_POINT ( 'NONE',  ( 4.962356264823608143, 39.61238188121388504, 14.21600504921214814 ) ) ;
#47651=CARTESIAN_POINT ( 'NONE',  ( 5.895596859100789899, 0.6684898708304538584, -20.10177366565161350 ) ) ;
#47654=CARTESIAN_POINT ( 'NONE',  ( 0.5817217712918341110, 43.35050981640732459, -17.88765643302514263 ) ) ;
#47663=CARTESIAN_POINT ( 'NONE',  ( 4.958415959904821868, 12.97383654755002347, -43.53025980924186911 ) ) ;
#47664=CARTESIAN_POINT ( 'NONE',  ( 0.9791128995231600518, -22.55462118696511098, -35.32175671393865457 ) ) ;
#47666=ORIENTED_EDGE ( 'NONE', *, *, #20595, .T. ) ;
#47667=CARTESIAN_POINT ( 'NONE',  ( 4.960386119450136633, 32.76426482034204213, 28.99895542006362703 ) ) ;
#47668=CIRCLE ( 'NONE', #36684, 47.09074272231896430 ) ;
#47673=( BOUNDED_SURFACE ( )  B_SPLINE_SURFACE ( 3, 1, ( 
 ( #49566, #6624 ),
 ( #21691, #12014 ),
 ( #30151, #25772 ),
 ( #45220, #2255 ) ),
 .UNSPECIFIED., .F., .F., .F. ) 
 B_SPLINE_SURFACE_WITH_KNOTS ( ( 4, 4 ),
 ( 2, 2 ),
 ( 0.000000000000000000, 1.000000000000000000 ),
 ( 0.000000000000000000, 1.000000000000000000 ),
 .UNSPECIFIED. ) 
 GEOMETRIC_REPRESENTATION_ITEM ( )  RATIONAL_B_SPLINE_SURFACE ( (
 ( 1.000000000000000000, 1.000000000000000000),
 ( 0.7282232189291694135, 0.9929344683865672927),
 ( 0.7282232189291694135, 0.9929344683865672927),
 ( 1.000000000000000000, 1.000000000000000000) ) ) 
 REPRESENTATION_ITEM ( '' )  SURFACE ( )  );
#47676=EDGE_CURVE ( 'NONE', #46030, #14818, #33814, .T. ) ;
#47680=CARTESIAN_POINT ( 'NONE',  ( 4.956445790444005794, -28.36659270909926533, -37.58822246682746737 ) ) ;
#47690=FACE_OUTER_BOUND ( 'NONE', #55605, .T. ) ;
#47695=CARTESIAN_POINT ( 'NONE',  ( 4.962356264823593044, 12.88441948660167391, 40.06528837230087703 ) ) ;
#47696=EDGE_LOOP ( 'NONE', ( #35916, #1250, #44339, #4263 ) ) ;
#47700=VERTEX_POINT ( 'NONE', #48209 ) ;
#47708=VECTOR ( 'NONE', #43337, 1000.000000000000000 ) ;
#47712=VERTEX_POINT ( 'NONE', #15627 ) ;
#47716=ORIENTED_EDGE ( 'NONE', *, *, #18254, .T. ) ;
#47718=CARTESIAN_POINT ( 'NONE',  ( 2.618530812446111078, 23.81615347600983768, -40.52798567416525088 ) ) ;
#47736=CARTESIAN_POINT ( 'NONE',  ( 5.896782393890504181, 19.70854070425251692, -4.012419492878830596 ) ) ;
#47738=CARTESIAN_POINT ( 'NONE',  ( 4.962356264823593044, 18.10963840443015016, 37.99048031708913697 ) ) ;
#47744=CARTESIAN_POINT ( 'NONE',  ( 5.910764540655178756, -15.77444817831471013, 12.47669920847764580 ) ) ;
#47753=EDGE_CURVE ( 'NONE', #61317, #28755, #51519, .T. ) ;
#47754=CARTESIAN_POINT ( 'NONE',  ( 0.9791128995231609400, 41.90867939003388187, -0.005101912726580280430 ) ) ;
#47763=CARTESIAN_POINT ( 'NONE',  ( 0.8560838555295158248, -45.77741231505087427, -10.23725333375899105 ) ) ;
#47770=CARTESIAN_POINT ( 'NONE',  ( 4.960386119450151732, -34.04466635746562986, -27.48448939458741691 ) ) ;
#47771=CARTESIAN_POINT ( 'NONE',  ( 0.8560838555295223751, 9.983184696771347788, -45.83349056521751663 ) ) ;
#47782=EDGE_CURVE ( 'NONE', #10104, #13648, #5135, .T. ) ;
#47789=ORIENTED_EDGE ( 'NONE', *, *, #30455, .T. ) ;
#47794=CARTESIAN_POINT ( 'NONE',  ( 0.5782707292762423457, -35.26595510591648974, -30.92003823049223143 ) ) ;
#47801=CARTESIAN_POINT ( 'NONE',  ( 4.958415959904820092, 19.57736038521061417, -40.98696029434518096 ) ) ;
#47815=EDGE_CURVE ( 'NONE', #23761, #539, #12731, .T. ) ;
#47817=CARTESIAN_POINT ( 'NONE',  ( 1.231276596079881935, -34.07446381689681658, -24.41736444846283405 ) ) ;
#47818=EDGE_LOOP ( 'NONE', ( #42896, #46040, #18576, #25672 ) ) ;
#47835=ADVANCED_FACE ( 'NONE', ( #19867 ), #60550, .F. ) ;
#47842=FACE_OUTER_BOUND ( 'NONE', #14964, .T. ) ;
#47844=LINE ( 'NONE', #61595, #2793 ) ;
#47855=EDGE_LOOP ( 'NONE', ( #48284, #59036, #38132, #44140 ) ) ;
#47863=( BOUNDED_SURFACE ( )  B_SPLINE_SURFACE ( 3, 1, ( 
 ( #13493, #41704 ),
 ( #4049, #32597 ),
 ( #51681, #47308 ),
 ( #47017, #23191 ) ),
 .UNSPECIFIED., .F., .F., .F. ) 
 B_SPLINE_SURFACE_WITH_KNOTS ( ( 4, 4 ),
 ( 2, 2 ),
 ( 0.000000000000000000, 1.000000000000000000 ),
 ( 0.000000000000000000, 1.000000000000000000 ),
 .UNSPECIFIED. ) 
 GEOMETRIC_REPRESENTATION_ITEM ( )  RATIONAL_B_SPLINE_SURFACE ( (
 ( 1.000000000000000000, 1.000000000000000000),
 ( 0.7282232189291694135, 0.9929344683865672927),
 ( 0.7282232189291694135, 0.9929344683865672927),
 ( 1.000000000000000000, 1.000000000000000000) ) ) 
 REPRESENTATION_ITEM ( '' )  SURFACE ( )  );
#47867=CIRCLE ( 'NONE', #20848, 47.09074272231896430 ) ;
#47868=CARTESIAN_POINT ( 'NONE',  ( 0.9762797500689124330, 40.28286501695569655, 11.55922018180428168 ) ) ;
#47871=CARTESIAN_POINT ( 'NONE',  ( 5.917102823773431552, -2.004558746498307453, -20.01178308606155554 ) ) ;
#47872=CARTESIAN_POINT ( 'NONE',  ( 0.5834584762367743815, -25.08023035601203077, -39.62597676149527359 ) ) ;
#47880=CARTESIAN_POINT ( 'NONE',  ( 5.894904586330512508, -4.663773726906393691, 19.56472914931000417 ) ) ;
#47883=ORIENTED_EDGE ( 'NONE', *, *, #37418, .F. ) ;
#47885=EDGE_CURVE ( 'NONE', #50643, #8101, #43061, .T. ) ;
#47887=CARTESIAN_POINT ( 'NONE',  ( 1.231276596079887264, 41.91134057782999633, -0.8463462572780159343 ) ) ;
#47891=CARTESIAN_POINT ( 'NONE',  ( 0.5806925824938502512, -46.82446035038566379, -2.586943222941716858 ) ) ;
#47894=VECTOR ( 'NONE', #7965, 1000.000000000000341 ) ;
#47897=VERTEX_POINT ( 'NONE', #42445 ) ;
#47900=CARTESIAN_POINT ( 'NONE',  ( 5.917102823773431552, 8.458006992050780326, 18.24696785151336087 ) ) ;
#47902=ORIENTED_EDGE ( 'NONE', *, *, #32456, .F. ) ;
#47906=CARTESIAN_POINT ( 'NONE',  ( 4.956445790443991584, 34.56007374686787159, 31.98654955994301829 ) ) ;
#47910=EDGE_CURVE ( 'NONE', #6891, #36980, #20918, .T. ) ;
#47916=CARTESIAN_POINT ( 'NONE',  ( 0.5824935313925965197, -42.01861599602651864, -20.82484302059208403 ) ) ;
#47918=CARTESIAN_POINT ( 'NONE',  ( 0.9754292580325136797, 41.90451261907242042, 0.5824852461694604022 ) ) ;
#47923=DIRECTION ( 'NONE',  ( 0.000000000000000000, 0.000000000000000000, 1.000000000000000000 ) ) ;
#47924=B_SPLINE_CURVE_WITH_KNOTS ( 'NONE', 3,
 ( #52201, #56596, #9601, #13713 ),
 .UNSPECIFIED., .F., .F.,
 ( 4, 4 ),
 ( 1.409462824231155764E-18, 0.004446298630425058948 ),
 .UNSPECIFIED. ) ;
#47927=CARTESIAN_POINT ( 'NONE',  ( 0.5806925824938499181, 40.62497527030964051, -23.42720099863178973 ) ) ;
#47929=CARTESIAN_POINT ( 'NONE',  ( 0.6845945791218034371, 17.66463248440769718, -43.45534811625321225 ) ) ;
#47930=EDGE_CURVE ( 'NONE', #60718, #26211, #31350, .T. ) ;
#47937=CARTESIAN_POINT ( 'NONE',  ( 0.5782707292762423457, 39.98024706216853019, -24.52174950030242684 ) ) ;
#47956=CARTESIAN_POINT ( 'NONE',  ( 0.5848930533535030563, 45.18167862054185235, 12.56538894812371332 ) ) ;
#47958=CARTESIAN_POINT ( 'NONE',  ( 0.9762797500689124330, 35.79768877047989406, -21.79105926469756938 ) ) ;
#47961=CARTESIAN_POINT ( 'NONE',  ( 5.896278296736517710, 20.06830682785023612, -1.337924017888618256 ) ) ;
#47963=CARTESIAN_POINT ( 'NONE',  ( 0.5832655196449157975, 16.64216000364581305, 43.84374178131214705 ) ) ;
#47971=ORIENTED_EDGE ( 'NONE', *, *, #3147, .T. ) ;
#47973=FACE_OUTER_BOUND ( 'NONE', #33571, .T. ) ;
#47974=( BOUNDED_SURFACE ( )  B_SPLINE_SURFACE ( 3, 1, ( 
 ( #2754, #55676 ),
 ( #13414, #60083 ),
 ( #8374, #36611 ),
 ( #26572, #32521 ) ),
 .UNSPECIFIED., .F., .F., .F. ) 
 B_SPLINE_SURFACE_WITH_KNOTS ( ( 4, 4 ),
 ( 2, 2 ),
 ( 0.000000000000000000, 1.000000000000000000 ),
 ( 0.000000000000000000, 1.000000000000000000 ),
 .UNSPECIFIED. ) 
 GEOMETRIC_REPRESENTATION_ITEM ( )  RATIONAL_B_SPLINE_SURFACE ( (
 ( 1.000000000000000000, 1.000000000000000000),
 ( 0.9952954269826590483, 0.8620686068821339365),
 ( 0.9952954269826590483, 0.8620686068821339365),
 ( 1.000000000000000000, 1.000000000000000000) ) ) 
 REPRESENTATION_ITEM ( '' )  SURFACE ( )  );
#47984=FACE_OUTER_BOUND ( 'NONE', #42409, .T. ) ;
#47988=B_SPLINE_CURVE_WITH_KNOTS ( 'NONE', 3,
 ( #14980, #52544, #9638, #28749, #58160, #47872, #15283, #4921, #34389, #44124, #29666, #14670, #34091, #48467, #214, #57533 ),
 .UNSPECIFIED., .F., .F.,
 ( 4, 3, 3, 3, 3, 4 ),
 ( 1.250973872328959318E-17, 0.0002732102107931917343, 0.0004098135523333763298, 0.0005464168938824918781, 0.0008195847345945395405, 0.001092771384553104181 ),
 .UNSPECIFIED. ) ;
#47990=CARTESIAN_POINT ( 'NONE',  ( 0.9762797500689124330, -39.42083772998312696, -14.22400568939859866 ) ) ;
#47999=CARTESIAN_POINT ( 'NONE',  ( -69.95594261585600293, 0.000000000000000000, 0.000000000000000000 ) ) ;
#48003=EDGE_CURVE ( 'NONE', #39646, #21594, #32136, .T. ) ;
#48005=ORIENTED_EDGE ( 'NONE', *, *, #40620, .F. ) ;
#48009=ORIENTED_EDGE ( 'NONE', *, *, #12752, .F. ) ;
#48016=VERTEX_POINT ( 'NONE', #11379 ) ;
#48019=ORIENTED_EDGE ( 'NONE', *, *, #45080, .T. ) ;
#48033=VECTOR ( 'NONE', #24082, 1000.000000000000114 ) ;
#48040=VERTEX_POINT ( 'NONE', #59278 ) ;
#48043=EDGE_CURVE ( 'NONE', #32533, #57834, #25350, .T. ) ;
#48045=CARTESIAN_POINT ( 'NONE',  ( 0.8554163680231708922, -46.15020320557310640, 8.447734441619822121 ) ) ;
#48048=LINE ( 'NONE', #5098, #18657 ) ;
#48049=CARTESIAN_POINT ( 'NONE',  ( 1.091591847532197956, 33.37174725983657453, -25.35913002808713301 ) ) ;
#48051=ORIENTED_EDGE ( 'NONE', *, *, #1373, .T. ) ;
#48056=CARTESIAN_POINT ( 'NONE',  ( 0.7056313189692664523, -41.47346934225711834, 21.90205434826647490 ) ) ;
#48060=CARTESIAN_POINT ( 'NONE',  ( 4.291220156522059348, -28.73895862173575821, -37.32909394351617749 ) ) ;
#48071=CARTESIAN_POINT ( 'NONE',  ( 0.9762797500689124330, 19.69530149098661909, 36.99215976885973589 ) ) ;
#48079=CARTESIAN_POINT ( 'NONE',  ( 1.231276596079881935, 38.91607545535268997, -15.58254928345689017 ) ) ;
#48080=ORIENTED_EDGE ( 'NONE', *, *, #9400, .T. ) ;
#48086=VERTEX_POINT ( 'NONE', #55507 ) ;
#48088=LINE ( 'NONE', #10179, #43214 ) ;
#48099=CARTESIAN_POINT ( 'NONE',  ( 2.528100132419517365, -5.786187675422820753, 41.57852583746639397 ) ) ;
#48102=VERTEX_POINT ( 'NONE', #17628 ) ;
#48109=CARTESIAN_POINT ( 'NONE',  ( 0.5806925824938502512, 28.25565086187734920, 37.42780459384778879 ) ) ;
#48112=ORIENTED_EDGE ( 'NONE', *, *, #29156, .F. ) ;
#48113=ORIENTED_EDGE ( 'NONE', *, *, #40702, .T. ) ;
#48116=ADVANCED_FACE ( 'NONE', ( #46452 ), #11736, .F. ) ;
#48123=CARTESIAN_POINT ( 'NONE',  ( 0.5797568599927149791, -44.09074186209018364, -15.97597542316375119 ) ) ;
#48143=B_SPLINE_CURVE_WITH_KNOTS ( 'NONE', 3,
 ( #28724, #13717, #56907, #19040, #24025, #4579 ),
 .UNSPECIFIED., .F., .F.,
 ( 4, 2, 4 ),
 ( 7.208110037058612184E-18, 0.0002291472222819933421, 0.0004582944445639794743 ),
 .UNSPECIFIED. ) ;
#48147=CARTESIAN_POINT ( 'NONE',  ( 4.962356264823608143, 41.32726869310149453, -7.955655864260332777 ) ) ;
#48154=CARTESIAN_POINT ( 'NONE',  ( 0.9754292580325134576, -11.85895070474203195, -40.19568080138092370 ) ) ;
#48156=CARTESIAN_POINT ( 'NONE',  ( 1.231276596079881047, -0.5545928549373742023, -41.91621640586514985 ) ) ;
#48163=DIRECTION ( 'NONE',  ( 0.000000000000000000, 0.000000000000000000, 1.000000000000000000 ) ) ;
#48164=CARTESIAN_POINT ( 'NONE',  ( 5.894904586330512508, -11.93156318453012332, 16.19157842939372216 ) ) ;
#48166=CONICAL_SURFACE ( 'NONE', #38212, 42.08604991992415023, 1.569615340895231137 ) ;
#48173=ADVANCED_FACE ( 'NONE', ( #56433 ), #43777, .F. ) ;
#48176=B_SPLINE_CURVE_WITH_KNOTS ( 'NONE', 3,
 ( #8790, #22595, #3457, #23206 ),
 .UNSPECIFIED., .F., .F.,
 ( 4, 4 ),
 ( 0.000000000000000000, 0.004447772540403838876 ),
 .UNSPECIFIED. ) ;
#48186=CARTESIAN_POINT ( 'NONE',  ( 5.901463166500146684, 19.00451910135517508, 6.583777340316350646 ) ) ;
#48187=CARTESIAN_POINT ( 'NONE',  ( 5.895881250540457863, 18.99851645375293785, 6.601822033710092796 ) ) ;
#48188=CARTESIAN_POINT ( 'NONE',  ( 1.231276596079887264, -16.87422718933211030, 38.37365278131431268 ) ) ;
#48192=CARTESIAN_POINT ( 'NONE',  ( 0.9762797500689124330, -7.469026406145721886, -41.23758515880873432 ) ) ;
#48196=ORIENTED_EDGE ( 'NONE', *, *, #41476, .T. ) ;
#48209=CARTESIAN_POINT ( 'NONE',  ( 0.8560838555295223751, 9.983184696771347788, -45.83349056521751663 ) ) ;
#48212=CARTESIAN_POINT ( 'NONE',  ( 5.901463166500145796, -7.242130809805398250, 18.76351277544543450 ) ) ;
#48222=CARTESIAN_POINT ( 'NONE',  ( 1.231276596079881047, 20.88402890667877898, -36.34740854095476692 ) ) ;
#48223=B_SPLINE_CURVE_WITH_KNOTS ( 'NONE', 3,
 ( #28851, #322, #23, #9744, #33572, #9431 ),
 .UNSPECIFIED., .F., .F.,
 ( 4, 2, 4 ),
 ( 6.805474077711127748E-18, 0.0002291472222819918513, 0.0004582944445639769264 ),
 .UNSPECIFIED. ) ;
#48224=( BOUNDED_SURFACE ( )  B_SPLINE_SURFACE ( 3, 1, ( 
 ( #24637, #5193 ),
 ( #500, #4571 ),
 ( #48744, #47522 ),
 ( #14025, #19641 ) ),
 .UNSPECIFIED., .F., .F., .F. ) 
 B_SPLINE_SURFACE_WITH_KNOTS ( ( 4, 4 ),
 ( 2, 2 ),
 ( 0.000000000000000000, 1.000000000000000000 ),
 ( 0.000000000000000000, 1.000000000000000000 ),
 .UNSPECIFIED. ) 
 GEOMETRIC_REPRESENTATION_ITEM ( )  RATIONAL_B_SPLINE_SURFACE ( (
 ( 1.000000000000000000, 1.000000000000000000),
 ( 0.9729067724841187204, 0.9999501103223794596),
 ( 0.9729067724841187204, 0.9999501103223794596),
 ( 1.000000000000000000, 1.000000000000000000) ) ) 
 REPRESENTATION_ITEM ( '' )  SURFACE ( )  );
#48232=CARTESIAN_POINT ( 'NONE',  ( 0.9789889208857693870, -34.49671343044144578, 23.79730364012634070 ) ) ;
#48233=CARTESIAN_POINT ( 'NONE',  ( 1.231276596079881047, -6.136529359146127405, -41.46829847537036784 ) ) ;
#48237=EDGE_CURVE ( 'NONE', #25596, #48917, #25230, .T. ) ;
#48243=ORIENTED_EDGE ( 'NONE', *, *, #6408, .F. ) ;
#48245=CARTESIAN_POINT ( 'NONE',  ( 2.282816707992320282, 26.79502893056672264, -38.58138658755097339 ) ) ;
#48261=CARTESIAN_POINT ( 'NONE',  ( 3.661921753702003457, -47.02171908594613825, -1.260578453094312934 ) ) ;
#48262=EDGE_LOOP ( 'NONE', ( #42978, #22889, #7326, #25430 ) ) ;
#48275=CARTESIAN_POINT ( 'NONE',  ( 1.231276596079887264, 25.54232633153331733, 33.23952972879620660 ) ) ;
#48276=ORIENTED_EDGE ( 'NONE', *, *, #41173, .T. ) ;
#48277=CARTESIAN_POINT ( 'NONE',  ( 2.282803330402963571, -20.95673854281690751, 42.03941028493377274 ) ) ;
#48282=CARTESIAN_POINT ( 'NONE',  ( 2.891212509699203626, -1.730266096895115631E-16, -41.99381090189411481 ) ) ;
#48284=ORIENTED_EDGE ( 'NONE', *, *, #8137, .F. ) ;
#48290=VECTOR ( 'NONE', #15003, 1000.000000000000114 ) ;
#48291=CARTESIAN_POINT ( 'NONE',  ( 3.661921753702002125, 24.23902541992542936, 40.31253862666358145 ) ) ;
#48299=CARTESIAN_POINT ( 'NONE',  ( 0.5824935313925970748, -1.202929742068020502, 46.88060512716833017 ) ) ;
#48305=ORIENTED_EDGE ( 'NONE', *, *, #15160, .T. ) ;
#48316=EDGE_CURVE ( 'NONE', #27840, #31862, #1890, .T. ) ;
#48325=CIRCLE ( 'NONE', #35333, 47.09074272231896430 ) ;
#48330=CARTESIAN_POINT ( 'NONE',  ( 0.8554163680231738898, 23.34472558242499929, -40.69679668712380050 ) ) ;
#48337=CARTESIAN_POINT ( 'NONE',  ( 4.962356264823608143, 27.50309822711080443, -31.85616401533997077 ) ) ;
#48343=CARTESIAN_POINT ( 'NONE',  ( 5.896782393890504181, 10.82771479451271368, 16.94953330350728748 ) ) ;
#48350=CARTESIAN_POINT ( 'NONE',  ( 0.8560838555295158248, -35.39593983670192756, 30.78149244527153883 ) ) ;
#48356=B_SPLINE_CURVE_WITH_KNOTS ( 'NONE', 3,
 ( #44919, #55505, #50507, #7580 ),
 .UNSPECIFIED., .F., .F.,
 ( 4, 4 ),
 ( 3.252606517456513302E-19, 0.004446298630425065020 ),
 .UNSPECIFIED. ) ;
#48362=CARTESIAN_POINT ( 'NONE',  ( 4.962356264823603702, -10.17958088187380739, -40.83640203215431086 ) ) ;
#48363=CARTESIAN_POINT ( 'NONE',  ( 1.092182651088185130, 3.417759894675622245, -41.77415590702738513 ) ) ;
#48368=CARTESIAN_POINT ( 'NONE',  ( 0.5804410086790514622, 37.14246315962216016, 28.63489623329385125 ) ) ;
#48371=DIRECTION ( 'NONE',  ( 0.000000000000000000, 0.000000000000000000, 1.000000000000000000 ) ) ;
#48378=EDGE_LOOP ( 'NONE', ( #22709, #45736, #46116, #2788 ) ) ;
#48385=B_SPLINE_CURVE_WITH_KNOTS ( 'NONE', 3,
 ( #57357, #27338, #13878, #51747 ),
 .UNSPECIFIED., .F., .F.,
 ( 4, 4 ),
 ( 5.721958498152796815E-17, 0.005004948556313859077 ),
 .UNSPECIFIED. ) ;
#48386=ORIENTED_EDGE ( 'NONE', *, *, #48003, .T. ) ;
#48388=AXIS2_PLACEMENT_3D ( 'NONE', #23006, #61188, #56490 ) ;
#48391=ORIENTED_EDGE ( 'NONE', *, *, #51843, .T. ) ;
#48392=VERTEX_POINT ( 'NONE', #26632 ) ;
#48395=CARTESIAN_POINT ( 'NONE',  ( 4.962356264823608143, 0.000000000000000000, 0.000000000000000000 ) ) ;
#48397=EDGE_CURVE ( 'NONE', #21951, #13149, #23032, .T. ) ;
#48399=CARTESIAN_POINT ( 'NONE',  ( 0.8560838555295158248, -20.57050347530512724, 42.15717282805135113 ) ) ;
#48406=EDGE_LOOP ( 'NONE', ( #45581, #34787, #31754, #46346 ) ) ;
#48411=ORIENTED_EDGE ( 'NONE', *, *, #59521, .F. ) ;
#48414=CARTESIAN_POINT ( 'NONE',  ( 4.956445790444027999, 19.33052208089617352, -42.94029536716791995 ) ) ;
#48416=FACE_OUTER_BOUND ( 'NONE', #24051, .T. ) ;
#48419=EDGE_LOOP ( 'NONE', ( #6411, #16420 ) ) ;
#48423=ORIENTED_EDGE ( 'NONE', *, *, #3376, .T. ) ;
#48425=CARTESIAN_POINT ( 'NONE',  ( 3.238018933889920792, -12.74072440564281017, 4.132969149063494108 ) ) ;
#48429=CARTESIAN_POINT ( 'NONE',  ( 0.8560838555295158248, -38.14845555156047396, -27.29593693413630362 ) ) ;
#48434=ADVANCED_FACE ( 'NONE', ( #21325 ), #60925, .F. ) ;
#48437=CARTESIAN_POINT ( 'NONE',  ( 3.376099380956838925, -13.03750648666899181, -3.119584626537831085 ) ) ;
#48444=CARTESIAN_POINT ( 'NONE',  ( 4.291220156522060236, 29.64992983783088931, 36.60970715421529320 ) ) ;
#48449=VERTEX_POINT ( 'NONE', #12870 ) ;
#48456=FACE_OUTER_BOUND ( 'NONE', #7162, .T. ) ;
#48458=ORIENTED_EDGE ( 'NONE', *, *, #33567, .F. ) ;
#48459=AXIS2_PLACEMENT_3D ( 'NONE', #4384, #22924, #33873 ) ;
#48467=CARTESIAN_POINT ( 'NONE',  ( 0.5824935313925946323, -25.54019697864863758, -39.33111383301602615 ) ) ;
#48468=ORIENTED_EDGE ( 'NONE', *, *, #45769, .T. ) ;
#48480=CARTESIAN_POINT ( 'NONE',  ( 5.901463166500145796, 16.58986915973337517, -11.37075686150944165 ) ) ;
#48484=AXIS2_PLACEMENT_3D ( 'NONE', #55285, #31821, #50905 ) ;
#48486=CARTESIAN_POINT ( 'NONE',  ( 5.896278296736517710, -9.670675947513094783, 17.63533402951516038 ) ) ;
#48487=EDGE_LOOP ( 'NONE', ( #8126, #56399, #14242, #44466 ) ) ;
#48489=CARTESIAN_POINT ( 'NONE',  ( 0.9787284016396619046, 35.96249882395619579, -21.51824057086865949 ) ) ;
#48499=EDGE_CURVE ( 'NONE', #45323, #30629, #11043, .T. ) ;
#48501=DIRECTION ( 'NONE',  ( 0.000000000000000000, 0.000000000000000000, 1.000000000000000000 ) ) ;
#48510=FACE_OUTER_BOUND ( 'NONE', #57789, .T. ) ;
#48512=AXIS2_PLACEMENT_3D ( 'NONE', #17491, #31586, #26259 ) ;
#48515=AXIS2_PLACEMENT_3D ( 'NONE', #37501, #55331, #46282 ) ;
#48523=ADVANCED_FACE ( 'NONE', ( #29711 ), #15756, .F. ) ;
#48525=CARTESIAN_POINT ( 'NONE',  ( 0.9772918015221172539, -34.31474319015040919, 24.05899531453268736 ) ) ;
#48527=CARTESIAN_POINT ( 'NONE',  ( 5.896278296736517710, 3.350760724586278272, 19.83177708075989898 ) ) ;
#48528=EDGE_CURVE ( 'NONE', #22660, #37333, #21579, .T. ) ;
#48529=ORIENTED_EDGE ( 'NONE', *, *, #52383, .T. ) ;
#48530=CARTESIAN_POINT ( 'NONE',  ( 0.9762797500689124330, 24.45014227842982635, 34.03697001423955726 ) ) ;
#48535=VERTEX_POINT ( 'NONE', #15024 ) ;
#48536=CARTESIAN_POINT ( 'NONE',  ( 4.962356264823608143, 7.429277797797782412, -41.42513040734446861 ) ) ;
#48537=CARTESIAN_POINT ( 'NONE',  ( 5.910764540655178756, -15.79365219732140524, -12.45238084621602326 ) ) ;
#48539=CARTESIAN_POINT ( 'NONE',  ( 1.091591847532193738, 38.27654012929355076, 17.07821614473897398 ) ) ;
#48543=CIRCLE ( 'NONE', #58542, 42.08604991992415023 ) ;
#48544=CARTESIAN_POINT ( 'NONE',  ( 0.9754292589017242721, 15.60437141757889634, 38.89512899525495015 ) ) ;
#48545=VERTEX_POINT ( 'NONE', #58205 ) ;
#48550=VERTEX_POINT ( 'NONE', #15329 ) ;
#48551=CARTESIAN_POINT ( 'NONE',  ( 3.238018933889920792, 1.066824900592079794, -13.35175557741863450 ) ) ;
#48556=B_SPLINE_CURVE_WITH_KNOTS ( 'NONE', 3,
 ( #28782, #252, #29396, #15014, #33815, #14703 ),
 .UNSPECIFIED., .F., .F.,
 ( 4, 2, 4 ),
 ( 3.471140604459641645E-18, 0.0002291459268755735145, 0.0004582918537511435596 ),
 .UNSPECIFIED. ) ;
#48558=CARTESIAN_POINT ( 'NONE',  ( 0.9780303403264761775, 19.85596553096524985, -36.90637135005560765 ) ) ;
#48561=B_SPLINE_CURVE_WITH_KNOTS ( 'NONE', 3,
 ( #24726, #52914, #10950, #29417, #272, #47927 ),
 .UNSPECIFIED., .F., .F.,
 ( 4, 2, 4 ),
 ( 1.197050036191770715E-16, 0.0002448718616795901148, 0.0004897437233590605336 ),
 .UNSPECIFIED. ) ;
#48573=ADVANCED_FACE ( 'NONE', ( #1499 ), #5290, .F. ) ;
#48575=ORIENTED_EDGE ( 'NONE', *, *, #56212, .F. ) ;
#48578=VERTEX_POINT ( 'NONE', #60360 ) ;
#48579=CARTESIAN_POINT ( 'NONE',  ( 0.9784957157296357844, -12.63863412949661758, -39.95745217519625925 ) ) ;
#48584=ADVANCED_FACE ( 'NONE', ( #45085 ), #18132, .F. ) ;
#48586=CARTESIAN_POINT ( 'NONE',  ( 5.838029081930957709, 1.558325986592992818, -47.20843863413011832 ) ) ;
#48588=CARTESIAN_POINT ( 'NONE',  ( 0.9762797500689124330, 41.46413394121043439, -6.086902470967093137 ) ) ;
#48595=CARTESIAN_POINT ( 'NONE',  ( 0.6064515330803583737, 46.56800900943660082, 5.545707613471479114 ) ) ;
#48601=CARTESIAN_POINT ( 'NONE',  ( 0.5830082357119560355, -1.840022353388820919, 46.85985864978006532 ) ) ;
#48607=CARTESIAN_POINT ( 'NONE',  ( 0.9785694773339244090, -1.622802894008406271, 41.87722431682728086 ) ) ;
#48609=ORIENTED_EDGE ( 'NONE', *, *, #13387, .T. ) ;
#48610=DIRECTION ( 'NONE',  ( -0.07906939808003035641, -0.02523889567981928844, 0.9965495614529791268 ) ) ;
#48612=B_SPLINE_CURVE_WITH_KNOTS ( 'NONE', 3,
 ( #57002, #4358, #23495, #18195 ),
 .UNSPECIFIED., .F., .F.,
 ( 4, 4 ),
 ( 0.000000000000000000, 0.005004948556313816577 ),
 .UNSPECIFIED. ) ;
#48625=CARTESIAN_POINT ( 'NONE',  ( 0.9783242366443551941, -17.39724996613036012, -38.12702694706867845 ) ) ;
#48634=CARTESIAN_POINT ( 'NONE',  ( 5.896782393890504181, -7.234636363571307349, -18.76662259344776018 ) ) ;
#48635=LINE ( 'NONE', #4774, #4217 ) ;
#48651=EDGE_CURVE ( 'NONE', #38898, #36353, #10262, .T. ) ;
#48655=EDGE_CURVE ( 'NONE', #5070, #47280, #33438, .T. ) ;
#48664=CARTESIAN_POINT ( 'NONE',  ( 5.896782393890504181, 19.00205529748287248, 6.591508275760228130 ) ) ;
#48668=ORIENTED_EDGE ( 'NONE', *, *, #41633, .F. ) ;
#48669=B_SPLINE_CURVE_WITH_KNOTS ( 'NONE', 3,
 ( #34287, #433, #58668, #20194 ),
 .UNSPECIFIED., .F., .F.,
 ( 4, 4 ),
 ( 5.157703690291707425E-17, 0.005004948556313851271 ),
 .UNSPECIFIED. ) ;
#48688=CARTESIAN_POINT ( 'NONE',  ( 5.896782393890504181, -13.98685533979025131, 14.45316451791071266 ) ) ;
#48695=ORIENTED_EDGE ( 'NONE', *, *, #14173, .T. ) ;
#48697=( BOUNDED_SURFACE ( )  B_SPLINE_SURFACE ( 3, 1, ( 
 ( #45595, #51193 ),
 ( #50274, #12704 ),
 ( #50888, #35587 ),
 ( #59663, #49970 ) ),
 .UNSPECIFIED., .F., .F., .F. ) 
 B_SPLINE_SURFACE_WITH_KNOTS ( ( 4, 4 ),
 ( 2, 2 ),
 ( 0.000000000000000000, 1.000000000000000000 ),
 ( 0.000000000000000000, 1.000000000000000000 ),
 .UNSPECIFIED. ) 
 GEOMETRIC_REPRESENTATION_ITEM ( )  RATIONAL_B_SPLINE_SURFACE ( (
 ( 1.000000000000000000, 1.000000000000000000),
 ( 0.9729067724841187204, 0.9999501103223794596),
 ( 0.9729067724841187204, 0.9999501103223794596),
 ( 1.000000000000000000, 1.000000000000000000) ) ) 
 REPRESENTATION_ITEM ( '' )  SURFACE ( )  );
#48704=CARTESIAN_POINT ( 'NONE',  ( 0.9775691876210972353, -40.99194725836810704, -8.717451976188911544 ) ) ;
#48706=CARTESIAN_POINT ( 'NONE',  ( 0.5797568599927148680, -29.79412097160983208, -36.21513032145659139 ) ) ;
#48708=ORIENTED_EDGE ( 'NONE', *, *, #28555, .F. ) ;
#48710=CARTESIAN_POINT ( 'NONE',  ( 3.782542959838394836, 37.01845254676131702, -19.92164713169448120 ) ) ;
#48714=CARTESIAN_POINT ( 'NONE',  ( 0.8560838555295223751, -0.6537497281626496459, 46.90357604036880446 ) ) ;
#48720=CARTESIAN_POINT ( 'NONE',  ( 0.9762797500689124330, -37.62962005162893320, -18.44821075215020656 ) ) ;
#48721=VERTEX_POINT ( 'NONE', #8995 ) ;
#48723=ADVANCED_FACE ( 'NONE', ( #41922 ), #41756, .F. ) ;
#48724=CIRCLE ( 'NONE', #10728, 47.09074272231896430 ) ;
#48738=CARTESIAN_POINT ( 'NONE',  ( 0.5806925824938502512, 45.37089516811273882, 11.86188155343358197 ) ) ;
#48743=CARTESIAN_POINT ( 'NONE',  ( 0.9784957157296363395, 41.56508225881332663, 5.355090457728283404 ) ) ;
#48744=CARTESIAN_POINT ( 'NONE',  ( 5.894904586330512508, -15.78384355525793836, 12.46594138782888628 ) ) ;
#48746=CARTESIAN_POINT ( 'NONE',  ( 4.958415959904820092, 45.28449214630080633, 3.538181012081810461 ) ) ;
#48747=CARTESIAN_POINT ( 'NONE',  ( 4.956445790443989807, 42.27038699792205279, 20.75457619864928205 ) ) ;
#48751=CARTESIAN_POINT ( 'NONE',  ( 0.5782707292762442330, 33.12197115878082343, -33.20649605520746661 ) ) ;
#48752=B_SPLINE_CURVE_WITH_KNOTS ( 'NONE', 3,
 ( #24539, #18938, #24228, #33347 ),
 .UNSPECIFIED., .F., .F.,
 ( 4, 4 ),
 ( 6.505213034913026604E-19, 0.004041751736740997747 ),
 .UNSPECIFIED. ) ;
#48757=CARTESIAN_POINT ( 'NONE',  ( 1.000110580585052311, -11.78687190425167941, -40.21799514501766737 ) ) ;
#48759=EDGE_LOOP ( 'NONE', ( #6877, #57998, #25434, #40017 ) ) ;
#48772=CARTESIAN_POINT ( 'NONE',  ( 0.5848930533535030563, -13.72019472029248099, -44.84450177251183334 ) ) ;
#48775=B_SPLINE_CURVE_WITH_KNOTS ( 'NONE', 3,
 ( #33020, #4457, #9805, #23295, #61477, #19226, #29521, #23594, #4158, #42421, #28908, #18599, #38337, #9184, #378, #42722, #61782, #38043, #14219 ),
 .UNSPECIFIED., .F., .F.,
 ( 4, 3, 3, 3, 3, 3, 4 ),
 ( 6.939740885162003740E-18, 0.0002732106629380618898, 0.0004098138914053761368, 0.0005464171197651466897, 0.0006830203481512586933, 0.0008196235766963615730, 0.001011968216111140944 ),
 .UNSPECIFIED. ) ;
#48776=VECTOR ( 'NONE', #24310, 1000.000000000000000 ) ;
#48777=CYLINDRICAL_SURFACE ( 'NONE', #31794, 12.50000000000000000 ) ;
#48780=CARTESIAN_POINT ( 'NONE',  ( 0.5824936645240080813, 43.03133214971953890, 18.64249533889771726 ) ) ;
#48781=ORIENTED_EDGE ( 'NONE', *, *, #41440, .T. ) ;
#48783=EDGE_CURVE ( 'NONE', #1414, #35778, #47844, .T. ) ;
#48785=ORIENTED_EDGE ( 'NONE', *, *, #27378, .F. ) ;
#48788=ORIENTED_EDGE ( 'NONE', *, *, #60357, .F. ) ;
#48789=CARTESIAN_POINT ( 'NONE',  ( 5.896782393890504181, -17.30187591025955030, -10.25529994022567237 ) ) ;
#48797=CARTESIAN_POINT ( 'NONE',  ( 5.901463166500146684, -7.242130809805130021, -18.76351277544553753 ) ) ;
#48801=CARTESIAN_POINT ( 'NONE',  ( 0.8554163680231720024, 21.74163052365390669, -41.57531689939042963 ) ) ;
#48805=CARTESIAN_POINT ( 'NONE',  ( 5.838029081930955932, 1.558325986592309587, 47.20843863413013253 ) ) ;
#48812=EDGE_LOOP ( 'NONE', ( #45380, #11762, #9483, #36564 ) ) ;
#48821=ORIENTED_EDGE ( 'NONE', *, *, #44588, .F. ) ;
#48826=CARTESIAN_POINT ( 'NONE',  ( 5.896782393890504181, 0.6784186533438157918, 20.10138888258240186 ) ) ;
#48831=DIRECTION ( 'NONE',  ( -1.000000000000000000, -0.000000000000000000, -0.000000000000000000 ) ) ;
#48834=CARTESIAN_POINT ( 'NONE',  ( 5.896278296736517710, 17.95357321928074512, -9.066211351733914015 ) ) ;
#48843=CARTESIAN_POINT ( 'NONE',  ( 1.231276596079881935, -41.24008908601427237, 7.518764738683684001 ) ) ;
#48844=DIRECTION ( 'NONE',  ( -1.000000000000000000, -0.000000000000000000, -0.000000000000000000 ) ) ;
#48846=CARTESIAN_POINT ( 'NONE',  ( 1.231276596079887264, -30.51591784428387655, 28.74118176309011830 ) ) ;
#48849=EDGE_CURVE ( 'NONE', #7742, #21941, #7231, .T. ) ;
#48850=CARTESIAN_POINT ( 'NONE',  ( 4.958415959904820092, -31.93886907500617056, 32.29725369179636374 ) ) ;
#48853=CARTESIAN_POINT ( 'NONE',  ( 5.901463166500145796, 10.83443963266029186, -16.94499301229943455 ) ) ;
#48857=LINE ( 'NONE', #34468, #50955 ) ;
#48872=( BOUNDED_SURFACE ( )  B_SPLINE_SURFACE ( 3, 1, ( 
 ( #14369, #33477 ),
 ( #47880, #33791 ),
 ( #864, #14680 ),
 ( #544, #52870 ) ),
 .UNSPECIFIED., .F., .F., .F. ) 
 B_SPLINE_SURFACE_WITH_KNOTS ( ( 4, 4 ),
 ( 2, 2 ),
 ( 0.000000000000000000, 1.000000000000000000 ),
 ( 0.000000000000000000, 1.000000000000000000 ),
 .UNSPECIFIED. ) 
 GEOMETRIC_REPRESENTATION_ITEM ( )  RATIONAL_B_SPLINE_SURFACE ( (
 ( 1.000000000000000000, 1.000000000000000000),
 ( 0.9729067724841187204, 0.9999501103223794596),
 ( 0.9729067724841187204, 0.9999501103223794596),
 ( 1.000000000000000000, 1.000000000000000000) ) ) 
 REPRESENTATION_ITEM ( '' )  SURFACE ( )  );
#48874=ORIENTED_EDGE ( 'NONE', *, *, #38672, .F. ) ;
#48878=CARTESIAN_POINT ( 'NONE',  ( 0.6064782688330895288, -34.30055712449948402, -31.98134186315069272 ) ) ;
#48892=CARTESIAN_POINT ( 'NONE',  ( 0.5817216825391136048, 5.146892874490390568, 46.61270691502455321 ) ) ;
#48905=VECTOR ( 'NONE', #25805, 1000.000000000000114 ) ;
#48910=DIRECTION ( 'NONE',  ( -1.000000000000000000, -0.000000000000000000, -0.000000000000000000 ) ) ;
#48916=FACE_OUTER_BOUND ( 'NONE', #58153, .T. ) ;
#48917=VERTEX_POINT ( 'NONE', #26793 ) ;
#48918=CONICAL_SURFACE ( 'NONE', #15940, 42.08604991992415023, 1.569615340895231137 ) ;
#48933=EDGE_CURVE ( 'NONE', #41808, #19302, #414, .T. ) ;
#48936=VERTEX_POINT ( 'NONE', #22098 ) ;
#48941=B_SPLINE_CURVE_WITH_KNOTS ( 'NONE', 3,
 ( #31626, #60725, #13152, #21303, #26304, #3102 ),
 .UNSPECIFIED., .F., .F.,
 ( 4, 2, 4 ),
 ( 1.208080024524897422E-16, 0.0002448718616795926627, 0.0004897437233590644368 ),
 .UNSPECIFIED. ) ;
#48944=CARTESIAN_POINT ( 'NONE',  ( 1.091591847532197290, -34.10780222139759132, -24.36014816420187401 ) ) ;
#48948=CARTESIAN_POINT ( 'NONE',  ( 5.895881250540457863, -19.93402233083546093, 2.676272654655019512 ) ) ;
#48951=ORIENTED_EDGE ( 'NONE', *, *, #13387, .F. ) ;
#48953=VECTOR ( 'NONE', #26947, 1000.000000000000227 ) ;
#48956=CARTESIAN_POINT ( 'NONE',  ( 0.9783242366443563043, 35.92089602389015113, 21.58758251975879361 ) ) ;
#48961=DIRECTION ( 'NONE',  ( 0.07500201931887537365, -0.9232442575324723011, 0.3768218916562637855 ) ) ;
#48962=VERTEX_POINT ( 'NONE', #16173 ) ;
#48964=CARTESIAN_POINT ( 'NONE',  ( 4.956445790444004018, -46.59545590650535019, -6.811867512257778756 ) ) ;
#48984=CARTESIAN_POINT ( 'NONE',  ( 3.376099380956842921, 4.385778397990434563, -12.66780689289931949 ) ) ;
#48989=CARTESIAN_POINT ( 'NONE',  ( 0.5797568599927143129, 45.39179688724399142, -11.78176913787528157 ) ) ;
#48995=ORIENTED_EDGE ( 'NONE', *, *, #20374, .F. ) ;
#48996=ORIENTED_EDGE ( 'NONE', *, *, #17980, .F. ) ;
#48999=DIRECTION ( 'NONE',  ( 0.000000000000000000, 0.000000000000000000, 1.000000000000000000 ) ) ;
#49003=LINE ( 'NONE', #30195, #2265 ) ;
#49004=CARTESIAN_POINT ( 'NONE',  ( 0.9762797500689124330, 9.222352665238359393, 40.88120590813919364 ) ) ;
#49008=ORIENTED_EDGE ( 'NONE', *, *, #41820, .T. ) ;
#49010=EDGE_CURVE ( 'NONE', #22549, #55841, #4189, .T. ) ;
#49017=CARTESIAN_POINT ( 'NONE',  ( 0.9783242366443547500, -41.01462390377462697, -8.610175157245297584 ) ) ;
#49024=ORIENTED_EDGE ( 'NONE', *, *, #11747, .F. ) ;
#49027=CARTESIAN_POINT ( 'NONE',  ( 0.5804410086790514622, -20.23572001627618988, 42.30881098870866452 ) ) ;
#49030=CARTESIAN_POINT ( 'NONE',  ( 0.5830081025819953133, 46.44033818253048906, -6.521274712388932748 ) ) ;
#49038=CARTESIAN_POINT ( 'NONE',  ( 4.956445790443998689, -4.175462451062247560, 46.90526157542890218 ) ) ;
#49041=CARTESIAN_POINT ( 'NONE',  ( 5.894904586330512508, 0.6732998044285471995, 20.10164369983209198 ) ) ;
#49046=DIRECTION ( 'NONE',  ( -1.000000000000000000, -0.000000000000000000, -0.000000000000000000 ) ) ;
#49055=CARTESIAN_POINT ( 'NONE',  ( 0.9762797500689124330, 15.53330887509081215, 38.92352888134283262 ) ) ;
#49058=CARTESIAN_POINT ( 'NONE',  ( 3.782542959838397501, -32.30855296672242361, 26.89600822785905621 ) ) ;
#49062=B_SPLINE_CURVE_WITH_KNOTS ( 'NONE', 3,
 ( #50885, #7333, #59347, #21772, #8271, #46214 ),
 .UNSPECIFIED., .F., .F.,
 ( 4, 2, 4 ),
 ( 6.040475531737862511E-18, 0.0002291472222819939113, 0.0004582944445639817511 ),
 .UNSPECIFIED. ) ;
#49065=B_SPLINE_CURVE_WITH_KNOTS ( 'NONE', 3,
 ( #39414, #29987, #16512, #50024 ),
 .UNSPECIFIED., .F., .F.,
 ( 4, 4 ),
 ( 9.490380264008620755E-17, 0.005004948556313905915 ),
 .UNSPECIFIED. ) ;
#49067=CARTESIAN_POINT ( 'NONE',  ( 5.910764540655177868, -11.91768246006605381, -16.20092846876983828 ) ) ;
#49073=VERTEX_POINT ( 'NONE', #27405 ) ;
#49079=CARTESIAN_POINT ( 'NONE',  ( 5.838029081930957709, -37.05692651727552800, 29.28906374820066461 ) ) ;
#49085=CARTESIAN_POINT ( 'NONE',  ( 0.7056313189692725585, -38.18416368027698127, 27.23450546632662039 ) ) ;
#49093=CIRCLE ( 'NONE', #41122, 42.08604991992415023 ) ;
#49096=CARTESIAN_POINT ( 'NONE',  ( 4.960386119450151732, 17.98972314615696177, 39.88491351121328421 ) ) ;
#49107=CARTESIAN_POINT ( 'NONE',  ( 2.618530812446111078, 15.57291328060457225, 44.35325423408038148 ) ) ;
#49109=CARTESIAN_POINT ( 'NONE',  ( 4.962356264823593932, 7.429277797797228189, 41.42513040734459651 ) ) ;
#49111=CARTESIAN_POINT ( 'NONE',  ( 0.9789889208857709413, 4.290552630147678848, 41.68844031827409680 ) ) ;
#49116=ORIENTED_EDGE ( 'NONE', *, *, #43149, .F. ) ;
#49132=ORIENTED_EDGE ( 'NONE', *, *, #20661, .T. ) ;
#49133=CARTESIAN_POINT ( 'NONE',  ( 0.5835226383429279462, 36.91662246350897902, 28.92067531079992548 ) ) ;
#49135=CARTESIAN_POINT ( 'NONE',  ( -69.95594261585600293, 0.000000000000000000, -12.50000000000000000 ) ) ;
#49141=CARTESIAN_POINT ( 'NONE',  ( 5.910764540655178756, 8.479982303152816314, 18.23708141692025464 ) ) ;
#49142=CARTESIAN_POINT ( 'NONE',  ( 0.9762797500689124330, 10.20671408566037286, -40.64662068068250278 ) ) ;
#49147=DIRECTION ( 'NONE',  ( 0.000000000000000000, 0.000000000000000000, 1.000000000000000000 ) ) ;
#49152=CARTESIAN_POINT ( 'NONE',  ( 0.5837800005270563641, -19.74018744120785129, -42.53892639016367383 ) ) ;
#49155=CARTESIAN_POINT ( 'NONE',  ( 0.8560838555295223751, -44.00447048317975174, 16.24744323198866169 ) ) ;
#49170=VERTEX_POINT ( 'NONE', #11962 ) ;
#49175=EDGE_CURVE ( 'NONE', #45995, #1414, #10211, .T. ) ;
#49192=CARTESIAN_POINT ( 'NONE',  ( 0.5824936645240091915, -46.76557133587090931, -3.495642526042641141 ) ) ;
#49196=EDGE_LOOP ( 'NONE', ( #56544, #45506, #48609, #45345 ) ) ;
#49202=CARTESIAN_POINT ( 'NONE',  ( 5.910764540655178756, 0.6875337509666024083, 20.10046108452352698 ) ) ;
#49204=B_SPLINE_CURVE_WITH_KNOTS ( 'NONE', 3,
 ( #42581, #33492, #61950, #33805, #56339, #52567, #61642, #13450, #47581, #23766, #14382, #56957, #14079, #33181, #42899, #19089, #38199, #29082, #52881 ),
 .UNSPECIFIED., .F., .F.,
 ( 4, 3, 3, 3, 3, 3, 4 ),
 ( 6.938893903907228378E-18, 0.0002732106629380587999, 0.0004098138914053727757, 0.0005464171197651509181, 0.0006830203481512618375, 0.0008196235766963736076, 0.001011968216111140293 ),
 .UNSPECIFIED. ) ;
#49209=CARTESIAN_POINT ( 'NONE',  ( 4.956445790443988919, 44.65954324082213134, 14.93530206124989945 ) ) ;
#49217=CARTESIAN_POINT ( 'NONE',  ( 4.960386119450149955, -37.88391031994039793, 21.89168343328246991 ) ) ;
#49219=B_SPLINE_CURVE_WITH_KNOTS ( 'NONE', 3,
 ( #3826, #47377, #4733, #14191 ),
 .UNSPECIFIED., .F., .F.,
 ( 4, 4 ),
 ( 4.336808689942017255E-19, 0.004446298630425055479 ),
 .UNSPECIFIED. ) ;
#49222=CARTESIAN_POINT ( 'NONE',  ( 5.896782393890504181, 20.06749419425502978, 1.349727247095894089 ) ) ;
#49231=EDGE_LOOP ( 'NONE', ( #30371, #27655, #984, #9396 ) ) ;
#49233=( BOUNDED_SURFACE ( )  B_SPLINE_SURFACE ( 3, 1, ( 
 ( #1397, #26458 ),
 ( #40906, #11144 ),
 ( #20844, #58717 ),
 ( #54322, #39983 ) ),
 .UNSPECIFIED., .F., .F., .F. ) 
 B_SPLINE_SURFACE_WITH_KNOTS ( ( 4, 4 ),
 ( 2, 2 ),
 ( 0.000000000000000000, 1.000000000000000000 ),
 ( 0.000000000000000000, 1.000000000000000000 ),
 .UNSPECIFIED. ) 
 GEOMETRIC_REPRESENTATION_ITEM ( )  RATIONAL_B_SPLINE_SURFACE ( (
 ( 1.000000000000000000, 1.000000000000000000),
 ( 0.7282232189291694135, 0.9929344683865672927),
 ( 0.7282232189291694135, 0.9929344683865672927),
 ( 1.000000000000000000, 1.000000000000000000) ) ) 
 REPRESENTATION_ITEM ( '' )  SURFACE ( )  );
#49235=EDGE_LOOP ( 'NONE', ( #16650, #2311, #15755, #23749 ) ) ;
#49236=LINE ( 'NONE', #44570, #22978 ) ;
#49240=ORIENTED_EDGE ( 'NONE', *, *, #50336, .T. ) ;
#49243=B_SPLINE_CURVE_WITH_KNOTS ( 'NONE', 3,
 ( #46902, #52179, #3626, #28380, #52488, #8970 ),
 .UNSPECIFIED., .F., .F.,
 ( 4, 2, 4 ),
 ( 9.660965348001700255E-18, 0.0002448709889506567772, 0.0004897419779013039050 ),
 .UNSPECIFIED. ) ;
#49249=CARTESIAN_POINT ( 'NONE',  ( 0.6845945791218023269, 23.29905063694661749, 40.71315217630468908 ) ) ;
#49255=VECTOR ( 'NONE', #41191, 999.9999999999998863 ) ;
#49260=CARTESIAN_POINT ( 'NONE',  ( 0.8560838555295223751, 45.47430759461099115, 11.50913475776684791 ) ) ;
#49270=CARTESIAN_POINT ( 'NONE',  ( 2.528100132419516033, -18.76087228870760981, -37.55374082030813554 ) ) ;
#49271=B_SPLINE_CURVE_WITH_KNOTS ( 'NONE', 3,
 ( #31037, #13800, #60755, #37608, #41692, #37294 ),
 .UNSPECIFIED., .F., .F.,
 ( 4, 2, 4 ),
 ( 1.209554233810030470E-16, 0.0002448718616795917953, 0.0004897437233590627020 ),
 .UNSPECIFIED. ) ;
#49278=CARTESIAN_POINT ( 'NONE',  ( 0.9762797500689124330, 15.53330887509081215, 38.92352888134283262 ) ) ;
#49281=CARTESIAN_POINT ( 'NONE',  ( 5.910764540655178756, -17.31247307865842089, -10.23618651500110666 ) ) ;
#49283=FACE_OUTER_BOUND ( 'NONE', #54871, .T. ) ;
#49299=ORIENTED_EDGE ( 'NONE', *, *, #40512, .F. ) ;
#49309=CARTESIAN_POINT ( 'NONE',  ( 4.962356264823608143, 0.000000000000000000, 0.000000000000000000 ) ) ;
#49311=CARTESIAN_POINT ( 'NONE',  ( 0.5824936645240099686, -38.45573382456261413, -26.84016980301536393 ) ) ;
#49312=CARTESIAN_POINT ( 'NONE',  ( 0.5806925824938502512, 16.34374012233117313, -43.95571090492413191 ) ) ;
#49317=ADVANCED_FACE ( 'NONE', ( #589 ), #30932, .F. ) ;
#49322=DIRECTION ( 'NONE',  ( -1.000000000000000000, -0.000000000000000000, -0.000000000000000000 ) ) ;
#49329=VERTEX_POINT ( 'NONE', #14720 ) ;
#49332=FACE_OUTER_BOUND ( 'NONE', #13278, .T. ) ;
#49346=CARTESIAN_POINT ( 'NONE',  ( 3.238018933889920792, -13.37994740236393376, -0.6200805412425434149 ) ) ;
#49353=CARTESIAN_POINT ( 'NONE',  ( 1.000433927950262314, 29.60512436931191260, 29.66404033051502154 ) ) ;
#49369=CARTESIAN_POINT ( 'NONE',  ( 2.618530812446115519, 29.00550538245366283, 36.99199165639301867 ) ) ;
#49383=VERTEX_POINT ( 'NONE', #35068 ) ;
#49384=DIRECTION ( 'NONE',  ( 0.000000000000000000, 0.000000000000000000, 1.000000000000000000 ) ) ;
#49385=( BOUNDED_SURFACE ( )  B_SPLINE_SURFACE ( 3, 1, ( 
 ( #2850, #21983 ),
 ( #46114, #22288 ),
 ( #60473, #55470 ),
 ( #60783, #12595 ) ),
 .UNSPECIFIED., .F., .F., .F. ) 
 B_SPLINE_SURFACE_WITH_KNOTS ( ( 4, 4 ),
 ( 2, 2 ),
 ( 0.000000000000000000, 1.000000000000000000 ),
 ( 0.000000000000000000, 1.000000000000000000 ),
 .UNSPECIFIED. ) 
 GEOMETRIC_REPRESENTATION_ITEM ( )  RATIONAL_B_SPLINE_SURFACE ( (
 ( 1.000000000000000000, 1.000000000000000000),
 ( 0.9952954269826590483, 0.8620686068821339365),
 ( 0.9952954269826590483, 0.8620686068821339365),
 ( 1.000000000000000000, 1.000000000000000000) ) ) 
 REPRESENTATION_ITEM ( '' )  SURFACE ( )  );
#49387=CARTESIAN_POINT ( 'NONE',  ( 1.231276596079881047, 15.85305549123227564, -38.80666698661426040 ) ) ;
#49398=CARTESIAN_POINT ( 'NONE',  ( 0.5806925824938499181, -46.82446035038572063, 2.586943222941027631 ) ) ;
#49399=EDGE_LOOP ( 'NONE', ( #21362, #17444, #51452, #33377 ) ) ;
#49400=CARTESIAN_POINT ( 'NONE',  ( 3.238018933889920792, -1.956241471238032492, 13.25068344176485802 ) ) ;
#49407=CARTESIAN_POINT ( 'NONE',  ( 5.901463166500145796, 14.90686821212704061, 13.50196839156843076 ) ) ;
#49415=CARTESIAN_POINT ( 'NONE',  ( 0.9780106845699481077, 36.21705500758324803, -21.08687205426938505 ) ) ;
#49423=CARTESIAN_POINT ( 'NONE',  ( 0.9783242366443549720, -30.90115862380460499, -28.30994323401212398 ) ) ;
#49430=EDGE_CURVE ( 'NONE', #3915, #23687, #43069, .T. ) ;
#49438=CARTESIAN_POINT ( 'NONE',  ( 4.962356264823603702, -20.60668162140254722, -36.69605251817282010 ) ) ;
#49445=CARTESIAN_POINT ( 'NONE',  ( 5.901463166500146684, 8.479222689261950663, 18.23789058324843637 ) ) ;
#49446=CIRCLE ( 'NONE', #30427, 12.50000000000000000 ) ;
#49449=EDGE_CURVE ( 'NONE', #7001, #61, #21261, .T. ) ;
#49451=CARTESIAN_POINT ( 'NONE',  ( 0.9772918015221168098, 10.11840252319961664, 40.66884294062455751 ) ) ;
#49455=CARTESIAN_POINT ( 'NONE',  ( 4.962356264823608143, 12.88441948660223169, -40.06528837230067097 ) ) ;
#49457=ORIENTED_EDGE ( 'NONE', *, *, #38991, .T. ) ;
#49470=VECTOR ( 'NONE', #40859, 1000.000000000000114 ) ;
#49475=CARTESIAN_POINT ( 'NONE',  ( 3.238018933889920792, 11.66219248059504743, -6.587925235854247497 ) ) ;
#49476=EDGE_LOOP ( 'NONE', ( #40961, #13430, #34407, #32305 ) ) ;
#49487=FACE_OUTER_BOUND ( 'NONE', #10052, .T. ) ;
#49492=EDGE_LOOP ( 'NONE', ( #28652, #5549, #19000, #20690 ) ) ;
#49495=VECTOR ( 'NONE', #9919, 999.9999999999998863 ) ;
#49498=B_SPLINE_CURVE_WITH_KNOTS ( 'NONE', 3,
 ( #58387, #39030, #20215, #58085, #6681, #54301, #10814, #34619, #15205, #30207, #53389, #15511, #44961, #24596, #49017, #39640, #48704, #6067, #781 ),
 .UNSPECIFIED., .F., .F.,
 ( 4, 3, 3, 3, 3, 3, 4 ),
 ( 5.204170427930421283E-18, 0.0002732106629380602093, 0.0004098138914053775462, 0.0005464171197651487497, 0.0006830203481512609701, 0.0008196235766963675361, 0.001011968216111146148 ),
 .UNSPECIFIED. ) ;
#49508=EDGE_CURVE ( 'NONE', #31400, #32172, #28838, .T. ) ;
#49510=CARTESIAN_POINT ( 'NONE',  ( 4.956445790444036881, 42.27038699792232279, -20.75457619864872783 ) ) ;
#49512=EDGE_CURVE ( 'NONE', #15656, #5500, #44514, .T. ) ;
#49521=DIRECTION ( 'NONE',  ( 0.000000000000000000, 0.000000000000000000, 1.000000000000000000 ) ) ;
#49526=CARTESIAN_POINT ( 'NONE',  ( 2.282816707992318506, 21.41355441518730984, -41.80857153402610749 ) ) ;
#49540=B_SPLINE_CURVE_WITH_KNOTS ( 'NONE', 3,
 ( #8882, #46814, #27991, #17667 ),
 .UNSPECIFIED., .F., .F.,
 ( 4, 4 ),
 ( 0.000000000000000000, 0.004447772540403802446 ),
 .UNSPECIFIED. ) ;
#49542=ORIENTED_EDGE ( 'NONE', *, *, #55714, .F. ) ;
#49545=LINE ( 'NONE', #25750, #59090 ) ;
#49547=CARTESIAN_POINT ( 'NONE',  ( 0.9785694773339244090, -17.43866978178105853, -38.10811202298887679 ) ) ;
#49548=EDGE_LOOP ( 'NONE', ( #41270, #28054, #19150, #27452 ) ) ;
#49558=CARTESIAN_POINT ( 'NONE',  ( 0.9775691876210987896, 35.86428463458979365, 21.68148511147509794 ) ) ;
#49566=CARTESIAN_POINT ( 'NONE',  ( 5.896782393890504181, -2.006887468070398750, 20.01245835894516389 ) ) ;
#49567=CARTESIAN_POINT ( 'NONE',  ( 1.157643937452369043, 41.42449707914801849, -6.404163984035045942 ) ) ;
#49570=B_SPLINE_CURVE_WITH_KNOTS ( 'NONE', 3,
 ( #1311, #53935, #11061, #11357 ),
 .UNSPECIFIED., .F., .F.,
 ( 4, 4 ),
 ( 7.656893354757642997E-17, 0.005004948556313879027 ),
 .UNSPECIFIED. ) ;
#49572=ORIENTED_EDGE ( 'NONE', *, *, #1373, .F. ) ;
#49576=CARTESIAN_POINT ( 'NONE',  ( 4.956445790444026223, 2.113652668516905031, -47.04328350079857302 ) ) ;
#49588=CARTESIAN_POINT ( 'NONE',  ( 5.895596859100789899, 14.91916793517901496, 13.48875870250535058 ) ) ;
#49591=FACE_OUTER_BOUND ( 'NONE', #50239, .T. ) ;
#49593=CARTESIAN_POINT ( 'NONE',  ( 0.9787284016396593511, -22.39226333978123407, 35.42488590596618536 ) ) ;
#49594=( BOUNDED_SURFACE ( )  B_SPLINE_SURFACE ( 3, 1, ( 
 ( #36761, #9150 ),
 ( #12956, #61139 ),
 ( #55834, #60837 ),
 ( #17956, #4419 ) ),
 .UNSPECIFIED., .F., .F., .F. ) 
 B_SPLINE_SURFACE_WITH_KNOTS ( ( 4, 4 ),
 ( 2, 2 ),
 ( 0.000000000000000000, 1.000000000000000000 ),
 ( 0.000000000000000000, 1.000000000000000000 ),
 .UNSPECIFIED. ) 
 GEOMETRIC_REPRESENTATION_ITEM ( )  RATIONAL_B_SPLINE_SURFACE ( (
 ( 1.000000000000000000, 1.000000000000000000),
 ( 0.9729067724841187204, 0.9999501103223794596),
 ( 0.9729067724841187204, 0.9999501103223794596),
 ( 1.000000000000000000, 1.000000000000000000) ) ) 
 REPRESENTATION_ITEM ( '' )  SURFACE ( )  );
#49599=ORIENTED_EDGE ( 'NONE', *, *, #44873, .F. ) ;
#49601=CARTESIAN_POINT ( 'NONE',  ( 4.962356264823601038, -35.98698831890646943, 21.82137185415336589 ) ) ;
#49606=ORIENTED_EDGE ( 'NONE', *, *, #46606, .F. ) ;
#49607=CARTESIAN_POINT ( 'NONE',  ( 1.157643937452368599, -23.24616979670748407, -34.88004966133790674 ) ) ;
#49615=CARTESIAN_POINT ( 'NONE',  ( 4.956445790444035104, 41.78282513192535674, -21.71942849465849079 ) ) ;
#49619=ORIENTED_EDGE ( 'NONE', *, *, #24811, .T. ) ;
#49624=CARTESIAN_POINT ( 'NONE',  ( 0.7764139734771247081, -29.59659215482911421, -36.38794036116326680 ) ) ;
#49630=CARTESIAN_POINT ( 'NONE',  ( 0.9762797500689124330, -30.73989051779348003, 28.48480149377514437 ) ) ;
#49634=CARTESIAN_POINT ( 'NONE',  ( 0.8560838555295158248, -13.02223058219810881, -45.06433561859972059 ) ) ;
#49635=CARTESIAN_POINT ( 'NONE',  ( 5.895596859100789899, -11.93344155749883662, -16.19015613903236428 ) ) ;
#49637=ORIENTED_EDGE ( 'NONE', *, *, #982, .T. ) ;
#49641=VERTEX_POINT ( 'NONE', #48156 ) ;
#49645=CARTESIAN_POINT ( 'NONE',  ( 4.962356264823593044, 12.88441948660167391, 40.06528837230087703 ) ) ;
#49650=CARTESIAN_POINT ( 'NONE',  ( 0.5804410086790514622, 37.14246315962257938, -28.63489623329331479 ) ) ;
#49651=CARTESIAN_POINT ( 'NONE',  ( 1.231276596079887264, 24.17959027891153667, -34.24360064248551083 ) ) ;
#49661=CARTESIAN_POINT ( 'NONE',  ( 0.9789233960466692253, 14.93951272412277653, 39.15542984565634299 ) ) ;
#49669=ADVANCED_FACE ( 'NONE', ( #32518 ), #6805, .T. ) ;
#49672=CARTESIAN_POINT ( 'NONE',  ( 5.838029081930955932, -47.23414715677123610, -0.02001313068654116470 ) ) ;
#49680=ORIENTED_EDGE ( 'NONE', *, *, #43321, .T. ) ;
#49689=ORIENTED_EDGE ( 'NONE', *, *, #20303, .F. ) ;
#49694=CARTESIAN_POINT ( 'NONE',  ( 3.661921753702009230, -42.79842403921696814, -19.51732624089203227 ) ) ;
#49699=CARTESIAN_POINT ( 'NONE',  ( 1.157643937452369265, -27.68781119398633805, -31.47042080876771308 ) ) ;
#49701=ORIENTED_EDGE ( 'NONE', *, *, #44103, .F. ) ;
#49702=CARTESIAN_POINT ( 'NONE',  ( 4.962356264823594820, 34.94214251265108118, 23.45809613945535332 ) ) ;
#49711=FACE_OUTER_BOUND ( 'NONE', #61771, .T. ) ;
#49713=CARTESIAN_POINT ( 'NONE',  ( 0.8560838555295158248, -30.97734773434503808, 35.22466126774251194 ) ) ;
#49719=VERTEX_POINT ( 'NONE', #53738 ) ;
#49722=EDGE_CURVE ( 'NONE', #4545, #58288, #52676, .T. ) ;
#49725=EDGE_LOOP ( 'NONE', ( #12742, #7718, #13573, #45512 ) ) ;
#49726=CARTESIAN_POINT ( 'NONE',  ( 4.962356264823603702, -20.60668162140254722, -36.69605251817282010 ) ) ;
#49728=LINE ( 'NONE', #5557, #48290 ) ;
#49731=DIRECTION ( 'NONE',  ( -1.000000000000000000, -0.000000000000000000, -0.000000000000000000 ) ) ;
#49735=VECTOR ( 'NONE', #18169, 999.9999999999998863 ) ;
#49739=CARTESIAN_POINT ( 'NONE',  ( 0.9784957157296394481, 38.49170563740425877, -16.57472938288250575 ) ) ;
#49741=CARTESIAN_POINT ( 'NONE',  ( 0.5804410086790514622, -30.69452151258743200, 35.45935984995646351 ) ) ;
#49751=CARTESIAN_POINT ( 'NONE',  ( 4.960386119450153508, 42.96877549456534240, -8.253532405581291087 ) ) ;
#49762=FACE_OUTER_BOUND ( 'NONE', #53220, .T. ) ;
#49769=DIRECTION ( 'NONE',  ( 0.000000000000000000, 0.000000000000000000, 1.000000000000000000 ) ) ;
#49782=EDGE_CURVE ( 'NONE', #3829, #60616, #1862, .T. ) ;
#49784=VECTOR ( 'NONE', #12734, 1000.000000000000000 ) ;
#49785=ORIENTED_EDGE ( 'NONE', *, *, #44960, .T. ) ;
#49788=CARTESIAN_POINT ( 'NONE',  ( 5.896782393890504181, 3.339090646272624419, 19.83372281075811827 ) ) ;
#49792=EDGE_LOOP ( 'NONE', ( #43331, #4205, #42205, #61191 ) ) ;
#49793=CARTESIAN_POINT ( 'NONE',  ( 5.901463166500146684, -18.52233187494211819, -7.838436850236139897 ) ) ;
#49795=ORIENTED_EDGE ( 'NONE', *, *, #22307, .T. ) ;
#49796=ORIENTED_EDGE ( 'NONE', *, *, #22258, .F. ) ;
#49797=CARTESIAN_POINT ( 'NONE',  ( 0.9789233960466690032, 20.25576450497998948, -36.68842775523553001 ) ) ;
#49798=CARTESIAN_POINT ( 'NONE',  ( 1.000110580585058306, 28.65872797539951122, 30.57931970472783334 ) ) ;
#49799=ORIENTED_EDGE ( 'NONE', *, *, #58145, .T. ) ;
#49802=CARTESIAN_POINT ( 'NONE',  ( 5.894904586330512508, 3.346579165707272097, 19.83254446482590794 ) ) ;
#49806=CARTESIAN_POINT ( 'NONE',  ( 0.5837799406558222826, 32.53627130208564466, -33.77328232988735834 ) ) ;
#49807=CARTESIAN_POINT ( 'NONE',  ( 4.962356264823608143, 34.44911810793244200, 24.17630781256866612 ) ) ;
#49811=ORIENTED_EDGE ( 'NONE', *, *, #10423, .F. ) ;
#49812=CARTESIAN_POINT ( 'NONE',  ( 0.5817217712918335559, -46.75866061562757636, -3.586448304511290264 ) ) ;
#49816=EDGE_LOOP ( 'NONE', ( #12304, #34852, #38192, #57609 ) ) ;
#49821=B_SPLINE_CURVE_WITH_KNOTS ( 'NONE', 3,
 ( #3086, #22217, #18442, #61327 ),
 .UNSPECIFIED., .F., .F.,
 ( 4, 4 ),
 ( 8.673617379884035472E-19, 0.004041751736740996012 ),
 .UNSPECIFIED. ) ;
#49823=VERTEX_POINT ( 'NONE', #16181 ) ;
#49827=B_SPLINE_CURVE_WITH_KNOTS ( 'NONE', 3,
 ( #31981, #14117, #37614, #56068, #46703, #28486 ),
 .UNSPECIFIED., .F., .F.,
 ( 4, 2, 4 ),
 ( 9.929776742050823831E-18, 0.0002448709889506580240, 0.0004897419779013061818 ),
 .UNSPECIFIED. ) ;
#49834=AXIS2_PLACEMENT_3D ( 'NONE', #4878, #42833, #14320 ) ;
#49838=FACE_OUTER_BOUND ( 'NONE', #17755, .T. ) ;
#49849=CARTESIAN_POINT ( 'NONE',  ( 4.956445790443988031, 0.000000000000000000, 0.000000000000000000 ) ) ;
#49850=ORIENTED_EDGE ( 'NONE', *, *, #54275, .T. ) ;
#49866=B_SPLINE_CURVE_WITH_KNOTS ( 'NONE', 3,
 ( #18077, #9583, #42214, #9276 ),
 .UNSPECIFIED., .F., .F.,
 ( 4, 4 ),
 ( 4.207375016313971546E-17, 0.005004948556313856475 ),
 .UNSPECIFIED. ) ;
#49869=CARTESIAN_POINT ( 'NONE',  ( 0.9787464366903554369, -17.48005752276034741, -38.08912681975596826 ) ) ;
#49873=( BOUNDED_SURFACE ( )  B_SPLINE_SURFACE ( 3, 1, ( 
 ( #5810, #49672 ),
 ( #34068, #1130 ),
 ( #29337, #53438 ),
 ( #10242, #11171 ) ),
 .UNSPECIFIED., .F., .F., .F. ) 
 B_SPLINE_SURFACE_WITH_KNOTS ( ( 4, 4 ),
 ( 2, 2 ),
 ( 0.000000000000000000, 1.000000000000000000 ),
 ( 0.000000000000000000, 1.000000000000000000 ),
 .UNSPECIFIED. ) 
 GEOMETRIC_REPRESENTATION_ITEM ( )  RATIONAL_B_SPLINE_SURFACE ( (
 ( 1.000000000000000000, 1.000000000000000000),
 ( 0.7282232189291693025, 0.9929344683865674037),
 ( 0.7282232189291693025, 0.9929344683865674037),
 ( 1.000000000000000000, 1.000000000000000000) ) ) 
 REPRESENTATION_ITEM ( '' )  SURFACE ( )  );
#49874=CARTESIAN_POINT ( 'NONE',  ( 4.962356264823609031, -24.61258717641066696, -34.13877780978592824 ) ) ;
#49881=CARTESIAN_POINT ( 'NONE',  ( 0.9772918015221174759, 36.26796431592507020, 20.99932427792537126 ) ) ;
#49883=ADVANCED_FACE ( 'NONE', ( #58440 ), #7677, .F. ) ;
#49886=CARTESIAN_POINT ( 'NONE',  ( 5.896782393890504181, 5.952874097602427916, 19.21169895808557371 ) ) ;
#49896=CARTESIAN_POINT ( 'NONE',  ( 5.896782393890504181, 0.6784186533441023403, -20.10138888258239120 ) ) ;
#49899=CARTESIAN_POINT ( 'NONE',  ( 4.962356264823608143, 39.61238188121388504, 14.21600504921214814 ) ) ;
#49917=DIRECTION ( 'NONE',  ( -1.000000000000000000, -0.000000000000000000, -0.000000000000000000 ) ) ;
#49924=CARTESIAN_POINT ( 'NONE',  ( 5.896278296736517710, 3.339955767731749070, -19.83359965018905058 ) ) ;
#49928=CARTESIAN_POINT ( 'NONE',  ( 4.962356264823608143, 0.000000000000000000, 0.000000000000000000 ) ) ;
#49934=CARTESIAN_POINT ( 'NONE',  ( 4.956445790444005794, -40.23882117934059011, -24.46171131046819625 ) ) ;
#49940=EDGE_CURVE ( 'NONE', #36534, #2574, #41507, .T. ) ;
#49941=ORIENTED_EDGE ( 'NONE', *, *, #43840, .T. ) ;
#49943=B_SPLINE_CURVE_WITH_KNOTS ( 'NONE', 3,
 ( #59534, #26341, #16645, #2522 ),
 .UNSPECIFIED., .F., .F.,
 ( 4, 4 ),
 ( 1.734723475976807094E-17, 0.005004948556313820046 ),
 .UNSPECIFIED. ) ;
#49948=ORIENTED_EDGE ( 'NONE', *, *, #29281, .F. ) ;
#49956=EDGE_CURVE ( 'NONE', #36178, #29343, #45322, .T. ) ;
#49961=CARTESIAN_POINT ( 'NONE',  ( 5.895596859100789899, 14.91916793517919970, -13.48875870250514630 ) ) ;
#49966=VERTEX_POINT ( 'NONE', #8003 ) ;
#49967=CARTESIAN_POINT ( 'NONE',  ( 3.376099380956842921, 9.644725941468886177, 9.310620019419980409 ) ) ;
#49968=CARTESIAN_POINT ( 'NONE',  ( 5.895596859100789899, -15.78235929336536536, 12.46777118604649814 ) ) ;
#49970=CARTESIAN_POINT ( 'NONE',  ( 0.5804410086790514622, 32.20888702807361881, 34.08969709851039909 ) ) ;
#49974=FACE_OUTER_BOUND ( 'NONE', #31945, .T. ) ;
#49978=CARTESIAN_POINT ( 'NONE',  ( 5.896782393890504181, -18.51935720350340731, 7.845985957612901629 ) ) ;
#49979=CARTESIAN_POINT ( 'NONE',  ( 0.9775691876210974574, 14.70917054435504312, 39.24250260733978735 ) ) ;
#49987=CARTESIAN_POINT ( 'NONE',  ( 0.5817217712918323347, -34.47346716911549436, -31.79331714917915619 ) ) ;
#49989=EDGE_CURVE ( 'NONE', #53012, #39870, #58658, .T. ) ;
#49995=CARTESIAN_POINT ( 'NONE',  ( 4.956445790444041322, 46.03642002599030292, -9.908889005849065512 ) ) ;
#49996=ORIENTED_EDGE ( 'NONE', *, *, #12762, .T. ) ;
#50001=CARTESIAN_POINT ( 'NONE',  ( 3.376099380956838925, -9.627698927086731473, -9.328225822815406687 ) ) ;
#50002=EDGE_LOOP ( 'NONE', ( #15751, #25393, #59483, #33529 ) ) ;
#50008=ORIENTED_EDGE ( 'NONE', *, *, #58680, .F. ) ;
#50020=CARTESIAN_POINT ( 'NONE',  ( 0.8560838555295158248, -29.58154842764465542, -36.40473632241614155 ) ) ;
#50023=CARTESIAN_POINT ( 'NONE',  ( 0.5824936645240080813, -35.02382170666601979, 31.18605605234460398 ) ) ;
#50024=CARTESIAN_POINT ( 'NONE',  ( 4.962356264823608143, 12.88441948660223169, -40.06528837230067097 ) ) ;
#50030=EDGE_CURVE ( 'NONE', #41301, #50843, #28063, .T. ) ;
#50042=CARTESIAN_POINT ( 'NONE',  ( 0.9780106845699465534, 24.60614105318022737, 33.92446121792414004 ) ) ;
#50058=VERTEX_POINT ( 'NONE', #56532 ) ;
#50083=VECTOR ( 'NONE', #6601, 1000.000000000000000 ) ;
#50085=ORIENTED_EDGE ( 'NONE', *, *, #24690, .T. ) ;
#50103=CARTESIAN_POINT ( 'NONE',  ( 5.838029081930957709, 42.16639215765243165, 21.28521624414438662 ) ) ;
#50109=CARTESIAN_POINT ( 'NONE',  ( 0.8554163680231738898, 21.74163052365332760, 41.57531689939074226 ) ) ;
#50127=CARTESIAN_POINT ( 'NONE',  ( 0.9762797500689124330, 28.76866969767982951, 30.47438972336447804 ) ) ;
#50131=DIRECTION ( 'NONE',  ( 0.000000000000000000, 0.000000000000000000, 1.000000000000000000 ) ) ;
#50135=CARTESIAN_POINT ( 'NONE',  ( 3.376099380956842921, -5.222100608647028075, 12.34658045230481527 ) ) ;
#50142=CARTESIAN_POINT ( 'NONE',  ( 4.956445790444035104, 39.12691469764034480, -26.20348443209818967 ) ) ;
#50145=CARTESIAN_POINT ( 'NONE',  ( 1.231276596079881047, 15.85305549123227564, -38.80666698661426040 ) ) ;
#50149=( BOUNDED_SURFACE ( )  B_SPLINE_SURFACE ( 3, 1, ( 
 ( #54279, #17336 ),
 ( #40549, #22339 ),
 ( #12340, #30484 ),
 ( #45547, #2910 ) ),
 .UNSPECIFIED., .F., .F., .F. ) 
 B_SPLINE_SURFACE_WITH_KNOTS ( ( 4, 4 ),
 ( 2, 2 ),
 ( 0.000000000000000000, 1.000000000000000000 ),
 ( 0.000000000000000000, 1.000000000000000000 ),
 .UNSPECIFIED. ) 
 GEOMETRIC_REPRESENTATION_ITEM ( )  RATIONAL_B_SPLINE_SURFACE ( (
 ( 1.000000000000000000, 1.000000000000000000),
 ( 0.9729067724841187204, 0.9999501103223794596),
 ( 0.9729067724841187204, 0.9999501103223794596),
 ( 1.000000000000000000, 1.000000000000000000) ) ) 
 REPRESENTATION_ITEM ( '' )  SURFACE ( )  );
#50153=CARTESIAN_POINT ( 'NONE',  ( 0.5806925824938502512, 32.20670061096268455, -34.08739940358283604 ) ) ;
#50158=CARTESIAN_POINT ( 'NONE',  ( 5.910764540655177868, -19.39351348817910647, -5.328496321944700576 ) ) ;
#50175=ORIENTED_EDGE ( 'NONE', *, *, #18249, .T. ) ;
#50179=ORIENTED_EDGE ( 'NONE', *, *, #3035, .T. ) ;
#50187=CARTESIAN_POINT ( 'NONE',  ( 0.5806925824938499181, -30.69245420804209701, 35.45695442407318154 ) ) ;
#50191=CARTESIAN_POINT ( 'NONE',  ( 5.895596859100789899, 5.955534046174260965, 19.21092911436994299 ) ) ;
#50204=AXIS2_PLACEMENT_3D ( 'NONE', #21857, #37517, #8353 ) ;
#50207=CARTESIAN_POINT ( 'NONE',  ( 0.8560838555295223751, -45.77741231505103059, 10.23725333375835689 ) ) ;
#50208=EDGE_CURVE ( 'NONE', #55475, #37747, #14576, .T. ) ;
#50214=CARTESIAN_POINT ( 'NONE',  ( 0.9769922540276041456, 32.61418167833736703, 26.31818209030647893 ) ) ;
#50220=( BOUNDED_SURFACE ( )  B_SPLINE_SURFACE ( 3, 1, ( 
 ( #21402, #16095 ),
 ( #29561, #15478 ),
 ( #49281, #53966 ),
 ( #34587, #10782 ) ),
 .UNSPECIFIED., .F., .F., .F. ) 
 B_SPLINE_SURFACE_WITH_KNOTS ( ( 4, 4 ),
 ( 2, 2 ),
 ( 0.000000000000000000, 1.000000000000000000 ),
 ( 0.000000000000000000, 1.000000000000000000 ),
 .UNSPECIFIED. ) 
 GEOMETRIC_REPRESENTATION_ITEM ( )  RATIONAL_B_SPLINE_SURFACE ( (
 ( 1.000000000000000000, 1.000000000000000000),
 ( 0.7282232189291694135, 0.9929344683865672927),
 ( 0.7282232189291694135, 0.9929344683865672927),
 ( 1.000000000000000000, 1.000000000000000000) ) ) 
 REPRESENTATION_ITEM ( '' )  SURFACE ( )  );
#50225=CARTESIAN_POINT ( 'NONE',  ( 0.5797568599927135358, 23.08701878027053667, -40.81929534558918959 ) ) ;
#50227=ORIENTED_EDGE ( 'NONE', *, *, #36572, .T. ) ;
#50229=B_SPLINE_CURVE_WITH_KNOTS ( 'NONE', 3,
 ( #36847, #13036, #47161, #23343 ),
 .UNSPECIFIED., .F., .F.,
 ( 4, 4 ),
 ( 0.000000000000000000, 0.004447772540403802446 ),
 .UNSPECIFIED. ) ;
#50235=ORIENTED_EDGE ( 'NONE', *, *, #38557, .T. ) ;
#50239=EDGE_LOOP ( 'NONE', ( #86, #13303, #23065, #25991 ) ) ;
#50247=VECTOR ( 'NONE', #56719, 1000.000000000000114 ) ;
#50251=ORIENTED_EDGE ( 'NONE', *, *, #47047, .T. ) ;
#50253=CARTESIAN_POINT ( 'NONE',  ( 2.282816707992304739, 46.95498737082395024, -1.313821682622675180 ) ) ;
#50257=CARTESIAN_POINT ( 'NONE',  ( 5.894904586330512508, -11.92958617826537271, -16.19303509775059169 ) ) ;
#50259=EDGE_LOOP ( 'NONE', ( #48243, #38710, #14223, #55463 ) ) ;
#50260=CARTESIAN_POINT ( 'NONE',  ( 0.8560838555295158248, 11.76118766017326323, -45.40977096290972526 ) ) ;
#50262=B_SPLINE_CURVE_WITH_KNOTS ( 'NONE', 3,
 ( #53937, #34867, #59259, #25762 ),
 .UNSPECIFIED., .F., .F.,
 ( 4, 4 ),
 ( 0.000000000000000000, 0.005004948556313802699 ),
 .UNSPECIFIED. ) ;
#50264=CARTESIAN_POINT ( 'NONE',  ( 5.896278296736517710, 17.94863123379886005, 9.075991210192073666 ) ) ;
#50270=DIRECTION ( 'NONE',  ( 0.000000000000000000, 0.000000000000000000, 1.000000000000000000 ) ) ;
#50271=CARTESIAN_POINT ( 'NONE',  ( 0.5782707292762442330, 37.25243273660956334, -28.49548400908462042 ) ) ;
#50274=CARTESIAN_POINT ( 'NONE',  ( 5.894904586330512508, -13.98146465072115241, -14.45849432971074044 ) ) ;
#50275=CARTESIAN_POINT ( 'NONE',  ( 0.5837799406558235038, -46.78519619469427937, 3.223191989498096710 ) ) ;
#50279=EDGE_CURVE ( 'NONE', #30761, #29776, #3292, .T. ) ;
#50289=CONICAL_SURFACE ( 'NONE', #25255, 42.08604991992415023, 1.569615340895231137 ) ;
#50290=CARTESIAN_POINT ( 'NONE',  ( 0.9784957157296351182, -30.92500134937655787, 28.28387081948704918 ) ) ;
#50294=CARTESIAN_POINT ( 'NONE',  ( 5.917102823773431552, -4.670717611792517765, 19.56205804721562203 ) ) ;
#50296=CARTESIAN_POINT ( 'NONE',  ( 3.782542959838390839, 42.00313795915501203, 1.724602847255015670 ) ) ;
#50298=VERTEX_POINT ( 'NONE', #48079 ) ;
#50308=ORIENTED_EDGE ( 'NONE', *, *, #24178, .F. ) ;
#50311=CARTESIAN_POINT ( 'NONE',  ( 2.282816707992310512, -42.50075753973140280, -20.00456385320434549 ) ) ;
#50318=CARTESIAN_POINT ( 'NONE',  ( 0.8560838555295158248, 16.00311602465144745, 44.09391240957503300 ) ) ;
#50319=ORIENTED_EDGE ( 'NONE', *, *, #61454, .T. ) ;
#50322=ORIENTED_EDGE ( 'NONE', *, *, #52862, .T. ) ;
#50324=CARTESIAN_POINT ( 'NONE',  ( 0.5835226383429290564, -19.57482050365606696, 42.61535963470931421 ) ) ;
#50328=ADVANCED_FACE ( 'NONE', ( #50836 ), #50149, .F. ) ;
#50329=CARTESIAN_POINT ( 'NONE',  ( 0.5806925824938502512, 37.13995815321093374, 28.63295078613632683 ) ) ;
#50333=( BOUNDED_SURFACE ( )  B_SPLINE_SURFACE ( 3, 1, ( 
 ( #8093, #47243 ),
 ( #4291, #10184 ),
 ( #53079, #46033 ),
 ( #17503, #12819 ) ),
 .UNSPECIFIED., .F., .F., .F. ) 
 B_SPLINE_SURFACE_WITH_KNOTS ( ( 4, 4 ),
 ( 2, 2 ),
 ( 0.000000000000000000, 1.000000000000000000 ),
 ( 0.000000000000000000, 1.000000000000000000 ),
 .UNSPECIFIED. ) 
 GEOMETRIC_REPRESENTATION_ITEM ( )  RATIONAL_B_SPLINE_SURFACE ( (
 ( 1.000000000000000000, 1.000000000000000000),
 ( 0.7282232189291694135, 0.9929344683865672927),
 ( 0.7282232189291694135, 0.9929344683865672927),
 ( 1.000000000000000000, 1.000000000000000000) ) ) 
 REPRESENTATION_ITEM ( '' )  SURFACE ( )  );
#50336=EDGE_CURVE ( 'NONE', #33079, #5070, #57620, .T. ) ;
#50341=ORIENTED_EDGE ( 'NONE', *, *, #7694, .F. ) ;
#50344=CARTESIAN_POINT ( 'NONE',  ( 0.5848930533535030563, 17.02477461160209771, 43.69702657860951689 ) ) ;
#50347=B_SPLINE_CURVE_WITH_KNOTS ( 'NONE', 3,
 ( #18627, #47435, #9833, #4483 ),
 .UNSPECIFIED., .F., .F.,
 ( 4, 4 ),
 ( 1.084202172485504434E-18, 0.004446298630425059815 ),
 .UNSPECIFIED. ) ;
#50350=CARTESIAN_POINT ( 'NONE',  ( 4.960386119450153508, 6.813122688534127391, 43.22057176742715967 ) ) ;
#50353=FACE_OUTER_BOUND ( 'NONE', #29223, .T. ) ;
#50357=CARTESIAN_POINT ( 'NONE',  ( 5.917102823773431552, 20.06759006498879572, -1.334746056486034504 ) ) ;
#50362=CARTESIAN_POINT ( 'NONE',  ( 0.5817217712918323347, 36.52004312053393420, 29.41974514646100047 ) ) ;
#50366=CARTESIAN_POINT ( 'NONE',  ( -4.467300000000000715, 0.000000000000000000, -46.67105333295396719 ) ) ;
#50367=CARTESIAN_POINT ( 'NONE',  ( 0.8554163680231816613, 3.785871848717079935, -46.76401017296218043 ) ) ;
#50373=CARTESIAN_POINT ( 'NONE',  ( 1.231276596079881047, 8.892602616353681100, 40.96581977363184990 ) ) ;
#50376=CARTESIAN_POINT ( 'NONE',  ( 0.5848930533535030563, -38.55997537638119610, 26.69084826978029668 ) ) ;
#50378=B_SPLINE_CURVE_WITH_KNOTS ( 'NONE', 3,
 ( #5758, #11122, #36709, #55468 ),
 .UNSPECIFIED., .F., .F.,
 ( 4, 4 ),
 ( 2.168404344971008868E-19, 0.004041751736740987339 ),
 .UNSPECIFIED. ) ;
#50380=CARTESIAN_POINT ( 'NONE',  ( 0.9754292589017210524, -7.544321835733828863, -41.22390902054472406 ) ) ;
#50381=CARTESIAN_POINT ( 'NONE',  ( 1.231276596079887264, 38.91607545535247681, 15.58254928345742840 ) ) ;
#50383=CARTESIAN_POINT ( 'NONE',  ( 3.661921753701997684, 34.02818019380067938, 32.47636181182038229 ) ) ;
#50386=CARTESIAN_POINT ( 'NONE',  ( 4.956445790443998689, -27.49627641100115838, 38.22947597952995835 ) ) ;
#50390=B_SPLINE_CURVE_WITH_KNOTS ( 'NONE', 3,
 ( #56279, #52196, #47214, #13397, #32499, #8665 ),
 .UNSPECIFIED., .F., .F.,
 ( 4, 2, 4 ),
 ( 1.250652936113012808E-16, 0.0002448718616795918495, 0.0004897437233590586905 ),
 .UNSPECIFIED. ) ;
#50399=CARTESIAN_POINT ( 'NONE',  ( 5.894904586330512508, 20.06791991542433351, 1.344619771444058642 ) ) ;
#50400=ORIENTED_EDGE ( 'NONE', *, *, #4999, .F. ) ;
#50401=DIRECTION ( 'NONE',  ( 0.000000000000000000, 0.000000000000000000, 1.000000000000000000 ) ) ;
#50403=CARTESIAN_POINT ( 'NONE',  ( 5.896782393890504181, -18.51935720350329362, -7.845985957613155648 ) ) ;
#50413=EDGE_CURVE ( 'NONE', #41264, #35972, #53851, .T. ) ;
#50418=CARTESIAN_POINT ( 'NONE',  ( 1.231276596079887931, -37.78837162824473950, -18.14705873423390869 ) ) ;
#50419=FACE_OUTER_BOUND ( 'NONE', #28311, .T. ) ;
#50421=VERTEX_POINT ( 'NONE', #32061 ) ;
#50425=ORIENTED_EDGE ( 'NONE', *, *, #61838, .F. ) ;
#50426=VECTOR ( 'NONE', #16321, 999.9999999999998863 ) ;
#50427=VERTEX_POINT ( 'NONE', #9158 ) ;
#50431=CARTESIAN_POINT ( 'NONE',  ( 0.5834584762367737154, -44.36061497477145821, 15.21091148068631149 ) ) ;
#50432=VERTEX_POINT ( 'NONE', #28264 ) ;
#50441=CARTESIAN_POINT ( 'NONE',  ( 5.895596859100789899, 5.962379729971948983, 19.20880556328547684 ) ) ;
#50456=EDGE_CURVE ( 'NONE', #59315, #32617, #42693, .T. ) ;
#50458=CARTESIAN_POINT ( 'NONE',  ( 0.8560838555295158248, -46.73345513967312570, -4.044379407262746362 ) ) ;
#50460=CARTESIAN_POINT ( 'NONE',  ( 0.7056759521545007408, -46.12215779644467517, 8.514422430021223676 ) ) ;
#50463=EDGE_LOOP ( 'NONE', ( #61091, #37790, #60404, #3327 ) ) ;
#50464=CARTESIAN_POINT ( 'NONE',  ( 2.528100132419517809, -40.03693467153145491, -12.62131691780209408 ) ) ;
#50466=CARTESIAN_POINT ( 'NONE',  ( 0.5806925824938499181, 16.34374012233052653, 43.95571090492437349 ) ) ;
#50473=ORIENTED_EDGE ( 'NONE', *, *, #34815, .F. ) ;
#50474=VERTEX_POINT ( 'NONE', #60845 ) ;
#50475=CARTESIAN_POINT ( 'NONE',  ( 4.962356264823603702, -40.70360067759225586, -10.69824704058845022 ) ) ;
#50479=ORIENTED_EDGE ( 'NONE', *, *, #60873, .T. ) ;
#50492=DIRECTION ( 'NONE',  ( 0.000000000000000000, 0.000000000000000000, -1.000000000000000000 ) ) ;
#50494=CARTESIAN_POINT ( 'NONE',  ( 0.6064782688330855320, -30.81732999423350350, 35.35005825236059707 ) ) ;
#50504=EDGE_LOOP ( 'NONE', ( #22905, #38938, #25411, #15678 ) ) ;
#50506=CARTESIAN_POINT ( 'NONE',  ( 0.9791128995231614951, -39.59150764406756196, -13.74226897989937513 ) ) ;
#50507=CARTESIAN_POINT ( 'NONE',  ( 3.661921753702009674, -21.49231610627914080, -41.84150418211332578 ) ) ;
#50509=CARTESIAN_POINT ( 'NONE',  ( 1.231276596079881047, 20.88402890667877898, -36.34740854095476692 ) ) ;
#50535=ORIENTED_EDGE ( 'NONE', *, *, #25234, .T. ) ;
#50536=DIRECTION ( 'NONE',  ( -1.000000000000000000, -0.000000000000000000, -0.000000000000000000 ) ) ;
#50540=CARTESIAN_POINT ( 'NONE',  ( 5.896782393890504181, -19.39652907507971236, -5.319844614046497000 ) ) ;
#50542=CARTESIAN_POINT ( 'NONE',  ( 5.910764540655177868, -11.94262894392618435, 16.18254777149937951 ) ) ;
#50560=CARTESIAN_POINT ( 'NONE',  ( 0.5806925824938499181, -38.96949031362449745, 26.08833430941674436 ) ) ;
#50566=CARTESIAN_POINT ( 'NONE',  ( 0.5804410086790514622, 42.96136033320044589, 18.81067170986479553 ) ) ;
#50568=CARTESIAN_POINT ( 'NONE',  ( 1.000110580585053865, -21.99348401176059653, -35.67497924030694634 ) ) ;
#50579=CARTESIAN_POINT ( 'NONE',  ( -69.95594261585600293, 0.000000000000000000, 0.000000000000000000 ) ) ;
#50581=CARTESIAN_POINT ( 'NONE',  ( 1.231276596079881047, 24.17959027891106416, 34.24360064248583768 ) ) ;
#50585=CARTESIAN_POINT ( 'NONE',  ( 4.962356264823609031, 37.75702904547822669, -18.59145920903629090 ) ) ;
#50588=B_SPLINE_CURVE_WITH_KNOTS ( 'NONE', 3,
 ( #34144, #24414, #53219, #43548 ),
 .UNSPECIFIED., .F., .F.,
 ( 4, 4 ),
 ( 3.252606517456513302E-19, 0.004446298630425088438 ),
 .UNSPECIFIED. ) ;
#50590=CARTESIAN_POINT ( 'NONE',  ( 0.9775691876210974574, -31.33375233628529699, 27.83037321917057128 ) ) ;
#50599=VECTOR ( 'NONE', #20894, 1000.000000000000114 ) ;
#50600=CARTESIAN_POINT ( 'NONE',  ( 1.231276596079881935, 3.353048872156085825, 41.78556968953515849 ) ) ;
#50601=CARTESIAN_POINT ( 'NONE',  ( 0.5817217712918323347, -8.248776971688084103, 46.16484195228790810 ) ) ;
#50609=CARTESIAN_POINT ( 'NONE',  ( 4.956445790443988031, 0.000000000000000000, 0.000000000000000000 ) ) ;
#50618=CARTESIAN_POINT ( 'NONE',  ( 4.291220156522059348, -11.88564107118027025, -45.58640733412503465 ) ) ;
#50622=VERTEX_POINT ( 'NONE', #26598 ) ;
#50632=EDGE_LOOP ( 'NONE', ( #8478, #1135, #53340, #56059 ) ) ;
#50634=ORIENTED_EDGE ( 'NONE', *, *, #32751, .F. ) ;
#50636=VECTOR ( 'NONE', #39750, 999.9999999999998863 ) ;
#50637=ORIENTED_EDGE ( 'NONE', *, *, #17018, .F. ) ;
#50638=CARTESIAN_POINT ( 'NONE',  ( 4.962356264823608143, 30.91935898304044272, 28.55221248765537467 ) ) ;
#50640=EDGE_CURVE ( 'NONE', #38326, #13848, #53085, .T. ) ;
#50643=VERTEX_POINT ( 'NONE', #55097 ) ;
#50647=EDGE_CURVE ( 'NONE', #48917, #5400, #24700, .T. ) ;
#50652=CARTESIAN_POINT ( 'NONE',  ( 0.9754292589017238280, -26.60990437553315147, 32.37654175510806454 ) ) ;
#50653=CARTESIAN_POINT ( 'NONE',  ( 0.6064515330803567084, 27.24304339879380521, -38.17264625891847629 ) ) ;
#50657=ORIENTED_EDGE ( 'NONE', *, *, #58313, .F. ) ;
#50664=CARTESIAN_POINT ( 'NONE',  ( 2.618530812446111078, -39.53489722556214758, 25.43066437516798217 ) ) ;
#50666=CARTESIAN_POINT ( 'NONE',  ( 2.282816707992308736, -45.75239461778012640, 10.64027035121241127 ) ) ;
#50676=CARTESIAN_POINT ( 'NONE',  ( 0.8560838555295223751, 44.99141268455589682, -13.27198623905683128 ) ) ;
#50688=CARTESIAN_POINT ( 'NONE',  ( 5.910764540655177868, 0.6565643306762071196, 20.10149650520694209 ) ) ;
#50693=EDGE_CURVE ( 'NONE', #43662, #19259, #12839, .T. ) ;
#50695=CONICAL_SURFACE ( 'NONE', #40729, 47.09074272231896430, 0.04450589592586084303 ) ;
#50702=CARTESIAN_POINT ( 'NONE',  ( 0.8560838555295158248, 42.82099363437792050, 19.15033519931955297 ) ) ;
#50710=ORIENTED_EDGE ( 'NONE', *, *, #41440, .F. ) ;
#50712=CARTESIAN_POINT ( 'NONE',  ( 5.838029081930955932, 38.93046761018045032, 26.74852799324872876 ) ) ;
#50715=CARTESIAN_POINT ( 'NONE',  ( 0.8554163680231816613, -44.01281378489805007, 16.25046755781837149 ) ) ;
#50719=CARTESIAN_POINT ( 'NONE',  ( 0.9784957157296378938, -17.42937915973441676, 38.11233132594468032 ) ) ;
#50721=CARTESIAN_POINT ( 'NONE',  ( 0.7764146366350260786, -34.18255388834246844, 32.11842902975998726 ) ) ;
#50727=CARTESIAN_POINT ( 'NONE',  ( 0.5806925824938502512, -30.69245420804159252, -35.45695442407362208 ) ) ;
#50729=DIRECTION ( 'NONE',  ( -0.07500201931887529039, 0.7741482765856609882, -0.6285452592753698609 ) ) ;
#50730=CARTESIAN_POINT ( 'NONE',  ( 5.894904586330512508, -2.014437969560215702, -20.01178282233836470 ) ) ;
#50736=ORIENTED_EDGE ( 'NONE', *, *, #2954, .F. ) ;
#50739=CARTESIAN_POINT ( 'NONE',  ( 0.7056313189692714483, -44.02267996129995709, 16.17876055149217507 ) ) ;
#50740=CARTESIAN_POINT ( 'NONE',  ( 0.9784957157296367836, 9.488681859340672986, -40.82031324677200956 ) ) ;
#50742=PRESENTATION_STYLE_ASSIGNMENT (( #60750 ) ) ;
#50744=ORIENTED_EDGE ( 'NONE', *, *, #43405, .T. ) ;
#50748=CARTESIAN_POINT ( 'NONE',  ( 2.156377650103387111, -0.2527589248780885978, 46.96604083475408942 ) ) ;
#50752=CARTESIAN_POINT ( 'NONE',  ( 2.528190830796653188, 19.10480206427283179, 37.37995016366345880 ) ) ;
#50754=EDGE_CURVE ( 'NONE', #217, #57622, #3697, .T. ) ;
#50756=ADVANCED_FACE ( 'NONE', ( #13440 ), #30549, .F. ) ;
#50762=LINE ( 'NONE', #36086, #42545 ) ;
#50765=CARTESIAN_POINT ( 'NONE',  ( 4.962356264823608143, -40.47344704301786322, -11.53844366967987334 ) ) ;
#50774=ORIENTED_EDGE ( 'NONE', *, *, #29755, .T. ) ;
#50780=CARTESIAN_POINT ( 'NONE',  ( 0.7056759521544978542, 21.79701521802849129, 41.52877263659524232 ) ) ;
#50781=ORIENTED_EDGE ( 'NONE', *, *, #4069, .T. ) ;
#50785=CARTESIAN_POINT ( 'NONE',  ( 4.291220156522060236, 18.92432707711487438, 43.14230918696951278 ) ) ;
#50794=CARTESIAN_POINT ( 'NONE',  ( 0.5824935313925942992, -29.99830834406015256, 36.04635451121971812 ) ) ;
#50801=VERTEX_POINT ( 'NONE', #19078 ) ;
#50804=EDGE_LOOP ( 'NONE', ( #10579, #57334, #1927, #9875 ) ) ;
#50811=ORIENTED_EDGE ( 'NONE', *, *, #17535, .T. ) ;
#50812=CARTESIAN_POINT ( 'NONE',  ( 0.6845945791218023269, -0.7015599581314457822, 46.90324439033074810 ) ) ;
#50813=CARTESIAN_POINT ( 'NONE',  ( 0.9775691876210974574, -41.83858028429363429, 2.422170263360079456 ) ) ;
#50818=CARTESIAN_POINT ( 'NONE',  ( 1.231276596079887264, 20.88402890667827450, 36.34740854095507245 ) ) ;
#50827=CARTESIAN_POINT ( 'NONE',  ( 0.5837799406558229487, -13.98113914491203502, -44.76350408298939243 ) ) ;
#50829=CARTESIAN_POINT ( 'NONE',  ( 0.9785694773339237429, -22.73759263024291855, 35.20422257479631156 ) ) ;
#50836=FACE_OUTER_BOUND ( 'NONE', #28365, .T. ) ;
#50839=LINE ( 'NONE', #59931, #54881 ) ;
#50843=VERTEX_POINT ( 'NONE', #58171 ) ;
#50846=CARTESIAN_POINT ( 'NONE',  ( 3.376099380956838925, -12.50537924370748044, -4.829479641029388759 ) ) ;
#50853=EDGE_CURVE ( 'NONE', #32810, #38419, #27366, .T. ) ;
#50856=ORIENTED_EDGE ( 'NONE', *, *, #9749, .F. ) ;
#50862=ORIENTED_EDGE ( 'NONE', *, *, #46023, .F. ) ;
#50869=CARTESIAN_POINT ( 'NONE',  ( 0.5848930533535030563, 4.875316827623189297, -46.64230234688091059 ) ) ;
#50878=ORIENTED_EDGE ( 'NONE', *, *, #43902, .F. ) ;
#50880=CARTESIAN_POINT ( 'NONE',  ( 3.782542959838399721, -38.26640512950806539, 17.40459973285597428 ) ) ;
#50885=CARTESIAN_POINT ( 'NONE',  ( 1.231276596079887264, -41.76121777166943616, 3.643825084340432952 ) ) ;
#50886=CARTESIAN_POINT ( 'NONE',  ( 0.9762797500689124330, 20.58271139965541963, -36.50584578699964311 ) ) ;
#50888=CARTESIAN_POINT ( 'NONE',  ( 5.894904586330512508, -13.98322986223360864, -14.45678714934895126 ) ) ;
#50889=PRODUCT_DEFINITION_FORMATION_WITH_SPECIFIED_SOURCE ( 'ANY', '', #6712, .NOT_KNOWN. ) ;
#50893=CARTESIAN_POINT ( 'NONE',  ( 4.958415959904816539, 2.023024899602716253, 45.37743188059704380 ) ) ;
#50905=DIRECTION ( 'NONE',  ( 0.000000000000000000, 0.000000000000000000, 1.000000000000000000 ) ) ;
#50912=CARTESIAN_POINT ( 'NONE',  ( 0.5834584762367746036, -7.979694474790339775, 46.21212465470713227 ) ) ;
#50916=CARTESIAN_POINT ( 'NONE',  ( 4.956445790443989807, 42.27038699792205279, 20.75457619864928205 ) ) ;
#50924=CARTESIAN_POINT ( 'NONE',  ( 0.9788927965476016402, 32.80188811192217457, -26.08395577600753512 ) ) ;
#50928=CARTESIAN_POINT ( 'NONE',  ( 0.8560838555295158248, 36.24009790160309308, 29.78301761346479282 ) ) ;
#50946=( BOUNDED_SURFACE ( )  B_SPLINE_SURFACE ( 3, 1, ( 
 ( #18408, #34060 ),
 ( #502, #19644 ),
 ( #57195, #19331 ),
 ( #61288, #42532 ) ),
 .UNSPECIFIED., .F., .F., .F. ) 
 B_SPLINE_SURFACE_WITH_KNOTS ( ( 4, 4 ),
 ( 2, 2 ),
 ( 0.000000000000000000, 1.000000000000000000 ),
 ( 0.000000000000000000, 1.000000000000000000 ),
 .UNSPECIFIED. ) 
 GEOMETRIC_REPRESENTATION_ITEM ( )  RATIONAL_B_SPLINE_SURFACE ( (
 ( 1.000000000000000000, 1.000000000000000000),
 ( 0.9952954269826590483, 0.8620686068821339365),
 ( 0.9952954269826590483, 0.8620686068821339365),
 ( 1.000000000000000000, 1.000000000000000000) ) ) 
 REPRESENTATION_ITEM ( '' )  SURFACE ( )  );
#50948=VECTOR ( 'NONE', #54212, 999.9999999999998863 ) ;
#50955=VECTOR ( 'NONE', #28822, 999.9999999999998863 ) ;
#50959=CARTESIAN_POINT ( 'NONE',  ( 1.157643937452369265, -0.5751542567737857325, 41.91266481835375401 ) ) ;
#50964=CARTESIAN_POINT ( 'NONE',  ( 4.956445790443996913, 7.299064093730984304, 46.52162629890795387 ) ) ;
#50972=CARTESIAN_POINT ( 'NONE',  ( 0.9772918015221170318, -26.73923612106478132, 32.26995673087623118 ) ) ;
#50985=B_SPLINE_CURVE_WITH_KNOTS ( 'NONE', 3,
 ( #24530, #53028, #10441, #57710, #4780, #14840 ),
 .UNSPECIFIED., .F., .F.,
 ( 4, 2, 4 ),
 ( 8.673617379884034509E-19, 0.0002291459268755701264, 0.0004582918537511393854 ),
 .UNSPECIFIED. ) ;
#50993=ORIENTED_EDGE ( 'NONE', *, *, #21299, .T. ) ;
#51005=ORIENTED_EDGE ( 'NONE', *, *, #57592, .F. ) ;
#51008=B_SPLINE_CURVE_WITH_KNOTS ( 'NONE', 3,
 ( #46208, #22380, #17687, #24226, #57105, #19241 ),
 .UNSPECIFIED., .F., .F.,
 ( 4, 2, 4 ),
 ( 9.341771812940338307E-18, 0.0002291472222819920140, 0.0004582944445639746496 ),
 .UNSPECIFIED. ) ;
#51022=EDGE_CURVE ( 'NONE', #32724, #15442, #26525, .T. ) ;
#51023=EDGE_LOOP ( 'NONE', ( #54241, #13421, #45997, #59674 ) ) ;
#51024=EDGE_LOOP ( 'NONE', ( #24145, #21753, #19383, #30121 ) ) ;
#51032=CARTESIAN_POINT ( 'NONE',  ( 5.895596859100789899, 20.06773179721815126, -1.346968346846738385 ) ) ;
#51034=VERTEX_POINT ( 'NONE', #3931 ) ;
#51036=CARTESIAN_POINT ( 'NONE',  ( 3.782542959838396168, 27.96057807588762145, 31.39178120239056469 ) ) ;
#51045=CARTESIAN_POINT ( 'NONE',  ( 0.9762797500689124330, 9.222352665238926051, -40.88120590813907285 ) ) ;
#51049=ORIENTED_EDGE ( 'NONE', *, *, #21358, .T. ) ;
#51051=DIRECTION ( 'NONE',  ( -1.000000000000000000, -0.000000000000000000, -0.000000000000000000 ) ) ;
#51054=VECTOR ( 'NONE', #54900, 1000.000000000000000 ) ;
#51077=CARTESIAN_POINT ( 'NONE',  ( 5.917102823773431552, -18.51268610137626425, 7.859400191086610477 ) ) ;
#51086=ORIENTED_EDGE ( 'NONE', *, *, #28172, .T. ) ;
#51087=CARTESIAN_POINT ( 'NONE',  ( 4.956445790443987143, 47.01859095792193699, -2.605792484304513934 ) ) ;
#51089=CARTESIAN_POINT ( 'NONE',  ( 4.962356264823593932, 7.429277797797228189, 41.42513040734459651 ) ) ;
#51107=CARTESIAN_POINT ( 'NONE',  ( 4.960386119450144626, -43.29863790797085699, 6.297969513007277698 ) ) ;
#51113=CARTESIAN_POINT ( 'NONE',  ( 0.8560838555295158248, 44.99141268455571208, 13.27198623905747432 ) ) ;
#51114=FACE_OUTER_BOUND ( 'NONE', #25492, .T. ) ;
#51127=CARTESIAN_POINT ( 'NONE',  ( 0.9762797500689124330, 32.57381952463229169, 26.36799322592426975 ) ) ;
#51128=CARTESIAN_POINT ( 'NONE',  ( 3.782542959838397056, -36.71077845802598461, -20.48308078396187426 ) ) ;
#51130=CARTESIAN_POINT ( 'NONE',  ( 4.962356264823596597, 37.75702904547799932, 18.59145920903680249 ) ) ;
#51137=CARTESIAN_POINT ( 'NONE',  ( 0.7056759521544971880, -13.08829070999385102, -45.03826678956104246 ) ) ;
#51138=DIRECTION ( 'NONE',  ( 1.000000000000000000, 0.000000000000000000, 0.000000000000000000 ) ) ;
#51140=ORIENTED_EDGE ( 'NONE', *, *, #52630, .F. ) ;
#51149=B_SPLINE_CURVE_WITH_KNOTS ( 'NONE', 3,
 ( #3001, #32773, #51230, #8311, #60312, #50924, #42188, #27432, #46562, #17127, #12745, #56550, #36240, #22742, #51851, #8950, #17425, #41875, #36549 ),
 .UNSPECIFIED., .F., .F.,
 ( 4, 3, 3, 3, 3, 3, 4 ),
 ( 0.000000000000000000, 0.0002732106629380697503, 0.0004098138914053829672, 0.0005464171197651475570, 0.0006830203481512520797, 0.0008196235766963617898, 0.001011968216111154388 ),
 .UNSPECIFIED. ) ;
#51150=DIRECTION ( 'NONE',  ( 0.07500201931887537365, 0.9374924185315435254, 0.3398274007403879748 ) ) ;
#51152=ORIENTED_EDGE ( 'NONE', *, *, #41906, .T. ) ;
#51156=CARTESIAN_POINT ( 'NONE',  ( 4.962356264823608143, 0.000000000000000000, 0.000000000000000000 ) ) ;
#51176=VECTOR ( 'NONE', #40998, 1000.000000000000000 ) ;
#51180=CARTESIAN_POINT ( 'NONE',  ( 5.895881250540457863, -18.51869114342256495, -7.847659520062246763 ) ) ;
#51187=ADVANCED_FACE ( 'NONE', ( #58707 ), #28540, .F. ) ;
#51191=CARTESIAN_POINT ( 'NONE',  ( 1.157643937452369265, 40.63757547730140374, 10.27568654258122827 ) ) ;
#51193=CARTESIAN_POINT ( 'NONE',  ( 0.5804410086790514622, 32.99440095573996246, 33.33000686209445718 ) ) ;
#51214=VERTEX_POINT ( 'NONE', #9895 ) ;
#51215=CARTESIAN_POINT ( 'NONE',  ( 5.895596859100789899, 10.82540956478658423, 16.95106754653271608 ) ) ;
#51216=DIRECTION ( 'NONE',  ( -1.000000000000000000, -0.000000000000000000, -0.000000000000000000 ) ) ;
#51218=EDGE_CURVE ( 'NONE', #56041, #20493, #56741, .T. ) ;
#51223=CIRCLE ( 'NONE', #54200, 47.09074272231896430 ) ;
#51230=CARTESIAN_POINT ( 'NONE',  ( 0.9780303403264775097, 32.68824397619722077, -26.22629060976198900 ) ) ;
#51242=CARTESIAN_POINT ( 'NONE',  ( 0.9772918015221172539, 3.781849303984199828, -41.73768646670097837 ) ) ;
#51245=VERTEX_POINT ( 'NONE', #24610 ) ;
#51253=EDGE_CURVE ( 'NONE', #129, #7149, #53401, .T. ) ;
#51263=CARTESIAN_POINT ( 'NONE',  ( 0.5832655196449135770, -41.95774188719079945, 20.94714965576949339 ) ) ;
#51267=AXIS2_PLACEMENT_3D ( 'NONE', #27069, #37414, #22369 ) ;
#51269=CARTESIAN_POINT ( 'NONE',  ( 0.8560838555295158248, 21.73747136795142154, 41.56747734237938374 ) ) ;
#51285=DIRECTION ( 'NONE',  ( 0.000000000000000000, 0.000000000000000000, 1.000000000000000000 ) ) ;
#51291=CARTESIAN_POINT ( 'NONE',  ( 2.528190830796654076, 35.48724657021211470, 22.42564306810345442 ) ) ;
#51293=CARTESIAN_POINT ( 'NONE',  ( 0.5804410086790514622, 40.62771722849963396, 23.42879520283685935 ) ) ;
#51295=CARTESIAN_POINT ( 'NONE',  ( 4.962356264823593932, 7.429277797797228189, 41.42513040734459651 ) ) ;
#51340=ORIENTED_EDGE ( 'NONE', *, *, #38715, .F. ) ;
#51344=CARTESIAN_POINT ( 'NONE',  ( 1.091591847532192627, 40.21132067974347279, 11.82407206281648548 ) ) ;
#51347=EDGE_CURVE ( 'NONE', #48086, #19405, #54391, .T. ) ;
#51357=CARTESIAN_POINT ( 'NONE',  ( 1.000433927950263424, 41.61836910708317561, 4.932548075734225712 ) ) ;
#51363=B_SPLINE_CURVE_WITH_KNOTS ( 'NONE', 3,
 ( #54271, #29567, #30478, #58666 ),
 .UNSPECIFIED., .F., .F.,
 ( 4, 4 ),
 ( 0.000000000000000000, 0.005004948556313810505 ),
 .UNSPECIFIED. ) ;
#51365=VECTOR ( 'NONE', #39343, 999.9999999999998863 ) ;
#51367=EDGE_CURVE ( 'NONE', #39717, #40072, #13390, .T. ) ;
#51371=CARTESIAN_POINT ( 'NONE',  ( 0.9789889208857691649, 20.22481679127239218, 36.70547212340194676 ) ) ;
#51388=CARTESIAN_POINT ( 'NONE',  ( 5.896278296736517710, 5.953715084307799721, -19.21146158701282758 ) ) ;
#51391=CARTESIAN_POINT ( 'NONE',  ( 4.960386119450151732, 43.68547429165921159, -2.452712903118141607 ) ) ;
#51398=CARTESIAN_POINT ( 'NONE',  ( 0.5797568665920715958, 46.89167813730860956, -0.6291502753107942603 ) ) ;
#51404=ORIENTED_EDGE ( 'NONE', *, *, #37497, .T. ) ;
#51405=DIRECTION ( 'NONE',  ( 0.000000000000000000, 0.000000000000000000, 1.000000000000000000 ) ) ;
#51407=CARTESIAN_POINT ( 'NONE',  ( 4.960386119450153508, 0.9915941002484534028, 43.74303608361783802 ) ) ;
#51409=ORIENTED_EDGE ( 'NONE', *, *, #60869, .T. ) ;
#51419=CARTESIAN_POINT ( 'NONE',  ( 0.5782707292762423457, 45.03824936633927223, -13.08787407194379604 ) ) ;
#51423=CARTESIAN_POINT ( 'NONE',  ( 1.157644175074337367, 41.90847804166124035, 0.8256777281599040341 ) ) ;
#51424=B_SPLINE_CURVE_WITH_KNOTS ( 'NONE', 3,
 ( #53221, #52919, #29730, #29117 ),
 .UNSPECIFIED., .F., .F.,
 ( 4, 4 ),
 ( 3.496446946337351263E-17, 0.005004948556313842598 ),
 .UNSPECIFIED. ) ;
#51431=CARTESIAN_POINT ( 'NONE',  ( 0.5806925824938499181, 46.54710689580866756, -5.708695295225145294 ) ) ;
#51436=CARTESIAN_POINT ( 'NONE',  ( 5.895596859100789899, -4.659086063546006073, 19.56581458219818259 ) ) ;
#51437=CARTESIAN_POINT ( 'NONE',  ( 4.958415959904820092, -10.03736369554633079, -44.29960816831192716 ) ) ;
#51445=VERTEX_POINT ( 'NONE', #55878 ) ;
#51452=ORIENTED_EDGE ( 'NONE', *, *, #53084, .T. ) ;
#51455=CARTESIAN_POINT ( 'NONE',  ( 0.7764146366350244133, 3.807011318490865825, -46.74983570548722156 ) ) ;
#51458=ORIENTED_EDGE ( 'NONE', *, *, #14232, .F. ) ;
#51466=EDGE_CURVE ( 'NONE', #37333, #59460, #45412, .T. ) ;
#51473=CARTESIAN_POINT ( 'NONE',  ( 0.5817217712918331118, -38.91886904608055175, 26.16403229975087186 ) ) ;
#51475=ADVANCED_FACE ( 'NONE', ( #46824, #3863 ), #47124, .T. ) ;
#51479=ADVANCED_FACE ( 'NONE', ( #32712 ), #39372, .F. ) ;
#51480=( BOUNDED_SURFACE ( )  B_SPLINE_SURFACE ( 3, 1, ( 
 ( #29707, #43850 ),
 ( #44165, #1195 ),
 ( #20329, #7114 ),
 ( #60354, #54735 ) ),
 .UNSPECIFIED., .F., .F., .F. ) 
 B_SPLINE_SURFACE_WITH_KNOTS ( ( 4, 4 ),
 ( 2, 2 ),
 ( 0.000000000000000000, 1.000000000000000000 ),
 ( 0.000000000000000000, 1.000000000000000000 ),
 .UNSPECIFIED. ) 
 GEOMETRIC_REPRESENTATION_ITEM ( )  RATIONAL_B_SPLINE_SURFACE ( (
 ( 1.000000000000000000, 1.000000000000000000),
 ( 0.9952954269826590483, 0.8620686068821307169),
 ( 0.9952954269826590483, 0.8620686068821307169),
 ( 1.000000000000000000, 1.000000000000000000) ) ) 
 REPRESENTATION_ITEM ( '' )  SURFACE ( )  );
#51482=VECTOR ( 'NONE', #12786, 1000.000000000000000 ) ;
#51483=VERTEX_POINT ( 'NONE', #53554 ) ;
#51489=ORIENTED_EDGE ( 'NONE', *, *, #38579, .T. ) ;
#51498=( BOUNDED_SURFACE ( )  B_SPLINE_SURFACE ( 3, 1, ( 
 ( #37334, #18848 ),
 ( #47961, #52018 ),
 ( #9115, #38575 ),
 ( #28221, #28524 ) ),
 .UNSPECIFIED., .F., .F., .F. ) 
 B_SPLINE_SURFACE_WITH_KNOTS ( ( 4, 4 ),
 ( 2, 2 ),
 ( 0.000000000000000000, 1.000000000000000000 ),
 ( 0.000000000000000000, 1.000000000000000000 ),
 .UNSPECIFIED. ) 
 GEOMETRIC_REPRESENTATION_ITEM ( )  RATIONAL_B_SPLINE_SURFACE ( (
 ( 1.000000000000000000, 1.000000000000000000),
 ( 0.9952954269826590483, 0.8620686068821307169),
 ( 0.9952954269826590483, 0.8620686068821307169),
 ( 1.000000000000000000, 1.000000000000000000) ) ) 
 REPRESENTATION_ITEM ( '' )  SURFACE ( )  );
#51502=CARTESIAN_POINT ( 'NONE',  ( 0.9762797500689124330, -1.905951756780080775, -41.86516610604251554 ) ) ;
#51505=CARTESIAN_POINT ( 'NONE',  ( 0.5806925824938494740, -46.75147433417404841, 3.677228565731047283 ) ) ;
#51508=CARTESIAN_POINT ( 'NONE',  ( 0.5817216825391108292, -35.08429596696358743, -31.11795508560874524 ) ) ;
#51514=CARTESIAN_POINT ( 'NONE',  ( 0.8554163680231816613, 9.985124899324974379, -45.84215040611314862 ) ) ;
#51515=CARTESIAN_POINT ( 'NONE',  ( 0.8560838555295158248, -18.91252766612255698, -42.92655508376930129 ) ) ;
#51519=B_SPLINE_CURVE_WITH_KNOTS ( 'NONE', 3,
 ( #30945, #17166, #50653, #60061, #20930, #11537 ),
 .UNSPECIFIED., .F., .F.,
 ( 4, 2, 4 ),
 ( 9.872790465222285426E-18, 0.0002448709889506573193, 0.0004897419779013047723 ),
 .UNSPECIFIED. ) ;
#51522=CARTESIAN_POINT ( 'NONE',  ( 5.917102823773431552, 17.95415397368203614, -9.063005745394821844 ) ) ;
#51537=CARTESIAN_POINT ( 'NONE',  ( 4.960386119450139297, 39.26151414358965042, 19.31243050019988772 ) ) ;
#51548=CARTESIAN_POINT ( 'NONE',  ( 0.9790320750461898314, 4.280404874073830968, -41.68951027124445119 ) ) ;
#51551=ORIENTED_EDGE ( 'NONE', *, *, #31323, .T. ) ;
#51554=ADVANCED_FACE ( 'NONE', ( #49487 ), #44148, .F. ) ;
#51565=CARTESIAN_POINT ( 'NONE',  ( 0.5835226383429291674, -41.77317149982144429, 21.31301521119128140 ) ) ;
#51580=CARTESIAN_POINT ( 'NONE',  ( 0.9785694773339250752, -27.22697983396325583, 31.85948798765653223 ) ) ;
#51598=B_SPLINE_CURVE_WITH_KNOTS ( 'NONE', 3,
 ( #21637, #59844, #40165, #55132 ),
 .UNSPECIFIED., .F., .F.,
 ( 4, 4 ),
 ( 2.602085213965210642E-18, 0.004042984057420973693 ),
 .UNSPECIFIED. ) ;
#51602=ADVANCED_FACE ( 'NONE', ( #6233 ), #20147, .F. ) ;
#51604=( BOUNDED_SURFACE ( )  B_SPLINE_SURFACE ( 3, 1, ( 
 ( #52553, #1162 ),
 ( #20296, #24065 ),
 ( #48187, #24680 ),
 ( #39418, #29072 ) ),
 .UNSPECIFIED., .F., .F., .F. ) 
 B_SPLINE_SURFACE_WITH_KNOTS ( ( 4, 4 ),
 ( 2, 2 ),
 ( 0.000000000000000000, 1.000000000000000000 ),
 ( 0.000000000000000000, 1.000000000000000000 ),
 .UNSPECIFIED. ) 
 GEOMETRIC_REPRESENTATION_ITEM ( )  RATIONAL_B_SPLINE_SURFACE ( (
 ( 1.000000000000000000, 1.000000000000000000),
 ( 0.9952954269826590483, 0.8620686068821307169),
 ( 0.9952954269826590483, 0.8620686068821307169),
 ( 1.000000000000000000, 1.000000000000000000) ) ) 
 REPRESENTATION_ITEM ( '' )  SURFACE ( )  );
#51605=ORIENTED_EDGE ( 'NONE', *, *, #4023, .F. ) ;
#51611=CARTESIAN_POINT ( 'NONE',  ( 0.5804410086790514622, -25.69437916690352353, -39.23415261073942162 ) ) ;
#51612=EDGE_CURVE ( 'NONE', #26084, #20677, #15603, .T. ) ;
#51616=B_SPLINE_CURVE_WITH_KNOTS ( 'NONE', 3,
 ( #37714, #37396, #42113, #13903 ),
 .UNSPECIFIED., .F., .F.,
 ( 4, 4 ),
 ( 0.000000000000000000, 0.004447772540403824131 ),
 .UNSPECIFIED. ) ;
#51640=CONICAL_SURFACE ( 'NONE', #19694, 42.08604991992415023, 1.569615340895231137 ) ;
#51646=FACE_OUTER_BOUND ( 'NONE', #7092, .T. ) ;
#51650=ORIENTED_EDGE ( 'NONE', *, *, #39532, .F. ) ;
#51658=ORIENTED_EDGE ( 'NONE', *, *, #14789, .F. ) ;
#51665=( NAMED_UNIT ( * ) SI_UNIT ( $, .STERADIAN. ) SOLID_ANGLE_UNIT ( ) );
#51667=EDGE_LOOP ( 'NONE', ( #3924, #39440, #40965, #56519 ) ) ;
#51669=FACE_OUTER_BOUND ( 'NONE', #59346, .T. ) ;
#51671=CARTESIAN_POINT ( 'NONE',  ( 3.376099380956838925, -12.16518930220327555, 5.631745100199947451 ) ) ;
#51677=CARTESIAN_POINT ( 'NONE',  ( 0.5835226383429301666, 22.37749966153948478, -41.21274054759963690 ) ) ;
#51681=CARTESIAN_POINT ( 'NONE',  ( 5.910764540655178756, -13.99299321836462440, -14.44636214622783577 ) ) ;
#51687=CARTESIAN_POINT ( 'NONE',  ( 0.9762797500689124330, 40.28286501695585997, -11.55922018180369548 ) ) ;
#51692=CARTESIAN_POINT ( 'NONE',  ( 0.9780303403264775097, -41.83550024410291712, -2.475991260233099123 ) ) ;
#51697=CARTESIAN_POINT ( 'NONE',  ( 3.238018933889920792, 9.507325605900218690, 9.434948446655496923 ) ) ;
#51699=CARTESIAN_POINT ( 'NONE',  ( 3.782542959838389951, 26.30383675830739421, -32.79246903160672133 ) ) ;
#51700=VERTEX_POINT ( 'NONE', #12848 ) ;
#51707=CARTESIAN_POINT ( 'NONE',  ( 1.231276596079887264, 24.17959027891153667, -34.24360064248551083 ) ) ;
#51709=DIRECTION ( 'NONE',  ( -1.000000000000000000, -0.000000000000000000, -0.000000000000000000 ) ) ;
#51725=CARTESIAN_POINT ( 'NONE',  ( 5.910764540655177868, 12.99683459030034349, -15.34873053713353563 ) ) ;
#51727=CARTESIAN_POINT ( 'NONE',  ( 0.5806925824938511393, 10.33919002968708689, -45.74192291403568333 ) ) ;
#51729=CARTESIAN_POINT ( 'NONE',  ( 0.9790320750461898314, -34.50252855204712432, -23.78891876604240707 ) ) ;
#51736=CARTESIAN_POINT ( 'NONE',  ( 0.9762797500689124330, 35.79768877047958853, 21.79105926469807741 ) ) ;
#51739=DIRECTION ( 'NONE',  ( 0.07906939808003034253, 0.9390317839750903506, 0.3346152103115173637 ) ) ;
#51740=CARTESIAN_POINT ( 'NONE',  ( 2.282803330402963127, -26.37305679751943188, 38.87105327376399799 ) ) ;
#51742=CARTESIAN_POINT ( 'NONE',  ( 0.9787464366903569912, -12.58548318642580455, 39.97423677638705186 ) ) ;
#51745=CARTESIAN_POINT ( 'NONE',  ( 0.7764139734771229318, 33.24270203466717533, -33.09022865350438281 ) ) ;
#51747=CARTESIAN_POINT ( 'NONE',  ( 4.962356264823608143, -40.70360067759239087, 10.69824704058788711 ) ) ;
#51755=CARTESIAN_POINT ( 'NONE',  ( 4.960386119450151732, -9.684723978931470967, -42.66898857629802677 ) ) ;
#51763=ORIENTED_EDGE ( 'NONE', *, *, #32073, .F. ) ;
#51777=ORIENTED_EDGE ( 'NONE', *, *, #27156, .F. ) ;
#51787=B_SPLINE_CURVE_WITH_KNOTS ( 'NONE', 3,
 ( #61200, #46830, #50568, #18315, #17080, #13304 ),
 .UNSPECIFIED., .F., .F.,
 ( 4, 2, 4 ),
 ( 0.000000000000000000, 0.0002291459268755674972, 0.0004582918537511349944 ),
 .UNSPECIFIED. ) ;
#51793=CARTESIAN_POINT ( 'NONE',  ( 0.5837799406558233928, -38.61146441179320732, 26.61575408576708313 ) ) ;
#51800=ORIENTED_EDGE ( 'NONE', *, *, #37865, .F. ) ;
#51802=CARTESIAN_POINT ( 'NONE',  ( 5.894904586330512508, 3.344157678208643514, -19.83295291894076229 ) ) ;
#51809=CARTESIAN_POINT ( 'NONE',  ( 0.5804410086790514622, 22.05813747677437320, 41.38790189066267544 ) ) ;
#51811=CARTESIAN_POINT ( 'NONE',  ( 0.5806925824938502512, -30.69245420804159252, -35.45695442407362208 ) ) ;
#51817=CARTESIAN_POINT ( 'NONE',  ( 0.6064782688330845328, 11.56181350407003983, -45.44952051359700107 ) ) ;
#51818=ORIENTED_EDGE ( 'NONE', *, *, #31443, .T. ) ;
#51829=AXIS2_PLACEMENT_3D ( 'NONE', #54031, #49046, #19634 ) ;
#51833=ORIENTED_EDGE ( 'NONE', *, *, #35542, .T. ) ;
#51835=CARTESIAN_POINT ( 'NONE',  ( 5.896782393890504181, 5.952874097602693482, -19.21169895808549200 ) ) ;
#51838=ORIENTED_EDGE ( 'NONE', *, *, #40946, .F. ) ;
#51843=EDGE_CURVE ( 'NONE', #6162, #35188, #49204, .T. ) ;
#51851=CARTESIAN_POINT ( 'NONE',  ( 0.9783242366443551941, 33.05536268497406382, -25.76193874636278380 ) ) ;
#51854=B_SPLINE_CURVE_WITH_KNOTS ( 'NONE', 3,
 ( #14381, #37578, #61041, #60723 ),
 .UNSPECIFIED., .F., .F.,
 ( 4, 4 ),
 ( 0.000000000000000000, 0.005004948556313805301 ),
 .UNSPECIFIED. ) ;
#51855=CARTESIAN_POINT ( 'NONE',  ( 4.956445790443988031, 0.000000000000000000, 0.000000000000000000 ) ) ;
#51863=CARTESIAN_POINT ( 'NONE',  ( 0.9789233960466705575, -37.34478551170388272, -19.01850998151991234 ) ) ;
#51865=CARTESIAN_POINT ( 'NONE',  ( 5.917102823773431552, -13.97547681749000681, -14.46291000371437718 ) ) ;
#51874=ORIENTED_EDGE ( 'NONE', *, *, #24538, .T. ) ;
#51876=ORIENTED_EDGE ( 'NONE', *, *, #28397, .T. ) ;
#51878=CARTESIAN_POINT ( 'NONE',  ( 0.5824936645240093025, 27.52370025514170848, 37.96951544733510531 ) ) ;
#51881=B_SPLINE_CURVE_WITH_KNOTS ( 'NONE', 3,
 ( #40118, #21904, #59798, #45117 ),
 .UNSPECIFIED., .F., .F.,
 ( 4, 4 ),
 ( 0.000000000000000000, 0.005004948556313800097 ),
 .UNSPECIFIED. ) ;
#51882=CARTESIAN_POINT ( 'NONE',  ( 4.956445790444010235, -22.15545010017738647, -41.55326799420456751 ) ) ;
#51886=CARTESIAN_POINT ( 'NONE',  ( 4.962356264823608143, 0.000000000000000000, 0.000000000000000000 ) ) ;
#51891=CARTESIAN_POINT ( 'NONE',  ( 2.618530812446111078, 44.94501346709284206, 13.77216590232064952 ) ) ;
#51897=CARTESIAN_POINT ( 'NONE',  ( 5.895596859100789899, 19.70914391261467102, 4.009716878325924050 ) ) ;
#51899=CARTESIAN_POINT ( 'NONE',  ( 0.8560838555295158248, 39.88643293834648063, 24.68694597426990001 ) ) ;
#51902=DIRECTION ( 'NONE',  ( -0.07906939808003035641, 0.4719801263062105012, -0.8780562571152461526 ) ) ;
#51905=CARTESIAN_POINT ( 'NONE',  ( 3.782625744892853081, 31.89518695616269639, -27.38494391315110832 ) ) ;
#51916=CARTESIAN_POINT ( 'NONE',  ( 0.7056313189692671184, 31.99428634539452077, -34.29452267063153670 ) ) ;
#51917=B_SPLINE_CURVE_WITH_KNOTS ( 'NONE', 3,
 ( #57231, #47256, #14368, #61628 ),
 .UNSPECIFIED., .F., .F.,
 ( 4, 4 ),
 ( 3.469446951953614189E-18, 0.005004948556313816577 ),
 .UNSPECIFIED. ) ;
#51923=CARTESIAN_POINT ( 'NONE',  ( 0.5830082357119558134, 46.44034146464806412, 6.521251381845879713 ) ) ;
#51925=EDGE_CURVE ( 'NONE', #7001, #26439, #5791, .T. ) ;
#51928=ORIENTED_EDGE ( 'NONE', *, *, #40913, .F. ) ;
#51931=CARTESIAN_POINT ( 'NONE',  ( 0.5804410086790514622, 45.08525424748425792, 12.91664435118884846 ) ) ;
#51932=ORIENTED_EDGE ( 'NONE', *, *, #37386, .T. ) ;
#51937=VECTOR ( 'NONE', #6019, 1000.000000000000114 ) ;
#51946=CARTESIAN_POINT ( 'NONE',  ( 5.910764540655177868, 16.59011036809723905, -11.36967354164205624 ) ) ;
#51947=ORIENTED_EDGE ( 'NONE', *, *, #54584, .T. ) ;
#51953=VECTOR ( 'NONE', #13165, 1000.000000000000114 ) ;
#51959=CARTESIAN_POINT ( 'NONE',  ( 0.5848930533535030563, 45.18167862054202999, -12.56538894812305784 ) ) ;
#51961=ORIENTED_EDGE ( 'NONE', *, *, #31491, .F. ) ;
#51978=( BOUNDED_SURFACE ( )  B_SPLINE_SURFACE ( 3, 1, ( 
 ( #51835, #37159 ),
 ( #23654, #28047 ),
 ( #13973, #61533 ),
 ( #42476, #46868 ) ),
 .UNSPECIFIED., .F., .F., .F. ) 
 B_SPLINE_SURFACE_WITH_KNOTS ( ( 4, 4 ),
 ( 2, 2 ),
 ( 0.000000000000000000, 1.000000000000000000 ),
 ( 0.000000000000000000, 1.000000000000000000 ),
 .UNSPECIFIED. ) 
 GEOMETRIC_REPRESENTATION_ITEM ( )  RATIONAL_B_SPLINE_SURFACE ( (
 ( 1.000000000000000000, 1.000000000000000000),
 ( 0.7282232189291694135, 0.9929344683865672927),
 ( 0.7282232189291694135, 0.9929344683865672927),
 ( 1.000000000000000000, 1.000000000000000000) ) ) 
 REPRESENTATION_ITEM ( '' )  SURFACE ( )  );
#51983=EDGE_CURVE ( 'NONE', #5475, #58971, #13340, .T. ) ;
#51987=CARTESIAN_POINT ( 'NONE',  ( 0.9769922540276048117, 28.81531089420057157, 30.43040277677394201 ) ) ;
#51989=CARTESIAN_POINT ( 'NONE',  ( 3.376099380956838925, 8.317686564981734421, -10.51306205816314332 ) ) ;
#51997=CARTESIAN_POINT ( 'NONE',  ( 0.6064782688330873084, -2.277226958765353526, 46.84174082799485461 ) ) ;
#51999=CARTESIAN_POINT ( 'NONE',  ( 4.962356264823602814, -29.56943756613081931, -29.94802096775409339 ) ) ;
#52002=ORIENTED_EDGE ( 'NONE', *, *, #36572, .F. ) ;
#52006=ORIENTED_EDGE ( 'NONE', *, *, #14088, .T. ) ;
#52008=ORIENTED_EDGE ( 'NONE', *, *, #5018, .T. ) ;
#52018=CARTESIAN_POINT ( 'NONE',  ( 0.6845945791218023269, -46.73791075327836353, 3.996776092368905964 ) ) ;
#52023=CARTESIAN_POINT ( 'NONE',  ( 0.5804410086790514622, -1.020940616196085671, 46.88792522722238942 ) ) ;
#52026=VERTEX_POINT ( 'NONE', #23693 ) ;
#52030=CIRCLE ( 'NONE', #60042, 42.08604991992415023 ) ;
#52034=CARTESIAN_POINT ( 'NONE',  ( 0.9789233960466710016, -34.47665692943588311, -23.82638986087320632 ) ) ;
#52038=EDGE_CURVE ( 'NONE', #4083, #19166, #18695, .T. ) ;
#52040=VECTOR ( 'NONE', #48961, 1000.000000000000000 ) ;
#52043=EDGE_CURVE ( 'NONE', #48086, #39870, #26422, .T. ) ;
#52046=CARTESIAN_POINT ( 'NONE',  ( 5.896278296736517710, 10.81775449038677905, -16.95591835908926726 ) ) ;
#52048=B_SPLINE_CURVE_WITH_KNOTS ( 'NONE', 3,
 ( #18999, #13992, #57781, #19296 ),
 .UNSPECIFIED., .F., .F.,
 ( 4, 4 ),
 ( 2.059984127722458425E-18, 0.004446298630425059815 ),
 .UNSPECIFIED. ) ;
#52049=CYLINDRICAL_SURFACE ( 'NONE', #33321, 8.000000000000000000 ) ;
#52050=( BOUNDED_SURFACE ( )  B_SPLINE_SURFACE ( 3, 1, ( 
 ( #32750, #41855 ),
 ( #60922, #8930 ),
 ( #57134, #32437 ),
 ( #14268, #28041 ) ),
 .UNSPECIFIED., .F., .F., .F. ) 
 B_SPLINE_SURFACE_WITH_KNOTS ( ( 4, 4 ),
 ( 2, 2 ),
 ( 0.000000000000000000, 1.000000000000000000 ),
 ( 0.000000000000000000, 1.000000000000000000 ),
 .UNSPECIFIED. ) 
 GEOMETRIC_REPRESENTATION_ITEM ( )  RATIONAL_B_SPLINE_SURFACE ( (
 ( 1.000000000000000000, 1.000000000000000000),
 ( 0.7282232189291693025, 0.9929344683865674037),
 ( 0.7282232189291693025, 0.9929344683865674037),
 ( 1.000000000000000000, 1.000000000000000000) ) ) 
 REPRESENTATION_ITEM ( '' )  SURFACE ( )  );
#52054=CARTESIAN_POINT ( 'NONE',  ( 0.5830082357119558134, 40.48789625336803510, -23.66352239027072457 ) ) ;
#52062=CARTESIAN_POINT ( 'NONE',  ( 0.5830082357119558134, 45.30112170676081718, -12.12602189704361955 ) ) ;
#52063=AXIS2_PLACEMENT_3D ( 'NONE', #11181, #7688, #40635 ) ;
#52066=ORIENTED_EDGE ( 'NONE', *, *, #50640, .F. ) ;
#52068=CARTESIAN_POINT ( 'NONE',  ( 0.5806925824938499181, -19.24316026636448029, -42.76591101925195204 ) ) ;
#52070=ORIENTED_EDGE ( 'NONE', *, *, #8204, .T. ) ;
#52076=EDGE_CURVE ( 'NONE', #17824, #36573, #49866, .T. ) ;
#52082=EDGE_LOOP ( 'NONE', ( #7577, #4746, #16925, #28065 ) ) ;
#52086=CARTESIAN_POINT ( 'NONE',  ( 4.958415959904820092, 40.30989464198759720, 20.93600601295518970 ) ) ;
#52089=ORIENTED_EDGE ( 'NONE', *, *, #52548, .F. ) ;
#52091=ORIENTED_EDGE ( 'NONE', *, *, #22786, .T. ) ;
#52096=CARTESIAN_POINT ( 'NONE',  ( 0.6064782688330866423, -14.57168774873476380, 44.57578224296398162 ) ) ;
#52098=CARTESIAN_POINT ( 'NONE',  ( 4.956445790444038657, 44.30493387627053181, -15.95653108789415953 ) ) ;
#52100=EDGE_CURVE ( 'NONE', #11923, #60728, #32756, .T. ) ;
#52105=CARTESIAN_POINT ( 'NONE',  ( 0.5835871038041873238, 36.88843343318914236, -28.95648341471509823 ) ) ;
#52112=VERTEX_POINT ( 'NONE', #19942 ) ;
#52118=CARTESIAN_POINT ( 'NONE',  ( 0.5797568665920720399, -41.56795284195428053, 21.71014981825170409 ) ) ;
#52137=CARTESIAN_POINT ( 'NONE',  ( 4.962356264823608143, 0.000000000000000000, 0.000000000000000000 ) ) ;
#52139=CARTESIAN_POINT ( 'NONE',  ( 0.5830081025819933149, -25.00319000804665137, 39.67458284347498676 ) ) ;
#52144=ORIENTED_EDGE ( 'NONE', *, *, #8833, .F. ) ;
#52145=ORIENTED_EDGE ( 'NONE', *, *, #36715, .F. ) ;
#52148=CARTESIAN_POINT ( 'NONE',  ( 5.896782393890504181, 17.95394716461052909, -9.065421561537322148 ) ) ;
#52162=CIRCLE ( 'NONE', #46203, 42.08604991992415023 ) ;
#52163=CARTESIAN_POINT ( 'NONE',  ( 3.782625744892852193, -5.285730353412130711, 41.70490569136944714 ) ) ;
#52170=CARTESIAN_POINT ( 'NONE',  ( 0.9780106845699496620, -37.26171966602630192, -19.18060202355250610 ) ) ;
#52171=CARTESIAN_POINT ( 'NONE',  ( 4.962356264823608143, -38.57439820587617163, -16.83007429920747811 ) ) ;
#52174=B_SPLINE_CURVE_WITH_KNOTS ( 'NONE', 3,
 ( #27302, #31390, #41738, #60801, #17923, #37043, #56106, #27612, #46740, #42052, #56411, #13527, #32632, #2559, #21679, #40823 ),
 .UNSPECIFIED., .F., .F.,
 ( 4, 3, 3, 3, 3, 4 ),
 ( 3.469446951953614189E-18, 0.0002732102107931864759, 0.0004098135523333763840, 0.0005464168938824969738, 0.0008195847345945471299, 0.001092771384553112637 ),
 .UNSPECIFIED. ) ;
#52176=ORIENTED_EDGE ( 'NONE', *, *, #16564, .T. ) ;
#52179=CARTESIAN_POINT ( 'NONE',  ( 0.5797568665920715958, -2.195683281786883434, -46.84446908150365374 ) ) ;
#52188=EDGE_CURVE ( 'NONE', #34245, #15772, #42461, .T. ) ;
#52191=EDGE_LOOP ( 'NONE', ( #41477, #8226, #4168, #11849 ) ) ;
#52196=CARTESIAN_POINT ( 'NONE',  ( 0.7764139734771262624, 36.25149465805695570, 29.76356171501883452 ) ) ;
#52198=CARTESIAN_POINT ( 'NONE',  ( 0.9762797500689124330, 41.59901070109194876, 5.084003725032276932 ) ) ;
#52199=CARTESIAN_POINT ( 'NONE',  ( 0.5797568599927144239, 4.067663806613229127, 46.71915474221869147 ) ) ;
#52201=CARTESIAN_POINT ( 'NONE',  ( 0.8560838555295223751, -29.58154842764516701, 36.40473632241573654 ) ) ;
#52204=ADVANCED_FACE ( 'NONE', ( #31793 ), #2926, .F. ) ;
#52207=CARTESIAN_POINT ( 'NONE',  ( 2.282803330402959574, 46.95498684800680422, 1.313817932779367315 ) ) ;
#52209=AXIS2_PLACEMENT_3D ( 'NONE', #60213, #7273, #59916 ) ;
#52212=CARTESIAN_POINT ( 'NONE',  ( 0.5837800304671223461, 10.82717547783941292, 45.62904341920361873 ) ) ;
#52215=CARTESIAN_POINT ( 'NONE',  ( 0.9790724872846782167, 29.16362883271026263, -30.09680985236413164 ) ) ;
#52220=CARTESIAN_POINT ( 'NONE',  ( 0.5797568665920712627, 23.08701827164173181, 40.81929563241816084 ) ) ;
#52223=( BOUNDED_SURFACE ( )  B_SPLINE_SURFACE ( 3, 1, ( 
 ( #12878, #31977 ),
 ( #3743, #22572 ),
 ( #61676, #56372 ),
 ( #60758, #42615 ) ),
 .UNSPECIFIED., .F., .F., .F. ) 
 B_SPLINE_SURFACE_WITH_KNOTS ( ( 4, 4 ),
 ( 2, 2 ),
 ( 0.000000000000000000, 1.000000000000000000 ),
 ( 0.000000000000000000, 1.000000000000000000 ),
 .UNSPECIFIED. ) 
 GEOMETRIC_REPRESENTATION_ITEM ( )  RATIONAL_B_SPLINE_SURFACE ( (
 ( 1.000000000000000000, 1.000000000000000000),
 ( 0.9729067724841187204, 0.9999501103223794596),
 ( 0.9729067724841187204, 0.9999501103223794596),
 ( 1.000000000000000000, 1.000000000000000000) ) ) 
 REPRESENTATION_ITEM ( '' )  SURFACE ( )  );
#52227=FACE_OUTER_BOUND ( 'NONE', #43682, .T. ) ;
#52232=CARTESIAN_POINT ( 'NONE',  ( 0.5830081025819919827, 43.28069043797167836, 18.05585416408522903 ) ) ;
#52236=CARTESIAN_POINT ( 'NONE',  ( -4.467300000000000715, 5.741254171069846846E-15, 46.67105333295396719 ) ) ;
#52247=ORIENTED_EDGE ( 'NONE', *, *, #3323, .T. ) ;
#52248=CARTESIAN_POINT ( 'NONE',  ( 0.9790320750461909416, -6.885858362131810573, -41.33911086560582504 ) ) ;
#52249=ORIENTED_EDGE ( 'NONE', *, *, #11013, .F. ) ;
#52250=CARTESIAN_POINT ( 'NONE',  ( 0.9762797500689124330, -37.62962005162918899, 18.44821075214967721 ) ) ;
#52262=CARTESIAN_POINT ( 'NONE',  ( 0.5797568665920721509, -46.07736677682986226, -8.723621926434374174 ) ) ;
#52268=CARTESIAN_POINT ( 'NONE',  ( 0.5835226383429289454, -44.24119678963662494, 15.55503073499414413 ) ) ;
#52281=VERTEX_POINT ( 'NONE', #60893 ) ;
#52284=CARTESIAN_POINT ( 'NONE',  ( 5.895596859100789899, 3.348897116308617417, -19.83212220910478507 ) ) ;
#52286=CARTESIAN_POINT ( 'NONE',  ( 0.9789233960466696693, 29.03992057262557935, 30.21621650650424584 ) ) ;
#52287=CARTESIAN_POINT ( 'NONE',  ( 4.962356264823601926, -41.76635909427990612, -5.177532797579353918 ) ) ;
#52293=CARTESIAN_POINT ( 'NONE',  ( 0.5806925824938499181, -2.112975627976999782, 46.84824112321762613 ) ) ;
#52295=CARTESIAN_POINT ( 'NONE',  ( 3.661933894777869902, -15.72363048476816161, 44.33281639293991816 ) ) ;
#52301=CARTESIAN_POINT ( 'NONE',  ( 5.895596859100789899, 18.99884588797239005, -6.600911917118875039 ) ) ;
#52308=EDGE_CURVE ( 'NONE', #45323, #42702, #28314, .T. ) ;
#52318=CARTESIAN_POINT ( 'NONE',  ( 1.092182651088185130, 24.22945109136152908, -34.20080239195573313 ) ) ;
#52320=FACE_OUTER_BOUND ( 'NONE', #9261, .T. ) ;
#52323=B_SPLINE_CURVE_WITH_KNOTS ( 'NONE', 3,
 ( #15340, #14415, #908, #14722, #20643, #43240 ),
 .UNSPECIFIED., .F., .F.,
 ( 4, 2, 4 ),
 ( 4.336808689942017736E-19, 0.0002291459268755705330, 0.0004582918537511406322 ),
 .UNSPECIFIED. ) ;
#52346=CARTESIAN_POINT ( 'NONE',  ( 2.282803330402964903, -42.50075538189024371, 20.00456696421370850 ) ) ;
#52347=CARTESIAN_POINT ( 'NONE',  ( 0.9787284016396595732, -22.70791007621392410, -35.22338454634100202 ) ) ;
#52350=CARTESIAN_POINT ( 'NONE',  ( 5.895596859100789899, -15.78680134203104579, -12.46214614742317295 ) ) ;
#52357=CARTESIAN_POINT ( 'NONE',  ( 0.5830081025819920937, 40.20945637685019136, -24.13362078637243968 ) ) ;
#52360=CARTESIAN_POINT ( 'NONE',  ( 0.6064515330803595949, 33.10959316660201779, 33.21278633868569585 ) ) ;
#52363=FACE_OUTER_BOUND ( 'NONE', #51024, .T. ) ;
#52368=CARTESIAN_POINT ( 'NONE',  ( 5.895596859100789899, -18.51552686702066808, 7.855154234585303819 ) ) ;
#52370=FACE_OUTER_BOUND ( 'NONE', #45359, .T. ) ;
#52374=CARTESIAN_POINT ( 'NONE',  ( 0.8560838555295223751, -13.02223058219873764, 45.06433561859954295 ) ) ;
#52375=B_SPLINE_CURVE_WITH_KNOTS ( 'NONE', 3,
 ( #15416, #34528, #53595, #10719 ),
 .UNSPECIFIED., .F., .F.,
 ( 4, 4 ),
 ( 3.878959614448864246E-18, 0.004042984057420970223 ),
 .UNSPECIFIED. ) ;
#52378=ORIENTED_EDGE ( 'NONE', *, *, #59757, .T. ) ;
#52381=EDGE_CURVE ( 'NONE', #36178, #61953, #47609, .T. ) ;
#52382=EDGE_LOOP ( 'NONE', ( #7315, #42893, #3319, #35194 ) ) ;
#52383=EDGE_CURVE ( 'NONE', #10343, #52281, #9427, .T. ) ;
#52388=CARTESIAN_POINT ( 'NONE',  ( 4.956445790444036881, 42.27038699792232279, -20.75457619864872783 ) ) ;
#52397=( BOUNDED_SURFACE ( )  B_SPLINE_SURFACE ( 3, 1, ( 
 ( #6774, #40974 ),
 ( #12767, #60332 ),
 ( #21524, #2709 ),
 ( #59727, #32167 ) ),
 .UNSPECIFIED., .F., .F., .F. ) 
 B_SPLINE_SURFACE_WITH_KNOTS ( ( 4, 4 ),
 ( 2, 2 ),
 ( 0.000000000000000000, 1.000000000000000000 ),
 ( 0.000000000000000000, 1.000000000000000000 ),
 .UNSPECIFIED. ) 
 GEOMETRIC_REPRESENTATION_ITEM ( )  RATIONAL_B_SPLINE_SURFACE ( (
 ( 1.000000000000000000, 1.000000000000000000),
 ( 0.9952954269826590483, 0.8620686068821307169),
 ( 0.9952954269826590483, 0.8620686068821307169),
 ( 1.000000000000000000, 1.000000000000000000) ) ) 
 REPRESENTATION_ITEM ( '' )  SURFACE ( )  );
#52398=EDGE_CURVE ( 'NONE', #42400, #26123, #14778, .T. ) ;
#52400=EDGE_LOOP ( 'NONE', ( #37639, #19058, #18010, #11444 ) ) ;
#52403=ORIENTED_EDGE ( 'NONE', *, *, #7905, .F. ) ;
#52405=DIRECTION ( 'NONE',  ( -1.000000000000000000, -0.000000000000000000, -0.000000000000000000 ) ) ;
#52407=CARTESIAN_POINT ( 'NONE',  ( 0.8560838555295158248, 43.53454501559585310, -17.46757637357826454 ) ) ;
#52409=CARTESIAN_POINT ( 'NONE',  ( 0.6064782688330846439, 16.18998450771341524, 44.01384836683529755 ) ) ;
#52410=CARTESIAN_POINT ( 'NONE',  ( 4.956445790444038657, 44.30493387627053181, -15.95653108789415953 ) ) ;
#52412=CARTESIAN_POINT ( 'NONE',  ( 0.5782707292762442330, -46.10024953908504841, 8.631532085424261425 ) ) ;
#52422=CARTESIAN_POINT ( 'NONE',  ( 0.5806925824938502512, -41.60618895332704170, 21.63671424046659908 ) ) ;
#52426=CARTESIAN_POINT ( 'NONE',  ( 0.8554163680231738898, -29.58718577084389523, -36.41159034254604165 ) ) ;
#52427=EDGE_CURVE ( 'NONE', #58761, #59315, #43186, .T. ) ;
#52430=CARTESIAN_POINT ( 'NONE',  ( 0.9790850452238872847, 41.90864786853558854, -0.05063688658461517472 ) ) ;
#52439=CARTESIAN_POINT ( 'NONE',  ( 2.282803330402960462, 21.41355745235515684, 41.80856927343567975 ) ) ;
#52444=CARTESIAN_POINT ( 'NONE',  ( 0.7764146366350255235, 10.00418648031552138, -45.82528479492778217 ) ) ;
#52446=B_SPLINE_CURVE_WITH_KNOTS ( 'NONE', 3,
 ( #23239, #57639, #28854, #61420, #32644, #325, #4397, #32962, #19172, #57335, #51729, #52034, #5028, #52649, #28236, #47353, #42663, #61728, #38284 ),
 .UNSPECIFIED., .F., .F.,
 ( 4, 3, 3, 3, 3, 3, 4 ),
 ( 9.813676791237317679E-18, 0.0002732106629380691540, 0.0004098138914053827504, 0.0005464171197651536286, 0.0006830203481512645480, 0.0008196235766963743665, 0.001011968216111141161 ),
 .UNSPECIFIED. ) ;
#52447=CARTESIAN_POINT ( 'NONE',  ( 4.962356264823597485, -14.71877352713633158, 39.42833123173257803 ) ) ;
#52451=CARTESIAN_POINT ( 'NONE',  ( 4.956445790444004018, -43.56224489968113289, 17.88487823385560205 ) ) ;
#52453=MANIFOLD_SOLID_BREP ( 'Move Face1', #39064 ) ;
#52456=CARTESIAN_POINT ( 'NONE',  ( 0.5837800005270560311, -45.95628241222482302, 9.341058049793774742 ) ) ;
#52460=CIRCLE ( 'NONE', #57447, 47.09074272231896430 ) ;
#52484=B_SPLINE_CURVE_WITH_KNOTS ( 'NONE', 3,
 ( #56781, #52086, #14215, #47405 ),
 .UNSPECIFIED., .F., .F.,
 ( 4, 4 ),
 ( 0.000000000000000000, 0.005004948556313804434 ),
 .UNSPECIFIED. ) ;
#52486=CARTESIAN_POINT ( 'NONE',  ( 0.9754292580325127915, -31.46929222874847554, 27.67690577946956054 ) ) ;
#52488=CARTESIAN_POINT ( 'NONE',  ( 0.7764146366350248574, -2.458100050502026956, -46.84013469035808441 ) ) ;
#52492=CARTESIAN_POINT ( 'NONE',  ( 5.895881250540457863, -9.661888320804171926, 17.64016994489023915 ) ) ;
#52494=( BOUNDED_SURFACE ( )  B_SPLINE_SURFACE ( 3, 1, ( 
 ( #2899, #39930 ),
 ( #6338, #59294 ),
 ( #11711, #16396 ),
 ( #25476, #26101 ) ),
 .UNSPECIFIED., .F., .F., .F. ) 
 B_SPLINE_SURFACE_WITH_KNOTS ( ( 4, 4 ),
 ( 2, 2 ),
 ( 0.000000000000000000, 1.000000000000000000 ),
 ( 0.000000000000000000, 1.000000000000000000 ),
 .UNSPECIFIED. ) 
 GEOMETRIC_REPRESENTATION_ITEM ( )  RATIONAL_B_SPLINE_SURFACE ( (
 ( 1.000000000000000000, 1.000000000000000000),
 ( 0.9952954269826590483, 0.8620686068821307169),
 ( 0.9952954269826590483, 0.8620686068821307169),
 ( 1.000000000000000000, 1.000000000000000000) ) ) 
 REPRESENTATION_ITEM ( '' )  SURFACE ( )  );
#52495=ORIENTED_EDGE ( 'NONE', *, *, #22187, .F. ) ;
#52499=ORIENTED_EDGE ( 'NONE', *, *, #26465, .T. ) ;
#52511=ORIENTED_EDGE ( 'NONE', *, *, #15155, .T. ) ;
#52513=CARTESIAN_POINT ( 'NONE',  ( 0.5806925824938502512, 16.34374012233117313, -43.95571090492413191 ) ) ;
#52514=CARTESIAN_POINT ( 'NONE',  ( 0.8554163680231816613, 46.61139063278402972, 5.346376005279853239 ) ) ;
#52515=CARTESIAN_POINT ( 'NONE',  ( 2.618530812446111078, -33.90288491188655229, -32.56257336037148775 ) ) ;
#52529=CARTESIAN_POINT ( 'NONE',  ( 0.9762797500689124330, -1.905951756780688733, 41.86516610604248712 ) ) ;
#52530=CARTESIAN_POINT ( 'NONE',  ( 5.896278296736517710, -19.93266788971478221, 2.686211163091445808 ) ) ;
#52532=CARTESIAN_POINT ( 'NONE',  ( 1.000110580585050979, -17.04223752418473481, -38.28811333744679501 ) ) ;
#52537=CARTESIAN_POINT ( 'NONE',  ( 0.8560838555295223751, -38.14845555156087187, 27.29593693413575295 ) ) ;
#52543=CARTESIAN_POINT ( 'NONE',  ( 0.5837799406558226156, 43.21036104660473143, 18.22383735109779224 ) ) ;
#52544=CARTESIAN_POINT ( 'NONE',  ( 0.5817217712918331118, -24.84894824081227682, -39.77140587575206609 ) ) ;
#52546=EDGE_LOOP ( 'NONE', ( #38041, #6930, #35964, #26415 ) ) ;
#52548=EDGE_CURVE ( 'NONE', #13205, #36503, #47067, .T. ) ;
#52553=CARTESIAN_POINT ( 'NONE',  ( 5.896782393890504181, 18.99788783847851548, 6.603510017755907846 ) ) ;
#52554=CARTESIAN_POINT ( 'NONE',  ( 3.238018933889920792, -5.886379020808710116, 12.03154330877946876 ) ) ;
#52557=ORIENTED_EDGE ( 'NONE', *, *, #38628, .T. ) ;
#52559=CARTESIAN_POINT ( 'NONE',  ( 0.9790724872846779947, -6.930766400444295705, -41.33158219913587317 ) ) ;
#52560=VERTEX_POINT ( 'NONE', #4102 ) ;
#52562=B_SPLINE_CURVE_WITH_KNOTS ( 'NONE', 3,
 ( #52098, #57099, #33337, #52407 ),
 .UNSPECIFIED., .F., .F.,
 ( 4, 4 ),
 ( 0.000000000000000000, 0.004447772540403838876 ),
 .UNSPECIFIED. ) ;
#52563=CONICAL_SURFACE ( 'NONE', #34564, 42.08604991992415023, 1.569615340895231137 ) ;
#52567=CARTESIAN_POINT ( 'NONE',  ( 0.9788927965476035276, -37.34015262922740419, 19.02760137951648645 ) ) ;
#52572=CARTESIAN_POINT ( 'NONE',  ( 0.5782707292762423457, 11.57561326132651836, 45.45042938556048995 ) ) ;
#52573=CARTESIAN_POINT ( 'NONE',  ( 0.7764146366350269668, -46.13398395504711402, -8.467348941942809404 ) ) ;
#52577=ORIENTED_EDGE ( 'NONE', *, *, #13530, .T. ) ;
#52584=ORIENTED_EDGE ( 'NONE', *, *, #30683, .F. ) ;
#52597=DIRECTION ( 'NONE',  ( 0.07500201931887538753, 0.8960136144483816789, -0.4376463181854017281 ) ) ;
#52598=CARTESIAN_POINT ( 'NONE',  ( 0.6845945791218034371, -46.73791075327830669, -3.996776092369579203 ) ) ;
#52600=CARTESIAN_POINT ( 'NONE',  ( 0.9775691876210967912, -34.76360227320881791, 23.40567593512611566 ) ) ;
#52602=ORIENTED_EDGE ( 'NONE', *, *, #60193, .F. ) ;
#52605=FACE_OUTER_BOUND ( 'NONE', #32766, .T. ) ;
#52609=CARTESIAN_POINT ( 'NONE',  ( 1.231276596079887931, 40.64579686208652731, 10.25650859035686757 ) ) ;
#52613=CONICAL_SURFACE ( 'NONE', #36639, 42.08604991992415023, 1.569615340895231137 ) ;
#52616=CARTESIAN_POINT ( 'NONE',  ( 0.9754292580325132356, 38.35198880093447116, 16.89533728331584328 ) ) ;
#52619=CARTESIAN_POINT ( 'NONE',  ( 0.8560838555295158248, 39.88643293834648063, 24.68694597426990001 ) ) ;
#52628=ORIENTED_EDGE ( 'NONE', *, *, #30706, .F. ) ;
#52629=CARTESIAN_POINT ( 'NONE',  ( 0.9754292589017206083, 24.38796673385399316, -34.08158660455394084 ) ) ;
#52630=EDGE_CURVE ( 'NONE', #30850, #37991, #9543, .T. ) ;
#52637=CARTESIAN_POINT ( 'NONE',  ( 4.962356264823603702, 41.96072444189417183, -3.245489512195726789 ) ) ;
#52643=ORIENTED_EDGE ( 'NONE', *, *, #36306, .T. ) ;
#52644=CARTESIAN_POINT ( 'NONE',  ( 0.5797568665920720399, 46.38942905901759417, -6.873585685815319479 ) ) ;
#52649=CARTESIAN_POINT ( 'NONE',  ( 0.9785694773339257413, -34.42478712511277195, -23.90124342174149774 ) ) ;
#52658=CARTESIAN_POINT ( 'NONE',  ( 5.894904586330512508, -15.78536547177689364, -12.46401416013623376 ) ) ;
#52659=CARTESIAN_POINT ( 'NONE',  ( 0.5782707292762442330, -25.84399470232805385, 39.13852694639462015 ) ) ;
#52661=EDGE_CURVE ( 'NONE', #58092, #48936, #40206, .T. ) ;
#52662=CARTESIAN_POINT ( 'NONE',  ( 4.956445790444004018, -43.14021684453488348, -18.88014143872194950 ) ) ;
#52673=CARTESIAN_POINT ( 'NONE',  ( 4.962356264823608143, 1.841560470688809792, -42.04574000888963781 ) ) ;
#52674=CARTESIAN_POINT ( 'NONE',  ( 0.9762797500689124330, 10.20671408565980975, 40.64662068068264489 ) ) ;
#52676=B_SPLINE_CURVE_WITH_KNOTS ( 'NONE', 3,
 ( #10871, #58749, #35294, #15877, #34994, #1432 ),
 .UNSPECIFIED., .F., .F.,
 ( 4, 2, 4 ),
 ( 9.885284284422817346E-18, 0.0002448709889506582409, 0.0004897419779013066155 ),
 .UNSPECIFIED. ) ;
#52678=CARTESIAN_POINT ( 'NONE',  ( 4.956445790443996025, 14.46717203539371610, 44.81337951368942640 ) ) ;
#52697=ORIENTED_EDGE ( 'NONE', *, *, #50279, .F. ) ;
#52699=ORIENTED_EDGE ( 'NONE', *, *, #2787, .T. ) ;
#52705=EDGE_LOOP ( 'NONE', ( #16828, #28750, #23383, #26135 ) ) ;
#52712=ORIENTED_EDGE ( 'NONE', *, *, #41906, .F. ) ;
#52718=CARTESIAN_POINT ( 'NONE',  ( 0.5806925824938502512, 40.06810415365508504, -24.36738377166110325 ) ) ;
#52719=ORIENTED_EDGE ( 'NONE', *, *, #56245, .F. ) ;
#52723=CARTESIAN_POINT ( 'NONE',  ( 5.896782393890504181, -19.93422257774822626, -2.674482585249919442 ) ) ;
#52727=B_SPLINE_CURVE_WITH_KNOTS ( 'NONE', 3,
 ( #3652, #12172, #30951, #26240 ),
 .UNSPECIFIED., .F., .F.,
 ( 4, 4 ),
 ( 0.000000000000000000, 0.004041751736740996880 ),
 .UNSPECIFIED. ) ;
#52729=CARTESIAN_POINT ( 'NONE',  ( 5.901463166500146684, -15.77541139567720130, 12.47614786854398083 ) ) ;
#52730=CARTESIAN_POINT ( 'NONE',  ( 0.8560838555295223751, 43.53454501559562573, 17.46757637357886850 ) ) ;
#52734=CARTESIAN_POINT ( 'NONE',  ( 0.5804410086790514622, -44.12183670707857175, -15.89916279082930295 ) ) ;
#52735=EDGE_CURVE ( 'NONE', #22979, #10045, #17767, .T. ) ;
#52749=CARTESIAN_POINT ( 'NONE',  ( 0.5797568599927142019, -45.82673081884099986, -9.956708850242389275 ) ) ;
#52765=CARTESIAN_POINT ( 'NONE',  ( 0.8560838555295223751, -44.00447048317975174, 16.24744323198866169 ) ) ;
#52768=CARTESIAN_POINT ( 'NONE',  ( 0.5837800304671211249, 22.49746046441963898, 41.14731588854093758 ) ) ;
#52772=( BOUNDED_SURFACE ( )  B_SPLINE_SURFACE ( 3, 1, ( 
 ( #44441, #38812 ),
 ( #53177, #5546 ),
 ( #49407, #43826 ),
 ( #869, #11209 ) ),
 .UNSPECIFIED., .F., .F., .F. ) 
 B_SPLINE_SURFACE_WITH_KNOTS ( ( 4, 4 ),
 ( 2, 2 ),
 ( 0.000000000000000000, 1.000000000000000000 ),
 ( 0.000000000000000000, 1.000000000000000000 ),
 .UNSPECIFIED. ) 
 GEOMETRIC_REPRESENTATION_ITEM ( )  RATIONAL_B_SPLINE_SURFACE ( (
 ( 1.000000000000000000, 1.000000000000000000),
 ( 0.7282232189291693025, 0.9929344683865674037),
 ( 0.7282232189291693025, 0.9929344683865674037),
 ( 1.000000000000000000, 1.000000000000000000) ) ) 
 REPRESENTATION_ITEM ( '' )  SURFACE ( )  );
#52773=ORIENTED_EDGE ( 'NONE', *, *, #57264, .T. ) ;
#52778=FACE_OUTER_BOUND ( 'NONE', #39623, .T. ) ;
#52781=( BOUNDED_SURFACE ( )  B_SPLINE_SURFACE ( 3, 1, ( 
 ( #14946, #39679 ),
 ( #53123, #10229 ),
 ( #24950, #29323 ),
 ( #15548, #39068 ) ),
 .UNSPECIFIED., .F., .F., .F. ) 
 B_SPLINE_SURFACE_WITH_KNOTS ( ( 4, 4 ),
 ( 2, 2 ),
 ( 0.000000000000000000, 1.000000000000000000 ),
 ( 0.000000000000000000, 1.000000000000000000 ),
 .UNSPECIFIED. ) 
 GEOMETRIC_REPRESENTATION_ITEM ( )  RATIONAL_B_SPLINE_SURFACE ( (
 ( 1.000000000000000000, 1.000000000000000000),
 ( 0.7282232189291693025, 0.9929344683865674037),
 ( 0.7282232189291693025, 0.9929344683865674037),
 ( 1.000000000000000000, 1.000000000000000000) ) ) 
 REPRESENTATION_ITEM ( '' )  SURFACE ( )  );
#52786=CARTESIAN_POINT ( 'NONE',  ( 4.960386119450149955, 18.84353550694778434, -39.48870261569428664 ) ) ;
#52791=CARTESIAN_POINT ( 'NONE',  ( 0.6064515330803581517, -0.8565989750148934601, 46.88923729634646520 ) ) ;
#52798=CARTESIAN_POINT ( 'NONE',  ( 5.896782393890504181, 5.965008392937153126, -19.20793486427423247 ) ) ;
#52812=B_SPLINE_CURVE_WITH_KNOTS ( 'NONE', 3,
 ( #36934, #28119, #55997, #12814 ),
 .UNSPECIFIED., .F., .F.,
 ( 4, 4 ),
 ( 8.673617379884035472E-19, 0.004446298630425071091 ),
 .UNSPECIFIED. ) ;
#52814=ORIENTED_EDGE ( 'NONE', *, *, #33773, .F. ) ;
#52816=LINE ( 'NONE', #9591, #49495 ) ;
#52818=CARTESIAN_POINT ( 'NONE',  ( 1.092182651088185574, -40.91119942363535245, 9.112351297103435499 ) ) ;
#52826=CARTESIAN_POINT ( 'NONE',  ( 0.5830082357119575898, 28.03719174367731881, -37.59185967821500185 ) ) ;
#52829=CARTESIAN_POINT ( 'NONE',  ( 4.962356264823608143, 0.000000000000000000, 0.000000000000000000 ) ) ;
#52830=CARTESIAN_POINT ( 'NONE',  ( 5.910764540655177868, -19.93069368583278234, -2.696050383555225860 ) ) ;
#52838=CARTESIAN_POINT ( 'NONE',  ( 4.956445790444002242, -32.34643101787113295, 34.22347806032784234 ) ) ;
#52859=CARTESIAN_POINT ( 'NONE',  ( 5.896782393890504181, -2.006887468070122527, -20.01245835894519587 ) ) ;
#52860=DIRECTION ( 'NONE',  ( -0.07906939808003035641, 0.5848023231963220825, -0.8073129957280794633 ) ) ;
#52862=EDGE_CURVE ( 'NONE', #36737, #15825, #52816, .T. ) ;
#52864=ORIENTED_EDGE ( 'NONE', *, *, #33052, .F. ) ;
#52865=( BOUNDED_SURFACE ( )  B_SPLINE_SURFACE ( 3, 1, ( 
 ( #10489, #33386 ),
 ( #19908, #34300 ),
 ( #29584, #5749 ),
 ( #23971, #43097 ) ),
 .UNSPECIFIED., .F., .F., .F. ) 
 B_SPLINE_SURFACE_WITH_KNOTS ( ( 4, 4 ),
 ( 2, 2 ),
 ( 0.000000000000000000, 1.000000000000000000 ),
 ( 0.000000000000000000, 1.000000000000000000 ),
 .UNSPECIFIED. ) 
 GEOMETRIC_REPRESENTATION_ITEM ( )  RATIONAL_B_SPLINE_SURFACE ( (
 ( 1.000000000000000000, 1.000000000000000000),
 ( 0.9952954269826590483, 0.8620686068821339365),
 ( 0.9952954269826590483, 0.8620686068821339365),
 ( 1.000000000000000000, 1.000000000000000000) ) ) 
 REPRESENTATION_ITEM ( '' )  SURFACE ( )  );
#52868=ORIENTED_EDGE ( 'NONE', *, *, #3299, .T. ) ;
#52869=CARTESIAN_POINT ( 'NONE',  ( 0.8554163680231738898, -44.01281378489782981, -16.25046755781900742 ) ) ;
#52870=CARTESIAN_POINT ( 'NONE',  ( 0.5804410086790514622, 11.40290849443534960, -45.49168638029296119 ) ) ;
#52874=VERTEX_POINT ( 'NONE', #56274 ) ;
#52875=CARTESIAN_POINT ( 'NONE',  ( 5.838029081930957709, 19.90064824094122997, 42.83724148148714761 ) ) ;
#52876=ORIENTED_EDGE ( 'NONE', *, *, #45708, .T. ) ;
#52880=DIRECTION ( 'NONE',  ( 0.000000000000000000, 0.000000000000000000, 1.000000000000000000 ) ) ;
#52881=CARTESIAN_POINT ( 'NONE',  ( 0.9762797500689124330, -37.62962005162918899, 18.44821075214967721 ) ) ;
#52884=CARTESIAN_POINT ( 'NONE',  ( 0.5804410086790514622, -24.77328595090390451, 39.82215658462187946 ) ) ;
#52885=ORIENTED_EDGE ( 'NONE', *, *, #45387, .F. ) ;
#52910=CARTESIAN_POINT ( 'NONE',  ( 1.091591847532195292, -39.84368319171721140, 13.00922367683450354 ) ) ;
#52914=CARTESIAN_POINT ( 'NONE',  ( 0.7764139734771244861, 40.80384766507922478, -23.13193650846973881 ) ) ;
#52919=CARTESIAN_POINT ( 'NONE',  ( 4.958415959904820980, -5.049385427348767941, 45.14097540626162441 ) ) ;
#52926=DIRECTION ( 'NONE',  ( 0.000000000000000000, 0.000000000000000000, 1.000000000000000000 ) ) ;
#52938=ORIENTED_EDGE ( 'NONE', *, *, #8063, .F. ) ;
#52951=ORIENTED_EDGE ( 'NONE', *, *, #8369, .T. ) ;
#52955=ORIENTED_EDGE ( 'NONE', *, *, #34332, .T. ) ;
#52958=VERTEX_POINT ( 'NONE', #25852 ) ;
#52959=VECTOR ( 'NONE', #25116, 1000.000000000000114 ) ;
#52963=CARTESIAN_POINT ( 'NONE',  ( 0.5837800005270570303, 4.694119656474818214, 46.66048113010067766 ) ) ;
#52972=CARTESIAN_POINT ( 'NONE',  ( 2.282803330402966235, -46.27578309073107476, 8.065284049343492967 ) ) ;
#52986=CARTESIAN_POINT ( 'NONE',  ( 0.5837157313716023754, -1.658013562071385394, 46.86670518193070478 ) ) ;
#52987=CARTESIAN_POINT ( 'NONE',  ( 0.9784957157296378938, 9.941547056922068748, 40.71238999502944722 ) ) ;
#52997=ORIENTED_EDGE ( 'NONE', *, *, #30610, .F. ) ;
#53003=VERTEX_POINT ( 'NONE', #57807 ) ;
#53005=ORIENTED_EDGE ( 'NONE', *, *, #12418, .T. ) ;
#53009=B_SPLINE_CURVE_WITH_KNOTS ( 'NONE', 3,
 ( #61262, #3936, #28078, #22761 ),
 .UNSPECIFIED., .F., .F.,
 ( 4, 4 ),
 ( 0.000000000000000000, 0.005004948556313802699 ),
 .UNSPECIFIED. ) ;
#53010=EDGE_CURVE ( 'NONE', #19405, #47199, #34646, .T. ) ;
#53012=VERTEX_POINT ( 'NONE', #29621 ) ;
#53015=FACE_OUTER_BOUND ( 'NONE', #23620, .T. ) ;
#53025=CARTESIAN_POINT ( 'NONE',  ( 0.6064515330803591509, 39.98349652191225090, -24.50825048670992956 ) ) ;
#53028=CARTESIAN_POINT ( 'NONE',  ( 0.9754292580325135686, 41.45298142384850593, 6.162612918079117819 ) ) ;
#53029=CARTESIAN_POINT ( 'NONE',  ( 5.901463166500146684, 10.83443963266005028, 16.94499301229958732 ) ) ;
#53031=ORIENTED_EDGE ( 'NONE', *, *, #39766, .T. ) ;
#53035=CARTESIAN_POINT ( 'NONE',  ( 0.9754292580325126805, 33.24763091048475161, -25.51318297947520364 ) ) ;
#53043=B_SPLINE_CURVE_WITH_KNOTS ( 'NONE', 3,
 ( #46713, #3753, #13499, #51997, #33226, #47622 ),
 .UNSPECIFIED., .F., .F.,
 ( 4, 2, 4 ),
 ( 1.193026433010871187E-16, 0.0002448718616795929879, 0.0004897437233590666052 ),
 .UNSPECIFIED. ) ;
#53048=CARTESIAN_POINT ( 'NONE',  ( 0.8560838555295158248, -26.00596412780176081, 39.03924517540291106 ) ) ;
#53069=ORIENTED_EDGE ( 'NONE', *, *, #58189, .F. ) ;
#53070=LINE ( 'NONE', #43715, #18921 ) ;
#53076=ORIENTED_EDGE ( 'NONE', *, *, #8939, .F. ) ;
#53078=( BOUNDED_SURFACE ( )  B_SPLINE_SURFACE ( 3, 1, ( 
 ( #31145, #7316 ),
 ( #59960, #55553 ),
 ( #31780, #17067 ),
 ( #36179, #3241 ) ),
 .UNSPECIFIED., .F., .F., .F. ) 
 B_SPLINE_SURFACE_WITH_KNOTS ( ( 4, 4 ),
 ( 2, 2 ),
 ( 0.000000000000000000, 1.000000000000000000 ),
 ( 0.000000000000000000, 1.000000000000000000 ),
 .UNSPECIFIED. ) 
 GEOMETRIC_REPRESENTATION_ITEM ( )  RATIONAL_B_SPLINE_SURFACE ( (
 ( 1.000000000000000000, 1.000000000000000000),
 ( 0.9952954269826590483, 0.8620686068821339365),
 ( 0.9952954269826590483, 0.8620686068821339365),
 ( 1.000000000000000000, 1.000000000000000000) ) ) 
 REPRESENTATION_ITEM ( '' )  SURFACE ( )  );
#53079=CARTESIAN_POINT ( 'NONE',  ( 5.910764540655178756, -11.94262894392596408, -16.18254777149955004 ) ) ;
#53080=CARTESIAN_POINT ( 'NONE',  ( -4.467299999999993609, 1.530808498934191521E-15, 12.50000000000000000 ) ) ;
#53082=CARTESIAN_POINT ( 'NONE',  ( 1.231276596079881047, 41.42457922925067493, 6.425029704024775690 ) ) ;
#53083=CARTESIAN_POINT ( 'NONE',  ( 0.5834584762367771571, 46.89565892744833775, 0.1821064897865646570 ) ) ;
#53084=EDGE_CURVE ( 'NONE', #4099, #10045, #7652, .T. ) ;
#53085=B_SPLINE_CURVE_WITH_KNOTS ( 'NONE', 3,
 ( #21598, #59806, #60111, #16917 ),
 .UNSPECIFIED., .F., .F.,
 ( 4, 4 ),
 ( 0.000000000000000000, 0.005004948556313801832 ),
 .UNSPECIFIED. ) ;
#53086=CARTESIAN_POINT ( 'NONE',  ( 5.896782393890504181, 14.91246379622012874, 13.49609241241464375 ) ) ;
#53087=EDGE_CURVE ( 'NONE', #36885, #60718, #23473, .T. ) ;
#53092=ORIENTED_EDGE ( 'NONE', *, *, #48655, .T. ) ;
#53100=ORIENTED_EDGE ( 'NONE', *, *, #14810, .T. ) ;
#53101=ORIENTED_EDGE ( 'NONE', *, *, #43815, .T. ) ;
#53102=CARTESIAN_POINT ( 'NONE',  ( 0.5837799406558235038, -13.80714289583679033, 44.81747822703933082 ) ) ;
#53103=CARTESIAN_POINT ( 'NONE',  ( 4.956445790444040433, 44.65954324082233029, -14.93530206124928128 ) ) ;
#53107=CARTESIAN_POINT ( 'NONE',  ( 0.5806925824938499181, 22.05663578530122493, 41.38510819338441138 ) ) ;
#53109=CARTESIAN_POINT ( 'NONE',  ( 0.8554163680231708922, 23.34472558242500284, -40.69679668712378628 ) ) ;
#53111=ADVANCED_FACE ( 'NONE', ( #13018 ), #48697, .F. ) ;
#53113=EDGE_CURVE ( 'NONE', #27845, #19228, #30391, .T. ) ;
#53116=EDGE_CURVE ( 'NONE', #40503, #42430, #26627, .T. ) ;
#53122=ORIENTED_EDGE ( 'NONE', *, *, #29778, .T. ) ;
#53123=CARTESIAN_POINT ( 'NONE',  ( 5.910764540655177868, -20.11221018249587544, -0.01549336220058925018 ) ) ;
#53124=LINE ( 'NONE', #48437, #33834 ) ;
#53126=DIRECTION ( 'NONE',  ( -0.000000000000000000, 0.000000000000000000, 1.000000000000000000 ) ) ;
#53129=CARTESIAN_POINT ( 'NONE',  ( 5.895596859100789899, 19.71057157537855176, 4.002693016503615198 ) ) ;
#53130=EDGE_CURVE ( 'NONE', #19501, #16409, #16780, .T. ) ;
#53131=B_SPLINE_CURVE_WITH_KNOTS ( 'NONE', 3,
 ( #36964, #61038, #23760, #14377, #37574, #32557 ),
 .UNSPECIFIED., .F., .F.,
 ( 4, 2, 4 ),
 ( 3.511543213478341086E-18, 0.0002448709889506563977, 0.0004897419779013092176 ),
 .UNSPECIFIED. ) ;
#53140=CARTESIAN_POINT ( 'NONE',  ( 4.960386119450145515, -34.62801484853829237, -26.74578569273583994 ) ) ;
#53144=CARTESIAN_POINT ( 'NONE',  ( 3.661921753702004789, -23.70324447415902114, 40.62988217103625033 ) ) ;
#53145=CARTESIAN_POINT ( 'NONE',  ( 5.896782393890504181, -19.93252920631905667, 2.687073932226298201 ) ) ;
#53148=CARTESIAN_POINT ( 'NONE',  ( 0.5848930533535030563, 27.96442382265512450, -37.64656800631999545 ) ) ;
#53153=LINE ( 'NONE', #44420, #54292 ) ;
#53157=ORIENTED_EDGE ( 'NONE', *, *, #53645, .F. ) ;
#53173=CARTESIAN_POINT ( 'NONE',  ( 5.896782393890504181, -20.11283288166117345, 0.006352352428115353410 ) ) ;
#53174=CARTESIAN_POINT ( 'NONE',  ( 0.9790850452238869517, 40.43297707001163843, 11.02323434927842172 ) ) ;
#53177=CARTESIAN_POINT ( 'NONE',  ( 5.910764540655177868, 14.90587032029957193, 13.50245416446859714 ) ) ;
#53185=CARTESIAN_POINT ( 'NONE',  ( 0.8554163680231816613, -0.6539261334255772606, 46.91244881397518895 ) ) ;
#53197=DIRECTION ( 'NONE',  ( 0.07500201931887537365, 0.1525301372901526897, 0.9854487578338805287 ) ) ;
#53198=CARTESIAN_POINT ( 'NONE',  ( 3.531714409328638116, 0.2975961151483291212, -47.02729187627043217 ) ) ;
#53199=CARTESIAN_POINT ( 'NONE',  ( 4.291220156522060236, 14.90393520085178558, -44.69073408251991708 ) ) ;
#53213=CARTESIAN_POINT ( 'NONE',  ( 0.9762797500689124330, 15.53330887509137703, -38.92352888134260525 ) ) ;
#53219=CARTESIAN_POINT ( 'NONE',  ( 3.661921753702022997, 9.064111102371878559, -46.15704728162205583 ) ) ;
#53220=EDGE_LOOP ( 'NONE', ( #13918, #38092, #15492, #16991 ) ) ;
#53221=CARTESIAN_POINT ( 'NONE',  ( 4.956445790443998689, -5.251077430596073903, 46.79705371022326688 ) ) ;
#53228=CARTESIAN_POINT ( 'NONE',  ( 5.894904586330512508, 18.99964780500594941, -6.598696488502509006 ) ) ;
#53239=CARTESIAN_POINT ( 'NONE',  ( 4.958415959904820980, -35.95869674887559597, 27.75204644607389426 ) ) ;
#53242=EDGE_CURVE ( 'NONE', #26618, #14, #44528, .T. ) ;
#53249=CARTESIAN_POINT ( 'NONE',  ( 4.962356264823608143, 0.000000000000000000, 0.000000000000000000 ) ) ;
#53253=VERTEX_POINT ( 'NONE', #57728 ) ;
#53254=CARTESIAN_POINT ( 'NONE',  ( 0.5848930533535030563, -7.620589013869776274, -46.27309915565679432 ) ) ;
#53257=CARTESIAN_POINT ( 'NONE',  ( 0.5830081025819927598, 32.40478957890073985, -33.89928681741567118 ) ) ;
#53259=ORIENTED_EDGE ( 'NONE', *, *, #55490, .F. ) ;
#53260=CARTESIAN_POINT ( 'NONE',  ( 0.9762797500689124330, 40.55021165774366665, -10.58324712448374605 ) ) ;
#53264=CARTESIAN_POINT ( 'NONE',  ( 0.7764146366350251904, 46.35884964802752961, -7.134250695114612739 ) ) ;
#53267=CARTESIAN_POINT ( 'NONE',  ( 0.9788927965476030835, 40.38195116180627053, -11.20868560524691127 ) ) ;
#53272=CARTESIAN_POINT ( 'NONE',  ( 0.5797568599927149791, -39.01551438537359218, 26.01951087003197927 ) ) ;
#53275=DIRECTION ( 'NONE',  ( 1.000000000000000000, -0.000000000000000000, -0.000000000000000000 ) ) ;
#53285=CARTESIAN_POINT ( 'NONE',  ( 0.8560838555295223751, 33.26091945577352504, 33.07694168205818386 ) ) ;
#53288=B_SPLINE_CURVE_WITH_KNOTS ( 'NONE', 3,
 ( #14077, #23454, #8413, #42580, #46979, #42281 ),
 .UNSPECIFIED., .F., .F.,
 ( 4, 2, 4 ),
 ( 5.637851296924622286E-18, 0.0002291472222819946974, 0.0004582944445639837569 ),
 .UNSPECIFIED. ) ;
#53289=B_SPLINE_CURVE_WITH_KNOTS ( 'NONE', 3,
 ( #1050, #25472, #45240, #44013 ),
 .UNSPECIFIED., .F., .F.,
 ( 4, 4 ),
 ( 0.000000000000000000, 0.005004948556313808770 ),
 .UNSPECIFIED. ) ;
#53295=CARTESIAN_POINT ( 'NONE',  ( 0.9790320750461913857, -1.486294019886972739, 41.88231204970227850 ) ) ;
#53297=ORIENTED_EDGE ( 'NONE', *, *, #40157, .T. ) ;
#53305=CARTESIAN_POINT ( 'NONE',  ( 1.000110580585050091, -41.85483763260385359, 2.142440085572930197 ) ) ;
#53311=CARTESIAN_POINT ( 'NONE',  ( 0.5804410086790514622, -46.82762660194600102, -2.587129429332121422 ) ) ;
#53318=CARTESIAN_POINT ( 'NONE',  ( 5.896782393890504181, -9.660289833039602314, 17.64100017628490136 ) ) ;
#53319=EDGE_LOOP ( 'NONE', ( #41809, #17809, #10765, #56073 ) ) ;
#53323=CARTESIAN_POINT ( 'NONE',  ( 4.962356264823608143, 0.000000000000000000, 0.000000000000000000 ) ) ;
#53325=CARTESIAN_POINT ( 'NONE',  ( 0.5806925824938499181, -1.020860314012482561, -46.88475452172953339 ) ) ;
#53330=CARTESIAN_POINT ( 'NONE',  ( 0.7764139734771259294, 46.59651765548695579, -5.367030211277017848 ) ) ;
#53332=CARTESIAN_POINT ( 'NONE',  ( 0.5806925824938499181, 37.13995815321135296, -28.63295078613577971 ) ) ;
#53333=CARTESIAN_POINT ( 'NONE',  ( 4.962356264823609031, -3.779019546646985361, -41.91604238389410853 ) ) ;
#53340=ORIENTED_EDGE ( 'NONE', *, *, #55119, .F. ) ;
#53343=CARTESIAN_POINT ( 'NONE',  ( 0.9787284016396611275, 14.88741976570966585, -39.17525662517586937 ) ) ;
#53349=CARTESIAN_POINT ( 'NONE',  ( 0.8560838555295158248, 33.26091945577399400, -33.07694168205770069 ) ) ;
#53358=CARTESIAN_POINT ( 'NONE',  ( 0.6845945791218023269, 37.34424629630195369, 28.38685944719991738 ) ) ;
#53362=FACE_OUTER_BOUND ( 'NONE', #49196, .T. ) ;
#53369=ORIENTED_EDGE ( 'NONE', *, *, #29679, .T. ) ;
#53371=CARTESIAN_POINT ( 'NONE',  ( 0.6064515330803592619, -24.63255479555527572, 39.90703672638513666 ) ) ;
#53377=AXIS2_PLACEMENT_3D ( 'NONE', #8567, #56185, #27693 ) ;
#53378=DIRECTION ( 'NONE',  ( 0.07500201931887537365, 0.1791611824599123881, -0.9809566594899373770 ) ) ;
#53381=ORIENTED_EDGE ( 'NONE', *, *, #59980, .T. ) ;
#53389=CARTESIAN_POINT ( 'NONE',  ( 0.9790320750461907195, -41.05168775549098825, -8.431848253370196389 ) ) ;
#53399=CARTESIAN_POINT ( 'NONE',  ( 0.8554163680231720024, -2.480940174720139613, -46.85136507041474374 ) ) ;
#53400=CARTESIAN_POINT ( 'NONE',  ( 5.901463166500145796, -13.97174733644455635, -14.46748584610301513 ) ) ;
#53401=LINE ( 'NONE', #44063, #51365 ) ;
#53405=CARTESIAN_POINT ( 'NONE',  ( 0.8560838555295223751, -46.14148336882287538, -8.446084690930739214 ) ) ;
#53406=CARTESIAN_POINT ( 'NONE',  ( 0.8554163680231720024, -13.02474486562579514, 45.07284652978080430 ) ) ;
#53407=CARTESIAN_POINT ( 'NONE',  ( 4.962356264823609919, 39.89814050050791394, -13.39305724859256763 ) ) ;
#53409=B_SPLINE_CURVE_WITH_KNOTS ( 'NONE', 3,
 ( #13475, #22864, #41683, #56051, #3731, #32582 ),
 .UNSPECIFIED., .F., .F.,
 ( 4, 2, 4 ),
 ( 7.372574772901430151E-18, 0.0002291472222819920411, 0.0004582944445639767096 ),
 .UNSPECIFIED. ) ;
#53417=CARTESIAN_POINT ( 'NONE',  ( 5.896278296736517710, -11.93494920661357561, -16.18900759929210764 ) ) ;
#53426=CARTESIAN_POINT ( 'NONE',  ( 4.956445790444029775, 29.98832127573299289, -36.30755619981957949 ) ) ;
#53427=CARTESIAN_POINT ( 'NONE',  ( 0.9762797500689124330, 14.58899758184696971, -39.28722355604386252 ) ) ;
#53428=CARTESIAN_POINT ( 'NONE',  ( 0.8560838555295158248, 3.785103201470073397, 46.75516899590838449 ) ) ;
#53433=CARTESIAN_POINT ( 'NONE',  ( 0.6064515330803568194, -44.53023827495938747, -14.71027583740118772 ) ) ;
#53434=CARTESIAN_POINT ( 'NONE',  ( 5.895881250540457863, -13.97904524590158459, 14.46077368681693898 ) ) ;
#53438=CARTESIAN_POINT ( 'NONE',  ( 2.618530812446115519, -46.97577780651594281, -1.732942200722220161 ) ) ;
#53442=CARTESIAN_POINT ( 'NONE',  ( 0.9780303403264782869, 28.90096030599704946, -30.34920273724279127 ) ) ;
#53448=CARTESIAN_POINT ( 'NONE',  ( 0.9762797500689124330, 40.55021165774351743, 10.58324712448433580 ) ) ;
#53454=CARTESIAN_POINT ( 'NONE',  ( 0.7764146366350218598, -38.15852726313939058, 27.27576343161479500 ) ) ;
#53455=ADVANCED_FACE ( 'NONE', ( #55094 ), #42502, .T. ) ;
#53461=CARTESIAN_POINT ( 'NONE',  ( 1.231276596079881047, 25.54232633153377208, -33.23952972879584422 ) ) ;
#53467=CARTESIAN_POINT ( 'NONE',  ( 0.5837157313716023754, -34.84153614343021133, 31.38955913593036939 ) ) ;
#53469=ORIENTED_EDGE ( 'NONE', *, *, #40784, .T. ) ;
#53471=DIRECTION ( 'NONE',  ( -1.000000000000000000, -0.000000000000000000, -0.000000000000000000 ) ) ;
#53479=DIRECTION ( 'NONE',  ( -1.000000000000000000, -0.000000000000000000, -0.000000000000000000 ) ) ;
#53483=CARTESIAN_POINT ( 'NONE',  ( 5.896782393890504181, 0.6784186533441023403, -20.10138888258239120 ) ) ;
#53484=CARTESIAN_POINT ( 'NONE',  ( 0.9785694773339239649, 36.17119032496986364, -21.16554738695601046 ) ) ;
#53495=CARTESIAN_POINT ( 'NONE',  ( 2.788021980277358036, 6.069845295522647588E-12, -46.99417130740492610 ) ) ;
#53496=CARTESIAN_POINT ( 'NONE',  ( 5.917102823773431552, -7.236410236534137397, 18.76496962268593549 ) ) ;
#53505=CARTESIAN_POINT ( 'NONE',  ( 0.5804410086790514622, -1.020940616195395556, -46.88792522722239653 ) ) ;
#53511=CARTESIAN_POINT ( 'NONE',  ( 0.6845945791218023269, 40.79463988471306379, 23.15607646797107577 ) ) ;
#53512=( BOUNDED_SURFACE ( )  B_SPLINE_SURFACE ( 3, 1, ( 
 ( #53734, #20563 ),
 ( #49067, #48444 ),
 ( #29957, #49369 ),
 ( #20268, #39695 ) ),
 .UNSPECIFIED., .F., .F., .F. ) 
 B_SPLINE_SURFACE_WITH_KNOTS ( ( 4, 4 ),
 ( 2, 2 ),
 ( 0.000000000000000000, 1.000000000000000000 ),
 ( 0.000000000000000000, 1.000000000000000000 ),
 .UNSPECIFIED. ) 
 GEOMETRIC_REPRESENTATION_ITEM ( )  RATIONAL_B_SPLINE_SURFACE ( (
 ( 1.000000000000000000, 1.000000000000000000),
 ( 0.7282232189291693025, 0.9929344683865674037),
 ( 0.7282232189291693025, 0.9929344683865674037),
 ( 1.000000000000000000, 1.000000000000000000) ) ) 
 REPRESENTATION_ITEM ( '' )  SURFACE ( )  );
#53516=EDGE_CURVE ( 'NONE', #18712, #26439, #30362, .T. ) ;
#53524=ORIENTED_EDGE ( 'NONE', *, *, #29751, .T. ) ;
#53525=LINE ( 'NONE', #1215, #37301 ) ;
#53529=CARTESIAN_POINT ( 'NONE',  ( 5.896278296736517710, -19.93266788971473957, -2.686211163091726029 ) ) ;
#53550=CARTESIAN_POINT ( 'NONE',  ( 0.9775691876210979014, 20.47097313734579060, -36.56874304375333651 ) ) ;
#53554=CARTESIAN_POINT ( 'NONE',  ( 0.5806925824938499181, -20.23436166722466467, 42.30594485723624132 ) ) ;
#53557=CARTESIAN_POINT ( 'NONE',  ( 1.157643937452369043, -18.38969994869442459, -37.66724320137780069 ) ) ;
#53562=CARTESIAN_POINT ( 'NONE',  ( 0.5832655196449141322, -46.77552346137193950, -3.359402906465947858 ) ) ;
#53572=CARTESIAN_POINT ( 'NONE',  ( 0.9775691876210995668, 41.58336652501495223, -5.211270232511006739 ) ) ;
#53573=EDGE_CURVE ( 'NONE', #12846, #32685, #49821, .T. ) ;
#53583=LINE ( 'NONE', #10705, #50426 ) ;
#53586=CARTESIAN_POINT ( 'NONE',  ( 1.231276596079881047, 40.64579686208666232, -10.25650859035628315 ) ) ;
#53587=DIRECTION ( 'NONE',  ( 0.000000000000000000, 0.000000000000000000, -1.000000000000000000 ) ) ;
#53590=CARTESIAN_POINT ( 'NONE',  ( 4.956445790444005794, -27.49627641100061837, -38.22947597953034204 ) ) ;
#53591=CARTESIAN_POINT ( 'NONE',  ( 0.5804410086790514622, -46.82762660194600102, -2.587129429332111208 ) ) ;
#53595=CARTESIAN_POINT ( 'NONE',  ( 2.528100132419515145, 5.404255688820265746, 41.62989069264931175 ) ) ;
#53596=ORIENTED_EDGE ( 'NONE', *, *, #35598, .T. ) ;
#53604=ORIENTED_EDGE ( 'NONE', *, *, #37649, .T. ) ;
#53608=ORIENTED_EDGE ( 'NONE', *, *, #43149, .T. ) ;
#53609=CARTESIAN_POINT ( 'NONE',  ( 2.618530812446115519, -9.204197330483806283, -46.09782576976612489 ) ) ;
#53615=ORIENTED_EDGE ( 'NONE', *, *, #6379, .T. ) ;
#53619=CARTESIAN_POINT ( 'NONE',  ( 0.9762797500689124330, 14.58899758184639595, 39.28722355604407568 ) ) ;
#53627=CARTESIAN_POINT ( 'NONE',  ( 3.376099380956838925, 12.51418204574271087, -4.806623696325517336 ) ) ;
#53637=CARTESIAN_POINT ( 'NONE',  ( 0.9787464366903572133, 15.22736283113052913, -39.04435188474212026 ) ) ;
#53645=EDGE_CURVE ( 'NONE', #41497, #7082, #40095, .T. ) ;
#53651=CARTESIAN_POINT ( 'NONE',  ( 4.956445790444004018, -45.27177431812773278, -12.96165499572285817 ) ) ;
#53661=CARTESIAN_POINT ( 'NONE',  ( 2.528100132419515145, -26.16755375504030212, 32.82549175730883917 ) ) ;
#53663=DIRECTION ( 'NONE',  ( 0.07500201931887537365, -0.5805833823197799060, -0.8107389427381760383 ) ) ;
#53672=ADVANCED_FACE ( 'NONE', ( #543 ), #31026, .F. ) ;
#53677=( BOUNDED_SURFACE ( )  B_SPLINE_SURFACE ( 3, 1, ( 
 ( #12788, #46001 ),
 ( #17467, #22470 ),
 ( #3044, #31879 ),
 ( #37208, #32186 ) ),
 .UNSPECIFIED., .F., .F., .F. ) 
 B_SPLINE_SURFACE_WITH_KNOTS ( ( 4, 4 ),
 ( 2, 2 ),
 ( 0.000000000000000000, 1.000000000000000000 ),
 ( 0.000000000000000000, 1.000000000000000000 ),
 .UNSPECIFIED. ) 
 GEOMETRIC_REPRESENTATION_ITEM ( )  RATIONAL_B_SPLINE_SURFACE ( (
 ( 1.000000000000000000, 1.000000000000000000),
 ( 0.7282232189291693025, 0.9929344683865674037),
 ( 0.7282232189291693025, 0.9929344683865674037),
 ( 1.000000000000000000, 1.000000000000000000) ) ) 
 REPRESENTATION_ITEM ( '' )  SURFACE ( )  );
#53690=CARTESIAN_POINT ( 'NONE',  ( 1.231276596079881047, 36.49189576017899839, -20.63051901543672884 ) ) ;
#53696=CARTESIAN_POINT ( 'NONE',  ( 0.5804410086790514622, -8.338934868870371275, -46.15172821366643774 ) ) ;
#53707=CARTESIAN_POINT ( 'NONE',  ( 5.895596859100789899, -9.662743138698489886, 17.63971593444811603 ) ) ;
#53712=CARTESIAN_POINT ( 'NONE',  ( 5.895596859100789899, -11.93344155749883662, -16.19015613903236428 ) ) ;
#53713=LINE ( 'NONE', #44078, #32850 ) ;
#53716=CARTESIAN_POINT ( 'NONE',  ( 4.960386119450142850, -42.07286811692948447, 12.01291942401176271 ) ) ;
#53719=DIRECTION ( 'NONE',  ( -1.000000000000000000, -0.000000000000000000, -0.000000000000000000 ) ) ;
#53725=CARTESIAN_POINT ( 'NONE',  ( 0.7764146366350244133, 16.02283669739539462, -44.08298059158165216 ) ) ;
#53729=CARTESIAN_POINT ( 'NONE',  ( 0.7056313189692677845, -44.57575722724908474, -14.58596968236639668 ) ) ;
#53734=CARTESIAN_POINT ( 'NONE',  ( 5.917102823773431552, -11.92306321980329464, -16.19661327278996055 ) ) ;
#53737=FACE_OUTER_BOUND ( 'NONE', #22922, .T. ) ;
#53738=CARTESIAN_POINT ( 'NONE',  ( 4.962356264823608143, 41.15374796524913847, 8.809348799718396350 ) ) ;
#53742=CARTESIAN_POINT ( 'NONE',  ( 0.5806925824938494740, -35.14454992382308518, -31.04968555389040219 ) ) ;
#53743=CARTESIAN_POINT ( 'NONE',  ( 4.960386119450151732, -40.09630699761650163, -17.51349850330398539 ) ) ;
#53748=B_SPLINE_CURVE_WITH_KNOTS ( 'NONE', 3,
 ( #60585, #12394, #17700, #55898 ),
 .UNSPECIFIED., .F., .F.,
 ( 4, 4 ),
 ( 8.673617379884035472E-19, 0.004042984057420974560 ),
 .UNSPECIFIED. ) ;
#53758=LINE ( 'NONE', #59708, #50599 ) ;
#53763=CARTESIAN_POINT ( 'NONE',  ( 0.5806925824938506953, -38.96949031362410665, -26.08833430941730924 ) ) ;
#53768=CARTESIAN_POINT ( 'NONE',  ( 0.9775691876210974574, 40.31814568763066831, 11.43594496755648926 ) ) ;
#53770=EDGE_CURVE ( 'NONE', #58714, #58688, #51917, .T. ) ;
#53772=ORIENTED_EDGE ( 'NONE', *, *, #37311, .F. ) ;
#53797=CARTESIAN_POINT ( 'NONE',  ( 5.910764540655177868, -7.242942773736444906, 18.76275615269627650 ) ) ;
#53799=VERTEX_POINT ( 'NONE', #21210 ) ;
#53818=CARTESIAN_POINT ( 'NONE',  ( 0.5804410086790514622, -41.60900809504538955, 21.63816760268401040 ) ) ;
#53822=ADVANCED_FACE ( 'NONE', ( #49711 ), #26626, .F. ) ;
#53825=CARTESIAN_POINT ( 'NONE',  ( 5.895881250540457863, 3.349849349787409114, 19.83194874292564336 ) ) ;
#53829=CARTESIAN_POINT ( 'NONE',  ( 0.5837157313716019313, -19.65754995710837960, -42.57719804385690310 ) ) ;
#53837=ORIENTED_EDGE ( 'NONE', *, *, #61029, .F. ) ;
#53839=CARTESIAN_POINT ( 'NONE',  ( 1.000433927950261870, 15.67543119259813267, 38.86771841231447411 ) ) ;
#53841=AXIS2_PLACEMENT_3D ( 'NONE', #30340, #7681, #6504 ) ;
#53843=CONICAL_SURFACE ( 'NONE', #2882, 42.08604991992415023, 1.569615340895231137 ) ;
#53844=VERTEX_POINT ( 'NONE', #35327 ) ;
#53846=ORIENTED_EDGE ( 'NONE', *, *, #39512, .F. ) ;
#53849=EDGE_CURVE ( 'NONE', #33340, #20260, #31732, .T. ) ;
#53851=B_SPLINE_CURVE_WITH_KNOTS ( 'NONE', 3,
 ( #59612, #55217, #16720, #31117, #50225, #26413 ),
 .UNSPECIFIED., .F., .F.,
 ( 4, 2, 4 ),
 ( 1.176834411578111192E-16, 0.0002448718616795923374, 0.0004897437233590669304 ),
 .UNSPECIFIED. ) ;
#53852=CARTESIAN_POINT ( 'NONE',  ( 0.8554163680231720024, -18.91615390926536122, 42.93465493506153052 ) ) ;
#53853=ORIENTED_EDGE ( 'NONE', *, *, #13738, .T. ) ;
#53856=( BOUNDED_SURFACE ( )  B_SPLINE_SURFACE ( 3, 1, ( 
 ( #46453, #37679 ),
 ( #47075, #56743 ),
 ( #47362, #4410 ),
 ( #23865, #3810 ) ),
 .UNSPECIFIED., .F., .F., .F. ) 
 B_SPLINE_SURFACE_WITH_KNOTS ( ( 4, 4 ),
 ( 2, 2 ),
 ( 0.000000000000000000, 1.000000000000000000 ),
 ( 0.000000000000000000, 1.000000000000000000 ),
 .UNSPECIFIED. ) 
 GEOMETRIC_REPRESENTATION_ITEM ( )  RATIONAL_B_SPLINE_SURFACE ( (
 ( 1.000000000000000000, 1.000000000000000000),
 ( 0.9952954269826590483, 0.8620686068821339365),
 ( 0.9952954269826590483, 0.8620686068821339365),
 ( 1.000000000000000000, 1.000000000000000000) ) ) 
 REPRESENTATION_ITEM ( '' )  SURFACE ( )  );
#53858=EDGE_CURVE ( 'NONE', #33488, #35234, #39416, .T. ) ;
#53860=CARTESIAN_POINT ( 'NONE',  ( 5.896278296736517710, 16.57877312360411892, 11.38732898139179284 ) ) ;
#53865=CARTESIAN_POINT ( 'NONE',  ( 0.9762797500689124330, -18.09842611962761083, -37.79909730639192844 ) ) ;
#53871=CARTESIAN_POINT ( 'NONE',  ( 0.5817216825391124946, -46.81948311678352326, -2.677863492540627277 ) ) ;
#53875=( BOUNDED_SURFACE ( )  B_SPLINE_SURFACE ( 3, 1, ( 
 ( #39674, #39062 ),
 ( #34347, #58728 ),
 ( #10529, #1109 ),
 ( #29622, #9920 ) ),
 .UNSPECIFIED., .F., .F., .F. ) 
 B_SPLINE_SURFACE_WITH_KNOTS ( ( 4, 4 ),
 ( 2, 2 ),
 ( 0.000000000000000000, 1.000000000000000000 ),
 ( 0.000000000000000000, 1.000000000000000000 ),
 .UNSPECIFIED. ) 
 GEOMETRIC_REPRESENTATION_ITEM ( )  RATIONAL_B_SPLINE_SURFACE ( (
 ( 1.000000000000000000, 1.000000000000000000),
 ( 0.7282232189291694135, 0.9929344683865672927),
 ( 0.7282232189291694135, 0.9929344683865672927),
 ( 1.000000000000000000, 1.000000000000000000) ) ) 
 REPRESENTATION_ITEM ( '' )  SURFACE ( )  );
#53880=CARTESIAN_POINT ( 'NONE',  ( 0.9772918015221170318, -12.81218603359625519, -39.90218972426451671 ) ) ;
#53887=CARTESIAN_POINT ( 'NONE',  ( 0.9784957157296378938, 41.50303087276166991, -5.816483935072919387 ) ) ;
#53891=CARTESIAN_POINT ( 'NONE',  ( 4.956445790443988031, 0.000000000000000000, 0.000000000000000000 ) ) ;
#53892=AXIS2_PLACEMENT_3D ( 'NONE', #29976, #31211, #40033 ) ;
#53904=ORIENTED_EDGE ( 'NONE', *, *, #30529, .F. ) ;
#53908=CARTESIAN_POINT ( 'NONE',  ( 4.956445790443988031, 0.000000000000000000, 0.000000000000000000 ) ) ;
#53909=VERTEX_POINT ( 'NONE', #60032 ) ;
#53913=ORIENTED_EDGE ( 'NONE', *, *, #58669, .F. ) ;
#53916=VERTEX_POINT ( 'NONE', #55944 ) ;
#53924=CARTESIAN_POINT ( 'NONE',  ( 0.9790320750461900534, -17.56280114220697186, -38.05108603682009516 ) ) ;
#53932=EDGE_CURVE ( 'NONE', #26593, #14707, #6276, .T. ) ;
#53935=CARTESIAN_POINT ( 'NONE',  ( 4.958415959904820092, -4.043245302072359770, -45.24219403665024686 ) ) ;
#53937=CARTESIAN_POINT ( 'NONE',  ( 4.962356264823596597, 41.32726869310139506, 7.955655864260913646 ) ) ;
#53943=CARTESIAN_POINT ( 'NONE',  ( 0.8560838555295158248, 45.47430759461114747, -11.50913475776619599 ) ) ;
#53946=ORIENTED_EDGE ( 'NONE', *, *, #1116, .F. ) ;
#53950=CARTESIAN_POINT ( 'NONE',  ( 0.9762797500689124330, 33.20096159360354449, -25.57383300261748360 ) ) ;
#53952=ORIENTED_EDGE ( 'NONE', *, *, #16524, .F. ) ;
#53953=VERTEX_POINT ( 'NONE', #22139 ) ;
#53955=CARTESIAN_POINT ( 'NONE',  ( 0.9780303403264770656, 14.75966257217395672, -39.22361500614967866 ) ) ;
#53966=CARTESIAN_POINT ( 'NONE',  ( 4.291220156522059348, 39.39367666905470600, 25.83654844981566967 ) ) ;
#53970=CARTESIAN_POINT ( 'NONE',  ( 0.6064782688330851990, 45.41335037835364830, -11.70307881848435017 ) ) ;
#53976=CARTESIAN_POINT ( 'NONE',  ( 0.5804410086790514622, 46.55025363952962181, 5.709092568075566199 ) ) ;
#54006=CARTESIAN_POINT ( 'NONE',  ( 1.231276596079881047, -2.246340108600348717, 41.85965512441018888 ) ) ;
#54010=EDGE_CURVE ( 'NONE', #34712, #48535, #16093, .T. ) ;
#54013=ORIENTED_EDGE ( 'NONE', *, *, #3030, .T. ) ;
#54014=CARTESIAN_POINT ( 'NONE',  ( 0.9762797500689124330, -41.77809974471944088, 3.303810967046753255 ) ) ;
#54025=VERTEX_POINT ( 'NONE', #9569 ) ;
#54031=CARTESIAN_POINT ( 'NONE',  ( 4.956445790443988031, 0.000000000000000000, 0.000000000000000000 ) ) ;
#54034=CARTESIAN_POINT ( 'NONE',  ( 0.6845945791218023269, 16.04817208170968357, -44.07791616614580477 ) ) ;
#54036=CARTESIAN_POINT ( 'NONE',  ( 1.092182651088184464, 29.69432493936918505, 29.58053837977669787 ) ) ;
#54042=B_SPLINE_CURVE_WITH_KNOTS ( 'NONE', 3,
 ( #50702, #21912, #7792, #12219, #26597, #36336 ),
 .UNSPECIFIED., .F., .F.,
 ( 4, 2, 4 ),
 ( 1.182369072465671822E-16, 0.0002448718616795935842, 0.0004897437233590689904 ),
 .UNSPECIFIED. ) ;
#54043=CARTESIAN_POINT ( 'NONE',  ( 4.962356264823600149, -32.75738977283805298, 26.42326651140453109 ) ) ;
#54065=ORIENTED_EDGE ( 'NONE', *, *, #14734, .F. ) ;
#54093=ORIENTED_EDGE ( 'NONE', *, *, #30042, .F. ) ;
#54095=CARTESIAN_POINT ( 'NONE',  ( 0.9789233960466692253, 36.12512514380552631, -21.24410648101569166 ) ) ;
#54102=ORIENTED_EDGE ( 'NONE', *, *, #18404, .F. ) ;
#54104=CARTESIAN_POINT ( 'NONE',  ( 0.9772918015221172539, -31.35844505642634061, -27.80260382399047714 ) ) ;
#54108=CARTESIAN_POINT ( 'NONE',  ( 0.9788927965476035276, -27.16546388611207519, -31.91197556535973234 ) ) ;
#54110=ORIENTED_EDGE ( 'NONE', *, *, #13038, .F. ) ;
#54118=CARTESIAN_POINT ( 'NONE',  ( 0.9762797500689124330, -12.89881610234921006, -39.87411852747946028 ) ) ;
#54120=EDGE_CURVE ( 'NONE', #20443, #40951, #1500, .T. ) ;
#54123=( BOUNDED_SURFACE ( )  B_SPLINE_SURFACE ( 3, 1, ( 
 ( #2146, #53311 ),
 ( #50399, #29515 ),
 ( #25985, #20139 ),
 ( #41042, #26591 ) ),
 .UNSPECIFIED., .F., .F., .F. ) 
 B_SPLINE_SURFACE_WITH_KNOTS ( ( 4, 4 ),
 ( 2, 2 ),
 ( 0.000000000000000000, 1.000000000000000000 ),
 ( 0.000000000000000000, 1.000000000000000000 ),
 .UNSPECIFIED. ) 
 GEOMETRIC_REPRESENTATION_ITEM ( )  RATIONAL_B_SPLINE_SURFACE ( (
 ( 1.000000000000000000, 1.000000000000000000),
 ( 0.9729067724841187204, 0.9999501103223794596),
 ( 0.9729067724841187204, 0.9999501103223794596),
 ( 1.000000000000000000, 1.000000000000000000) ) ) 
 REPRESENTATION_ITEM ( '' )  SURFACE ( )  );
#54136=CARTESIAN_POINT ( 'NONE',  ( 0.5830081025819934260, -19.98762393432967244, -42.42318851574051308 ) ) ;
#54140=ORIENTED_EDGE ( 'NONE', *, *, #19763, .T. ) ;
#54146=CARTESIAN_POINT ( 'NONE',  ( 4.962356264823596597, 37.75702904547799932, 18.59145920903680249 ) ) ;
#54155=CARTESIAN_POINT ( 'NONE',  ( 2.618530812446111078, 42.70834099002623674, 19.63986759318516562 ) ) ;
#54158=VECTOR ( 'NONE', #41742, 1000.000000000000114 ) ;
#54163=AXIS2_PLACEMENT_3D ( 'NONE', #37546, #3067, #56616 ) ;
#54168=CARTESIAN_POINT ( 'NONE',  ( 2.282816707992314065, -39.45519661757836616, -25.49086946881566718 ) ) ;
#54169=CARTESIAN_POINT ( 'NONE',  ( 0.9754292589017217185, -18.16743306764310617, -37.76601438632337704 ) ) ;
#54173=B_SPLINE_CURVE_WITH_KNOTS ( 'NONE', 3,
 ( #58327, #15149, #58027, #38969 ),
 .UNSPECIFIED., .F., .F.,
 ( 4, 4 ),
 ( 0.000000000000000000, 0.004041751736740998614 ),
 .UNSPECIFIED. ) ;
#54176=B_SPLINE_CURVE_WITH_KNOTS ( 'NONE', 3,
 ( #22005, #32024, #37051, #22618, #2873, #46750 ),
 .UNSPECIFIED., .F., .F.,
 ( 4, 2, 4 ),
 ( 1.578957240921675292E-17, 0.0002448709889506574277, 0.0004897419779012991345 ),
 .UNSPECIFIED. ) ;
#54179=B_SPLINE_CURVE_WITH_KNOTS ( 'NONE', 3,
 ( #48738, #15854, #5796, #24944, #1110, #20251 ),
 .UNSPECIFIED., .F., .F.,
 ( 4, 2, 4 ),
 ( 8.805430561888389713E-18, 0.0002448709889506567772, 0.0004897419779013047723 ),
 .UNSPECIFIED. ) ;
#54180=CARTESIAN_POINT ( 'NONE',  ( 0.7056313189692735577, 36.27982945926389391, -29.72410836954218638 ) ) ;
#54181=ORIENTED_EDGE ( 'NONE', *, *, #32456, .T. ) ;
#54186=ORIENTED_EDGE ( 'NONE', *, *, #639, .T. ) ;
#54191=FACE_OUTER_BOUND ( 'NONE', #17541, .T. ) ;
#54196=CARTESIAN_POINT ( 'NONE',  ( 5.910764540655178756, -17.29668172820431238, 10.26284754161173751 ) ) ;
#54199=CARTESIAN_POINT ( 'NONE',  ( 5.895596859100789899, 5.955534046174526530, -19.21092911436986128 ) ) ;
#54200=AXIS2_PLACEMENT_3D ( 'NONE', #55515, #22329, #31733 ) ;
#54201=DIRECTION ( 'NONE',  ( 0.07906939808003035641, 0.5431863341251763622, -0.8358807550762931138 ) ) ;
#54207=CARTESIAN_POINT ( 'NONE',  ( 4.956445790443991584, 30.81386304088947625, 35.60960396630300551 ) ) ;
#54208=CARTESIAN_POINT ( 'NONE',  ( 5.896782393890504181, -4.668739246792323883, 19.56345983519973686 ) ) ;
#54212=DIRECTION ( 'NONE',  ( 0.07906939808003035641, 0.9951496949144252868, -0.05852448204801217330 ) ) ;
#54216=CARTESIAN_POINT ( 'NONE',  ( 2.528190830796658961, -5.786163172919478015, -41.57853354664349865 ) ) ;
#54228=CARTESIAN_POINT ( 'NONE',  ( 0.9769922540276041456, -17.23900502197182050, -38.19879920807139939 ) ) ;
#54231=ADVANCED_FACE ( 'NONE', ( #35869 ), #53078, .F. ) ;
#54236=CARTESIAN_POINT ( 'NONE',  ( 1.157644175074338477, -37.03171702379126629, -19.63808060246803322 ) ) ;
#54237=CARTESIAN_POINT ( 'NONE',  ( 3.238018933889920792, 13.39148516828231372, 0.2749861002446604696 ) ) ;
#54238=CARTESIAN_POINT ( 'NONE',  ( 0.9790850452238883950, 36.08407221087763617, 21.31377636514384122 ) ) ;
#54241=ORIENTED_EDGE ( 'NONE', *, *, #48316, .F. ) ;
#54254=CARTESIAN_POINT ( 'NONE',  ( 0.7764146366350259676, 21.75555901402215753, -41.55401455523356447 ) ) ;
#54256=CARTESIAN_POINT ( 'NONE',  ( 4.956445790443988031, 0.000000000000000000, 0.000000000000000000 ) ) ;
#54262=CARTESIAN_POINT ( 'NONE',  ( 0.5797568599927130917, -24.70127811531111917, -39.86316806453116612 ) ) ;
#54271=CARTESIAN_POINT ( 'NONE',  ( 4.962356264823601038, -35.98698831890646943, 21.82137185415336589 ) ) ;
#54275=EDGE_CURVE ( 'NONE', #32480, #50058, #296, .T. ) ;
#54276=CARTESIAN_POINT ( 'NONE',  ( 5.894904586330512508, -19.93362243062206218, -2.679572513488613250 ) ) ;
#54279=CARTESIAN_POINT ( 'NONE',  ( 5.895596859100789899, 17.94951300836806141, 9.074313526372865368 ) ) ;
#54283=DIRECTION ( 'NONE',  ( -0.07500201931887529039, -0.7304373162253511298, 0.6788490437229748320 ) ) ;
#54284=EDGE_CURVE ( 'NONE', #48535, #19440, #1742, .T. ) ;
#54292=VECTOR ( 'NONE', #38473, 1000.000000000000000 ) ;
#54295=EDGE_CURVE ( 'NONE', #715, #37468, #41400, .T. ) ;
#54299=LINE ( 'NONE', #12285, #41959 ) ;
#54301=CARTESIAN_POINT ( 'NONE',  ( 0.9788927965476039716, -41.09688267176417042, -8.208705579750407821 ) ) ;
#54304=DIRECTION ( 'NONE',  ( 0.07500201931887538753, 0.5478996815936139075, -0.8331750332359386668 ) ) ;
#54313=CARTESIAN_POINT ( 'NONE',  ( 1.231276596079887264, 41.65019306089983786, 4.747440258480190245 ) ) ;
#54314=EDGE_CURVE ( 'NONE', #54358, #25579, #49570, .T. ) ;
#54315=ORIENTED_EDGE ( 'NONE', *, *, #54314, .F. ) ;
#54322=CARTESIAN_POINT ( 'NONE',  ( 5.917102823773431552, 10.81462311420893663, -16.95681706421814638 ) ) ;
#54326=ORIENTED_EDGE ( 'NONE', *, *, #22012, .F. ) ;
#54327=CARTESIAN_POINT ( 'NONE',  ( 5.894904586330512508, 0.6708454810751377506, 20.10172575681410834 ) ) ;
#54328=CARTESIAN_POINT ( 'NONE',  ( 5.896278296736517710, -15.78116101695085582, 12.46923961480628051 ) ) ;
#54335=( BOUNDED_SURFACE ( )  B_SPLINE_SURFACE ( 3, 1, ( 
 ( #54208, #36394 ),
 ( #12582, #41103 ),
 ( #31670, #60159 ),
 ( #16975, #3149 ) ),
 .UNSPECIFIED., .F., .F., .F. ) 
 B_SPLINE_SURFACE_WITH_KNOTS ( ( 4, 4 ),
 ( 2, 2 ),
 ( 0.000000000000000000, 1.000000000000000000 ),
 ( 0.000000000000000000, 1.000000000000000000 ),
 .UNSPECIFIED. ) 
 GEOMETRIC_REPRESENTATION_ITEM ( )  RATIONAL_B_SPLINE_SURFACE ( (
 ( 1.000000000000000000, 1.000000000000000000),
 ( 0.9952954269826590483, 0.8620686068821307169),
 ( 0.9952954269826590483, 0.8620686068821307169),
 ( 1.000000000000000000, 1.000000000000000000) ) ) 
 REPRESENTATION_ITEM ( '' )  SURFACE ( )  );
#54338=CARTESIAN_POINT ( 'NONE',  ( 4.962356264823608143, 0.000000000000000000, 0.000000000000000000 ) ) ;
#54340=CARTESIAN_POINT ( 'NONE',  ( 0.9791128995231613841, 15.06706612816901369, 39.10653337404819752 ) ) ;
#54353=ADVANCED_FACE ( 'NONE', ( #6612 ), #41954, .F. ) ;
#54358=VERTEX_POINT ( 'NONE', #706 ) ;
#54365=CARTESIAN_POINT ( 'NONE',  ( 5.896782393890504181, 14.91246379622031526, -13.49609241241443947 ) ) ;
#54369=ORIENTED_EDGE ( 'NONE', *, *, #46928, .T. ) ;
#54374=EDGE_CURVE ( 'NONE', #33554, #46030, #43617, .T. ) ;
#54380=VERTEX_POINT ( 'NONE', #7560 ) ;
#54391=B_SPLINE_CURVE_WITH_KNOTS ( 'NONE', 3,
 ( #30517, #39976, #35568, #54313 ),
 .UNSPECIFIED., .F., .F.,
 ( 4, 4 ),
 ( 0.000000000000000000, 0.004042984057420973693 ),
 .UNSPECIFIED. ) ;
#54393=ORIENTED_EDGE ( 'NONE', *, *, #30683, .T. ) ;
#54396=( BOUNDED_SURFACE ( )  B_SPLINE_SURFACE ( 3, 1, ( 
 ( #59877, #45816 ),
 ( #60482, #50785 ),
 ( #46424, #2859 ),
 ( #7876, #13211 ) ),
 .UNSPECIFIED., .F., .F., .F. ) 
 B_SPLINE_SURFACE_WITH_KNOTS ( ( 4, 4 ),
 ( 2, 2 ),
 ( 0.000000000000000000, 1.000000000000000000 ),
 ( 0.000000000000000000, 1.000000000000000000 ),
 .UNSPECIFIED. ) 
 GEOMETRIC_REPRESENTATION_ITEM ( )  RATIONAL_B_SPLINE_SURFACE ( (
 ( 1.000000000000000000, 1.000000000000000000),
 ( 0.7282232189291693025, 0.9929344683865674037),
 ( 0.7282232189291693025, 0.9929344683865674037),
 ( 1.000000000000000000, 1.000000000000000000) ) ) 
 REPRESENTATION_ITEM ( '' )  SURFACE ( )  );
#54398=LINE ( 'NONE', #26216, #21191 ) ;
#54400=EDGE_LOOP ( 'NONE', ( #10486, #51005, #39878, #38014 ) ) ;
#54401=CARTESIAN_POINT ( 'NONE',  ( 0.9762797500689124330, 3.691134646837550104, 41.74566217230983511 ) ) ;
#54404=CARTESIAN_POINT ( 'NONE',  ( 5.910764540655178756, 19.71228184310533038, 3.990887496177151217 ) ) ;
#54422=ORIENTED_EDGE ( 'NONE', *, *, #46559, .F. ) ;
#54425=CARTESIAN_POINT ( 'NONE',  ( 0.5830082357119567016, 45.15677922592038129, 12.65295715948731825 ) ) ;
#54436=CARTESIAN_POINT ( 'NONE',  ( 4.962356264823599261, -28.94323483023637777, 30.55363735178087126 ) ) ;
#54439=VECTOR ( 'NONE', #20980, 999.9999999999998863 ) ;
#54443=CARTESIAN_POINT ( 'NONE',  ( 4.956445790443988031, 0.000000000000000000, 0.000000000000000000 ) ) ;
#54445=CARTESIAN_POINT ( 'NONE',  ( 0.5837799406558239479, -19.82278343636528817, -42.50059771829290867 ) ) ;
#54450=ADVANCED_FACE ( 'NONE', ( #2864 ), #59476, .F. ) ;
#54456=CIRCLE ( 'NONE', #39484, 47.09074272231896430 ) ;
#54472=CARTESIAN_POINT ( 'NONE',  ( 4.962356264823608143, 0.000000000000000000, 0.000000000000000000 ) ) ;
#54482=CARTESIAN_POINT ( 'NONE',  ( 0.5806925824938499181, -46.75147433417400578, -3.677228565731735621 ) ) ;
#54485=CARTESIAN_POINT ( 'NONE',  ( 3.661921753702006566, -46.77018590444192370, 5.018050846492144501 ) ) ;
#54486=CARTESIAN_POINT ( 'NONE',  ( 1.231276596079881047, 28.52807286890743654, 30.71523773966879745 ) ) ;
#54487=CARTESIAN_POINT ( 'NONE',  ( 0.6064515330803568194, 36.36011321167069354, -29.61885384804041976 ) ) ;
#54499=CARTESIAN_POINT ( 'NONE',  ( 0.8560838555295158248, 17.70877843982841782, -43.43698884880027578 ) ) ;
#54501=CARTESIAN_POINT ( 'NONE',  ( 4.962356264823608143, -10.17958088187436871, 40.83640203215416165 ) ) ;
#54511=ADVANCED_FACE ( 'NONE', ( #4084 ), #39953, .F. ) ;
#54523=AXIS2_PLACEMENT_3D ( 'NONE', #8747, #22856, #32264 ) ;
#54524=CARTESIAN_POINT ( 'NONE',  ( 3.238018933889920792, -13.37994740236394087, 0.6200805412423465723 ) ) ;
#54526=ORIENTED_EDGE ( 'NONE', *, *, #35583, .T. ) ;
#54533=ORIENTED_EDGE ( 'NONE', *, *, #44101, .T. ) ;
#54540=CARTESIAN_POINT ( 'NONE',  ( 5.896782393890504181, -19.93422257774826889, 2.674482585249640110 ) ) ;
#54551=ADVANCED_FACE ( 'NONE', ( #8485 ), #20712, .F. ) ;
#54557=CARTESIAN_POINT ( 'NONE',  ( 4.956445790443989807, 46.03642002599014660, 9.908889005849758291 ) ) ;
#54559=CARTESIAN_POINT ( 'NONE',  ( 5.896278296736517710, -20.11285533178147844, -0.005478796673508855644 ) ) ;
#54560=( NAMED_UNIT ( * ) PLANE_ANGLE_UNIT ( ) SI_UNIT ( $, .RADIAN. ) );
#54564=CARTESIAN_POINT ( 'NONE',  ( 0.9789889208857681657, -39.62124817252024656, -13.65619241567479492 ) ) ;
#54572=CARTESIAN_POINT ( 'NONE',  ( 0.8560838555295158248, -24.46533024579895610, -40.02274915652004239 ) ) ;
#54578=LINE ( 'NONE', #35831, #51054 ) ;
#54584=EDGE_CURVE ( 'NONE', #23687, #9918, #18191, .T. ) ;
#54606=CARTESIAN_POINT ( 'NONE',  ( 5.895596859100789899, 18.99884588797239005, -6.600911917118875039 ) ) ;
#54607=CARTESIAN_POINT ( 'NONE',  ( 4.962356264823596597, 1.841560470688234474, 42.04574000888969465 ) ) ;
#54609=CARTESIAN_POINT ( 'NONE',  ( 0.5837800304671215690, -38.63726306782081821, -26.57817214948214968 ) ) ;
#54612=CARTESIAN_POINT ( 'NONE',  ( 5.910764540655178756, 18.99430111539264843, -6.611940986348606941 ) ) ;
#54614=VERTEX_POINT ( 'NONE', #39430 ) ;
#54619=B_SPLINE_CURVE_WITH_KNOTS ( 'NONE', 3,
 ( #58958, #11065, #1628, #35806 ),
 .UNSPECIFIED., .F., .F.,
 ( 4, 4 ),
 ( 0.000000000000000000, 0.004447772540403802446 ),
 .UNSPECIFIED. ) ;
#54634=CARTESIAN_POINT ( 'NONE',  ( 0.7764146366350256345, 5.581186775678419032, 46.57135200790456508 ) ) ;
#54635=EDGE_CURVE ( 'NONE', #14061, #59068, #4723, .T. ) ;
#54638=CARTESIAN_POINT ( 'NONE',  ( 0.7764139734771243750, -41.45356087563890668, -21.94636101126028649 ) ) ;
#54645=B_SPLINE_CURVE_WITH_KNOTS ( 'NONE', 3,
 ( #60094, #17202, #59159, #36321, #55386, #30049 ),
 .UNSPECIFIED., .F., .F.,
 ( 4, 2, 4 ),
 ( 2.168404344971008868E-19, 0.0002291459268755698282, 0.0004582918537511394396 ),
 .UNSPECIFIED. ) ;
#54649=CARTESIAN_POINT ( 'NONE',  ( 0.5782707292762423457, 16.17912178775543453, -44.02240761117678147 ) ) ;
#54650=DIRECTION ( 'NONE',  ( -1.000000000000000000, -0.000000000000000000, -0.000000000000000000 ) ) ;
#54656=CARTESIAN_POINT ( 'NONE',  ( 0.9785694773339239649, 14.85438594643830434, 39.18778666713557612 ) ) ;
#54657=ORIENTED_EDGE ( 'NONE', *, *, #51843, .F. ) ;
#54665=CARTESIAN_POINT ( 'NONE',  ( 2.618530812446115519, -12.57566640959698923, 45.29436392701340708 ) ) ;
#54671=CARTESIAN_POINT ( 'NONE',  ( 4.962356264823602814, 41.15374796524927348, -8.809348799717806600 ) ) ;
#54672=ORIENTED_EDGE ( 'NONE', *, *, #20041, .T. ) ;
#54678=CARTESIAN_POINT ( 'NONE',  ( 3.661933894777862797, 42.53630112315261869, 20.08218742348897123 ) ) ;
#54679=FACE_OUTER_BOUND ( 'NONE', #56840, .T. ) ;
#54680=CARTESIAN_POINT ( 'NONE',  ( 0.8560838555295158248, 40.81790744942473737, -23.11430867518922128 ) ) ;
#54682=EDGE_CURVE ( 'NONE', #46849, #12584, #13516, .T. ) ;
#54687=ORIENTED_EDGE ( 'NONE', *, *, #48043, .F. ) ;
#54691=ORIENTED_EDGE ( 'NONE', *, *, #44873, .T. ) ;
#54696=CARTESIAN_POINT ( 'NONE',  ( 0.9754292580325131246, 4.774021070332235439, -41.63575614449710827 ) ) ;
#54702=CARTESIAN_POINT ( 'NONE',  ( 0.8560838555295223751, 44.99141268455589682, -13.27198623905683128 ) ) ;
#54707=EDGE_CURVE ( 'NONE', #2564, #46325, #3628, .T. ) ;
#54709=DIRECTION ( 'NONE',  ( -1.000000000000000000, -0.000000000000000000, -0.000000000000000000 ) ) ;
#54720=FACE_OUTER_BOUND ( 'NONE', #11940, .T. ) ;
#54725=AXIS2_PLACEMENT_3D ( 'NONE', #45152, #2182, #50131 ) ;
#54726=B_SPLINE_CURVE_WITH_KNOTS ( 'NONE', 3,
 ( #45696, #3058, #22185, #8076, #17482, #12802, #31897, #14036, #52212, #61903, #33137, #57508, #14648, #24029, #28111, #23724 ),
 .UNSPECIFIED., .F., .F.,
 ( 4, 3, 3, 3, 3, 4 ),
 ( 1.214354834101861570E-17, 0.0002732102107931896743, 0.0004098135523333821303, 0.0005464168938824984917, 0.0008195847345945436605, 0.001092771384553106566 ),
 .UNSPECIFIED. ) ;
#54732=CARTESIAN_POINT ( 'NONE',  ( 0.5835226383429287234, -30.41628309188208945, -35.69442810048165171 ) ) ;
#54734=EDGE_LOOP ( 'NONE', ( #23203, #42723, #38531, #37244 ) ) ;
#54735=CARTESIAN_POINT ( 'NONE',  ( 0.5804410086790514622, 28.25755288515070518, 37.43034272883842561 ) ) ;
#54739=CARTESIAN_POINT ( 'NONE',  ( 0.5830081025819917606, 36.97261815548455388, 28.84887417406409682 ) ) ;
#54742=CARTESIAN_POINT ( 'NONE',  ( 1.231276596079881935, -37.02495017545860634, -19.65781868679418309 ) ) ;
#54744=DIRECTION ( 'NONE',  ( -1.000000000000000000, -0.000000000000000000, -0.000000000000000000 ) ) ;
#54754=CARTESIAN_POINT ( 'NONE',  ( 4.291220156522059348, -9.951772474099044530, 46.04727160136049235 ) ) ;
#54762=CARTESIAN_POINT ( 'NONE',  ( 0.5837800304671224572, -19.69888330479335181, -42.55809357482583266 ) ) ;
#54767=EDGE_LOOP ( 'NONE', ( #50008, #27789, #51340, #38268 ) ) ;
#54773=EDGE_LOOP ( 'NONE', ( #14194, #43927, #3835, #40294 ) ) ;
#54776=VECTOR ( 'NONE', #54987, 999.9999999999998863 ) ;
#54778=CARTESIAN_POINT ( 'NONE',  ( 4.956445790443998689, -27.49627641100115838, 38.22947597952995835 ) ) ;
#54796=LINE ( 'NONE', #40433, #37481 ) ;
#54802=CARTESIAN_POINT ( 'NONE',  ( 0.9785694773339257413, -17.84245254737231434, 37.92073697608524441 ) ) ;
#54806=B_SPLINE_CURVE_WITH_KNOTS ( 'NONE', 3,
 ( #5772, #15218, #5163, #153, #23987, #5471 ),
 .UNSPECIFIED., .F., .F.,
 ( 4, 2, 4 ),
 ( 1.222218565161306604E-16, 0.0002448718616795921748, 0.0004897437233590620515 ),
 .UNSPECIFIED. ) ;
#54809=CARTESIAN_POINT ( 'NONE',  ( 0.9780106845699476636, 40.50128780264890338, -10.76925869233542699 ) ) ;
#54810=VERTEX_POINT ( 'NONE', #53107 ) ;
#54811=LINE ( 'NONE', #8135, #8522 ) ;
#54822=CARTESIAN_POINT ( 'NONE',  ( 2.618530812446111078, -42.57172246446608455, 19.93427288883829718 ) ) ;
#54824=CARTESIAN_POINT ( 'NONE',  ( 0.9762797500689124330, 41.59901070109194876, 5.084003725032276932 ) ) ;
#54829=B_SPLINE_CURVE_WITH_KNOTS ( 'NONE', 3,
 ( #45424, #30674, #17518, #40736, #59805, #2473 ),
 .UNSPECIFIED., .F., .F.,
 ( 4, 2, 4 ),
 ( 3.471140604459641645E-18, 0.0002291459268755729724, 0.0004582918537511424754 ),
 .UNSPECIFIED. ) ;
#54831=CARTESIAN_POINT ( 'NONE',  ( 5.894904586330512508, 19.70964338679892691, -4.007414331817491515 ) ) ;
#54841=CARTESIAN_POINT ( 'NONE',  ( 1.231276596079881047, -30.51591784428347154, -28.74118176309054107 ) ) ;
#54846=CARTESIAN_POINT ( 'NONE',  ( 0.9762797500689124330, 41.90547441298052433, -0.5059638413352701702 ) ) ;
#54848=CARTESIAN_POINT ( 'NONE',  ( 0.5806925824938499181, 11.40214825760356376, -45.48860711711441240 ) ) ;
#54852=VECTOR ( 'NONE', #14882, 1000.000000000000000 ) ;
#54853=ORIENTED_EDGE ( 'NONE', *, *, #10402, .F. ) ;
#54855=CARTESIAN_POINT ( 'NONE',  ( 0.5806925824938499181, 22.05663578530122493, 41.38510819338441138 ) ) ;
#54863=ORIENTED_EDGE ( 'NONE', *, *, #50693, .F. ) ;
#54864=CARTESIAN_POINT ( 'NONE',  ( 4.962356264823601038, -35.98698831890646943, 21.82137185415336589 ) ) ;
#54871=EDGE_LOOP ( 'NONE', ( #17275, #17654, #48874, #36902 ) ) ;
#54876=ORIENTED_EDGE ( 'NONE', *, *, #3443, .T. ) ;
#54881=VECTOR ( 'NONE', #12344, 1000.000000000000227 ) ;
#54885=VERTEX_POINT ( 'NONE', #42510 ) ;
#54886=CARTESIAN_POINT ( 'NONE',  ( 0.6064515330803575965, 21.91205122295670904, -41.46319268025084881 ) ) ;
#54891=CARTESIAN_POINT ( 'NONE',  ( 5.896278296736517710, -19.39967646272030422, 5.308439766650788094 ) ) ;
#54900=DIRECTION ( 'NONE',  ( 0.07500201931887538753, 0.7485533666540395981, -0.6588190604171937359 ) ) ;
#54902=CARTESIAN_POINT ( 'NONE',  ( 0.5824935313925944103, -14.24163328556457309, -44.68124951714464999 ) ) ;
#54910=ORIENTED_EDGE ( 'NONE', *, *, #59619, .F. ) ;
#54926=CARTESIAN_POINT ( 'NONE',  ( 0.5817216825391119395, -38.91887341143593915, -26.16402577188925349 ) ) ;
#54929=B_SPLINE_CURVE_WITH_KNOTS ( 'NONE', 3,
 ( #15396, #34500, #27557, #8136 ),
 .UNSPECIFIED., .F., .F.,
 ( 4, 4 ),
 ( 0.000000000000000000, 0.005004948556313808770 ),
 .UNSPECIFIED. ) ;
#54934=ORIENTED_EDGE ( 'NONE', *, *, #20277, .T. ) ;
#54938=VERTEX_POINT ( 'NONE', #34955 ) ;
#54940=CARTESIAN_POINT ( 'NONE',  ( 3.661921753702025217, 15.13536876490557681, -44.53708270850657414 ) ) ;
#54944=CARTESIAN_POINT ( 'NONE',  ( 4.956445790444026223, 13.43466403631445338, -45.13366650706537797 ) ) ;
#54956=DIRECTION ( 'NONE',  ( -0.07906939808003035641, -0.5295738273858142664, 0.8445706552060647798 ) ) ;
#54960=DIRECTION ( 'NONE',  ( -0.07500201931887527651, -0.9744221909196664200, 0.2118397765798677723 ) ) ;
#54975=CARTESIAN_POINT ( 'NONE',  ( 0.9785694773339244090, -31.23050093752737411, 27.94622008261178792 ) ) ;
#54977=CARTESIAN_POINT ( 'NONE',  ( 5.895881250540457863, 17.94906520686009088, -9.075171613153402816 ) ) ;
#54978=CARTESIAN_POINT ( 'NONE',  ( 0.9790724872846775506, -7.010505575501338349, 41.31813187400074838 ) ) ;
#54979=CARTESIAN_POINT ( 'NONE',  ( 0.9762797500689124330, 29.49606728235556830, -29.77090526101713763 ) ) ;
#54983=VERTEX_POINT ( 'NONE', #11763 ) ;
#54987=DIRECTION ( 'NONE',  ( 0.07500201931887538753, 0.7304373162253416929, 0.6788490437229849350 ) ) ;
#54991=CARTESIAN_POINT ( 'NONE',  ( 5.917102823773431552, 3.353685953999505642, 19.83034312798667642 ) ) ;
#55002=ORIENTED_EDGE ( 'NONE', *, *, #38299, .T. ) ;
#55016=CARTESIAN_POINT ( 'NONE',  ( 0.5837800005270550319, -19.74012976957846632, 42.53895315263395815 ) ) ;
#55021=CARTESIAN_POINT ( 'NONE',  ( 0.8560838555295223751, -18.91252766612315739, 42.92655508376904550 ) ) ;
#55034=DIRECTION ( 'NONE',  ( 0.000000000000000000, 0.000000000000000000, 1.000000000000000000 ) ) ;
#55043=EDGE_CURVE ( 'NONE', #10045, #21039, #51787, .T. ) ;
#55045=CARTESIAN_POINT ( 'NONE',  ( 0.5837800304671205698, -30.24261836534340731, -35.84161501087377388 ) ) ;
#55048=FACE_OUTER_BOUND ( 'NONE', #11049, .T. ) ;
#55050=ORIENTED_EDGE ( 'NONE', *, *, #6926, .F. ) ;
#55052=CARTESIAN_POINT ( 'NONE',  ( 0.5837800304671219020, 36.77575525172623827, 29.09950442610023558 ) ) ;
#55059=CARTESIAN_POINT ( 'NONE',  ( 4.962356264823602814, -33.29728444345256122, -25.73958909062380229 ) ) ;
#55066=CARTESIAN_POINT ( 'NONE',  ( 5.896782393890504181, 3.339090646272911300, -19.83372281075806853 ) ) ;
#55073=ORIENTED_EDGE ( 'NONE', *, *, #486, .T. ) ;
#55074=FACE_OUTER_BOUND ( 'NONE', #52705, .T. ) ;
#55077=CARTESIAN_POINT ( 'NONE',  ( 0.5806925824938502512, -20.23436166722406426, -42.30594485723652554 ) ) ;
#55079=DIRECTION ( 'NONE',  ( -1.000000000000000000, -0.000000000000000000, -0.000000000000000000 ) ) ;
#55081=EDGE_CURVE ( 'NONE', #19905, #29740, #51008, .T. ) ;
#55084=FACE_OUTER_BOUND ( 'NONE', #2623, .T. ) ;
#55085=DIRECTION ( 'NONE',  ( 0.000000000000000000, 0.000000000000000000, 1.000000000000000000 ) ) ;
#55094=FACE_OUTER_BOUND ( 'NONE', #35652, .T. ) ;
#55096=CARTESIAN_POINT ( 'NONE',  ( 4.291220156522059348, 42.48586100259134923, 20.35535831603521117 ) ) ;
#55097=CARTESIAN_POINT ( 'NONE',  ( 0.9762797500689124330, 36.31338395866797697, 20.92039508843128814 ) ) ;
#55101=CARTESIAN_POINT ( 'NONE',  ( 1.091591847532204618, 28.57213991056969959, 30.66580851513083417 ) ) ;
#55106=DIRECTION ( 'NONE',  ( -0.07500201931887529039, 0.3709639164044522541, 0.9256135639801102988 ) ) ;
#55110=CARTESIAN_POINT ( 'NONE',  ( 1.000433927950260982, -39.36980744151690459, 14.36791354618788041 ) ) ;
#55111=CARTESIAN_POINT ( 'NONE',  ( 0.9790724872846782167, -17.67747698414031277, 37.99792122546497097 ) ) ;
#55113=B_SPLINE_CURVE_WITH_KNOTS ( 'NONE', 3,
 ( #50886, #41210, #60271, #17087, #31164, #12090 ),
 .UNSPECIFIED., .F., .F.,
 ( 4, 2, 4 ),
 ( 3.476216610979977084E-18, 0.0002291459268755724032, 0.0004582918537511413370 ),
 .UNSPECIFIED. ) ;
#55115=ORIENTED_EDGE ( 'NONE', *, *, #35598, .F. ) ;
#55119=EDGE_CURVE ( 'NONE', #10982, #26672, #26390, .T. ) ;
#55132=CARTESIAN_POINT ( 'NONE',  ( 1.231276596079887264, -39.31472542100218703, 14.54747868495677743 ) ) ;
#55139=CARTESIAN_POINT ( 'NONE',  ( 0.8560838555295223751, -6.899551485032601406, 46.39794201672221163 ) ) ;
#55142=B_SPLINE_CURVE_WITH_KNOTS ( 'NONE', 3,
 ( #20806, #10796, #39015, #1065, #57440, #6352 ),
 .UNSPECIFIED., .F., .F.,
 ( 4, 2, 4 ),
 ( 0.000000000000000000, 0.0002291459268755708853, 0.0004582918537511417706 ),
 .UNSPECIFIED. ) ;
#55147=ADVANCED_FACE ( 'NONE', ( #43361 ), #3484, .F. ) ;
#55149=DIRECTION ( 'NONE',  ( -1.000000000000000000, -0.000000000000000000, -0.000000000000000000 ) ) ;
#55158=( BOUNDED_SURFACE ( )  B_SPLINE_SURFACE ( 3, 1, ( 
 ( #6279, #25414 ),
 ( #354, #38619 ),
 ( #44561, #10096 ),
 ( #57672, #1592 ) ),
 .UNSPECIFIED., .F., .F., .F. ) 
 B_SPLINE_SURFACE_WITH_KNOTS ( ( 4, 4 ),
 ( 2, 2 ),
 ( 0.000000000000000000, 1.000000000000000000 ),
 ( 0.000000000000000000, 1.000000000000000000 ),
 .UNSPECIFIED. ) 
 GEOMETRIC_REPRESENTATION_ITEM ( )  RATIONAL_B_SPLINE_SURFACE ( (
 ( 1.000000000000000000, 1.000000000000000000),
 ( 0.9729067724841187204, 0.9999501103223794596),
 ( 0.9729067724841187204, 0.9999501103223794596),
 ( 1.000000000000000000, 1.000000000000000000) ) ) 
 REPRESENTATION_ITEM ( '' )  SURFACE ( )  );
#55159=EDGE_LOOP ( 'NONE', ( #21153, #25745, #37345, #33683 ) ) ;
#55162=VERTEX_POINT ( 'NONE', #9205 ) ;
#55166=VERTEX_POINT ( 'NONE', #28926 ) ;
#55167=CARTESIAN_POINT ( 'NONE',  ( 3.782542959838389951, -16.11620932553572771, -38.82661008087216459 ) ) ;
#55168=EDGE_CURVE ( 'NONE', #20677, #51214, #30818, .T. ) ;
#55191=CARTESIAN_POINT ( 'NONE',  ( 0.5782707292762423457, 46.89575936232450459, -0.7239527184646502578 ) ) ;
#55193=ORIENTED_EDGE ( 'NONE', *, *, #37410, .T. ) ;
#55199=VECTOR ( 'NONE', #44025, 1000.000000000000114 ) ;
#55202=CARTESIAN_POINT ( 'NONE',  ( 1.231276596079881047, -2.246340108600348717, 41.85965512441018888 ) ) ;
#55205=FACE_OUTER_BOUND ( 'NONE', #42497, .T. ) ;
#55206=CARTESIAN_POINT ( 'NONE',  ( 3.376099380956838925, -13.39845304004337123, 0.4357060543757622639 ) ) ;
#55217=CARTESIAN_POINT ( 'NONE',  ( 0.7764139734771229318, 23.31927515082854541, -40.69707455514238603 ) ) ;
#55225=ORIENTED_EDGE ( 'NONE', *, *, #34032, .T. ) ;
#55229=ORIENTED_EDGE ( 'NONE', *, *, #44717, .T. ) ;
#55230=CARTESIAN_POINT ( 'NONE',  ( 1.157643937452369487, 19.41637196408613875, -37.14844242154714493 ) ) ;
#55232=CARTESIAN_POINT ( 'NONE',  ( 0.5797568665920714848, 17.44034444229498604, 43.53228335771030544 ) ) ;
#55241=ORIENTED_EDGE ( 'NONE', *, *, #4969, .T. ) ;
#55242=CARTESIAN_POINT ( 'NONE',  ( 0.8560838555295158248, 9.983184696770717181, 45.83349056521764453 ) ) ;
#55257=ORIENTED_EDGE ( 'NONE', *, *, #35034, .F. ) ;
#55262=ORIENTED_EDGE ( 'NONE', *, *, #58313, .T. ) ;
#55264=CARTESIAN_POINT ( 'NONE',  ( 4.956445790443988031, 0.000000000000000000, 0.000000000000000000 ) ) ;
#55267=B_SPLINE_CURVE_WITH_KNOTS ( 'NONE', 3,
 ( #10358, #58556, #48558, #5924, #30679, #1545, #21296, #40132, #44209, #10983, #45128, #49797, #6855, #30368, #20682, #6228, #53550, #40426, #58872 ),
 .UNSPECIFIED., .F., .F.,
 ( 4, 3, 3, 3, 3, 3, 4 ),
 ( 1.250973872328959318E-17, 0.0002732106629380557099, 0.0004098138914053751068, 0.0005464171197651450634, 0.0006830203481512486102, 0.0008196235766963579951, 0.001011968216111138342 ),
 .UNSPECIFIED. ) ;
#55277=CARTESIAN_POINT ( 'NONE',  ( 4.962356264823603702, 37.36413190407388640, -19.36897635181878030 ) ) ;
#55280=B_SPLINE_CURVE_WITH_KNOTS ( 'NONE', 3,
 ( #18046, #22733, #41865, #60935, #57144, #37163, #33692, #32446, #52768, #9872, #18660, #9550, #14277, #28660, #46552, #18357 ),
 .UNSPECIFIED., .F., .F.,
 ( 4, 3, 3, 3, 3, 4 ),
 ( 9.813676791237319219E-18, 0.0002732102107931875601, 0.0004098135523333767635, 0.0005464168938824943717, 0.0008195847345945264217, 0.001092771384553102012 ),
 .UNSPECIFIED. ) ;
#55282=CARTESIAN_POINT ( 'NONE',  ( 0.9783242366443549720, -31.26083830869256275, 27.91226394336910488 ) ) ;
#55285=CARTESIAN_POINT ( 'NONE',  ( 4.962356264823608143, 0.000000000000000000, 0.000000000000000000 ) ) ;
#55293=CARTESIAN_POINT ( 'NONE',  ( 3.238018933889920792, -12.07617426668434568, 5.794265048159582321 ) ) ;
#55297=EDGE_LOOP ( 'NONE', ( #56465, #19472, #22751, #42420 ) ) ;
#55304=AXIS2_PLACEMENT_3D ( 'NONE', #22347, #50536, #26738 ) ;
#55307=CARTESIAN_POINT ( 'NONE',  ( 2.788021980277358036, 6.069845295522647588E-12, -46.99417130740492610 ) ) ;
#55312=ORIENTED_EDGE ( 'NONE', *, *, #54635, .T. ) ;
#55316=B_SPLINE_CURVE_WITH_KNOTS ( 'NONE', 3,
 ( #26878, #36602, #8074, #22793 ),
 .UNSPECIFIED., .F., .F.,
 ( 4, 4 ),
 ( 1.084202172485504434E-19, 0.004446298630425056346 ),
 .UNSPECIFIED. ) ;
#55321=CARTESIAN_POINT ( 'NONE',  ( 2.618530812446115519, 21.34567399517413477, -41.88184560033076309 ) ) ;
#55322=CARTESIAN_POINT ( 'NONE',  ( 2.528190830796658517, 5.404281357458566859, -41.62989165446426654 ) ) ;
#55324=ORIENTED_EDGE ( 'NONE', *, *, #14589, .F. ) ;
#55330=ORIENTED_EDGE ( 'NONE', *, *, #47183, .F. ) ;
#55331=DIRECTION ( 'NONE',  ( -1.000000000000000000, -0.000000000000000000, -0.000000000000000000 ) ) ;
#55344=ORIENTED_EDGE ( 'NONE', *, *, #41820, .F. ) ;
#55356=CARTESIAN_POINT ( 'NONE',  ( 0.9787464366903561030, -27.19233698969872037, 31.88903889942633896 ) ) ;
#55362=DIRECTION ( 'NONE',  ( -0.07500201931887527651, -0.9798016564749993940, -0.1853737065145389662 ) ) ;
#55373=CARTESIAN_POINT ( 'NONE',  ( 4.956445790444004018, -43.56224489968113289, 17.88487823385560205 ) ) ;
#55386=CARTESIAN_POINT ( 'NONE',  ( 1.157644175074336479, -0.5751541904189192422, -41.91266482981518493 ) ) ;
#55389=B_SPLINE_CURVE_WITH_KNOTS ( 'NONE', 3,
 ( #9793, #57999, #53305, #18908, #5674, #57077 ),
 .UNSPECIFIED., .F., .F.,
 ( 4, 2, 4 ),
 ( 0.000000000000000000, 0.0002291459268755698824, 0.0004582918537511397649 ),
 .UNSPECIFIED. ) ;
#55390=FACE_OUTER_BOUND ( 'NONE', #39952, .T. ) ;
#55396=CARTESIAN_POINT ( 'NONE',  ( 5.910764540655177868, 3.329973395294289151, 19.83462920388972961 ) ) ;
#55405=CARTESIAN_POINT ( 'NONE',  ( 0.9754292580325132356, 28.71299566771950751, 30.52689546432007717 ) ) ;
#55408=CARTESIAN_POINT ( 'NONE',  ( 4.291220156522060236, 38.26855966511092078, 27.47555892904714625 ) ) ;
#55417=CARTESIAN_POINT ( 'NONE',  ( 0.5806925824938494740, -1.020860314013172454, 46.88475452172951918 ) ) ;
#55424=CARTESIAN_POINT ( 'NONE',  ( 1.092182651088184908, 40.21120180690577683, -11.82456906980473654 ) ) ;
#55425=ORIENTED_EDGE ( 'NONE', *, *, #61318, .F. ) ;
#55427=CARTESIAN_POINT ( 'NONE',  ( 3.376099380956838925, 2.658192826266143616, 13.13934528545674318 ) ) ;
#55430=ORIENTED_EDGE ( 'NONE', *, *, #15293, .T. ) ;
#55432=ORIENTED_EDGE ( 'NONE', *, *, #44960, .F. ) ;
#55439=EDGE_CURVE ( 'NONE', #29740, #40143, #52446, .T. ) ;
#55441=CARTESIAN_POINT ( 'NONE',  ( 0.9754292589017217185, 10.28092790612040908, 40.62794590284416074 ) ) ;
#55442=CARTESIAN_POINT ( 'NONE',  ( 3.782542959838393504, 16.70562020489267141, -38.57667827802765714 ) ) ;
#55443=ADVANCED_FACE ( 'NONE', ( #57038 ), #61117, .F. ) ;
#55447=CARTESIAN_POINT ( 'NONE',  ( 0.5806925824938511393, 32.99217760300656010, 33.32774488853447536 ) ) ;
#55461=CARTESIAN_POINT ( 'NONE',  ( 0.8560838555295223751, -14.76796170096679894, -44.52280473286144513 ) ) ;
#55463=ORIENTED_EDGE ( 'NONE', *, *, #17116, .F. ) ;
#55468=CARTESIAN_POINT ( 'NONE',  ( 4.962356264823596597, 1.841560470688234474, 42.04574000888969465 ) ) ;
#55470=CARTESIAN_POINT ( 'NONE',  ( 0.6845945791218034371, 5.556290360845241416, -46.57825842751017120 ) ) ;
#55472=ORIENTED_EDGE ( 'NONE', *, *, #18044, .T. ) ;
#55475=VERTEX_POINT ( 'NONE', #19473 ) ;
#55482=CARTESIAN_POINT ( 'NONE',  ( 5.917102823773431552, -19.39506196288392559, 5.321775033542383682 ) ) ;
#55485=CARTESIAN_POINT ( 'NONE',  ( 0.5832655196449139101, -30.45084774278391393, 35.66484339961580474 ) ) ;
#55488=ORIENTED_EDGE ( 'NONE', *, *, #44796, .T. ) ;
#55490=EDGE_CURVE ( 'NONE', #31937, #10199, #8396, .T. ) ;
#55492=VECTOR ( 'NONE', #26497, 1000.000000000000114 ) ;
#55502=ORIENTED_EDGE ( 'NONE', *, *, #9381, .T. ) ;
#55503=FACE_OUTER_BOUND ( 'NONE', #23747, .T. ) ;
#55504=EDGE_CURVE ( 'NONE', #10852, #40429, #33070, .T. ) ;
#55505=CARTESIAN_POINT ( 'NONE',  ( 2.282816707992310956, -20.95674216433703663, -42.03940918073735844 ) ) ;
#55507=CARTESIAN_POINT ( 'NONE',  ( 4.962356264823608143, 41.96072444189411499, 3.245489512196318316 ) ) ;
#55509=( BOUNDED_SURFACE ( )  B_SPLINE_SURFACE ( 3, 1, ( 
 ( #41983, #18459 ),
 ( #4952, #24081 ),
 ( #56963, #37906 ),
 ( #9993, #33187 ) ),
 .UNSPECIFIED., .F., .F., .F. ) 
 B_SPLINE_SURFACE_WITH_KNOTS ( ( 4, 4 ),
 ( 2, 2 ),
 ( 0.000000000000000000, 1.000000000000000000 ),
 ( 0.000000000000000000, 1.000000000000000000 ),
 .UNSPECIFIED. ) 
 GEOMETRIC_REPRESENTATION_ITEM ( )  RATIONAL_B_SPLINE_SURFACE ( (
 ( 1.000000000000000000, 1.000000000000000000),
 ( 0.7282232189291694135, 0.9929344683865672927),
 ( 0.7282232189291694135, 0.9929344683865672927),
 ( 1.000000000000000000, 1.000000000000000000) ) ) 
 REPRESENTATION_ITEM ( '' )  SURFACE ( )  );
#55512=CARTESIAN_POINT ( 'NONE',  ( 4.962356264823608143, 22.27740539909265394, 35.70648129607319277 ) ) ;
#55515=CARTESIAN_POINT ( 'NONE',  ( 4.956445790443988031, 0.000000000000000000, 0.000000000000000000 ) ) ;
#55516=CARTESIAN_POINT ( 'NONE',  ( 0.9788927965476027504, 32.97753259754014010, 25.86153430115767193 ) ) ;
#55518=CARTESIAN_POINT ( 'NONE',  ( 0.5806925824938499181, 32.99217760300705748, -33.32774488853398509 ) ) ;
#55527=VERTEX_POINT ( 'NONE', #11298 ) ;
#55528=VERTEX_POINT ( 'NONE', #24465 ) ;
#55537=ORIENTED_EDGE ( 'NONE', *, *, #9809, .T. ) ;
#55553=CARTESIAN_POINT ( 'NONE',  ( 0.5782707292762442330, -35.26595510591691607, 30.92003823049173405 ) ) ;
#55555=LINE ( 'NONE', #12685, #1620 ) ;
#55556=CARTESIAN_POINT ( 'NONE',  ( 4.962356264823609031, -20.60668162140307658, 36.69605251817252878 ) ) ;
#55560=CARTESIAN_POINT ( 'NONE',  ( 0.5824935313925969638, -13.54582896752205201, 44.89709004642145374 ) ) ;
#55578=CARTESIAN_POINT ( 'NONE',  ( 0.5797568665920721509, 40.66629937448812626, 23.35545768736671945 ) ) ;
#55579=DIRECTION ( 'NONE',  ( -1.000000000000000000, 0.000000000000000000, 0.000000000000000000 ) ) ;
#55580=CARTESIAN_POINT ( 'NONE',  ( 2.282803330402964015, -41.31566501690780768, -22.34978146800645149 ) ) ;
#55581=CARTESIAN_POINT ( 'NONE',  ( 4.291220156522060236, 42.48586100259165477, -20.35535831603462853 ) ) ;
#55582=FACE_OUTER_BOUND ( 'NONE', #31745, .T. ) ;
#55590=CARTESIAN_POINT ( 'NONE',  ( 5.917102823773431552, -11.92306321980351846, 16.19661327278979357 ) ) ;
#55594=CARTESIAN_POINT ( 'NONE',  ( 0.9783242366443549720, -7.234864208425438648, 41.27942865510820525 ) ) ;
#55597=ORIENTED_EDGE ( 'NONE', *, *, #4139, .F. ) ;
#55600=B_SPLINE_CURVE_WITH_KNOTS ( 'NONE', 3,
 ( #11512, #55322, #20601, #21520 ),
 .UNSPECIFIED., .F., .F.,
 ( 4, 4 ),
 ( 4.336808689942017736E-19, 0.004041751736740997747 ),
 .UNSPECIFIED. ) ;
#55603=CARTESIAN_POINT ( 'NONE',  ( 5.895596859100789899, -9.662743138698489886, 17.63971593444811603 ) ) ;
#55605=EDGE_LOOP ( 'NONE', ( #30893, #11975, #5095, #55915 ) ) ;
#55610=ORIENTED_EDGE ( 'NONE', *, *, #34815, .T. ) ;
#55611=ORIENTED_EDGE ( 'NONE', *, *, #47815, .F. ) ;
#55620=B_SPLINE_CURVE_WITH_KNOTS ( 'NONE', 3,
 ( #45931, #2976, #22097, #56214, #17397, #13326 ),
 .UNSPECIFIED., .F., .F.,
 ( 4, 2, 4 ),
 ( 0.000000000000000000, 0.0002291459268755710480, 0.0004582918537511420959 ),
 .UNSPECIFIED. ) ;
#55626=CARTESIAN_POINT ( 'NONE',  ( 2.528100132419515589, -31.93277260506748760, -27.24980389626917443 ) ) ;
#55630=ORIENTED_EDGE ( 'NONE', *, *, #11624, .T. ) ;
#55633=LINE ( 'NONE', #17757, #40045 ) ;
#55635=DIRECTION ( 'NONE',  ( 0.000000000000000000, 0.000000000000000000, 1.000000000000000000 ) ) ;
#55642=CARTESIAN_POINT ( 'NONE',  ( 0.9780303403264775097, 25.11936797697908119, 33.54634057288815541 ) ) ;
#55650=CARTESIAN_POINT ( 'NONE',  ( 0.5848930533535030563, 43.10374212188040133, 18.47540249840287530 ) ) ;
#55652=EDGE_CURVE ( 'NONE', #17422, #38487, #7534, .T. ) ;
#55654=DIRECTION ( 'NONE',  ( 0.07906939808003035641, 0.1737655548591788279, -0.9816076416938406268 ) ) ;
#55655=CARTESIAN_POINT ( 'NONE',  ( 5.917102823773431552, 10.81462311420869327, 16.95681706421830270 ) ) ;
#55658=B_SPLINE_CURVE_WITH_KNOTS ( 'NONE', 3,
 ( #14584, #38398, #29273, #24270 ),
 .UNSPECIFIED., .F., .F.,
 ( 4, 4 ),
 ( 0.000000000000000000, 0.002290414566844504660 ),
 .UNSPECIFIED. ) ;
#55661=CIRCLE ( 'NONE', #13666, 42.08604991992415023 ) ;
#55663=CARTESIAN_POINT ( 'NONE',  ( 0.5806925824938499181, 40.06810415365472977, 24.36738377166168235 ) ) ;
#55669=CARTESIAN_POINT ( 'NONE',  ( 2.618530812446111078, -41.30116959783728703, -22.44861196263326164 ) ) ;
#55674=CARTESIAN_POINT ( 'NONE',  ( 1.091591847532196846, 10.47380871615908582, -40.58396631593750215 ) ) ;
#55676=CARTESIAN_POINT ( 'NONE',  ( 0.5804410086790514622, -41.60900809504508402, -21.63816760268459660 ) ) ;
#55680=CARTESIAN_POINT ( 'NONE',  ( 0.5830081025819934260, 46.51316544950417864, 5.979755367010718636 ) ) ;
#55682=CARTESIAN_POINT ( 'NONE',  ( 4.956445790443991584, 34.56007374686787159, 31.98654955994301829 ) ) ;
#55685=FACE_OUTER_BOUND ( 'NONE', #46477, .T. ) ;
#55689=EDGE_CURVE ( 'NONE', #51034, #6891, #54811, .T. ) ;
#55696=B_SPLINE_CURVE_WITH_KNOTS ( 'NONE', 3,
 ( #12673, #17665, #32083, #7308 ),
 .UNSPECIFIED., .F., .F.,
 ( 4, 4 ),
 ( 7.589415207398531038E-19, 0.004446298630425064152 ),
 .UNSPECIFIED. ) ;
#55698=CARTESIAN_POINT ( 'NONE',  ( 0.7056759521545038494, 37.32480390860856545, -28.40084228153992285 ) ) ;
#55707=CARTESIAN_POINT ( 'NONE',  ( 0.9762797500689124330, 41.59901070109202692, -5.084003725031680077 ) ) ;
#55714=EDGE_CURVE ( 'NONE', #36411, #4970, #24060, .T. ) ;
#55731=CARTESIAN_POINT ( 'NONE',  ( 0.5830081025819926488, -44.21080646010828019, 15.64086399560760832 ) ) ;
#55732=VERTEX_POINT ( 'NONE', #9364 ) ;
#55747=B_SPLINE_CURVE_WITH_KNOTS ( 'NONE', 3,
 ( #37797, #18666, #36861, #12743, #37168, #47175, #41871, #46558, #56546, #27130, #61547, #8946, #31837, #28057, #55930, #3298, #60617, #4222, #41556 ),
 .UNSPECIFIED., .F., .F.,
 ( 4, 3, 3, 3, 3, 3, 4 ),
 ( 1.250973872328959318E-17, 0.0002732106629380557099, 0.0004098138914053684389, 0.0005464171197651389918, 0.0006830203481512434061, 0.0008196235766963545256, 0.001011968216111132270 ),
 .UNSPECIFIED. ) ;
#55750=CARTESIAN_POINT ( 'NONE',  ( 5.896782393890504181, 8.471952691971306848, -18.24149403045190354 ) ) ;
#55754=FACE_OUTER_BOUND ( 'NONE', #25457, .T. ) ;
#55756=DIRECTION ( 'NONE',  ( 0.07500201931887538753, -0.6023261099427925647, 0.7947187894968092969 ) ) ;
#55758=CARTESIAN_POINT ( 'NONE',  ( 0.5830082357119570347, 22.77652504489005025, -40.99343778969789298 ) ) ;
#55759=CARTESIAN_POINT ( 'NONE',  ( 4.958415959904820092, 44.40884735405898454, 9.542443633919221568 ) ) ;
#55762=EDGE_CURVE ( 'NONE', #20260, #38326, #57563, .T. ) ;
#55764=CARTESIAN_POINT ( 'NONE',  ( 0.9772918015221165877, 20.50340863875699426, 36.55060998044800158 ) ) ;
#55765=FACE_OUTER_BOUND ( 'NONE', #45570, .T. ) ;
#55770=CARTESIAN_POINT ( 'NONE',  ( 0.9785694773339246311, -41.79961263450124420, -3.021223149705917432 ) ) ;
#55778=( BOUNDED_SURFACE ( )  B_SPLINE_SURFACE ( 3, 1, ( 
 ( #23499, #603 ),
 ( #29127, #23817 ),
 ( #48537, #13946 ),
 ( #5595, #285 ) ),
 .UNSPECIFIED., .F., .F., .F. ) 
 B_SPLINE_SURFACE_WITH_KNOTS ( ( 4, 4 ),
 ( 2, 2 ),
 ( 0.000000000000000000, 1.000000000000000000 ),
 ( 0.000000000000000000, 1.000000000000000000 ),
 .UNSPECIFIED. ) 
 GEOMETRIC_REPRESENTATION_ITEM ( )  RATIONAL_B_SPLINE_SURFACE ( (
 ( 1.000000000000000000, 1.000000000000000000),
 ( 0.7282232189291694135, 0.9929344683865672927),
 ( 0.7282232189291694135, 0.9929344683865672927),
 ( 1.000000000000000000, 1.000000000000000000) ) ) 
 REPRESENTATION_ITEM ( '' )  SURFACE ( )  );
#55813=CARTESIAN_POINT ( 'NONE',  ( 0.5824936645240084143, -1.202945444167589750, -46.88060474544526102 ) ) ;
#55814=VECTOR ( 'NONE', #14941, 1000.000000000000000 ) ;
#55817=CARTESIAN_POINT ( 'NONE',  ( 4.958415959904820092, 34.02476434053166088, 30.09184881980370108 ) ) ;
#55818=CARTESIAN_POINT ( 'NONE',  ( 0.9791128995231611620, -41.81475145202444565, 2.804281592776174836 ) ) ;
#55823=ADVANCED_FACE ( 'NONE', ( #58814 ), #44341, .F. ) ;
#55824=CARTESIAN_POINT ( 'NONE',  ( 1.000110580585051423, 41.90446991591855408, 0.6579390836365230921 ) ) ;
#55830=CARTESIAN_POINT ( 'NONE',  ( 0.9780106845699465534, 32.69455122756870935, 26.21826780096896314 ) ) ;
#55832=B_SPLINE_CURVE_WITH_KNOTS ( 'NONE', 3,
 ( #43910, #16610, #25689, #48878, #39508, #1868 ),
 .UNSPECIFIED., .F., .F.,
 ( 4, 2, 4 ),
 ( 1.159750240187440271E-16, 0.0002448718616795903858, 0.0004897437233590648704 ),
 .UNSPECIFIED. ) ;
#55834=CARTESIAN_POINT ( 'NONE',  ( 5.894904586330512508, -19.93329511855189295, 2.682006297225661751 ) ) ;
#55836=CARTESIAN_POINT ( 'NONE',  ( 5.895596859100789899, -7.225383168025214076, 18.77024297359267990 ) ) ;
#55838=CARTESIAN_POINT ( 'NONE',  ( 0.8560838555295158248, -13.02223058219810881, -45.06433561859972059 ) ) ;
#55841=VERTEX_POINT ( 'NONE', #25317 ) ;
#55856=CARTESIAN_POINT ( 'NONE',  ( 1.000110580585049647, -37.69726589122901572, 18.31211694747177177 ) ) ;
#55857=EDGE_CURVE ( 'NONE', #18232, #2143, #40504, .T. ) ;
#55862=ORIENTED_EDGE ( 'NONE', *, *, #44810, .T. ) ;
#55863=CARTESIAN_POINT ( 'NONE',  ( 0.9762797500689124330, 14.58899758184639595, 39.28722355604407568 ) ) ;
#55866=B_SPLINE_CURVE_WITH_KNOTS ( 'NONE', 3,
 ( #60693, #847, #6138, #49085, #53454, #52537 ),
 .UNSPECIFIED., .F., .F.,
 ( 4, 2, 4 ),
 ( 9.898949898072313973E-18, 0.0002448709889506559098, 0.0004897419779013018450 ),
 .UNSPECIFIED. ) ;
#55876=CARTESIAN_POINT ( 'NONE',  ( 0.5806925824938499181, -20.23436166722466467, 42.30594485723624132 ) ) ;
#55878=CARTESIAN_POINT ( 'NONE',  ( 0.8560838555295223751, -20.57050347530454104, -42.15717282805163535 ) ) ;
#55879=ORIENTED_EDGE ( 'NONE', *, *, #35007, .T. ) ;
#55881=CARTESIAN_POINT ( 'NONE',  ( 1.000110580585054532, 32.47884455641464285, 26.48664076571725445 ) ) ;
#55882=( BOUNDED_SURFACE ( )  B_SPLINE_SURFACE ( 3, 1, ( 
 ( #38150, #57196 ),
 ( #52830, #14955 ),
 ( #14330, #14640 ),
 ( #33437, #52514 ) ),
 .UNSPECIFIED., .F., .F., .F. ) 
 B_SPLINE_SURFACE_WITH_KNOTS ( ( 4, 4 ),
 ( 2, 2 ),
 ( 0.000000000000000000, 1.000000000000000000 ),
 ( 0.000000000000000000, 1.000000000000000000 ),
 .UNSPECIFIED. ) 
 GEOMETRIC_REPRESENTATION_ITEM ( )  RATIONAL_B_SPLINE_SURFACE ( (
 ( 1.000000000000000000, 1.000000000000000000),
 ( 0.7282232189291693025, 0.9929344683865674037),
 ( 0.7282232189291693025, 0.9929344683865674037),
 ( 1.000000000000000000, 1.000000000000000000) ) ) 
 REPRESENTATION_ITEM ( '' )  SURFACE ( )  );
#55883=CARTESIAN_POINT ( 'NONE',  ( 5.895596859100789899, -18.51832497669317945, -7.848555489392246010 ) ) ;
#55893=CARTESIAN_POINT ( 'NONE',  ( 1.231276596079887264, -13.22565419921979313, -39.77887431816952102 ) ) ;
#55894=DIRECTION ( 'NONE',  ( 0.07906939808003037029, 0.5295738273858020539, 0.8445706552060724404 ) ) ;
#55898=CARTESIAN_POINT ( 'NONE',  ( 1.231276596079887264, -23.26513148155214594, -34.87134107206314582 ) ) ;
#55901=CARTESIAN_POINT ( 'NONE',  ( 0.5806925824938499181, -45.84420715090598009, -9.875780123533834498 ) ) ;
#55902=CARTESIAN_POINT ( 'NONE',  ( 5.917102823773431552, -18.51940219202235838, 7.843561722958504845 ) ) ;
#55914=CARTESIAN_POINT ( 'NONE',  ( 4.962356264823602814, 42.01891079680549979, 2.376285612557970772 ) ) ;
#55915=ORIENTED_EDGE ( 'NONE', *, *, #28397, .F. ) ;
#55917=AXIS2_PLACEMENT_3D ( 'NONE', #1077, #15819, #2848 ) ;
#55919=DIRECTION ( 'NONE',  ( 0.000000000000000000, 0.000000000000000000, 1.000000000000000000 ) ) ;
#55924=CARTESIAN_POINT ( 'NONE',  ( 0.5824936645240094135, -46.02748468922020919, 8.983809449443411310 ) ) ;
#55930=CARTESIAN_POINT ( 'NONE',  ( 0.9783242366443551941, 25.07469261982136288, -33.57967063906372829 ) ) ;
#55944=CARTESIAN_POINT ( 'NONE',  ( 4.956445790443994248, 24.88142650099509723, 39.98065363916922621 ) ) ;
#55946=CARTESIAN_POINT ( 'NONE',  ( 0.9780303403264766215, 3.872540855671210647, -41.72940259237177685 ) ) ;
#55949=ORIENTED_EDGE ( 'NONE', *, *, #19763, .F. ) ;
#55954=CARTESIAN_POINT ( 'NONE',  ( 0.8560838555295158248, 17.70877843982841782, -43.43698884880027578 ) ) ;
#55961=VECTOR ( 'NONE', #54304, 1000.000000000000000 ) ;
#55966=CARTESIAN_POINT ( 'NONE',  ( 0.5817217712918330008, -42.05893918154934141, 20.74320584989474980 ) ) ;
#55969=CARTESIAN_POINT ( 'NONE',  ( 1.231276596079881935, -39.31472542100197387, -14.54747868495734053 ) ) ;
#55970=CARTESIAN_POINT ( 'NONE',  ( 3.376099380956838925, -8.298464850405457227, -10.52824129466323910 ) ) ;
#55971=FACE_OUTER_BOUND ( 'NONE', #28898, .T. ) ;
#55972=EDGE_CURVE ( 'NONE', #14312, #23007, #18078, .T. ) ;
#55980=CARTESIAN_POINT ( 'NONE',  ( 0.9762797500689124330, -27.44172181261435739, 31.67454323498272117 ) ) ;
#55981=DIRECTION ( 'NONE',  ( -0.07500201931887526263, 0.9127009170568879393, -0.4016861126571428797 ) ) ;
#55992=CARTESIAN_POINT ( 'NONE',  ( 1.091591847532195958, 8.955707924048176949, 40.94574808859866977 ) ) ;
#55994=CARTESIAN_POINT ( 'NONE',  ( 5.838029081930957709, -10.93035914537738584, 45.95206531926487514 ) ) ;
#55997=CARTESIAN_POINT ( 'NONE',  ( 3.661921753702011451, -26.87747736193279025, -38.60352748768983844 ) ) ;
#55999=( BOUNDED_SURFACE ( )  B_SPLINE_SURFACE ( 3, 1, ( 
 ( #12183, #8367 ),
 ( #31268, #26250 ),
 ( #17180, #2743 ),
 ( #46310, #50367 ) ),
 .UNSPECIFIED., .F., .F., .F. ) 
 B_SPLINE_SURFACE_WITH_KNOTS ( ( 4, 4 ),
 ( 2, 2 ),
 ( 0.000000000000000000, 1.000000000000000000 ),
 ( 0.000000000000000000, 1.000000000000000000 ),
 .UNSPECIFIED. ) 
 GEOMETRIC_REPRESENTATION_ITEM ( )  RATIONAL_B_SPLINE_SURFACE ( (
 ( 1.000000000000000000, 1.000000000000000000),
 ( 0.7282232189291693025, 0.9929344683865674037),
 ( 0.7282232189291693025, 0.9929344683865674037),
 ( 1.000000000000000000, 1.000000000000000000) ) ) 
 REPRESENTATION_ITEM ( '' )  SURFACE ( )  );
#56008=ADVANCED_FACE ( 'NONE', ( #50353 ), #11196, .F. ) ;
#56011=CARTESIAN_POINT ( 'NONE',  ( 4.291220156522059348, -37.58001468972560843, -28.41005971879863168 ) ) ;
#56014=ORIENTED_EDGE ( 'NONE', *, *, #9346, .F. ) ;
#56025=ORIENTED_EDGE ( 'NONE', *, *, #16371, .T. ) ;
#56030=EDGE_LOOP ( 'NONE', ( #5175, #12525, #18039, #45959 ) ) ;
#56032=CARTESIAN_POINT ( 'NONE',  ( 1.000110580585049869, -7.618717594574525798, 41.21131671017104026 ) ) ;
#56038=CARTESIAN_POINT ( 'NONE',  ( 0.9762797500689124330, -18.09842611962814019, 37.79909730639167265 ) ) ;
#56039=CARTESIAN_POINT ( 'NONE',  ( 0.5848930533535030563, -46.80349522319539091, 2.950579143131832005 ) ) ;
#56041=VERTEX_POINT ( 'NONE', #5417 ) ;
#56051=CARTESIAN_POINT ( 'NONE',  ( 1.000433927950262758, -17.04159546744087450, 38.28841471746964942 ) ) ;
#56059=ORIENTED_EDGE ( 'NONE', *, *, #2958, .F. ) ;
#56060=LINE ( 'NONE', #46086, #7689 ) ;
#56062=EDGE_CURVE ( 'NONE', #15046, #51445, #59094, .T. ) ;
#56068=CARTESIAN_POINT ( 'NONE',  ( 0.7056313189692711152, 37.32477945609016956, 28.40087115762097625 ) ) ;
#56073=ORIENTED_EDGE ( 'NONE', *, *, #19206, .F. ) ;
#56076=CARTESIAN_POINT ( 'NONE',  ( 0.9780106845699474416, 19.86490431973512472, 36.90144743534066407 ) ) ;
#56088=DIRECTION ( 'NONE',  ( -1.000000000000000000, -0.000000000000000000, -0.000000000000000000 ) ) ;
#56097=VERTEX_POINT ( 'NONE', #61508 ) ;
#56100=CARTESIAN_POINT ( 'NONE',  ( 5.896278296736517710, 8.461230214157993146, 18.24649453668850541 ) ) ;
#56106=CARTESIAN_POINT ( 'NONE',  ( 0.5835871038041877679, -44.25621114391295663, -15.51200271038183764 ) ) ;
#56108=EDGE_LOOP ( 'NONE', ( #37591, #41133, #39255, #1637 ) ) ;
#56109=CARTESIAN_POINT ( 'NONE',  ( 0.7764146366350271888, 43.52296033649982121, 17.48692074713635591 ) ) ;
#56113=CARTESIAN_POINT ( 'NONE',  ( 4.962356264823608143, 0.9708976703217077064, 42.07484944210865052 ) ) ;
#56120=ORIENTED_EDGE ( 'NONE', *, *, #28645, .F. ) ;
#56122=CARTESIAN_POINT ( 'NONE',  ( 0.9762797500689124330, -41.84568905980458453, 2.294143041716202092 ) ) ;
#56126=B_SPLINE_CURVE_WITH_KNOTS ( 'NONE', 3,
 ( #17165, #8985, #52818, #29319, #493, #28095 ),
 .UNSPECIFIED., .F., .F.,
 ( 4, 2, 4 ),
 ( 6.106282077343214115E-18, 0.0002291472222819941282, 0.0004582944445639821848 ),
 .UNSPECIFIED. ) ;
#56134=CARTESIAN_POINT ( 'NONE',  ( 0.9780106845699487739, -12.71570332633824840, 39.93297053027720978 ) ) ;
#56141=AXIS2_PLACEMENT_3D ( 'NONE', #42022, #3752, #4357 ) ;
#56144=ADVANCED_FACE ( 'NONE', ( #102 ), #24729, .F. ) ;
#56156=VERTEX_POINT ( 'NONE', #33969 ) ;
#56159=CARTESIAN_POINT ( 'NONE',  ( 1.091591847532198623, -39.33176300527454572, -14.48348748930166252 ) ) ;
#56164=ORIENTED_EDGE ( 'NONE', *, *, #20282, .F. ) ;
#56167=CARTESIAN_POINT ( 'NONE',  ( 1.092182651088184242, -2.180685162625981555, -41.85696831668280282 ) ) ;
#56172=CARTESIAN_POINT ( 'NONE',  ( 2.528100132419517365, 2.996127168110702677, -41.87215065678599757 ) ) ;
#56173=B_SPLINE_CURVE_WITH_KNOTS ( 'NONE', 3,
 ( #25818, #7303, #49311, #40263, #59013, #11121, #35549, #40567, #54609, #41180, #59629, #30203, #6366, #59945, #54926, #12059 ),
 .UNSPECIFIED., .F., .F.,
 ( 4, 3, 3, 3, 3, 4 ),
 ( 1.551621725782133898E-17, 0.0002732102107931876685, 0.0004098135523333712340, 0.0005464168938824954559, 0.0008195847345945416005, 0.001092771384553108084 ),
 .UNSPECIFIED. ) ;
#56182=CARTESIAN_POINT ( 'NONE',  ( 1.231276596079887264, 24.17959027891153667, -34.24360064248551083 ) ) ;
#56184=CARTESIAN_POINT ( 'NONE',  ( 0.5804410086790514622, 5.237717535875737518, -46.60564522533483967 ) ) ;
#56185=DIRECTION ( 'NONE',  ( -1.000000000000000000, -0.000000000000000000, -0.000000000000000000 ) ) ;
#56193=CARTESIAN_POINT ( 'NONE',  ( 0.6845945791218023269, -29.61886432666044300, 36.37484565895540811 ) ) ;
#56212=EDGE_CURVE ( 'NONE', #59068, #53799, #6327, .T. ) ;
#56214=CARTESIAN_POINT ( 'NONE',  ( 1.091591847532191073, -18.34768875777499275, 37.68449692119637717 ) ) ;
#56218=DIRECTION ( 'NONE',  ( 0.000000000000000000, 0.000000000000000000, 1.000000000000000000 ) ) ;
#56229=CARTESIAN_POINT ( 'NONE',  ( 0.5806925824938502512, -7.260877859417425029, 46.33035738103242096 ) ) ;
#56239=CARTESIAN_POINT ( 'NONE',  ( 4.962356264823608143, 37.36413190407361640, 19.36897635181929545 ) ) ;
#56245=EDGE_CURVE ( 'NONE', #39870, #5752, #47149, .T. ) ;
#56246=CARTESIAN_POINT ( 'NONE',  ( 0.8554163680231738898, -13.02474486562517519, -45.07284652978098904 ) ) ;
#56255=ORIENTED_EDGE ( 'NONE', *, *, #486, .F. ) ;
#56260=( BOUNDED_SURFACE ( )  B_SPLINE_SURFACE ( 3, 1, ( 
 ( #16890, #8692 ),
 ( #36004, #14044 ),
 ( #52530, #34077 ),
 ( #53145, #61307 ) ),
 .UNSPECIFIED., .F., .F., .F. ) 
 B_SPLINE_SURFACE_WITH_KNOTS ( ( 4, 4 ),
 ( 2, 2 ),
 ( 0.000000000000000000, 1.000000000000000000 ),
 ( 0.000000000000000000, 1.000000000000000000 ),
 .UNSPECIFIED. ) 
 GEOMETRIC_REPRESENTATION_ITEM ( )  RATIONAL_B_SPLINE_SURFACE ( (
 ( 1.000000000000000000, 1.000000000000000000),
 ( 0.9952954269826590483, 0.8620686068821339365),
 ( 0.9952954269826590483, 0.8620686068821339365),
 ( 1.000000000000000000, 1.000000000000000000) ) ) 
 REPRESENTATION_ITEM ( '' )  SURFACE ( )  );
#56264=CARTESIAN_POINT ( 'NONE',  ( 0.5832655196449145762, 27.63416530929389836, 37.88915531694979677 ) ) ;
#56265=B_SPLINE_CURVE_WITH_KNOTS ( 'NONE', 3,
 ( #4972, #43235, #270, #61369 ),
 .UNSPECIFIED., .F., .F.,
 ( 4, 4 ),
 ( 6.505213034913026604E-19, 0.004041751736740995145 ),
 .UNSPECIFIED. ) ;
#56267=VERTEX_POINT ( 'NONE', #42958 ) ;
#56269=CARTESIAN_POINT ( 'NONE',  ( 2.528190830796654520, 13.95207949221547672, 39.59284801572006529 ) ) ;
#56270=CARTESIAN_POINT ( 'NONE',  ( 0.9754292589017212745, -41.84984047562296894, -2.217728355815624219 ) ) ;
#56274=CARTESIAN_POINT ( 'NONE',  ( 0.5806925824938511393, 10.33919002968708689, -45.74192291403568333 ) ) ;
#56277=CARTESIAN_POINT ( 'NONE',  ( 5.910764540655177868, 10.80896614705642556, 16.96076322872739084 ) ) ;
#56279=CARTESIAN_POINT ( 'NONE',  ( 0.8560838555295158248, 36.24009790160309308, 29.78301761346479282 ) ) ;
#56284=FACE_OUTER_BOUND ( 'NONE', #7632, .T. ) ;
#56285=VERTEX_POINT ( 'NONE', #20068 ) ;
#56287=CARTESIAN_POINT ( 'NONE',  ( 4.956445790444010235, -22.15545010017738647, -41.55326799420456751 ) ) ;
#56301=EDGE_LOOP ( 'NONE', ( #20837, #41653, #50227, #21282 ) ) ;
#56304=CARTESIAN_POINT ( 'NONE',  ( 4.956445790443988031, 0.000000000000000000, 0.000000000000000000 ) ) ;
#56306=CARTESIAN_POINT ( 'NONE',  ( 0.8560838555295158248, -46.85553835019179303, 2.220666565569249684 ) ) ;
#56313=CARTESIAN_POINT ( 'NONE',  ( 5.896782393890504181, 0.6657210432555761281, 20.10181341000306077 ) ) ;
#56319=ORIENTED_EDGE ( 'NONE', *, *, #44042, .F. ) ;
#56330=ORIENTED_EDGE ( 'NONE', *, *, #22929, .F. ) ;
#56332=CARTESIAN_POINT ( 'NONE',  ( 0.9791128995231617171, -6.975674438753351581, -41.32405353266649684 ) ) ;
#56333=ORIENTED_EDGE ( 'NONE', *, *, #50853, .F. ) ;
#56335=B_SPLINE_CURVE_WITH_KNOTS ( 'NONE', 3,
 ( #35871, #45578, #54940, #12073 ),
 .UNSPECIFIED., .F., .F.,
 ( 4, 4 ),
 ( 8.673617379884035472E-19, 0.004446298630425088438 ),
 .UNSPECIFIED. ) ;
#56339=CARTESIAN_POINT ( 'NONE',  ( 0.9787284016396613495, -37.31945016035690799, 19.06815771535011095 ) ) ;
#56340=CARTESIAN_POINT ( 'NONE',  ( 0.5782707292762442330, 28.40044722094953400, -37.32493739254866227 ) ) ;
#56344=CARTESIAN_POINT ( 'NONE',  ( 0.5806925824938506953, -46.06186276235258958, -8.804950948515241294 ) ) ;
#56347=ORIENTED_EDGE ( 'NONE', *, *, #16394, .F. ) ;
#56362=( NAMED_UNIT ( * ) SI_UNIT ( $, .STERADIAN. ) SOLID_ANGLE_UNIT ( ) );
#56371=EDGE_CURVE ( 'NONE', #23457, #42423, #10039, .T. ) ;
#56372=CARTESIAN_POINT ( 'NONE',  ( 0.5848930533535030563, -45.92005787004946882, -9.519525597363942993 ) ) ;
#56374=EDGE_CURVE ( 'NONE', #37874, #30066, #55316, .T. ) ;
#56378=CARTESIAN_POINT ( 'NONE',  ( 0.5834584762367746036, 22.69689635113398651, -41.03762767313761373 ) ) ;
#56380=VERTEX_POINT ( 'NONE', #59767 ) ;
#56382=CARTESIAN_POINT ( 'NONE',  ( 0.9789233960466703355, 20.02512277535910457, 36.81482289328764068 ) ) ;
#56383=CARTESIAN_POINT ( 'NONE',  ( 0.5806925824938499181, -41.60618895332673617, -21.63671424046719594 ) ) ;
#56384=CARTESIAN_POINT ( 'NONE',  ( 0.7764146366350267447, 42.82684524705668139, -19.12855979559951436 ) ) ;
#56385=ORIENTED_EDGE ( 'NONE', *, *, #18044, .F. ) ;
#56387=CARTESIAN_POINT ( 'NONE',  ( 0.9769922540276037015, -41.78318551423056704, -3.239901753065929757 ) ) ;
#56399=ORIENTED_EDGE ( 'NONE', *, *, #39231, .F. ) ;
#56400=CARTESIAN_POINT ( 'NONE',  ( 0.6845945791218034371, -14.72268806499663718, 44.53817437720981331 ) ) ;
#56405=CARTESIAN_POINT ( 'NONE',  ( 0.8560838555295223751, 36.24009790160352651, -29.78301761346427767 ) ) ;
#56411=CARTESIAN_POINT ( 'NONE',  ( 0.5837799406558221715, -44.33108515927273174, -15.29700749096085843 ) ) ;
#56412=CARTESIAN_POINT ( 'NONE',  ( 0.5830082357119579228, 16.59956988142198497, 43.85984854841750291 ) ) ;
#56416=STYLED_ITEM ( 'NONE', ( #26699 ), #52453 ) ;
#56426=CARTESIAN_POINT ( 'NONE',  ( 0.5837799406558230597, -1.658065787041380634, -46.86677253047242431 ) ) ;
#56427=EDGE_CURVE ( 'NONE', #52560, #49823, #12755, .T. ) ;
#56433=FACE_OUTER_BOUND ( 'NONE', #36406, .T. ) ;
#56440=CARTESIAN_POINT ( 'NONE',  ( 0.9790850452238877288, -12.36814557455428876, 40.04205670679053952 ) ) ;
#56442=CARTESIAN_POINT ( 'NONE',  ( 1.231276596079881935, -37.02495017545860634, -19.65781868679418309 ) ) ;
#56443=ADVANCED_FACE ( 'NONE', ( #22183 ), #55999, .F. ) ;
#56444=CARTESIAN_POINT ( 'NONE',  ( 0.6845945791218023269, 42.84081778543567509, -19.10682737110073859 ) ) ;
#56450=CARTESIAN_POINT ( 'NONE',  ( 0.5837799406558222826, 45.20568596181698240, -12.47756011000493892 ) ) ;
#56462=VECTOR ( 'NONE', #54960, 1000.000000000000114 ) ;
#56463=CARTESIAN_POINT ( 'NONE',  ( 0.9754292580325134576, -39.39482823006320444, -14.29597760308189258 ) ) ;
#56465=ORIENTED_EDGE ( 'NONE', *, *, #12781, .F. ) ;
#56467=CARTESIAN_POINT ( 'NONE',  ( 0.8560838555295223751, 3.785103201470721768, -46.75516899590834186 ) ) ;
#56468=CARTESIAN_POINT ( 'NONE',  ( 0.9762797500689124330, -1.905951756780080775, -41.86516610604251554 ) ) ;
#56476=EDGE_CURVE ( 'NONE', #60419, #6142, #32606, .T. ) ;
#56478=ORIENTED_EDGE ( 'NONE', *, *, #33987, .F. ) ;
#56484=CARTESIAN_POINT ( 'NONE',  ( 0.5806925824938511393, 40.62497527030930655, 23.42720099863236882 ) ) ;
#56488=DIRECTION ( 'NONE',  ( 0.07906939808003035641, -0.2232318573464372458, -0.9715531730960079715 ) ) ;
#56490=DIRECTION ( 'NONE',  ( 0.000000000000000000, 0.000000000000000000, 1.000000000000000000 ) ) ;
#56491=EDGE_LOOP ( 'NONE', ( #41237, #39748, #31525, #37956 ) ) ;
#56495=CONICAL_SURFACE ( 'NONE', #49834, 42.08604991992415023, 1.569615340895231137 ) ;
#56499=CARTESIAN_POINT ( 'NONE',  ( 5.895596859100789899, 3.341829471547073549, -19.83331437242869910 ) ) ;
#56505=CARTESIAN_POINT ( 'NONE',  ( 5.838029081930957709, 38.93046761018084112, -26.74852799324816743 ) ) ;
#56509=CARTESIAN_POINT ( 'NONE',  ( 0.5835871038041848813, -30.17293921915137034, -35.90025336650005272 ) ) ;
#56515=FACE_OUTER_BOUND ( 'NONE', #15124, .T. ) ;
#56519=ORIENTED_EDGE ( 'NONE', *, *, #36666, .F. ) ;
#56521=CARTESIAN_POINT ( 'NONE',  ( 4.962356264823608143, -41.76635909427997717, 5.177532797578748180 ) ) ;
#56532=CARTESIAN_POINT ( 'NONE',  ( 0.5806925824938499181, -8.338382001838064994, 46.14860504863594315 ) ) ;
#56533=ORIENTED_EDGE ( 'NONE', *, *, #26112, .T. ) ;
#56534=ORIENTED_EDGE ( 'NONE', *, *, #59279, .F. ) ;
#56537=CARTESIAN_POINT ( 'NONE',  ( 5.838029081930955932, -40.65053383315998303, 24.05408816047773968 ) ) ;
#56540=CARTESIAN_POINT ( 'NONE',  ( 4.956445790443988031, 0.000000000000000000, 0.000000000000000000 ) ) ;
#56544=ORIENTED_EDGE ( 'NONE', *, *, #4069, .F. ) ;
#56546=CARTESIAN_POINT ( 'NONE',  ( 0.9791128995231614951, 24.85527234537524777, -33.74244909432907491 ) ) ;
#56550=CARTESIAN_POINT ( 'NONE',  ( 0.9789233960466712237, 32.97123601430887874, -25.86956363221230148 ) ) ;
#56557=ORIENTED_EDGE ( 'NONE', *, *, #43119, .T. ) ;
#56563=CARTESIAN_POINT ( 'NONE',  ( 0.9791128995231621612, -37.40658675588493054, -18.89668493468148824 ) ) ;
#56570=CARTESIAN_POINT ( 'NONE',  ( 1.157644175074336923, -31.63536299616512437, 27.49920150804474162 ) ) ;
#56578=CARTESIAN_POINT ( 'NONE',  ( 0.5834584762367733823, 27.67094651009132278, 37.86231250529817061 ) ) ;
#56579=EDGE_CURVE ( 'NONE', #30663, #52112, #32947, .T. ) ;
#56581=ORIENTED_EDGE ( 'NONE', *, *, #13379, .T. ) ;
#56582=CARTESIAN_POINT ( 'NONE',  ( 1.231276596079881047, 33.41651732065586344, -25.31033664684003170 ) ) ;
#56591=ORIENTED_EDGE ( 'NONE', *, *, #51367, .F. ) ;
#56596=CARTESIAN_POINT ( 'NONE',  ( 2.282816707992308736, -29.31214480238963915, 36.70551911486484897 ) ) ;
#56616=DIRECTION ( 'NONE',  ( 0.000000000000000000, 0.000000000000000000, 1.000000000000000000 ) ) ;
#56617=CARTESIAN_POINT ( 'NONE',  ( 0.8560838555295223751, -46.73345513967318965, 4.044379407262076676 ) ) ;
#56619=ORIENTED_EDGE ( 'NONE', *, *, #5204, .F. ) ;
#56625=CARTESIAN_POINT ( 'NONE',  ( 0.9762797500689124330, 32.57381952463267538, -26.36799322592379369 ) ) ;
#56644=CARTESIAN_POINT ( 'NONE',  ( 5.917102823773431552, 16.58597737984221610, -11.37519548874235298 ) ) ;
#56655=CARTESIAN_POINT ( 'NONE',  ( 0.5804410086790514622, 45.37396088368723923, -11.86269470150088168 ) ) ;
#56658=ORIENTED_EDGE ( 'NONE', *, *, #34617, .T. ) ;
#56666=CARTESIAN_POINT ( 'NONE',  ( 0.9772918015221174759, -40.98423817134506919, 8.753803588448938910 ) ) ;
#56669=( NAMED_UNIT ( * ) PLANE_ANGLE_UNIT ( ) SI_UNIT ( $, .RADIAN. ) );
#56676=CIRCLE ( 'NONE', #8653, 47.09074272231896430 ) ;
#56678=CARTESIAN_POINT ( 'NONE',  ( 0.9780106845699483298, 28.90828061660102577, 30.34209218638833505 ) ) ;
#56682=CARTESIAN_POINT ( 'NONE',  ( 0.5824935313925965197, 22.21726476033930453, -41.29928962612820698 ) ) ;
#56691=CARTESIAN_POINT ( 'NONE',  ( 5.895596859100789899, -4.659086063545737844, -19.56581458219824299 ) ) ;
#56695=CARTESIAN_POINT ( 'NONE',  ( 0.5834584762367761579, -45.91967682079450697, -9.519415406787116396 ) ) ;
#56696=ADVANCED_FACE ( 'NONE', ( #2665 ), #41579, .F. ) ;
#56705=EDGE_LOOP ( 'NONE', ( #56887, #53157, #40522, #52403 ) ) ;
#56706=CARTESIAN_POINT ( 'NONE',  ( 3.782625744892853525, 39.34346952798183850, 14.80977749987372150 ) ) ;
#56709=CARTESIAN_POINT ( 'NONE',  ( 0.6064515330803574855, 11.56175758416135047, 45.44953352458280449 ) ) ;
#56710=B_SPLINE_CURVE_WITH_KNOTS ( 'NONE', 3,
 ( #29148, #24136, #43904, #28521, #19765, #29449, #38267, #308, #4690, #946, #57625, #15376, #14758, #23836, #57314, #5615 ),
 .UNSPECIFIED., .F., .F.,
 ( 4, 3, 3, 3, 3, 4 ),
 ( 1.551621725782133898E-17, 0.0002732102107931821933, 0.0004098135523333748661, 0.0005464168938825010938, 0.0008195847345945432268, 0.001092771384553104397 ),
 .UNSPECIFIED. ) ;
#56715=CARTESIAN_POINT ( 'NONE',  ( 4.960386119450146403, 43.62260476509047891, -3.391875319206996142 ) ) ;
#56716=EDGE_CURVE ( 'NONE', #12754, #32617, #10521, .T. ) ;
#56717=CIRCLE ( 'NONE', #7711, 42.08604991992415023 ) ;
#56719=DIRECTION ( 'NONE',  ( -0.07906939808003035641, 0.5978040102392314648, 0.7977332860230633704 ) ) ;
#56725=CARTESIAN_POINT ( 'NONE',  ( 5.894904586330512508, 14.91596325940037815, -13.49234790930995764 ) ) ;
#56728=ORIENTED_EDGE ( 'NONE', *, *, #52381, .T. ) ;
#56730=( BOUNDED_SURFACE ( )  B_SPLINE_SURFACE ( 3, 1, ( 
 ( #54606, #1994 ),
 ( #20211, #35547 ),
 ( #29895, #25499 ),
 ( #21120, #1676 ) ),
 .UNSPECIFIED., .F., .F., .F. ) 
 B_SPLINE_SURFACE_WITH_KNOTS ( ( 4, 4 ),
 ( 2, 2 ),
 ( 0.000000000000000000, 1.000000000000000000 ),
 ( 0.000000000000000000, 1.000000000000000000 ),
 .UNSPECIFIED. ) 
 GEOMETRIC_REPRESENTATION_ITEM ( )  RATIONAL_B_SPLINE_SURFACE ( (
 ( 1.000000000000000000, 1.000000000000000000),
 ( 0.9952954269826590483, 0.8620686068821339365),
 ( 0.9952954269826590483, 0.8620686068821339365),
 ( 1.000000000000000000, 1.000000000000000000) ) ) 
 REPRESENTATION_ITEM ( '' )  SURFACE ( )  );
#56731=CARTESIAN_POINT ( 'NONE',  ( 0.5824935313925957425, 10.51678459559550838, -45.70159098788227681 ) ) ;
#56733=CARTESIAN_POINT ( 'NONE',  ( 0.5830082357119570347, 4.422203156529602275, 46.68700198321495520 ) ) ;
#56741=B_SPLINE_CURVE_WITH_KNOTS ( 'NONE', 3,
 ( #39043, #28998, #24926, #38416 ),
 .UNSPECIFIED., .F., .F.,
 ( 4, 4 ),
 ( 8.673617379884034509E-19, 0.004042984057420971090 ),
 .UNSPECIFIED. ) ;
#56743=CARTESIAN_POINT ( 'NONE',  ( 0.5782707292762442330, -46.83939014838222903, 2.409955235113546923 ) ) ;
#56744=ADVANCED_FACE ( 'NONE', ( #32126 ), #33158, .F. ) ;
#56747=CARTESIAN_POINT ( 'NONE',  ( 4.956445790443988031, 0.000000000000000000, 0.000000000000000000 ) ) ;
#56748=CARTESIAN_POINT ( 'NONE',  ( 0.9788927965476035276, -12.28110083706939903, 40.06883046535685367 ) ) ;
#56753=CARTESIAN_POINT ( 'NONE',  ( 1.231276596079887931, -41.87427716283724521, -1.954912557623687652 ) ) ;
#56754=CARTESIAN_POINT ( 'NONE',  ( 5.894904586330512508, -7.229884331608815273, 18.76854242111518190 ) ) ;
#56757=CARTESIAN_POINT ( 'NONE',  ( 0.8554163680231708922, 11.76336166872351008, -45.41837508500965725 ) ) ;
#56770=CARTESIAN_POINT ( 'NONE',  ( 0.8560838555295158248, -35.39593983670192756, 30.78149244527153883 ) ) ;
#56772=ORIENTED_EDGE ( 'NONE', *, *, #45387, .T. ) ;
#56773=CARTESIAN_POINT ( 'NONE',  ( 0.5806925824938502512, 4.150136846023314341, -46.71186922509998141 ) ) ;
#56778=CARTESIAN_POINT ( 'NONE',  ( 4.958415959904818315, 29.71032706691277880, 34.35841118852422937 ) ) ;
#56781=CARTESIAN_POINT ( 'NONE',  ( 4.956445790443991584, 41.78282513192503700, 21.71942849465911252 ) ) ;
#56786=( BOUNDED_SURFACE ( )  B_SPLINE_SURFACE ( 3, 1, ( 
 ( #5251, #48805 ),
 ( #555, #39125 ),
 ( #19692, #57872 ),
 ( #53483, #53185 ) ),
 .UNSPECIFIED., .F., .F., .F. ) 
 B_SPLINE_SURFACE_WITH_KNOTS ( ( 4, 4 ),
 ( 2, 2 ),
 ( 0.000000000000000000, 1.000000000000000000 ),
 ( 0.000000000000000000, 1.000000000000000000 ),
 .UNSPECIFIED. ) 
 GEOMETRIC_REPRESENTATION_ITEM ( )  RATIONAL_B_SPLINE_SURFACE ( (
 ( 1.000000000000000000, 1.000000000000000000),
 ( 0.7282232189291693025, 0.9929344683865674037),
 ( 0.7282232189291693025, 0.9929344683865674037),
 ( 1.000000000000000000, 1.000000000000000000) ) ) 
 REPRESENTATION_ITEM ( '' )  SURFACE ( )  );
#56792=ORIENTED_EDGE ( 'NONE', *, *, #30171, .T. ) ;
#56797=CARTESIAN_POINT ( 'NONE',  ( 5.894904586330512508, 16.58122937421105192, 11.38385894595691816 ) ) ;
#56803=CARTESIAN_POINT ( 'NONE',  ( 4.291220156522060236, -45.16379180774710278, -13.40227245105002751 ) ) ;
#56804=ORIENTED_EDGE ( 'NONE', *, *, #31167, .T. ) ;
#56805=CARTESIAN_POINT ( 'NONE',  ( 5.917102823773431552, -19.93362549613923207, -2.672132599892811822 ) ) ;
#56815=CARTESIAN_POINT ( 'NONE',  ( 5.894904586330512508, 19.00045333391150848, 6.596376669619000488 ) ) ;
#56821=CARTESIAN_POINT ( 'NONE',  ( 2.618530812446115519, 39.70953715621357816, -25.15709538157162584 ) ) ;
#56822=CARTESIAN_POINT ( 'NONE',  ( 0.9783242366443536397, -1.132393795794202296, -41.89334284224371174 ) ) ;
#56823=CARTESIAN_POINT ( 'NONE',  ( 0.9762797500689124330, 3.691134646838137190, -41.74566217230977117 ) ) ;
#56832=ADVANCED_FACE ( 'NONE', ( #46536 ), #4429, .T. ) ;
#56835=EDGE_CURVE ( 'NONE', #57176, #5968, #20477, .T. ) ;
#56840=EDGE_LOOP ( 'NONE', ( #19245, #26492, #7958, #30737 ) ) ;
#56841=CARTESIAN_POINT ( 'NONE',  ( 5.894904586330512508, 10.82137050184767268, 16.95368256525359740 ) ) ;
#56848=ORIENTED_EDGE ( 'NONE', *, *, #48933, .F. ) ;
#56855=CARTESIAN_POINT ( 'NONE',  ( 0.5830081025819935370, 46.89517456657120675, -0.2731972786442221079 ) ) ;
#56866=CARTESIAN_POINT ( 'NONE',  ( -4.467299999999993609, 0.000000000000000000, -12.50000000000000000 ) ) ;
#56867=CARTESIAN_POINT ( 'NONE',  ( 0.5806925824938490299, 46.40146083665128174, 6.791670970260652140 ) ) ;
#56884=CARTESIAN_POINT ( 'NONE',  ( 4.962356264823601926, 34.44911810793277596, -24.17630781256817940 ) ) ;
#56885=CARTESIAN_POINT ( 'NONE',  ( 5.917102823773431552, 0.6634426252563657700, -20.10098410363868027 ) ) ;
#56887=ORIENTED_EDGE ( 'NONE', *, *, #29679, .F. ) ;
#56890=CARTESIAN_POINT ( 'NONE',  ( 0.8554163680231738898, 44.99993935735606954, 13.27444654010463410 ) ) ;
#56894=VECTOR ( 'NONE', #38860, 999.9999999999998863 ) ;
#56901=( BOUNDED_SURFACE ( )  B_SPLINE_SURFACE ( 3, 1, ( 
 ( #54540, #2236 ),
 ( #26067, #11668 ),
 ( #48948, #59251 ),
 ( #16359, #45205 ) ),
 .UNSPECIFIED., .F., .F., .F. ) 
 B_SPLINE_SURFACE_WITH_KNOTS ( ( 4, 4 ),
 ( 2, 2 ),
 ( 0.000000000000000000, 1.000000000000000000 ),
 ( 0.000000000000000000, 1.000000000000000000 ),
 .UNSPECIFIED. ) 
 GEOMETRIC_REPRESENTATION_ITEM ( )  RATIONAL_B_SPLINE_SURFACE ( (
 ( 1.000000000000000000, 1.000000000000000000),
 ( 0.9952954269826590483, 0.8620686068821307169),
 ( 0.9952954269826590483, 0.8620686068821307169),
 ( 1.000000000000000000, 1.000000000000000000) ) ) 
 REPRESENTATION_ITEM ( '' )  SURFACE ( )  );
#56903=CARTESIAN_POINT ( 'NONE',  ( 0.9762797500689124330, 32.57381952463267538, -26.36799322592379369 ) ) ;
#56907=CARTESIAN_POINT ( 'NONE',  ( 1.092182651088184908, -6.200333517503296754, 41.45258796159785675 ) ) ;
#56916=CARTESIAN_POINT ( 'NONE',  ( 0.5782707292762423457, 43.45719891954316694, 17.64109451748601032 ) ) ;
#56931=EDGE_CURVE ( 'NONE', #34782, #55528, #27597, .T. ) ;
#56935=ADVANCED_FACE ( 'NONE', ( #49591 ), #52613, .T. ) ;
#56936=B_SPLINE_CURVE_WITH_KNOTS ( 'NONE', 3,
 ( #54207, #16974, #12580, #25412 ),
 .UNSPECIFIED., .F., .F.,
 ( 4, 4 ),
 ( 0.000000000000000000, 0.004447772540403788569 ),
 .UNSPECIFIED. ) ;
#56944=EDGE_LOOP ( 'NONE', ( #6953, #24664, #50637, #59395 ) ) ;
#56945=CARTESIAN_POINT ( 'NONE',  ( 5.838029081930957709, -43.49392513872139432, -18.42127938499984197 ) ) ;
#56953=EDGE_CURVE ( 'NONE', #30244, #48102, #21600, .T. ) ;
#56957=CARTESIAN_POINT ( 'NONE',  ( 0.9789233960466692253, -37.46340317803434772, 18.78377355997430342 ) ) ;
#56959=CARTESIAN_POINT ( 'NONE',  ( 5.896278296736517710, 10.82699056113231251, -16.95002227147609020 ) ) ;
#56961=ORIENTED_EDGE ( 'NONE', *, *, #61924, .F. ) ;
#56962=CARTESIAN_POINT ( 'NONE',  ( 0.8554163680231720024, 11.76336166872288302, 45.41837508500981357 ) ) ;
#56963=CARTESIAN_POINT ( 'NONE',  ( 5.910764540655178756, 12.97317151014757464, -15.36873642943551310 ) ) ;
#56979=LINE ( 'NONE', #61972, #57806 ) ;
#56982=( BOUNDED_SURFACE ( )  B_SPLINE_SURFACE ( 3, 1, ( 
 ( #10631, #29720 ),
 ( #48834, #5887 ),
 ( #44177, #30032 ),
 ( #58517, #53818 ) ),
 .UNSPECIFIED., .F., .F., .F. ) 
 B_SPLINE_SURFACE_WITH_KNOTS ( ( 4, 4 ),
 ( 2, 2 ),
 ( 0.000000000000000000, 1.000000000000000000 ),
 ( 0.000000000000000000, 1.000000000000000000 ),
 .UNSPECIFIED. ) 
 GEOMETRIC_REPRESENTATION_ITEM ( )  RATIONAL_B_SPLINE_SURFACE ( (
 ( 1.000000000000000000, 1.000000000000000000),
 ( 0.9952954269826590483, 0.8620686068821307169),
 ( 0.9952954269826590483, 0.8620686068821307169),
 ( 1.000000000000000000, 1.000000000000000000) ) ) 
 REPRESENTATION_ITEM ( '' )  SURFACE ( )  );
#56987=LINE ( 'NONE', #51671, #6817 ) ;
#56989=CARTESIAN_POINT ( 'NONE',  ( 5.896782393890504181, 20.06834277495332941, 1.337050913387667350 ) ) ;
#56992=CARTESIAN_POINT ( 'NONE',  ( 4.956445790443996913, 7.299064093730984304, 46.52162629890795387 ) ) ;
#56997=ORIENTED_EDGE ( 'NONE', *, *, #51925, .F. ) ;
#57002=CARTESIAN_POINT ( 'NONE',  ( 4.962356264823602814, -15.53171314616136200, -39.11523340858015274 ) ) ;
#57003=ORIENTED_EDGE ( 'NONE', *, *, #3177, .F. ) ;
#57005=CARTESIAN_POINT ( 'NONE',  ( 5.895596859100789899, 19.00119700155561020, -6.594141014609973261 ) ) ;
#57008=LINE ( 'NONE', #51697, #40103 ) ;
#57009=CARTESIAN_POINT ( 'NONE',  ( 0.5830082357119558134, -45.90106299026774650, -9.608561354428239554 ) ) ;
#57012=CARTESIAN_POINT ( 'NONE',  ( 4.962356264823602814, 39.61238188121407688, -14.21600504921160812 ) ) ;
#57014=CARTESIAN_POINT ( 'NONE',  ( 4.960386119450145515, 43.68547429165921159, 2.452712903118134946 ) ) ;
#57025=ORIENTED_EDGE ( 'NONE', *, *, #3757, .T. ) ;
#57026=CARTESIAN_POINT ( 'NONE',  ( 0.5782707292762442330, 46.38083794024484519, 6.968086227104402397 ) ) ;
#57027=CARTESIAN_POINT ( 'NONE',  ( 5.838029081930955932, -45.56116631979260490, 12.45974244248718144 ) ) ;
#57031=CARTESIAN_POINT ( 'NONE',  ( 5.895596859100789899, 0.6756533542676474990, -20.10153416427100836 ) ) ;
#57033=CARTESIAN_POINT ( 'NONE',  ( 0.5832655196449156865, 43.26316045182046111, -18.09790404144539266 ) ) ;
#57035=CARTESIAN_POINT ( 'NONE',  ( 5.917102823773431552, 12.99138957749423540, -15.35296436840508427 ) ) ;
#57038=FACE_OUTER_BOUND ( 'NONE', #28448, .T. ) ;
#57039=CARTESIAN_POINT ( 'NONE',  ( 2.528100132419516921, 36.72067332157243413, 20.34320351966313112 ) ) ;
#57041=CARTESIAN_POINT ( 'NONE',  ( 3.376099380956842921, 13.04318434631697521, 3.095759315589459604 ) ) ;
#57044=CARTESIAN_POINT ( 'NONE',  ( 4.956445790443991584, 35.28522167764473494, 31.18479086508529363 ) ) ;
#57045=CARTESIAN_POINT ( 'NONE',  ( 0.5848930533535030563, 36.69111421824725028, 29.20676667847867947 ) ) ;
#57046=CARTESIAN_POINT ( 'NONE',  ( 0.5804410086790514622, -25.69437916690408841, 39.23415261073904503 ) ) ;
#57054=ADVANCED_FACE ( 'NONE', ( #27959 ), #49594, .F. ) ;
#57065=EDGE_CURVE ( 'NONE', #57224, #43088, #9616, .T. ) ;
#57077=CARTESIAN_POINT ( 'NONE',  ( 1.231276596079881047, -41.87427716283725943, 1.954912557623087022 ) ) ;
#57082=VERTEX_POINT ( 'NONE', #51431 ) ;
#57083=CARTESIAN_POINT ( 'NONE',  ( 5.838029081930957709, 7.876159563729070889, 46.57285871276959455 ) ) ;
#57099=CARTESIAN_POINT ( 'NONE',  ( 3.661933894777898324, 44.00646638618364648, -16.61511604393246699 ) ) ;
#57103=CARTESIAN_POINT ( 'NONE',  ( 0.5834584762367761579, 36.91654477532374301, -28.92066235176340427 ) ) ;
#57105=CARTESIAN_POINT ( 'NONE',  ( 0.9754292589017237169, -34.87747755813919071, -23.23551217590808449 ) ) ;
#57106=CARTESIAN_POINT ( 'NONE',  ( 1.231276596079887931, 41.42457922925077440, -6.425029704024191268 ) ) ;
#57109=ORIENTED_EDGE ( 'NONE', *, *, #10176, .F. ) ;
#57129=DIRECTION ( 'NONE',  ( 0.07906939808003034253, 0.7338893160900376023, 0.6746513929550271849 ) ) ;
#57134=CARTESIAN_POINT ( 'NONE',  ( 5.901463166500145796, 16.57349776239436068, 11.39460584050830327 ) ) ;
#57144=CARTESIAN_POINT ( 'NONE',  ( 0.5832655196449135770, 22.33746898810849757, 41.23436263820043735 ) ) ;
#57147=( BOUNDED_SURFACE ( )  B_SPLINE_SURFACE ( 3, 1, ( 
 ( #8802, #38266 ),
 ( #27919, #32625 ),
 ( #47042, #47956 ),
 ( #37967, #19762 ) ),
 .UNSPECIFIED., .F., .F., .F. ) 
 B_SPLINE_SURFACE_WITH_KNOTS ( ( 4, 4 ),
 ( 2, 2 ),
 ( 0.000000000000000000, 1.000000000000000000 ),
 ( 0.000000000000000000, 1.000000000000000000 ),
 .UNSPECIFIED. ) 
 GEOMETRIC_REPRESENTATION_ITEM ( )  RATIONAL_B_SPLINE_SURFACE ( (
 ( 1.000000000000000000, 1.000000000000000000),
 ( 0.9729067724841187204, 0.9999501103223794596),
 ( 0.9729067724841187204, 0.9999501103223794596),
 ( 1.000000000000000000, 1.000000000000000000) ) ) 
 REPRESENTATION_ITEM ( '' )  SURFACE ( )  );
#57152=CARTESIAN_POINT ( 'NONE',  ( 0.5837800304671213469, 16.89725109513926782, -43.74608825492073549 ) ) ;
#57153=AXIS2_PLACEMENT_3D ( 'NONE', #22002, #31393, #50492 ) ;
#57162=CARTESIAN_POINT ( 'NONE',  ( 0.9783242366443567484, -37.28257179578840663, -19.14012357583945345 ) ) ;
#57164=CARTESIAN_POINT ( 'NONE',  ( 0.5797568665920713737, -13.29195617976572663, 44.97276075044824495 ) ) ;
#57171=CARTESIAN_POINT ( 'NONE',  ( 5.896782393890504181, 8.471952691971054605, 18.24149403045202078 ) ) ;
#57173=B_SPLINE_CURVE_WITH_KNOTS ( 'NONE', 3,
 ( #22089, #46221, #12392, #46841, #2965, #8275, #21464, #40603, #45919, #17699, #50275, #40917, #41837, #41215, #7981, #60904 ),
 .UNSPECIFIED., .F., .F.,
 ( 4, 3, 3, 3, 3, 4 ),
 ( 1.170988539753570110E-17, 0.0002732102107931889696, 0.0004098135523333795282, 0.0005464168938824970822, 0.0008195847345945433352, 0.001092771384553107650 ),
 .UNSPECIFIED. ) ;
#57176=VERTEX_POINT ( 'NONE', #1279 ) ;
#57178=CARTESIAN_POINT ( 'NONE',  ( 0.5837157313716011542, 27.74442730813685998, 37.80851513780375939 ) ) ;
#57181=CARTESIAN_POINT ( 'NONE',  ( 1.091591847532197512, -30.55658497080212044, -28.68891956623656370 ) ) ;
#57183=ORIENTED_EDGE ( 'NONE', *, *, #3147, .F. ) ;
#57195=CARTESIAN_POINT ( 'NONE',  ( 5.896278296736517710, 10.82699056113207092, 16.95002227147624652 ) ) ;
#57196=CARTESIAN_POINT ( 'NONE',  ( 5.838029081930955932, 47.12733084333029865, 3.174861530241645191 ) ) ;
#57201=VECTOR ( 'NONE', #46459, 999.9999999999998863 ) ;
#57208=VERTEX_POINT ( 'NONE', #14794 ) ;
#57212=ADVANCED_FACE ( 'NONE', ( #20114 ), #44, .T. ) ;
#57216=EDGE_LOOP ( 'NONE', ( #43961, #60928, #53853, #38589 ) ) ;
#57219=LINE ( 'NONE', #10263, #37224 ) ;
#57220=DIRECTION ( 'NONE',  ( 0.000000000000000000, 0.000000000000000000, -1.000000000000000000 ) ) ;
#57222=DIRECTION ( 'NONE',  ( 0.07500201931887537365, 0.2825166499419793920, 0.9563258020171012674 ) ) ;
#57223=CARTESIAN_POINT ( 'NONE',  ( 1.231276596079881047, -18.40965318903201364, 37.66113965983544887 ) ) ;
#57224=VERTEX_POINT ( 'NONE', #25104 ) ;
#57231=CARTESIAN_POINT ( 'NONE',  ( 4.956445790444031552, 30.81386304088997719, -35.60960396630257208 ) ) ;
#57233=CARTESIAN_POINT ( 'NONE',  ( 5.895881250540457863, 12.98195518060007103, 15.36217827318742657 ) ) ;
#57234=ADVANCED_FACE ( 'NONE', ( #34211 ), #30753, .F. ) ;
#57246=EDGE_LOOP ( 'NONE', ( #59586, #39136, #56658, #38951 ) ) ;
#57250=CARTESIAN_POINT ( 'NONE',  ( 1.231276596079887931, 41.42457922925077440, -6.425029704024191268 ) ) ;
#57264=EDGE_CURVE ( 'NONE', #32172, #33924, #9604, .T. ) ;
#57267=ADVANCED_FACE ( 'NONE', ( #31903 ), #47974, .F. ) ;
#57269=CARTESIAN_POINT ( 'NONE',  ( 0.9788927965476035276, -41.04043099582347054, 8.486438375951868451 ) ) ;
#57278=CARTESIAN_POINT ( 'NONE',  ( 4.962356264823608143, 0.000000000000000000, 0.000000000000000000 ) ) ;
#57280=CARTESIAN_POINT ( 'NONE',  ( 0.5782707292762442330, -46.74268073083581498, -3.854627323460666499 ) ) ;
#57289=LINE ( 'NONE', #29424, #56894 ) ;
#57291=CARTESIAN_POINT ( 'NONE',  ( 2.528190830796654964, 40.15110720712335279, 12.25327410103500725 ) ) ;
#57293=ORIENTED_EDGE ( 'NONE', *, *, #14108, .T. ) ;
#57297=ORIENTED_EDGE ( 'NONE', *, *, #34385, .T. ) ;
#57298=CARTESIAN_POINT ( 'NONE',  ( 0.8554163680231708922, -29.58718577084388102, -36.41159034254603455 ) ) ;
#57305=CARTESIAN_POINT ( 'NONE',  ( 0.5848930533535030563, -19.90539571549713926, 42.46231627922605867 ) ) ;
#57311=ORIENTED_EDGE ( 'NONE', *, *, #5811, .F. ) ;
#57312=EDGE_CURVE ( 'NONE', #41577, #539, #2443, .T. ) ;
#57313=DIRECTION ( 'NONE',  ( 0.000000000000000000, 0.000000000000000000, 1.000000000000000000 ) ) ;
#57314=CARTESIAN_POINT ( 'NONE',  ( 0.5817216825391117174, 40.57952703393794991, 23.50610426909058503 ) ) ;
#57317=EDGE_CURVE ( 'NONE', #13226, #44269, #44826, .T. ) ;
#57330=ORIENTED_EDGE ( 'NONE', *, *, #22087, .T. ) ;
#57334=ORIENTED_EDGE ( 'NONE', *, *, #5446, .F. ) ;
#57335=CARTESIAN_POINT ( 'NONE',  ( 0.9790724872846768845, -34.52833649645707226, -23.75140393258649496 ) ) ;
#57337=CARTESIAN_POINT ( 'NONE',  ( 0.9787464366903553259, -22.40087524910941141, -35.41941248756537419 ) ) ;
#57344=B_SPLINE_CURVE_WITH_KNOTS ( 'NONE', 3,
 ( #24174, #58592, #20115, #48601, #5658, #347, #15104, #52986, #10088, #15411, #24801, #29184, #25408, #48299, #57982, #981 ),
 .UNSPECIFIED., .F., .F.,
 ( 4, 3, 3, 3, 3, 4 ),
 ( 1.084256381238943740E-17, 0.0002732102107931898912, 0.0004098135523333806666, 0.0005464168938824980580, 0.0008195847345945435521, 0.001092771384553107216 ),
 .UNSPECIFIED. ) ;
#57348=CARTESIAN_POINT ( 'NONE',  ( 1.231276596079887931, -41.24008908601417289, -7.518764738684258653 ) ) ;
#57351=DIRECTION ( 'NONE',  ( -1.000000000000000000, -0.000000000000000000, -0.000000000000000000 ) ) ;
#57355=CARTESIAN_POINT ( 'NONE',  ( 0.9762797500689124330, 28.76866969768027715, -30.47438972336406238 ) ) ;
#57356=CARTESIAN_POINT ( 'NONE',  ( 5.838029081930957709, 35.01788019483870329, -31.69878743442473734 ) ) ;
#57357=CARTESIAN_POINT ( 'NONE',  ( 4.956445790444004018, -45.55738122058073003, 11.91902120403828036 ) ) ;
#57362=DIRECTION ( 'NONE',  ( 0.07500201931887538753, -0.9652320423656591819, 0.2504032777115935415 ) ) ;
#57371=ORIENTED_EDGE ( 'NONE', *, *, #16366, .T. ) ;
#57374=CARTESIAN_POINT ( 'NONE',  ( 0.5806925824938502512, 28.25565086187734920, 37.42780459384778879 ) ) ;
#57379=CARTESIAN_POINT ( 'NONE',  ( 5.917102823773431552, -4.670717611792251311, -19.56205804721567887 ) ) ;
#57385=DIRECTION ( 'NONE',  ( 0.000000000000000000, 0.000000000000000000, 1.000000000000000000 ) ) ;
#57391=VERTEX_POINT ( 'NONE', #9947 ) ;
#57401=CARTESIAN_POINT ( 'NONE',  ( 0.5837800304671211249, 36.83215615041540048, -29.02808304884970170 ) ) ;
#57404=CARTESIAN_POINT ( 'NONE',  ( 4.960386119450136633, 18.84353550694723012, 39.48870261569452822 ) ) ;
#57406=CARTESIAN_POINT ( 'NONE',  ( 1.000110580585055198, 33.29435990446771143, -25.45394038893929078 ) ) ;
#57415=CARTESIAN_POINT ( 'NONE',  ( 5.894904586330512508, 18.99964780500586059, 6.598696488502780788 ) ) ;
#57418=CARTESIAN_POINT ( 'NONE',  ( 5.910764540655178756, 12.99683459030013211, 15.34873053713371327 ) ) ;
#57420=CARTESIAN_POINT ( 'NONE',  ( 0.6845945791218034371, -44.02134436206625878, -16.20270845477142529 ) ) ;
#57428=DIRECTION ( 'NONE',  ( 0.07906939808003035641, -0.1078133555910006508, 0.9910218517487240364 ) ) ;
#57433=CARTESIAN_POINT ( 'NONE',  ( 120.0000507999999968, 0.000000000000000000, 8.000000000000000000 ) ) ;
#57434=EDGE_CURVE ( 'NONE', #19166, #7929, #11072, .T. ) ;
#57440=CARTESIAN_POINT ( 'NONE',  ( 1.157644175074337145, 36.47889980312224623, -20.64684345445932223 ) ) ;
#57441=FACE_OUTER_BOUND ( 'NONE', #25491, .T. ) ;
#57446=ORIENTED_EDGE ( 'NONE', *, *, #40120, .T. ) ;
#57447=AXIS2_PLACEMENT_3D ( 'NONE', #7281, #49917, #35527 ) ;
#57452=CARTESIAN_POINT ( 'NONE',  ( 4.962356264823608143, 22.27740539909265394, 35.70648129607319277 ) ) ;
#57460=CARTESIAN_POINT ( 'NONE',  ( 4.958415959904823644, -35.33199410137723362, 28.54565022280773690 ) ) ;
#57462=CONICAL_SURFACE ( 'NONE', #36502, 42.08604991992415023, 1.569615340895231137 ) ;
#57467=CARTESIAN_POINT ( 'NONE',  ( 0.7764146366350247463, -13.04263738120156191, 45.05474540835458441 ) ) ;
#57474=DIRECTION ( 'NONE',  ( -1.000000000000000000, -0.000000000000000000, -0.000000000000000000 ) ) ;
#57475=ORIENTED_EDGE ( 'NONE', *, *, #26651, .T. ) ;
#57479=CARTESIAN_POINT ( 'NONE',  ( 0.5837799406558225046, 27.89109207889182684, 37.70053755881976798 ) ) ;
#57482=CARTESIAN_POINT ( 'NONE',  ( 5.895596859100789899, -17.30333226730986240, 10.25294473112777105 ) ) ;
#57484=ADVANCED_FACE ( 'NONE', ( #19659 ), #57462, .T. ) ;
#57494=EDGE_LOOP ( 'NONE', ( #5178, #42307 ) ) ;
#57495=CARTESIAN_POINT ( 'NONE',  ( 5.896782393890504181, 19.70854070425246363, 4.012419492879101490 ) ) ;
#57496=CARTESIAN_POINT ( 'NONE',  ( 0.5817217712918330008, 28.18299969253300929, -37.48270911152311413 ) ) ;
#57499=PLANE ( 'NONE',  #30897 ) ;
#57504=CARTESIAN_POINT ( 'NONE',  ( 3.661933894777862797, 47.00091140061822870, 1.882947812046177116 ) ) ;
#57508=CARTESIAN_POINT ( 'NONE',  ( 0.5835226383429291674, 11.04855730340264408, 45.57600087830647340 ) ) ;
#57517=CIRCLE ( 'NONE', #25516, 42.08604991992415023 ) ;
#57530=CARTESIAN_POINT ( 'NONE',  ( -69.95594261585600293, 0.000000000000000000, 0.000000000000000000 ) ) ;
#57532=CARTESIAN_POINT ( 'NONE',  ( 4.291220156522060236, 6.853930411217474372, 46.60914754877937582 ) ) ;
#57533=CARTESIAN_POINT ( 'NONE',  ( 0.5806925824938502512, -25.69265091979982429, -39.23149310256842170 ) ) ;
#57535=APPLICATION_CONTEXT ( 'automotive_design' ) ;
#57541=ORIENTED_EDGE ( 'NONE', *, *, #58603, .F. ) ;
#57544=ADVANCED_FACE ( 'NONE', ( #840 ), #2486, .T. ) ;
#57545=CARTESIAN_POINT ( 'NONE',  ( 0.9772918015221170318, 40.52725854131377048, 10.67137155553071537 ) ) ;
#57552=ORIENTED_EDGE ( 'NONE', *, *, #52630, .T. ) ;
#57554=CARTESIAN_POINT ( 'NONE',  ( 0.7764146366350254125, -46.85094009729996856, -2.242740660079716175 ) ) ;
#57557=CARTESIAN_POINT ( 'NONE',  ( 5.895596859100789899, 10.82540956478682581, -16.95106754653256331 ) ) ;
#57558=EDGE_LOOP ( 'NONE', ( #31027, #33041, #11758, #1402 ) ) ;
#57562=CARTESIAN_POINT ( 'NONE',  ( 3.238018933889920792, 1.066824900591889724, 13.35175557741865404 ) ) ;
#57563=CIRCLE ( 'NONE', #54523, 42.08604991992415023 ) ;
#57579=CARTESIAN_POINT ( 'NONE',  ( 2.528190830796657185, 21.22731424743293260, -36.21678155211667871 ) ) ;
#57580=VERTEX_POINT ( 'NONE', #53742 ) ;
#57582=DIRECTION ( 'NONE',  ( 0.07500201931887537365, 0.9939633762263315742, 0.08007186658772948162 ) ) ;
#57583=CARTESIAN_POINT ( 'NONE',  ( 0.6845945791218023269, -6.946890923034354515, 46.39124084584727115 ) ) ;
#57587=CARTESIAN_POINT ( 'NONE',  ( 0.9762797500689124330, -34.26226594605947895, 24.13341909939818564 ) ) ;
#57592=EDGE_CURVE ( 'NONE', #18665, #13574, #22336, .T. ) ;
#57599=DIRECTION ( 'NONE',  ( -1.000000000000000000, -0.000000000000000000, -0.000000000000000000 ) ) ;
#57600=EDGE_LOOP ( 'NONE', ( #41568, #6172, #38276, #47623 ) ) ;
#57607=CARTESIAN_POINT ( 'NONE',  ( 4.956445790443988031, 0.000000000000000000, 0.000000000000000000 ) ) ;
#57609=ORIENTED_EDGE ( 'NONE', *, *, #6379, .F. ) ;
#57614=CARTESIAN_POINT ( 'NONE',  ( 4.962356264823602814, 42.01891079680549979, 2.376285612557970772 ) ) ;
#57617=DIRECTION ( 'NONE',  ( -0.07906939808003035641, 0.09174470402934598035, -0.9926383730089368695 ) ) ;
#57619=ORIENTED_EDGE ( 'NONE', *, *, #56931, .T. ) ;
#57620=B_SPLINE_CURVE_WITH_KNOTS ( 'NONE', 3,
 ( #16408, #58996, #35530, #16107 ),
 .UNSPECIFIED., .F., .F.,
 ( 4, 4 ),
 ( 5.553824967135426632E-18, 0.004042984057420970223 ),
 .UNSPECIFIED. ) ;
#57621=CARTESIAN_POINT ( 'NONE',  ( 5.895881250540457863, 8.470336106974158952, -18.24228844863469234 ) ) ;
#57622=VERTEX_POINT ( 'NONE', #6128 ) ;
#57625=CARTESIAN_POINT ( 'NONE',  ( 0.5837799406558225046, 40.39581629257541806, 23.82061241097095206 ) ) ;
#57633=ORIENTED_EDGE ( 'NONE', *, *, #42468, .F. ) ;
#57635=ORIENTED_EDGE ( 'NONE', *, *, #20661, .F. ) ;
#57636=CARTESIAN_POINT ( 'NONE',  ( 1.231276596079887264, 29.74482033789320568, 29.53849072116790353 ) ) ;
#57638=ORIENTED_EDGE ( 'NONE', *, *, #60237, .F. ) ;
#57639=CARTESIAN_POINT ( 'NONE',  ( 0.9772918015221174759, -34.78437337412577079, -23.37486309521597150 ) ) ;
#57645=VERTEX_POINT ( 'NONE', #2989 ) ;
#57646=CARTESIAN_POINT ( 'NONE',  ( 2.618530812446111078, -0.1622799276207554930, -47.00745105218204856 ) ) ;
#57648=CARTESIAN_POINT ( 'NONE',  ( 4.956445790443998689, -11.44166143952028314, 45.67960632101629415 ) ) ;
#57663=CARTESIAN_POINT ( 'NONE',  ( 0.9787284016396619046, 9.897315075569602882, 40.72320165733204789 ) ) ;
#57669=ORIENTED_EDGE ( 'NONE', *, *, #23698, .T. ) ;
#57672=CARTESIAN_POINT ( 'NONE',  ( 5.895596859100789899, -20.11288567981415909, 0.003583743010676893742 ) ) ;
#57676=ORIENTED_EDGE ( 'NONE', *, *, #57832, .F. ) ;
#57679=VECTOR ( 'NONE', #9340, 1000.000000000000000 ) ;
#57683=CARTESIAN_POINT ( 'NONE',  ( 4.956445790444041322, 46.25174887658561573, -8.849507104743011610 ) ) ;
#57699=ORIENTED_EDGE ( 'NONE', *, *, #59711, .F. ) ;
#57702=ORIENTED_EDGE ( 'NONE', *, *, #52308, .T. ) ;
#57707=ADVANCED_FACE ( 'NONE', ( #26810 ), #6439, .T. ) ;
#57710=CARTESIAN_POINT ( 'NONE',  ( 1.091591847532195514, 41.42852926003946124, 6.358927134815586690 ) ) ;
#57716=CARTESIAN_POINT ( 'NONE',  ( 3.782542959838397056, -8.686934394837271256, 41.13119283726600628 ) ) ;
#57718=DIRECTION ( 'NONE',  ( 0.9990097760809871774, 5.448601141172922046E-18, 0.04449120468829421277 ) ) ;
#57721=EDGE_LOOP ( 'NONE', ( #17008, #33778, #56164, #2393 ) ) ;
#57726=CARTESIAN_POINT ( 'NONE',  ( 0.5782707292762423457, 27.23478191391718894, -38.18380557001864872 ) ) ;
#57728=CARTESIAN_POINT ( 'NONE',  ( 0.9762797500689124330, 41.46413394121034912, 6.086902470967687329 ) ) ;
#57730=CARTESIAN_POINT ( 'NONE',  ( 0.9762797500689124330, -1.905951756780688733, 41.86516610604248712 ) ) ;
#57735=EDGE_LOOP ( 'NONE', ( #37767, #38400, #35115, #4846 ) ) ;
#57736=CONICAL_SURFACE ( 'NONE', #29722, 42.08604991992415023, 1.569615340895231137 ) ;
#57738=VECTOR ( 'NONE', #59565, 1000.000000000000000 ) ;
#57741=EDGE_CURVE ( 'NONE', #55162, #35188, #21487, .T. ) ;
#57743=CARTESIAN_POINT ( 'NONE',  ( 3.238018933889920792, -10.88486934301749365, 7.805582089318572336 ) ) ;
#57749=EDGE_CURVE ( 'NONE', #50058, #35234, #33491, .T. ) ;
#57754=EDGE_CURVE ( 'NONE', #13149, #30244, #14078, .T. ) ;
#57756=VERTEX_POINT ( 'NONE', #28969 ) ;
#57758=CARTESIAN_POINT ( 'NONE',  ( 5.896278296736517710, -13.98624301437829232, 14.45378794493464802 ) ) ;
#57759=EDGE_CURVE ( 'NONE', #33684, #41967, #23048, .T. ) ;
#57760=CARTESIAN_POINT ( 'NONE',  ( 1.092182651088180689, -34.10752689525531167, 24.36057867809628164 ) ) ;
#57765=CONICAL_SURFACE ( 'NONE', #3746, 42.08604991992415023, 1.569615340895231137 ) ;
#57773=CARTESIAN_POINT ( 'NONE',  ( 0.5837800005270532555, 46.89600471938711479, -3.178933284798639286E-05 ) ) ;
#57774=CARTESIAN_POINT ( 'NONE',  ( 0.8554163680231720024, 5.604726001788835177, 46.58103175710786559 ) ) ;
#57775=CARTESIAN_POINT ( 'NONE',  ( 5.896782393890504181, 18.99788783847860074, -6.603510017755636063 ) ) ;
#57778=( BOUNDED_SURFACE ( )  B_SPLINE_SURFACE ( 3, 1, ( 
 ( #3683, #61016 ),
 ( #50688, #22817 ),
 ( #46037, #41950 ),
 ( #56313, #31291 ) ),
 .UNSPECIFIED., .F., .F., .F. ) 
 B_SPLINE_SURFACE_WITH_KNOTS ( ( 4, 4 ),
 ( 2, 2 ),
 ( 0.000000000000000000, 1.000000000000000000 ),
 ( 0.000000000000000000, 1.000000000000000000 ),
 .UNSPECIFIED. ) 
 GEOMETRIC_REPRESENTATION_ITEM ( )  RATIONAL_B_SPLINE_SURFACE ( (
 ( 1.000000000000000000, 1.000000000000000000),
 ( 0.7282232189291693025, 0.9929344683865674037),
 ( 0.7282232189291693025, 0.9929344683865674037),
 ( 1.000000000000000000, 1.000000000000000000) ) ) 
 REPRESENTATION_ITEM ( '' )  SURFACE ( )  );
#57781=CARTESIAN_POINT ( 'NONE',  ( 3.661921753702005677, -45.01795958545552878, -13.63871103133745777 ) ) ;
#57789=EDGE_LOOP ( 'NONE', ( #16938, #13568, #34556, #12501 ) ) ;
#57790=CARTESIAN_POINT ( 'NONE',  ( 0.5824936645240086364, -14.24161832706174202, 44.68125430722158598 ) ) ;
#57795=CARTESIAN_POINT ( 'NONE',  ( 5.896782393890504181, -11.92541098582135994, 16.19600752337635541 ) ) ;
#57806=VECTOR ( 'NONE', #38224, 1000.000000000000000 ) ;
#57807=CARTESIAN_POINT ( 'NONE',  ( 0.8560838555295158248, 28.55542365806940452, -37.21505896528851309 ) ) ;
#57808=CARTESIAN_POINT ( 'NONE',  ( 3.661933894777874343, -37.68385588960657628, -28.15240967027540719 ) ) ;
#57812=ORIENTED_EDGE ( 'NONE', *, *, #43815, .F. ) ;
#57813=CARTESIAN_POINT ( 'NONE',  ( 4.962356264823608143, 0.000000000000000000, 0.000000000000000000 ) ) ;
#57816=CARTESIAN_POINT ( 'NONE',  ( 0.7764139734771250412, 3.807011500850922658, 46.74983566109357724 ) ) ;
#57818=CARTESIAN_POINT ( 'NONE',  ( 3.238018933889920792, 12.84302458974305949, -3.803184422941917830 ) ) ;
#57820=ADVANCED_FACE ( 'NONE', ( #57441 ), #51978, .F. ) ;
#57822=CARTESIAN_POINT ( 'NONE',  ( 5.896782393890504181, 19.71107130340470448, 3.999969368646206558 ) ) ;
#57823=CARTESIAN_POINT ( 'NONE',  ( 5.896278296736517710, -13.97836643676215296, 14.46140558085503081 ) ) ;
#57826=FACE_OUTER_BOUND ( 'NONE', #11064, .T. ) ;
#57828=CARTESIAN_POINT ( 'NONE',  ( 0.9772918015221170318, -6.561173980998255217, 41.39188147139184792 ) ) ;
#57831=CARTESIAN_POINT ( 'NONE',  ( 3.238018933889920792, 12.43622092696280390, -4.974726266180425682 ) ) ;
#57832=EDGE_CURVE ( 'NONE', #28331, #59869, #5444, .T. ) ;
#57834=VERTEX_POINT ( 'NONE', #25189 ) ;
#57845=B_SPLINE_CURVE_WITH_KNOTS ( 'NONE', 3,
 ( #46852, #36520, #60594, #3580, #41845, #27404 ),
 .UNSPECIFIED., .F., .F.,
 ( 4, 2, 4 ),
 ( 1.233980214667468354E-16, 0.0002448718616795902774, 0.0004897437233590571726 ),
 .UNSPECIFIED. ) ;
#57847=ADVANCED_FACE ( 'NONE', ( #19584 ), #18513, .T. ) ;
#57851=ORIENTED_EDGE ( 'NONE', *, *, #19611, .F. ) ;
#57852=ADVANCED_FACE ( 'NONE', ( #440 ), #37190, .F. ) ;
#57853=CARTESIAN_POINT ( 'NONE',  ( 1.231276596079887264, -27.70544295162332560, -31.45926257674220494 ) ) ;
#57857=ORIENTED_EDGE ( 'NONE', *, *, #46695, .F. ) ;
#57861=CARTESIAN_POINT ( 'NONE',  ( 3.661933894777874343, -47.02171970420939573, 1.260571699832463421 ) ) ;
#57863=CARTESIAN_POINT ( 'NONE',  ( 0.9787284016396609054, 40.46867782039604577, 10.89137798434224180 ) ) ;
#57866=FACE_OUTER_BOUND ( 'NONE', #17357, .T. ) ;
#57867=ORIENTED_EDGE ( 'NONE', *, *, #21046, .T. ) ;
#57872=CARTESIAN_POINT ( 'NONE',  ( 2.618530812446115519, -0.1622799276214294262, 47.00745105218204145 ) ) ;
#57873=CARTESIAN_POINT ( 'NONE',  ( 0.9769922540276052558, 36.28140764446582978, -20.97596277700310807 ) ) ;
#57889=CARTESIAN_POINT ( 'NONE',  ( 0.9762797500689124330, 38.77779312671030709, 15.89363222827819300 ) ) ;
#57891=DIRECTION ( 'NONE',  ( -1.000000000000000000, -0.000000000000000000, -0.000000000000000000 ) ) ;
#57895=CARTESIAN_POINT ( 'NONE',  ( 4.956445790443998689, 1.033212179477464909, 47.07940656732852602 ) ) ;
#57902=CARTESIAN_POINT ( 'NONE',  ( 0.8560838555295158248, -0.6537497281619772949, -46.90357604036880446 ) ) ;
#57912=CARTESIAN_POINT ( 'NONE',  ( 1.091591847532195736, 24.22985240271725971, 34.20048601260478449 ) ) ;
#57916=FACE_OUTER_BOUND ( 'NONE', #3891, .T. ) ;
#57919=ADVANCED_FACE ( 'NONE', ( #40867 ), #15962, .F. ) ;
#57924=CARTESIAN_POINT ( 'NONE',  ( 0.5804410086790514622, -29.86002002114358689, -36.16488706179379875 ) ) ;
#57940=CARTESIAN_POINT ( 'NONE',  ( 1.231276596079881047, -31.65135013586901991, 27.48579279545509380 ) ) ;
#57962=CARTESIAN_POINT ( 'NONE',  ( 3.601714094746197414, 0.2777834434958510457, -42.02545330641159183 ) ) ;
#57965=ORIENTED_EDGE ( 'NONE', *, *, #3414, .F. ) ;
#57973=( BOUNDED_SURFACE ( )  B_SPLINE_SURFACE ( 3, 1, ( 
 ( #14289, #57774 ),
 ( #14907, #34014 ),
 ( #25505, #39961 ),
 ( #58694, #21124 ) ),
 .UNSPECIFIED., .F., .F., .F. ) 
 B_SPLINE_SURFACE_WITH_KNOTS ( ( 4, 4 ),
 ( 2, 2 ),
 ( 0.000000000000000000, 1.000000000000000000 ),
 ( 0.000000000000000000, 1.000000000000000000 ),
 .UNSPECIFIED. ) 
 GEOMETRIC_REPRESENTATION_ITEM ( )  RATIONAL_B_SPLINE_SURFACE ( (
 ( 1.000000000000000000, 1.000000000000000000),
 ( 0.9952954269826590483, 0.8620686068821307169),
 ( 0.9952954269826590483, 0.8620686068821307169),
 ( 1.000000000000000000, 1.000000000000000000) ) ) 
 REPRESENTATION_ITEM ( '' )  SURFACE ( )  );
#57982=CARTESIAN_POINT ( 'NONE',  ( 0.5817216825391120505, -1.111896124582260059, 46.88281816631330656 ) ) ;
#57988=CARTESIAN_POINT ( 'NONE',  ( 0.9790724872846784388, -1.440786257245086910, 41.88387929672208543 ) ) ;
#57991=EDGE_CURVE ( 'NONE', #58158, #2726, #2835, .T. ) ;
#57998=ORIENTED_EDGE ( 'NONE', *, *, #57991, .F. ) ;
#57999=CARTESIAN_POINT ( 'NONE',  ( 0.9754292580325134576, -41.84984047986578304, 2.217728277718696184 ) ) ;
#58008=ORIENTED_EDGE ( 'NONE', *, *, #7949, .T. ) ;
#58026=CARTESIAN_POINT ( 'NONE',  ( 5.895596859100789899, 19.70914391261472076, -4.009716878325650491 ) ) ;
#58027=CARTESIAN_POINT ( 'NONE',  ( 3.782542959838393948, -41.50498340838394995, 6.676391665139376208 ) ) ;
#58033=CARTESIAN_POINT ( 'NONE',  ( 0.7764139734771210444, -35.37865056912503547, 30.79596653483400104 ) ) ;
#58039=DIRECTION ( 'NONE',  ( -0.07906939808003034253, 0.8617947135858000651, 0.5010567851280235407 ) ) ;
#58055=CARTESIAN_POINT ( 'NONE',  ( 5.896278296736517710, -15.78116101695068174, -12.46923961480650078 ) ) ;
#58058=CARTESIAN_POINT ( 'NONE',  ( 4.962356264823608143, 0.000000000000000000, 0.000000000000000000 ) ) ;
#58064=CARTESIAN_POINT ( 'NONE',  ( 3.238018933889920792, 13.23534742317150581, 2.057442819521426269 ) ) ;
#58067=VERTEX_POINT ( 'NONE', #27348 ) ;
#58069=CARTESIAN_POINT ( 'NONE',  ( 2.618530812446111078, -46.32565728282600759, 7.978738403554195280 ) ) ;
#58075=CARTESIAN_POINT ( 'NONE',  ( 0.5837799406558235038, -45.93814528060081415, 9.430289378148106749 ) ) ;
#58085=CARTESIAN_POINT ( 'NONE',  ( 0.9784957157296374497, -41.11458178947570019, -8.119373206651246733 ) ) ;
#58092=VERTEX_POINT ( 'NONE', #42097 ) ;
#58099=CARTESIAN_POINT ( 'NONE',  ( 0.5837157313716048179, 46.48964020809164310, -6.160390970077251893 ) ) ;
#58103=AXIS2_PLACEMENT_3D ( 'NONE', #23720, #42848, #19042 ) ;
#58104=CARTESIAN_POINT ( 'NONE',  ( 0.6845945791218034371, 28.51769667890559035, -37.24442907125682467 ) ) ;
#58113=CARTESIAN_POINT ( 'NONE',  ( 0.8560838555295158248, -44.00447048317951726, -16.24744323198929052 ) ) ;
#58116=CARTESIAN_POINT ( 'NONE',  ( 5.894904586330512508, 14.91761050190844529, 13.49052663816329911 ) ) ;
#58123=ORIENTED_EDGE ( 'NONE', *, *, #30455, .F. ) ;
#58124=DIRECTION ( 'NONE',  ( 0.000000000000000000, 0.000000000000000000, 1.000000000000000000 ) ) ;
#58126=DIRECTION ( 'NONE',  ( 0.07500201931887537365, 0.9744221909196634224, 0.2118397765798812338 ) ) ;
#58130=CARTESIAN_POINT ( 'NONE',  ( 0.9754292589017228288, 32.52564062645490850, -26.42745104496430031 ) ) ;
#58145=EDGE_CURVE ( 'NONE', #41543, #54380, #10362, .T. ) ;
#58152=EDGE_CURVE ( 'NONE', #61119, #19166, #25208, .T. ) ;
#58153=EDGE_LOOP ( 'NONE', ( #56772, #39482, #29814, #17038 ) ) ;
#58158=VERTEX_POINT ( 'NONE', #26973 ) ;
#58159=CARTESIAN_POINT ( 'NONE',  ( 0.5835871038041859915, 43.12129413706150416, 18.43335142741340960 ) ) ;
#58160=CARTESIAN_POINT ( 'NONE',  ( 0.5832655196449144652, -25.04173839001305524, -39.65030291661683748 ) ) ;
#58168=CARTESIAN_POINT ( 'NONE',  ( 2.618530812446111078, -43.92476656374593347, -16.74340680741610754 ) ) ;
#58169=CARTESIAN_POINT ( 'NONE',  ( 3.661921753701999016, 44.00646358689169801, 16.61512222072446932 ) ) ;
#58171=CARTESIAN_POINT ( 'NONE',  ( 4.962356264823597485, -14.71877352713633158, 39.42833123173257803 ) ) ;
#58176=ADVANCED_FACE ( 'NONE', ( #26657 ), #54335, .F. ) ;
#58177=ORIENTED_EDGE ( 'NONE', *, *, #60509, .T. ) ;
#58178=CARTESIAN_POINT ( 'NONE',  ( 0.5806925824938499181, 45.37089516811292356, -11.86188155343291584 ) ) ;
#58179=ORIENTED_EDGE ( 'NONE', *, *, #14603, .F. ) ;
#58184=CARTESIAN_POINT ( 'NONE',  ( 0.9784957157296378938, 35.93906772232310942, -21.55728341518576130 ) ) ;
#58185=EDGE_CURVE ( 'NONE', #26927, #21652, #29499, .T. ) ;
#58186=CARTESIAN_POINT ( 'NONE',  ( 5.838029081930957709, -45.56116631979244147, -12.45974244248782092 ) ) ;
#58189=EDGE_CURVE ( 'NONE', #49383, #39735, #50762, .T. ) ;
#58192=ORIENTED_EDGE ( 'NONE', *, *, #13006, .T. ) ;
#58194=AXIS2_PLACEMENT_3D ( 'NONE', #6778, #54709, #55635 ) ;
#58199=CARTESIAN_POINT ( 'NONE',  ( 5.838029081930955932, 14.01343897760574997, -45.10752250095143268 ) ) ;
#58203=VERTEX_POINT ( 'NONE', #21345 ) ;
#58205=CARTESIAN_POINT ( 'NONE',  ( 4.956445790444002242, -40.23882117934093827, 24.46171131046763136 ) ) ;
#58208=CARTESIAN_POINT ( 'NONE',  ( 3.661921753702030546, 39.48008016587397861, -25.57253202031822070 ) ) ;
#58216=CARTESIAN_POINT ( 'NONE',  ( 0.8554163680231708922, -6.900908941296512999, -46.40671211038068122 ) ) ;
#58219=CARTESIAN_POINT ( 'NONE',  ( 1.231276596079881047, 24.17959027891106416, 34.24360064248583768 ) ) ;
#58223=ORIENTED_EDGE ( 'NONE', *, *, #42197, .F. ) ;
#58227=CARTESIAN_POINT ( 'NONE',  ( 5.896782393890504181, 10.82771479451295349, -16.94953330350713117 ) ) ;
#58231=CARTESIAN_POINT ( 'NONE',  ( 3.661933894777889886, 6.578080033563746376, -46.57638916901656501 ) ) ;
#58239=VERTEX_POINT ( 'NONE', #1911 ) ;
#58240=CARTESIAN_POINT ( 'NONE',  ( 0.5782707292762423457, -19.08336439318405198, 42.84345407579288434 ) ) ;
#58241=ORIENTED_EDGE ( 'NONE', *, *, #31292, .T. ) ;
#58251=CARTESIAN_POINT ( 'NONE',  ( 0.5837157313716013762, 32.66713943747937066, -33.64662040315945291 ) ) ;
#58258=CARTESIAN_POINT ( 'NONE',  ( 0.5830081025819954244, -46.80869951554823416, -2.859665023277694118 ) ) ;
#58259=B_SPLINE_CURVE_WITH_KNOTS ( 'NONE', 3,
 ( #37646, #23217, #56709, #13836, #32940, #5006 ),
 .UNSPECIFIED., .F., .F.,
 ( 4, 2, 4 ),
 ( 8.770652787438942800E-18, 0.0002448709889506563977, 0.0004897419779013040134 ),
 .UNSPECIFIED. ) ;
#58263=CARTESIAN_POINT ( 'NONE',  ( 0.9789233960466683371, 40.45416489533057813, -10.94519389749430793 ) ) ;
#58265=CARTESIAN_POINT ( 'NONE',  ( 0.9783242366443549720, -12.16018745800449530, -40.10566457737252932 ) ) ;
#58272=CARTESIAN_POINT ( 'NONE',  ( 0.9780303403264778428, 41.49037090854766774, -5.906668711399428950 ) ) ;
#58273=VECTOR ( 'NONE', #40860, 1000.000000000000227 ) ;
#58284=CIRCLE ( 'NONE', #37317, 42.08604991992415023 ) ;
#58287=CARTESIAN_POINT ( 'NONE',  ( 0.5782707292762423457, -46.83939014838220771, -2.409955235114225047 ) ) ;
#58288=VERTEX_POINT ( 'NONE', #23492 ) ;
#58290=CARTESIAN_POINT ( 'NONE',  ( 0.9762797500689124330, -1.905951756780688733, 41.86516610604248712 ) ) ;
#58297=B_SPLINE_CURVE_WITH_KNOTS ( 'NONE', 3,
 ( #18256, #23871, #42382, #52054, #40, #13249, #13873, #47366, #4415, #23554, #42684, #61744, #52357, #8844, #41770, #4116 ),
 .UNSPECIFIED., .F., .F.,
 ( 4, 3, 3, 3, 3, 4 ),
 ( 1.250973872328959318E-17, 0.0002732102107931896201, 0.0004098135523333814798, 0.0005464168938824958896, 0.0008195847345945368300, 0.001092771384553101145 ),
 .UNSPECIFIED. ) ;
#58303=CARTESIAN_POINT ( 'NONE',  ( 1.231276596079881047, -16.87422718933157739, -38.37365278131454005 ) ) ;
#58309=ORIENTED_EDGE ( 'NONE', *, *, #31443, .F. ) ;
#58310=CARTESIAN_POINT ( 'NONE',  ( 1.157644175074336035, -34.08380111710984295, -24.39870441003963109 ) ) ;
#58313=EDGE_CURVE ( 'NONE', #58239, #48392, #21565, .T. ) ;
#58327=CARTESIAN_POINT ( 'NONE',  ( 1.231276596079881935, -41.24008908601427237, 7.518764738683684001 ) ) ;
#58337=CARTESIAN_POINT ( 'NONE',  ( 0.9789233960466714457, 15.18494337330411525, -39.06090400364393389 ) ) ;
#58363=CARTESIAN_POINT ( 'NONE',  ( 5.894904586330512508, -19.93329511855185032, -2.682006297225941083 ) ) ;
#58364=CARTESIAN_POINT ( 'NONE',  ( 1.091591847532195958, -27.65185104877846811, 31.49816065315580360 ) ) ;
#58366=ORIENTED_EDGE ( 'NONE', *, *, #51466, .T. ) ;
#58367=ORIENTED_EDGE ( 'NONE', *, *, #21729, .F. ) ;
#58373=ORIENTED_EDGE ( 'NONE', *, *, #24339, .F. ) ;
#58381=EDGE_LOOP ( 'NONE', ( #21689, #42405, #12053, #35900 ) ) ;
#58384=CARTESIAN_POINT ( 'NONE',  ( 1.092182651088186907, 36.45430330288407816, 20.68441333815433225 ) ) ;
#58387=CARTESIAN_POINT ( 'NONE',  ( 0.9762797500689124330, -41.16654106227468901, -7.851158013551661874 ) ) ;
#58403=CARTESIAN_POINT ( 'NONE',  ( 0.5824935313925976299, 46.42765273256021175, -6.611447556974842321 ) ) ;
#58404=CARTESIAN_POINT ( 'NONE',  ( 5.895881250540457863, 0.6675221664549164657, -20.10179334700245946 ) ) ;
#58407=CARTESIAN_POINT ( 'NONE',  ( 4.956445790443988031, 0.000000000000000000, 0.000000000000000000 ) ) ;
#58419=VECTOR ( 'NONE', #33274, 1000.000000000000114 ) ;
#58427=CARTESIAN_POINT ( 'NONE',  ( 0.9762797500689124330, 41.46413394121034912, 6.086902470967687329 ) ) ;
#58428=CARTESIAN_POINT ( 'NONE',  ( 0.5817216825391117174, 27.44988809114352790, -38.02286938134937344 ) ) ;
#58430=CARTESIAN_POINT ( 'NONE',  ( 4.956445790443988031, 46.94638516972315756, 3.684422564749393558 ) ) ;
#58431=CARTESIAN_POINT ( 'NONE',  ( 4.956445790444027999, 24.88142650099568698, -39.98065363916886383 ) ) ;
#58436=CARTESIAN_POINT ( 'NONE',  ( 5.917102823773431552, -9.657882276496579266, -17.64128759430771609 ) ) ;
#58439=CARTESIAN_POINT ( 'NONE',  ( 0.9791128995231621612, 29.13092919009531911, -30.12849811669700273 ) ) ;
#58440=FACE_OUTER_BOUND ( 'NONE', #46976, .T. ) ;
#58452=ORIENTED_EDGE ( 'NONE', *, *, #21824, .F. ) ;
#58458=DIRECTION ( 'NONE',  ( 0.07500201931887538753, -0.7908860163360090789, 0.6073499866322951135 ) ) ;
#58463=VERTEX_POINT ( 'NONE', #28124 ) ;
#58464=EDGE_CURVE ( 'NONE', #6747, #14, #29759, .T. ) ;
#58468=CARTESIAN_POINT ( 'NONE',  ( 0.5824935313925921898, -34.53515692764811007, 31.72634730057278318 ) ) ;
#58471=CARTESIAN_POINT ( 'NONE',  ( 5.901463166500146684, -20.11262442202718148, 0.01446371710612135916 ) ) ;
#58472=DIRECTION ( 'NONE',  ( -1.000000000000000000, -0.000000000000000000, -0.000000000000000000 ) ) ;
#58484=CARTESIAN_POINT ( 'NONE',  ( 5.896782393890504181, 8.460428369634545476, -18.24684188237228000 ) ) ;
#58491=ADVANCED_FACE ( 'NONE', ( #55685 ), #50333, .F. ) ;
#58492=ORIENTED_EDGE ( 'NONE', *, *, #40198, .F. ) ;
#58493=ORIENTED_EDGE ( 'NONE', *, *, #40293, .F. ) ;
#58494=CARTESIAN_POINT ( 'NONE',  ( 0.9787464366903563251, -30.96259958820174418, -28.24272330408581055 ) ) ;
#58499=CARTESIAN_POINT ( 'NONE',  ( 0.9791128995231607179, -27.06130672311420682, -32.00036113364502910 ) ) ;
#58503=CARTESIAN_POINT ( 'NONE',  ( 1.157644175074339143, -40.90424016553281206, -9.156714037229400915 ) ) ;
#58508=VECTOR ( 'NONE', #6453, 1000.000000000000227 ) ;
#58509=DIRECTION ( 'NONE',  ( 1.000000000000000000, -0.000000000000000000, -0.000000000000000000 ) ) ;
#58516=( BOUNDED_SURFACE ( )  B_SPLINE_SURFACE ( 3, 1, ( 
 ( #16912, #45420 ),
 ( #55396, #29208 ),
 ( #34544, #53609 ),
 ( #49788, #60105 ) ),
 .UNSPECIFIED., .F., .F., .F. ) 
 B_SPLINE_SURFACE_WITH_KNOTS ( ( 4, 4 ),
 ( 2, 2 ),
 ( 0.000000000000000000, 1.000000000000000000 ),
 ( 0.000000000000000000, 1.000000000000000000 ),
 .UNSPECIFIED. ) 
 GEOMETRIC_REPRESENTATION_ITEM ( )  RATIONAL_B_SPLINE_SURFACE ( (
 ( 1.000000000000000000, 1.000000000000000000),
 ( 0.7282232189291693025, 0.9929344683865674037),
 ( 0.7282232189291693025, 0.9929344683865674037),
 ( 1.000000000000000000, 1.000000000000000000) ) ) 
 REPRESENTATION_ITEM ( '' )  SURFACE ( )  );
#58517=CARTESIAN_POINT ( 'NONE',  ( 5.895596859100789899, 17.95274561709314654, -9.067916410092799140 ) ) ;
#58525=CARTESIAN_POINT ( 'NONE',  ( 2.528190830796656741, -39.24301646210592764, -14.90770925085041299 ) ) ;
#58533=ADVANCED_FACE ( 'NONE', ( #5453 ), #56730, .F. ) ;
#58536=CARTESIAN_POINT ( 'NONE',  ( 4.956445790444001354, -33.12351118015997997, 33.47194433010209025 ) ) ;
#58540=CARTESIAN_POINT ( 'NONE',  ( 0.5806925824938494740, -35.14454992382308518, -31.04968555389040219 ) ) ;
#58542=AXIS2_PLACEMENT_3D ( 'NONE', #12069, #49322, #20521 ) ;
#58543=CARTESIAN_POINT ( 'NONE',  ( 1.231276596079887264, 15.85305549123172320, 38.80666698661448777 ) ) ;
#58553=CARTESIAN_POINT ( 'NONE',  ( 5.896782393890504181, 8.471952691971306848, -18.24149403045190354 ) ) ;
#58556=CARTESIAN_POINT ( 'NONE',  ( 0.9772918015221170318, 19.77570429987702383, -36.94940290714458797 ) ) ;
#58559=CARTESIAN_POINT ( 'NONE',  ( 5.895596859100789899, 16.58392706178506160, 11.37987462241481929 ) ) ;
#58563=ORIENTED_EDGE ( 'NONE', *, *, #24771, .T. ) ;
#58569=CARTESIAN_POINT ( 'NONE',  ( 2.528100132419517365, -2.611617288031734319, -41.89789056471614970 ) ) ;
#58574=DIRECTION ( 'NONE',  ( -0.07906939808003032866, -0.8933371237229992268, -0.4423763258421279931 ) ) ;
#58576=CARTESIAN_POINT ( 'NONE',  ( 0.9772918015221170318, -22.89893354421215221, -35.09951136822897411 ) ) ;
#58577=ORIENTED_EDGE ( 'NONE', *, *, #13530, .F. ) ;
#58581=CARTESIAN_POINT ( 'NONE',  ( 0.9762797500689124330, 41.59901070109202692, -5.084003725031680077 ) ) ;
#58590=CARTESIAN_POINT ( 'NONE',  ( 2.618530812446111078, 33.67725335819547894, -32.79587467115508304 ) ) ;
#58591=B_SPLINE_CURVE_WITH_KNOTS ( 'NONE', 3,
 ( #45542, #35836, #11397, #30479, #49593, #12336, #31112, #22034, #31425, #41157, #31739, #7280, #59607, #50829, #21715, #21408, #40244, #7922, #36147 ),
 .UNSPECIFIED., .F., .F.,
 ( 4, 3, 3, 3, 3, 3, 4 ),
 ( 1.250973872328959318E-17, 0.0002732106629380534873, 0.0004098138914053662705, 0.0005464171197651318361, 0.0006830203481512379850, 0.0008196235766963388047, 0.001011968216111141161 ),
 .UNSPECIFIED. ) ;
#58592=CARTESIAN_POINT ( 'NONE',  ( 0.5817217712918323347, -2.022005932317454846, 46.85238997124955773 ) ) ;
#58594=ADVANCED_FACE ( 'NONE', ( #1368 ), #31569, .T. ) ;
#58603=EDGE_CURVE ( 'NONE', #45260, #13746, #31444, .T. ) ;
#58611=ORIENTED_EDGE ( 'NONE', *, *, #15506, .F. ) ;
#58615=ORIENTED_EDGE ( 'NONE', *, *, #29281, .T. ) ;
#58626=ORIENTED_EDGE ( 'NONE', *, *, #12762, .F. ) ;
#58627=CARTESIAN_POINT ( 'NONE',  ( 0.8554163680231720024, 23.34472558242442730, 40.69679668712412735 ) ) ;
#58629=CARTESIAN_POINT ( 'NONE',  ( 0.5804410086790514622, 16.34485605153925647, 43.95867983128994183 ) ) ;
#58630=CARTESIAN_POINT ( 'NONE',  ( 4.291220156522059348, 13.00516750528174015, -45.27973736082466871 ) ) ;
#58638=EDGE_CURVE ( 'NONE', #35188, #44257, #11812, .T. ) ;
#58643=CARTESIAN_POINT ( 'NONE',  ( 4.291220156522059348, -47.09990378333908012, 0.9940125280386750140 ) ) ;
#58648=CARTESIAN_POINT ( 'NONE',  ( 0.9762797500689124330, -39.75277516423506086, -13.26806888463731227 ) ) ;
#58650=ADVANCED_FACE ( 'NONE', ( #27360 ), #7511, .F. ) ;
#58652=CARTESIAN_POINT ( 'NONE',  ( 4.958415959904818315, 7.056061540673139731, -44.87110372340841025 ) ) ;
#58658=B_SPLINE_CURVE_WITH_KNOTS ( 'NONE', 3,
 ( #2049, #21181, #50296, #55914 ),
 .UNSPECIFIED., .F., .F.,
 ( 4, 4 ),
 ( 0.000000000000000000, 0.004041751736740998614 ),
 .UNSPECIFIED. ) ;
#58666=CARTESIAN_POINT ( 'NONE',  ( 4.956445790444002242, -40.23882117934093827, 24.46171131046763136 ) ) ;
#58668=CARTESIAN_POINT ( 'NONE',  ( 4.960386119450148179, -16.16390115411144279, 40.65912891531809237 ) ) ;
#58669=EDGE_CURVE ( 'NONE', #217, #30940, #29645, .T. ) ;
#58671=CARTESIAN_POINT ( 'NONE',  ( 5.895596859100789899, -19.93390588528919949, -2.677233529022096992 ) ) ;
#58680=EDGE_CURVE ( 'NONE', #35032, #40451, #40885, .T. ) ;
#58682=ORIENTED_EDGE ( 'NONE', *, *, #3806, .F. ) ;
#58686=B_SPLINE_CURVE_WITH_KNOTS ( 'NONE', 3,
 ( #30843, #20840, #39980, #59031 ),
 .UNSPECIFIED., .F., .F.,
 ( 4, 4 ),
 ( 4.443059973708341306E-17, 0.005004948556313864282 ),
 .UNSPECIFIED. ) ;
#58688=VERTEX_POINT ( 'NONE', #36474 ) ;
#58694=CARTESIAN_POINT ( 'NONE',  ( 5.895596859100789899, -2.009647457886758914, -20.01223376606161963 ) ) ;
#58695=B_SPLINE_CURVE_WITH_KNOTS ( 'NONE', 3,
 ( #18865, #24781, #43924, #32963 ),
 .UNSPECIFIED., .F., .F.,
 ( 4, 4 ),
 ( 0.000000000000000000, 0.005004948556313801832 ),
 .UNSPECIFIED. ) ;
#58699=ORIENTED_EDGE ( 'NONE', *, *, #26112, .F. ) ;
#58707=FACE_OUTER_BOUND ( 'NONE', #14612, .T. ) ;
#58709=CARTESIAN_POINT ( 'NONE',  ( 0.5834584762367726052, -14.06796895289726557, 44.73620724372500490 ) ) ;
#58710=CARTESIAN_POINT ( 'NONE',  ( 0.8560838555295223751, 46.35895890951135812, -7.156798369939577853 ) ) ;
#58711=CARTESIAN_POINT ( 'NONE',  ( 4.958415959904820092, -15.85236509608376565, -42.56649474273287126 ) ) ;
#58712=CARTESIAN_POINT ( 'NONE',  ( 5.838029081930955932, 44.62720369181031543, -15.47506862028700070 ) ) ;
#58714=VERTEX_POINT ( 'NONE', #4441 ) ;
#58717=CARTESIAN_POINT ( 'NONE',  ( 4.291220156522059348, -27.13845918422061843, 38.50835013879571278 ) ) ;
#58719=DIRECTION ( 'NONE',  ( -1.000000000000000000, -0.000000000000000000, -0.000000000000000000 ) ) ;
#58728=CARTESIAN_POINT ( 'NONE',  ( 2.618530812446111078, 18.20180174657095407, -43.34075682745660885 ) ) ;
#58731=( BOUNDED_SURFACE ( )  B_SPLINE_SURFACE ( 3, 1, ( 
 ( #47871, #4920 ),
 ( #213, #57532 ),
 ( #14669, #33780 ),
 ( #52859, #9960 ) ),
 .UNSPECIFIED., .F., .F., .F. ) 
 B_SPLINE_SURFACE_WITH_KNOTS ( ( 4, 4 ),
 ( 2, 2 ),
 ( 0.000000000000000000, 1.000000000000000000 ),
 ( 0.000000000000000000, 1.000000000000000000 ),
 .UNSPECIFIED. ) 
 GEOMETRIC_REPRESENTATION_ITEM ( )  RATIONAL_B_SPLINE_SURFACE ( (
 ( 1.000000000000000000, 1.000000000000000000),
 ( 0.7282232189291693025, 0.9929344683865674037),
 ( 0.7282232189291693025, 0.9929344683865674037),
 ( 1.000000000000000000, 1.000000000000000000) ) ) 
 REPRESENTATION_ITEM ( '' )  SURFACE ( )  );
#58748=CARTESIAN_POINT ( 'NONE',  ( 0.9787464366903556590, 29.26156609637415684, -30.00157899974586329 ) ) ;
#58749=CARTESIAN_POINT ( 'NONE',  ( 0.5797568665920711517, -29.79412142207816672, 36.21512994990259671 ) ) ;
#58750=EDGE_LOOP ( 'NONE', ( #52091, #4206, #27067, #6049, #44208, #31960, #59785, #34869, #6458, #47561, #54934, #8173, #59822, #13515, #52577, #54876, #53122, #44562, #39111, #9113, #5998, #54181, #24429, #43473, #46240, #30120, #14295, #21307, #3131, #33640, #31591, #52495, #10502, #3636, #4941, #33691, #44202, #9493, #45445, #38409, #33872, #39829, #58615, #56333, #49795, #47293, #50179, #19050, #52951, #24327, #32318, #52955, #48391, #19029, #45818, #37204, #25068, #12476, #33198, #3411, #51404, #41176, #42117, #21583, #13277, #25151, #33025, #2853, #38391, #49680, #33327, #34627, #44567, #60569, #16113, #16070, #55241, #56792, #14514, #52002, #35710, #29439, #54186, #6357, #4741, #3082, #39374, #55312, #26500, #32019, #38512, #5826, #30440, #26659, #46877, #16380, #25832, #33102, #45878, #22350, #28032, #48196, #54672, #3682, #17309, #53031, #44433, #39876, #18452, #21506, #33727, #42101, #29617, #44975, #3416, #53846, #57669, #31644, #7826, #2088, #51932, #50878, #9245, #12860, #24659, #2883, #43918, #4789, #23210, #27274, #19819, #34740, #7887, #56014, #25061, #41033, #45018, #12978, #11367, #26330, #14467, #8544, #38906, #47275, #27823, #33650 ) ) ;
#58754=CARTESIAN_POINT ( 'NONE',  ( 5.894904586330512508, -9.664823957841555568, 17.63861077085082485 ) ) ;
#58759=EDGE_CURVE ( 'NONE', #3997, #26672, #4527, .T. ) ;
#58761=VERTEX_POINT ( 'NONE', #56770 ) ;
#58762=CARTESIAN_POINT ( 'NONE',  ( 2.528100132419517809, 30.04137667667142964, 29.32182576174984234 ) ) ;
#58770=CARTESIAN_POINT ( 'NONE',  ( 4.962356264823591268, 23.01169039590626753, 35.23773124060775785 ) ) ;
#58775=CARTESIAN_POINT ( 'NONE',  ( 0.5837799406558231707, -34.71942033614858047, 31.52467923863832411 ) ) ;
#58777=AXIS2_PLACEMENT_3D ( 'NONE', #54256, #21083, #25461 ) ;
#58785=ORIENTED_EDGE ( 'NONE', *, *, #42614, .T. ) ;
#58790=CARTESIAN_POINT ( 'NONE',  ( 4.958415959904820092, 8.053194174018676321, 44.70290837762335912 ) ) ;
#58792=CARTESIAN_POINT ( 'NONE',  ( 0.9772918015221174759, 4.607494702701409928, 41.65462577331908278 ) ) ;
#58799=ORIENTED_EDGE ( 'NONE', *, *, #60511, .F. ) ;
#58805=B_SPLINE_CURVE_WITH_KNOTS ( 'NONE', 3,
 ( #56582, #32487, #9585, #56884 ),
 .UNSPECIFIED., .F., .F.,
 ( 4, 4 ),
 ( 1.517883041479706208E-18, 0.004041751736740996880 ),
 .UNSPECIFIED. ) ;
#58807=B_SPLINE_CURVE_WITH_KNOTS ( 'NONE', 3,
 ( #11507, #35325, #30592, #35019, #7391, #49398 ),
 .UNSPECIFIED., .F., .F.,
 ( 4, 2, 4 ),
 ( 1.215487348918874797E-16, 0.0002448718616795927711, 0.0004897437233590640031 ),
 .UNSPECIFIED. ) ;
#58808=EDGE_LOOP ( 'NONE', ( #57702, #47579, #59004, #17769 ) ) ;
#58814=FACE_OUTER_BOUND ( 'NONE', #48487, .T. ) ;
#58821=VECTOR ( 'NONE', #1208, 999.9999999999998863 ) ;
#58822=CARTESIAN_POINT ( 'NONE',  ( 0.5837799406558232818, 36.86040723981035683, 28.99230807804954679 ) ) ;
#58823=CARTESIAN_POINT ( 'NONE',  ( 0.5804410086790514622, 4.150428748651738609, 46.71502748642841851 ) ) ;
#58827=CARTESIAN_POINT ( 'NONE',  ( 4.956445790443988031, 0.000000000000000000, 0.000000000000000000 ) ) ;
#58829=CARTESIAN_POINT ( 'NONE',  ( 5.838029081930957709, -16.99499549701665657, -44.07079743105749259 ) ) ;
#58832=CARTESIAN_POINT ( 'NONE',  ( 0.9762797500689124330, 9.222352665238359393, 40.88120590813919364 ) ) ;
#58849=ORIENTED_EDGE ( 'NONE', *, *, #18718, .T. ) ;
#58851=CARTESIAN_POINT ( 'NONE',  ( 0.5804410086790514622, 10.33990028284761209, 45.74501408892737686 ) ) ;
#58853=B_SPLINE_CURVE_WITH_KNOTS ( 'NONE', 3,
 ( #3426, #22561, #41685, #60747, #17868, #42605, #18476, #61667, #36993, #18174, #30023, #10942, #29100, #47916, #29404, #39452 ),
 .UNSPECIFIED., .F., .F.,
 ( 4, 3, 3, 3, 3, 4 ),
 ( 1.551621725782133898E-17, 0.0002732102107931892406, 0.0004098135523333850034, 0.0005464168938824949138, 0.0008195847345945449615, 0.001092771384553106349 ),
 .UNSPECIFIED. ) ;
#58855=ORIENTED_EDGE ( 'NONE', *, *, #57317, .T. ) ;
#58863=VECTOR ( 'NONE', #35581, 1000.000000000000114 ) ;
#58865=CARTESIAN_POINT ( 'NONE',  ( 4.962356264823608143, 0.000000000000000000, 0.000000000000000000 ) ) ;
#58872=CARTESIAN_POINT ( 'NONE',  ( 0.9762797500689124330, 20.58271139965541963, -36.50584578699964311 ) ) ;
#58874=VERTEX_POINT ( 'NONE', #20428 ) ;
#58881=ORIENTED_EDGE ( 'NONE', *, *, #58638, .F. ) ;
#58884=ORIENTED_EDGE ( 'NONE', *, *, #15356, .F. ) ;
#58887=ORIENTED_EDGE ( 'NONE', *, *, #59980, .F. ) ;
#58903=CARTESIAN_POINT ( 'NONE',  ( 0.9785694773339257413, 41.56380497646738803, -5.365214030479795504 ) ) ;
#58907=CARTESIAN_POINT ( 'NONE',  ( 1.231276596079887264, -11.60895935156443848, 40.28037777618019533 ) ) ;
#58908=CARTESIAN_POINT ( 'NONE',  ( 0.8560838555295158248, 43.53454501559585310, -17.46757637357826454 ) ) ;
#58912=CARTESIAN_POINT ( 'NONE',  ( 4.291220156522059348, 41.58924158504531476, -22.12970812474565108 ) ) ;
#58915=B_SPLINE_CURVE_WITH_KNOTS ( 'NONE', 3,
 ( #14412, #5886, #10014, #52910, #33212, #4971 ),
 .UNSPECIFIED., .F., .F.,
 ( 4, 2, 4 ),
 ( 1.738108305489988542E-18, 0.0002291459268755710208, 0.0004582918537511403070 ),
 .UNSPECIFIED. ) ;
#58916=CARTESIAN_POINT ( 'NONE',  ( 5.895596859100789899, 5.962379729972213660, -19.20880556328539512 ) ) ;
#58921=ORIENTED_EDGE ( 'NONE', *, *, #48651, .T. ) ;
#58924=CARTESIAN_POINT ( 'NONE',  ( 3.661921753702003457, -36.12137287706547539, -30.13100637731890785 ) ) ;
#58929=ADVANCED_FACE ( 'NONE', ( #35470 ), #20347, .F. ) ;
#58940=ORIENTED_EDGE ( 'NONE', *, *, #35384, .F. ) ;
#58946=ORIENTED_EDGE ( 'NONE', *, *, #15871, .F. ) ;
#58949=DIRECTION ( 'NONE',  ( -0.07906939808003035641, -0.04137963570463473045, -0.9960099176394847653 ) ) ;
#58953=CARTESIAN_POINT ( 'NONE',  ( 1.231276596079881935, -37.02495017545860634, -19.65781868679418309 ) ) ;
#58954=CARTESIAN_POINT ( 'NONE',  ( 5.917102823773431552, -4.653982686480137687, 19.56604618224349679 ) ) ;
#58958=CARTESIAN_POINT ( 'NONE',  ( 4.956445790444004018, -46.73954499432459642, -5.740468958468717631 ) ) ;
#58959=EDGE_CURVE ( 'NONE', #1414, #40743, #9445, .T. ) ;
#58971=VERTEX_POINT ( 'NONE', #47321 ) ;
#58975=CARTESIAN_POINT ( 'NONE',  ( 0.8560838555295223751, 3.785103201470721768, -46.75516899590834186 ) ) ;
#58976=CARTESIAN_POINT ( 'NONE',  ( 2.282816707992322058, 36.03600438247134008, -30.13143465808543553 ) ) ;
#58981=CARTESIAN_POINT ( 'NONE',  ( 4.956445790444040433, 44.65954324082233029, -14.93530206124928128 ) ) ;
#58984=LINE ( 'NONE', #25171, #27911 ) ;
#58988=LINE ( 'NONE', #30791, #12137 ) ;
#58990=CARTESIAN_POINT ( 'NONE',  ( 4.962356264823591268, 23.01169039590626753, 35.23773124060775785 ) ) ;
#58994=LINE ( 'NONE', #58064, #55199 ) ;
#58996=CARTESIAN_POINT ( 'NONE',  ( 3.782625744892855302, 37.99690091417294013, -17.98537252918400853 ) ) ;
#59002=CARTESIAN_POINT ( 'NONE',  ( 4.956445790444005794, -27.49627641100061837, -38.22947597953034204 ) ) ;
#59004=ORIENTED_EDGE ( 'NONE', *, *, #35384, .T. ) ;
#59008=ORIENTED_EDGE ( 'NONE', *, *, #18067, .F. ) ;
#59013=CARTESIAN_POINT ( 'NONE',  ( 0.5832655196449151314, -38.53372662657736925, -26.72802078795826830 ) ) ;
#59018=CARTESIAN_POINT ( 'NONE',  ( 3.376099380956838925, -7.596917057716860100, 11.04514530688653906 ) ) ;
#59026=CARTESIAN_POINT ( 'NONE',  ( 5.896278296736517710, 8.461230214158247165, -18.24649453668839172 ) ) ;
#59029=CARTESIAN_POINT ( 'NONE',  ( 0.5837799406558239479, 46.46543369090721853, -6.340900684690216060 ) ) ;
#59030=CARTESIAN_POINT ( 'NONE',  ( 3.661921753702033655, 46.33057357019549016, -8.130748827183058580 ) ) ;
#59031=CARTESIAN_POINT ( 'NONE',  ( 4.962356264823608143, -25.31392337492896161, 33.62202970123266965 ) ) ;
#59036=ORIENTED_EDGE ( 'NONE', *, *, #45144, .F. ) ;
#59043=CARTESIAN_POINT ( 'NONE',  ( 0.9762797500689124330, 36.31338395866826829, -20.92039508843077300 ) ) ;
#59044=B_SPLINE_CURVE_WITH_KNOTS ( 'NONE', 3,
 ( #14438, #53239, #9402, #33546 ),
 .UNSPECIFIED., .F., .F.,
 ( 4, 4 ),
 ( 4.234999717485957107E-17, 0.005004948556313839128 ),
 .UNSPECIFIED. ) ;
#59053=CARTESIAN_POINT ( 'NONE',  ( 0.9789889208857684988, 15.15199999899948935, 39.07367136669768115 ) ) ;
#59064=CARTESIAN_POINT ( 'NONE',  ( 4.291220156522060236, 24.50578158393188843, 40.23500548361242579 ) ) ;
#59066=CARTESIAN_POINT ( 'NONE',  ( 4.956445790443998689, -4.175462451062247560, 46.90526157542890218 ) ) ;
#59068=VERTEX_POINT ( 'NONE', #29129 ) ;
#59079=ORIENTED_EDGE ( 'NONE', *, *, #57749, .T. ) ;
#59090=VECTOR ( 'NONE', #35478, 1000.000000000000114 ) ;
#59094=B_SPLINE_CURVE_WITH_KNOTS ( 'NONE', 3,
 ( #37758, #14248, #47438, #24236, #19868, #10457 ),
 .UNSPECIFIED., .F., .F.,
 ( 4, 2, 4 ),
 ( 7.007167689862070887E-18, 0.0002448709889506557472, 0.0004897419779013045555 ),
 .UNSPECIFIED. ) ;
#59095=CARTESIAN_POINT ( 'NONE',  ( 0.5837800304671217910, -34.81104335575551545, 31.42337653186251600 ) ) ;
#59101=ORIENTED_EDGE ( 'NONE', *, *, #44581, .T. ) ;
#59107=ORIENTED_EDGE ( 'NONE', *, *, #16655, .F. ) ;
#59108=CARTESIAN_POINT ( 'NONE',  ( 0.9791128995231623833, 4.199954538575370044, 41.69769557325756182 ) ) ;
#59109=EDGE_CURVE ( 'NONE', #15825, #57224, #33446, .T. ) ;
#59111=CARTESIAN_POINT ( 'NONE',  ( 2.528190830796659405, -40.87987336052400167, -9.544112854557406322 ) ) ;
#59113=CARTESIAN_POINT ( 'NONE',  ( 0.8554163680231738898, -45.78608427674269166, -10.23913862172186917 ) ) ;
#59117=CARTESIAN_POINT ( 'NONE',  ( 0.8560838555295223751, -42.27062166135446120, -20.33635607586480631 ) ) ;
#59121=ORIENTED_EDGE ( 'NONE', *, *, #24811, .F. ) ;
#59122=DIRECTION ( 'NONE',  ( -1.000000000000000000, -0.000000000000000000, -0.000000000000000000 ) ) ;
#59126=CARTESIAN_POINT ( 'NONE',  ( 0.5817216825391123836, -30.62363842979834772, -35.51658375362750064 ) ) ;
#59127=CARTESIAN_POINT ( 'NONE',  ( 0.9790320750461890542, 38.54957592690705326, 16.43980925673472981 ) ) ;
#59129=CARTESIAN_POINT ( 'NONE',  ( 1.231276596079881047, -21.83837404314779462, -35.78214904347746739 ) ) ;
#59138=CARTESIAN_POINT ( 'NONE',  ( 2.282816707992322947, 39.73059989313451723, -25.05945726745943958 ) ) ;
#59147=CARTESIAN_POINT ( 'NONE',  ( 0.9788927965476029724, 9.853064299072418208, 40.73393838741991146 ) ) ;
#59148=B_SPLINE_CURVE_WITH_KNOTS ( 'NONE', 3,
 ( #34222, #24494, #43633, #33917, #39548, #15733 ),
 .UNSPECIFIED., .F., .F.,
 ( 4, 2, 4 ),
 ( 6.619851161367215630E-18, 0.0002291472222819930168, 0.0004582944445639794201 ),
 .UNSPECIFIED. ) ;
#59155=CARTESIAN_POINT ( 'NONE',  ( 0.5804410086790514622, 32.99440095574044562, -33.33000686209396690 ) ) ;
#59159=CARTESIAN_POINT ( 'NONE',  ( 1.000110580585050313, -0.7426652321698243853, -41.90305395940526267 ) ) ;
#59163=( BOUNDED_SURFACE ( )  B_SPLINE_SURFACE ( 3, 1, ( 
 ( #2943, #37115 ),
 ( #60256, #36490 ),
 ( #27692, #50869 ),
 ( #27071, #56184 ) ),
 .UNSPECIFIED., .F., .F., .F. ) 
 B_SPLINE_SURFACE_WITH_KNOTS ( ( 4, 4 ),
 ( 2, 2 ),
 ( 0.000000000000000000, 1.000000000000000000 ),
 ( 0.000000000000000000, 1.000000000000000000 ),
 .UNSPECIFIED. ) 
 GEOMETRIC_REPRESENTATION_ITEM ( )  RATIONAL_B_SPLINE_SURFACE ( (
 ( 1.000000000000000000, 1.000000000000000000),
 ( 0.9729067724841187204, 0.9999501103223794596),
 ( 0.9729067724841187204, 0.9999501103223794596),
 ( 1.000000000000000000, 1.000000000000000000) ) ) 
 REPRESENTATION_ITEM ( '' )  SURFACE ( )  );
#59164=CARTESIAN_POINT ( 'NONE',  ( 4.962356264823597485, -14.71877352713633158, 39.42833123173257803 ) ) ;
#59167=ADVANCED_FACE ( 'NONE', ( #289 ), #11570, .F. ) ;
#59168=CARTESIAN_POINT ( 'NONE',  ( 1.231276596079887264, 20.88402890667827450, 36.34740854095507245 ) ) ;
#59173=ORIENTED_EDGE ( 'NONE', *, *, #28172, .F. ) ;
#59179=FACE_OUTER_BOUND ( 'NONE', #33464, .T. ) ;
#59189=CARTESIAN_POINT ( 'NONE',  ( 0.5824935313925951874, 32.33894943514273734, -33.96219260420503616 ) ) ;
#59195=DIRECTION ( 'NONE',  ( 0.000000000000000000, 0.000000000000000000, 1.000000000000000000 ) ) ;
#59196=EDGE_CURVE ( 'NONE', #7974, #40686, #57517, .T. ) ;
#59199=CARTESIAN_POINT ( 'NONE',  ( 0.9762797500689124330, -22.97506929404158171, -35.04955029839458547 ) ) ;
#59207=ORIENTED_EDGE ( 'NONE', *, *, #30614, .T. ) ;
#59209=CARTESIAN_POINT ( 'NONE',  ( 0.9783242366443571925, 41.56959898774839246, -5.320049830998810236 ) ) ;
#59212=CARTESIAN_POINT ( 'NONE',  ( 5.910764540655178756, 17.94353875551737332, -9.084638429701483275 ) ) ;
#59214=DIRECTION ( 'NONE',  ( 0.000000000000000000, 0.000000000000000000, 1.000000000000000000 ) ) ;
#59216=CARTESIAN_POINT ( 'NONE',  ( 0.5806925824938499181, -30.69245420804209701, 35.45695442407318154 ) ) ;
#59231=EDGE_CURVE ( 'NONE', #37909, #15172, #23553, .T. ) ;
#59233=B_SPLINE_CURVE_WITH_KNOTS ( 'NONE', 3,
 ( #15446, #49881, #16364, #15759, #35181, #21376, #6939, #54238, #34555, #44281, #26072, #40507, #6306, #10437, #48956, #10749, #49558, #1941, #45210 ),
 .UNSPECIFIED., .F., .F.,
 ( 4, 3, 3, 3, 3, 3, 4 ),
 ( 9.813676791237319219E-18, 0.0002732106629380556557, 0.0004098138914053659453, 0.0005464171197651452802, 0.0006830203481512486102, 0.0008196235766963462857, 0.001011968216111144197 ),
 .UNSPECIFIED. ) ;
#59240=DIRECTION ( 'NONE',  ( -0.07500201931887527651, 0.4910262002617658550, 0.8679101150203188952 ) ) ;
#59247=CARTESIAN_POINT ( 'NONE',  ( 0.9780106845699478857, -17.35579871403585628, -38.14587130284626681 ) ) ;
#59248=VERTEX_POINT ( 'NONE', #41036 ) ;
#59249=CARTESIAN_POINT ( 'NONE',  ( 3.661933894777867238, 35.71932967730839437, 30.60654590696914212 ) ) ;
#59251=CARTESIAN_POINT ( 'NONE',  ( 0.5782707292762423457, 46.38083794024497308, -6.968086227103744257 ) ) ;
#59256=B_SPLINE_CURVE_WITH_KNOTS ( 'NONE', 3,
 ( #31534, #21834, #40971, #59723, #11840, #54702 ),
 .UNSPECIFIED., .F., .F.,
 ( 4, 2, 4 ),
 ( 8.805430561888389713E-18, 0.0002448709889506569940, 0.0004897419779013052060 ),
 .UNSPECIFIED. ) ;
#59259=CARTESIAN_POINT ( 'NONE',  ( 4.958415959904816539, 44.61026793747944197, 8.551488079213465099 ) ) ;
#59270=CARTESIAN_POINT ( 'NONE',  ( 0.8554163680231738898, -46.86440027434178290, 2.221139355847132624 ) ) ;
#59273=EDGE_LOOP ( 'NONE', ( #13286, #48386, #39013, #6841 ) ) ;
#59278=CARTESIAN_POINT ( 'NONE',  ( 4.956445790443996025, 13.43466403631381567, 45.13366650706556982 ) ) ;
#59279=EDGE_CURVE ( 'NONE', #50843, #13524, #10244, .T. ) ;
#59281=B_SPLINE_CURVE_WITH_KNOTS ( 'NONE', 3,
 ( #9909, #24936, #25228, #19941, #48123, #33416 ),
 .UNSPECIFIED., .F., .F.,
 ( 4, 2, 4 ),
 ( 1.179429090023230705E-16, 0.0002448718616795931505, 0.0004897437233590683399 ),
 .UNSPECIFIED. ) ;
#59285=CIRCLE ( 'NONE', #55304, 47.09074272231896430 ) ;
#59287=CARTESIAN_POINT ( 'NONE',  ( 0.5806925824938499181, -24.77160101449041463, -39.81946942793766198 ) ) ;
#59294=CARTESIAN_POINT ( 'NONE',  ( 0.6845945791218023269, -34.20288208893713744, 32.10248241996572460 ) ) ;
#59305=CARTESIAN_POINT ( 'NONE',  ( 3.238018933889920792, -8.435922058907914689, 10.40397574889925458 ) ) ;
#59308=VERTEX_POINT ( 'NONE', #35709 ) ;
#59315=VERTEX_POINT ( 'NONE', #60097 ) ;
#59324=VECTOR ( 'NONE', #46348, 1000.000000000000114 ) ;
#59337=CARTESIAN_POINT ( 'NONE',  ( 2.528100132419517365, 40.79053833512498528, 9.918959671395732869 ) ) ;
#59345=CARTESIAN_POINT ( 'NONE',  ( 0.5797568599927142019, -41.56795257228133522, -21.71015033618085255 ) ) ;
#59346=EDGE_LOOP ( 'NONE', ( #10620, #57109, #56319, #57857 ) ) ;
#59347=CARTESIAN_POINT ( 'NONE',  ( 1.092182651088186018, -41.76072632286304298, 3.578117022851349915 ) ) ;
#59356=ADVANCED_FACE ( 'NONE', ( #22514 ), #26744, .F. ) ;
#59369=CARTESIAN_POINT ( 'NONE',  ( 5.838029081930955932, -10.96929503790549809, 45.94278642533886625 ) ) ;
#59374=CARTESIAN_POINT ( 'NONE',  ( 0.8554163680231816613, 43.54276151446858734, 17.47092993535067507 ) ) ;
#59375=ORIENTED_EDGE ( 'NONE', *, *, #20277, .F. ) ;
#59378=B_SPLINE_CURVE_WITH_KNOTS ( 'NONE', 3,
 ( #36644, #55405, #49798, #55101, #21297, #59490 ),
 .UNSPECIFIED., .F., .F.,
 ( 4, 2, 4 ),
 ( 9.828040028768063295E-18, 0.0002291459268755722677, 0.0004582918537511346691 ),
 .UNSPECIFIED. ) ;
#59388=ADVANCED_FACE ( 'NONE', ( #55390 ), #21993, .F. ) ;
#59394=VECTOR ( 'NONE', #47367, 1000.000000000000227 ) ;
#59395=ORIENTED_EDGE ( 'NONE', *, *, #26544, .F. ) ;
#59399=ORIENTED_EDGE ( 'NONE', *, *, #24046, .F. ) ;
#59400=CARTESIAN_POINT ( 'NONE',  ( 2.282803330402964459, -29.31214732841990767, -36.70551629461151322 ) ) ;
#59408=CARTESIAN_POINT ( 'NONE',  ( 1.231276596079887264, -21.83837404314831332, 35.78214904347716185 ) ) ;
#59417=CARTESIAN_POINT ( 'NONE',  ( 5.896782393890504181, -7.222780579330470019, -18.77118876312469808 ) ) ;
#59418=ORIENTED_EDGE ( 'NONE', *, *, #31621, .T. ) ;
#59422=CARTESIAN_POINT ( 'NONE',  ( 0.9775691876210963471, 24.55423032742939071, 33.96208889361105321 ) ) ;
#59430=ORIENTED_EDGE ( 'NONE', *, *, #41401, .F. ) ;
#59433=CARTESIAN_POINT ( 'NONE',  ( 0.9780106845699492180, 38.70451287974908183, -16.07146319402109214 ) ) ;
#59436=CARTESIAN_POINT ( 'NONE',  ( 0.5817217712918331118, -29.92824280590621555, -36.10450438046610344 ) ) ;
#59441=ORIENTED_EDGE ( 'NONE', *, *, #44588, .T. ) ;
#59444=CARTESIAN_POINT ( 'NONE',  ( 4.291220156522059348, -40.01826627095215372, 24.85814478139649353 ) ) ;
#59445=CARTESIAN_POINT ( 'NONE',  ( 0.5835871038041864356, 45.19346916843720408, 12.52137362364909556 ) ) ;
#59447=CARTESIAN_POINT ( 'NONE',  ( 5.910764540655178756, 17.95751408178354680, 9.056982194512078976 ) ) ;
#59453=DIRECTION ( 'NONE',  ( 0.000000000000000000, 0.000000000000000000, 1.000000000000000000 ) ) ;
#59455=CARTESIAN_POINT ( 'NONE',  ( 2.618530812446111078, -9.204197330484477746, 46.09782576976600410 ) ) ;
#59460=VERTEX_POINT ( 'NONE', #27826 ) ;
#59467=ORIENTED_EDGE ( 'NONE', *, *, #27230, .T. ) ;
#59468=EDGE_CURVE ( 'NONE', #16352, #24828, #9637, .T. ) ;
#59471=B_SPLINE_CURVE_WITH_KNOTS ( 'NONE', 3,
 ( #51113, #8203, #37356, #61425, #27631, #33 ),
 .UNSPECIFIED., .F., .F.,
 ( 4, 2, 4 ),
 ( 1.218313306513762119E-16, 0.0002448718616795917411, 0.0004897437233590617263 ),
 .UNSPECIFIED. ) ;
#59475=AXIS2_PLACEMENT_3D ( 'NONE', #56304, #42248, #23732 ) ;
#59476=( BOUNDED_SURFACE ( )  B_SPLINE_SURFACE ( 3, 1, ( 
 ( #12920, #60487 ),
 ( #17298, #21998 ),
 ( #17603, #36417 ),
 ( #12610, #31701 ) ),
 .UNSPECIFIED., .F., .F., .F. ) 
 B_SPLINE_SURFACE_WITH_KNOTS ( ( 4, 4 ),
 ( 2, 2 ),
 ( 0.000000000000000000, 1.000000000000000000 ),
 ( 0.000000000000000000, 1.000000000000000000 ),
 .UNSPECIFIED. ) 
 GEOMETRIC_REPRESENTATION_ITEM ( )  RATIONAL_B_SPLINE_SURFACE ( (
 ( 1.000000000000000000, 1.000000000000000000),
 ( 0.7282232189291694135, 0.9929344683865672927),
 ( 0.7282232189291694135, 0.9929344683865672927),
 ( 1.000000000000000000, 1.000000000000000000) ) ) 
 REPRESENTATION_ITEM ( '' )  SURFACE ( )  );
#59483=ORIENTED_EDGE ( 'NONE', *, *, #41186, .F. ) ;
#59490=CARTESIAN_POINT ( 'NONE',  ( 1.231276596079881047, 28.52807286890743654, 30.71523773966879745 ) ) ;
#59500=VERTEX_POINT ( 'NONE', #5833 ) ;
#59501=CARTESIAN_POINT ( 'NONE',  ( 4.291220156522060236, -42.97446925027709597, -19.30243481954249773 ) ) ;
#59508=CARTESIAN_POINT ( 'NONE',  ( 3.661921753702000348, 29.39588796543542060, 36.72210362380682369 ) ) ;
#59511=CARTESIAN_POINT ( 'NONE',  ( 3.238018933889920792, -12.07617426668426575, -5.794265048159754627 ) ) ;
#59514=VERTEX_POINT ( 'NONE', #53461 ) ;
#59519=CARTESIAN_POINT ( 'NONE',  ( 0.8554163680231708922, -13.02474486562516631, -45.07284652978098194 ) ) ;
#59521=EDGE_CURVE ( 'NONE', #36737, #50427, #10116, .T. ) ;
#59527=ADVANCED_FACE ( 'NONE', ( #4598 ), #58731, .F. ) ;
#59530=CARTESIAN_POINT ( 'NONE',  ( 0.8560838555295223751, -2.480523550130904642, -46.84250032821665854 ) ) ;
#59533=FACE_OUTER_BOUND ( 'NONE', #13494, .T. ) ;
#59534=CARTESIAN_POINT ( 'NONE',  ( 4.956445790443991584, 38.51510088324707226, 27.09474218539341450 ) ) ;
#59535=( BOUNDED_SURFACE ( )  B_SPLINE_SURFACE ( 3, 1, ( 
 ( #55655, #7419 ),
 ( #56277, #60659 ),
 ( #61280, #41912 ),
 ( #60979, #13394 ) ),
 .UNSPECIFIED., .F., .F., .F. ) 
 B_SPLINE_SURFACE_WITH_KNOTS ( ( 4, 4 ),
 ( 2, 2 ),
 ( 0.000000000000000000, 1.000000000000000000 ),
 ( 0.000000000000000000, 1.000000000000000000 ),
 .UNSPECIFIED. ) 
 GEOMETRIC_REPRESENTATION_ITEM ( )  RATIONAL_B_SPLINE_SURFACE ( (
 ( 1.000000000000000000, 1.000000000000000000),
 ( 0.7282232189291693025, 0.9929344683865674037),
 ( 0.7282232189291693025, 0.9929344683865674037),
 ( 1.000000000000000000, 1.000000000000000000) ) ) 
 REPRESENTATION_ITEM ( '' )  SURFACE ( )  );
#59540=ORIENTED_EDGE ( 'NONE', *, *, #16920, .F. ) ;
#59546=EDGE_CURVE ( 'NONE', #25455, #18232, #30300, .T. ) ;
#59548=CARTESIAN_POINT ( 'NONE',  ( 5.896782393890504181, -15.78847575145207038, -12.45994062280484016 ) ) ;
#59551=( BOUNDED_SURFACE ( )  B_SPLINE_SURFACE ( 3, 1, ( 
 ( #29420, #34758 ),
 ( #53825, #33525 ),
 ( #48527, #19126 ),
 ( #25038, #58216 ) ),
 .UNSPECIFIED., .F., .F., .F. ) 
 B_SPLINE_SURFACE_WITH_KNOTS ( ( 4, 4 ),
 ( 2, 2 ),
 ( 0.000000000000000000, 1.000000000000000000 ),
 ( 0.000000000000000000, 1.000000000000000000 ),
 .UNSPECIFIED. ) 
 GEOMETRIC_REPRESENTATION_ITEM ( )  RATIONAL_B_SPLINE_SURFACE ( (
 ( 1.000000000000000000, 1.000000000000000000),
 ( 0.9952954269826590483, 0.8620686068821339365),
 ( 0.9952954269826590483, 0.8620686068821339365),
 ( 1.000000000000000000, 1.000000000000000000) ) ) 
 REPRESENTATION_ITEM ( '' )  SURFACE ( )  );
#59559=CARTESIAN_POINT ( 'NONE',  ( 0.7764139734771241530, 21.75555916458111838, 41.55401444317116244 ) ) ;
#59562=EDGE_CURVE ( 'NONE', #44630, #13851, #53758, .T. ) ;
#59563=B_SPLINE_CURVE_WITH_KNOTS ( 'NONE', 3,
 ( #54146, #51537, #36866, #44809 ),
 .UNSPECIFIED., .F., .F.,
 ( 4, 4 ),
 ( 0.000000000000000000, 0.005004948556313789688 ),
 .UNSPECIFIED. ) ;
#59565=DIRECTION ( 'NONE',  ( 0.07906939808003035641, 0.3030506235706640905, -0.9496885541274535658 ) ) ;
#59571=CARTESIAN_POINT ( 'NONE',  ( 3.661933894777883669, -5.960912430808857465, -46.65939013686185888 ) ) ;
#59575=B_SPLINE_CURVE_WITH_KNOTS ( 'NONE', 3,
 ( #43943, #39861, #49217, #33596 ),
 .UNSPECIFIED., .F., .F.,
 ( 4, 4 ),
 ( 3.273069708340168845E-17, 0.005004948556313846934 ),
 .UNSPECIFIED. ) ;
#59586=ORIENTED_EDGE ( 'NONE', *, *, #43659, .F. ) ;
#59587=VERTEX_POINT ( 'NONE', #7073 ) ;
#59588=CARTESIAN_POINT ( 'NONE',  ( 0.8560838555295214869, 21.73747136795201129, -41.56747734237908531 ) ) ;
#59604=LINE ( 'NONE', #35833, #2122 ) ;
#59607=CARTESIAN_POINT ( 'NONE',  ( 0.9787464366903548818, -22.69932013610837274, 35.22889237896830394 ) ) ;
#59612=CARTESIAN_POINT ( 'NONE',  ( 0.8560838555295158248, 23.34035564869604684, -40.68907263964262455 ) ) ;
#59619=EDGE_CURVE ( 'NONE', #28607, #41301, #35012, .T. ) ;
#59625=VERTEX_POINT ( 'NONE', #50928 ) ;
#59627=CARTESIAN_POINT ( 'NONE',  ( 0.6845945791218023269, 45.46290160446743300, 11.55556569002393452 ) ) ;
#59628=CARTESIAN_POINT ( 'NONE',  ( 2.788021980263895028, 5.971756191165462832E-15, 46.99417130740431503 ) ) ;
#59629=CARTESIAN_POINT ( 'NONE',  ( 0.5837799406558229487, -38.71456609132658855, -26.46556105465191067 ) ) ;
#59633=ADVANCED_FACE ( 'NONE', ( #22436 ), #28752, .F. ) ;
#59637=VERTEX_POINT ( 'NONE', #32776 ) ;
#59649=DIRECTION ( 'NONE',  ( -1.000000000000000000, -0.000000000000000000, -0.000000000000000000 ) ) ;
#59663=CARTESIAN_POINT ( 'NONE',  ( 5.895596859100789899, -13.98490190264553412, -14.45512718677593611 ) ) ;
#59667=CARTESIAN_POINT ( 'NONE',  ( 1.231276596079887264, 29.74482033789320568, 29.53849072116790353 ) ) ;
#59674=ORIENTED_EDGE ( 'NONE', *, *, #8724, .T. ) ;
#59676=VECTOR ( 'NONE', #28587, 999.9999999999998863 ) ;
#59679=CARTESIAN_POINT ( 'NONE',  ( 4.960386119450153508, -30.07757850721712245, -31.77696863790710324 ) ) ;
#59681=CARTESIAN_POINT ( 'NONE',  ( 0.5834584762367747146, -34.65810993668216611, -31.59195157995216263 ) ) ;
#59683=CARTESIAN_POINT ( 'NONE',  ( 5.917102823773431552, 5.966888710896763648, -19.20640406644395171 ) ) ;
#59686=EDGE_CURVE ( 'NONE', #20443, #10729, #7091, .T. ) ;
#59688=CARTESIAN_POINT ( 'NONE',  ( 0.9785694773339246311, 29.29415779573593426, -29.96978019193998222 ) ) ;
#59693=CARTESIAN_POINT ( 'NONE',  ( 0.5806925824938499181, -8.338382001838064994, 46.14860504863594315 ) ) ;
#59699=ORIENTED_EDGE ( 'NONE', *, *, #59521, .T. ) ;
#59704=ORIENTED_EDGE ( 'NONE', *, *, #39777, .T. ) ;
#59705=B_SPLINE_CURVE_WITH_KNOTS ( 'NONE', 3,
 ( #28076, #24928, #15222, #5169, #10206, #5777, #39658, #58099, #29001, #34329, #59029, #15836, #49030, #58403, #11137, #39045 ),
 .UNSPECIFIED., .F., .F.,
 ( 4, 3, 3, 3, 3, 4 ),
 ( 1.040890552917501732E-17, 0.0002732102107931913548, 0.0004098135523333831061, 0.0005464168938825005517, 0.0008195847345945455036, 0.001092771384553108084 ),
 .UNSPECIFIED. ) ;
#59706=ORIENTED_EDGE ( 'NONE', *, *, #57759, .T. ) ;
#59707=B_SPLINE_CURVE_WITH_KNOTS ( 'NONE', 3,
 ( #4232, #23067, #42196, #38726 ),
 .UNSPECIFIED., .F., .F.,
 ( 4, 4 ),
 ( 0.000000000000000000, 0.004447772540403804181 ),
 .UNSPECIFIED. ) ;
#59708=CARTESIAN_POINT ( 'NONE',  ( 3.376099380956842921, 8.317686564981586983, 10.51306205816325701 ) ) ;
#59710=VERTEX_POINT ( 'NONE', #48399 ) ;
#59711=EDGE_CURVE ( 'NONE', #4749, #26927, #16907, .T. ) ;
#59718=COLOUR_RGB ( '', 0.08235294, 0.09019608, 0.10196078) ;
#59722=CARTESIAN_POINT ( 'NONE',  ( 0.5837157313716021534, -19.82270906330415983, 42.50055610193381028 ) ) ;
#59723=CARTESIAN_POINT ( 'NONE',  ( 0.7056313189692701160, 45.00499400157819707, -13.20224067631960274 ) ) ;
#59727=CARTESIAN_POINT ( 'NONE',  ( 5.895596859100789899, -15.78680134203122165, 12.46214614742294913 ) ) ;
#59728=CARTESIAN_POINT ( 'NONE',  ( 0.5806925824938494740, -19.24316026636509136, 42.76591101925167493 ) ) ;
#59736=CARTESIAN_POINT ( 'NONE',  ( 0.9769922540276034795, 24.50223020450938449, 33.99959220478024946 ) ) ;
#59737=AXIS2_PLACEMENT_3D ( 'NONE', #53908, #1287, #11030 ) ;
#59744=EDGE_LOOP ( 'NONE', ( #54013, #6977, #54853, #33994 ) ) ;
#59749=CARTESIAN_POINT ( 'NONE',  ( 0.9783242366443563043, 38.68706413997891502, -16.11352098194802807 ) ) ;
#59751=CARTESIAN_POINT ( 'NONE',  ( 5.895596859100789899, 12.98817590332826200, -15.35693556399487392 ) ) ;
#59757=EDGE_CURVE ( 'NONE', #54380, #60616, #9600, .T. ) ;
#59759=ORIENTED_EDGE ( 'NONE', *, *, #51347, .T. ) ;
#59767=CARTESIAN_POINT ( 'NONE',  ( 0.9762797500689124330, -0.8945891712298984499, -41.89897964629236782 ) ) ;
#59780=CARTESIAN_POINT ( 'NONE',  ( 0.5804410086790514622, 40.07081992599716358, 24.36902218624511107 ) ) ;
#59785=ORIENTED_EDGE ( 'NONE', *, *, #16394, .T. ) ;
#59787=CARTESIAN_POINT ( 'NONE',  ( 0.5835226383429296115, -19.90526368527538992, -42.46201775899989883 ) ) ;
#59798=CARTESIAN_POINT ( 'NONE',  ( 4.958415959904820092, -39.33684062738365839, -22.71160327406363422 ) ) ;
#59805=CARTESIAN_POINT ( 'NONE',  ( 1.157644175074338699, 35.63734157974641192, 22.06767229699724453 ) ) ;
#59806=CARTESIAN_POINT ( 'NONE',  ( 4.960386119450146403, -42.32154583640180334, -11.10509895001766090 ) ) ;
#59808=CARTESIAN_POINT ( 'NONE',  ( 5.917102823773431552, -9.672968949170799746, -17.63301987068918208 ) ) ;
#59815=LINE ( 'NONE', #16927, #41467 ) ;
#59818=VERTEX_POINT ( 'NONE', #43418 ) ;
#59820=CARTESIAN_POINT ( 'NONE',  ( 0.9783242366443540838, -17.88363875728391506, 37.90131864467907263 ) ) ;
#59822=ORIENTED_EDGE ( 'NONE', *, *, #55168, .T. ) ;
#59831=ADVANCED_FACE ( 'NONE', ( #458 ), #32797, .F. ) ;
#59832=AXIS2_PLACEMENT_3D ( 'NONE', #34966, #11774, #35271 ) ;
#59844=CARTESIAN_POINT ( 'NONE',  ( 3.782625744892853970, -39.11333962259882213, 15.40729592310875695 ) ) ;
#59856=CARTESIAN_POINT ( 'NONE',  ( 0.8560838555295223751, -18.91252766612315739, 42.92655508376904550 ) ) ;
#59869=VERTEX_POINT ( 'NONE', #1080 ) ;
#59876=ORIENTED_EDGE ( 'NONE', *, *, #44796, .F. ) ;
#59877=CARTESIAN_POINT ( 'NONE',  ( 5.917102823773431552, -7.220356195166304225, -18.77115272077518071 ) ) ;
#59900=AXIS2_PLACEMENT_3D ( 'NONE', #41209, #31163, #50270 ) ;
#59903=CARTESIAN_POINT ( 'NONE',  ( 5.896278296736517710, 0.6775463355849699054, -20.10144051001119436 ) ) ;
#59905=EDGE_CURVE ( 'NONE', #50801, #14312, #36328, .T. ) ;
#59910=( BOUNDED_SURFACE ( )  B_SPLINE_SURFACE ( 3, 1, ( 
 ( #47359, #13545 ),
 ( #8506, #37357 ),
 ( #27322, #17625 ),
 ( #3194, #4403 ) ),
 .UNSPECIFIED., .F., .F., .F. ) 
 B_SPLINE_SURFACE_WITH_KNOTS ( ( 4, 4 ),
 ( 2, 2 ),
 ( 0.000000000000000000, 1.000000000000000000 ),
 ( 0.000000000000000000, 1.000000000000000000 ),
 .UNSPECIFIED. ) 
 GEOMETRIC_REPRESENTATION_ITEM ( )  RATIONAL_B_SPLINE_SURFACE ( (
 ( 1.000000000000000000, 1.000000000000000000),
 ( 0.9952954269826590483, 0.8620686068821339365),
 ( 0.9952954269826590483, 0.8620686068821339365),
 ( 1.000000000000000000, 1.000000000000000000) ) ) 
 REPRESENTATION_ITEM ( '' )  SURFACE ( )  );
#59912=CARTESIAN_POINT ( 'NONE',  ( 5.896278296736517710, 12.98123568145699736, -15.36276341667902479 ) ) ;
#59916=DIRECTION ( 'NONE',  ( 0.000000000000000000, 0.000000000000000000, 1.000000000000000000 ) ) ;
#59931=CARTESIAN_POINT ( 'NONE',  ( 3.376099380956842921, -6.056959685666165605, -11.95916481190396041 ) ) ;
#59934=ORIENTED_EDGE ( 'NONE', *, *, #27378, .T. ) ;
#59935=ORIENTED_EDGE ( 'NONE', *, *, #34721, .T. ) ;
#59940=ORIENTED_EDGE ( 'NONE', *, *, #44863, .T. ) ;
#59945=CARTESIAN_POINT ( 'NONE',  ( 0.5824935313925965197, -38.86802447473060340, -26.23956650719635775 ) ) ;
#59951=B_SPLINE_CURVE_WITH_KNOTS ( 'NONE', 3,
 ( #12642, #32050, #22330, #7593, #17027, #55516, #21711, #27030, #32354, #13251, #17634, #16710, #3204, #40852, #36757, #55830, #36447, #50214, #51127 ),
 .UNSPECIFIED., .F., .F.,
 ( 4, 3, 3, 3, 3, 3, 4 ),
 ( 1.250973872328959318E-17, 0.0002732106629380587999, 0.0004098138914053716915, 0.0005464171197651381245, 0.0006830203481512576091, 0.0008196235766963599467, 0.001011968216111139643 ),
 .UNSPECIFIED. ) ;
#59954=EDGE_CURVE ( 'NONE', #539, #58203, #55696, .T. ) ;
#59960=CARTESIAN_POINT ( 'NONE',  ( 5.895881250540457863, 14.91370150166961039, -13.49478377475528568 ) ) ;
#59972=CARTESIAN_POINT ( 'NONE',  ( 4.962356264823608143, -28.94323483023595145, -30.55363735178127271 ) ) ;
#59979=CARTESIAN_POINT ( 'NONE',  ( 0.9762797500689124330, 40.55021165774351743, 10.58324712448433580 ) ) ;
#59980=EDGE_CURVE ( 'NONE', #10639, #2564, #31760, .T. ) ;
#59997=CARTESIAN_POINT ( 'NONE',  ( 0.9780106845699478857, -7.279703251777206674, 41.27150550950986485 ) ) ;
#59998=CARTESIAN_POINT ( 'NONE',  ( 0.9783242366443536397, 29.32669543984089700, -29.93792619379875575 ) ) ;
#59999=CARTESIAN_POINT ( 'NONE',  ( 4.960386119450145515, 42.78128882305005476, -9.175935446106471716 ) ) ;
#60000=EDGE_LOOP ( 'NONE', ( #1154, #52584, #15413, #56330 ) ) ;
#60015=FACE_OUTER_BOUND ( 'NONE', #24691, .T. ) ;
#60016=ORIENTED_EDGE ( 'NONE', *, *, #19206, .T. ) ;
#60021=EDGE_LOOP ( 'NONE', ( #59121, #48005, #19768, #49948 ) ) ;
#60032=CARTESIAN_POINT ( 'NONE',  ( 0.5806925824938499181, -7.260877859416734026, -46.33035738103254175 ) ) ;
#60042=AXIS2_PLACEMENT_3D ( 'NONE', #38719, #23669, #28061 ) ;
#60054=CARTESIAN_POINT ( 'NONE',  ( 1.000433927950263424, -0.7419564671726880389, 41.90308077282223564 ) ) ;
#60055=CARTESIAN_POINT ( 'NONE',  ( 0.5806925824938502512, -41.60618895332704170, 21.63671424046659908 ) ) ;
#60061=CARTESIAN_POINT ( 'NONE',  ( 0.7056313189692676735, 27.13780443373282480, -38.25295040221118370 ) ) ;
#60074=CARTESIAN_POINT ( 'NONE',  ( 4.956445790444041322, 46.25174887658561573, -8.849507104743011610 ) ) ;
#60076=CARTESIAN_POINT ( 'NONE',  ( 4.956445790443988031, 0.000000000000000000, 0.000000000000000000 ) ) ;
#60077=EDGE_CURVE ( 'NONE', #36411, #8407, #44599, .T. ) ;
#60083=CARTESIAN_POINT ( 'NONE',  ( 0.5782707292762442330, -41.52883855096524712, -21.79660345823360146 ) ) ;
#60085=CARTESIAN_POINT ( 'NONE',  ( 5.894904586330512508, 16.58261916749260223, -11.38183436918451186 ) ) ;
#60090=CARTESIAN_POINT ( 'NONE',  ( 5.895881250540457863, -2.017740640757351933, 20.01140685496492466 ) ) ;
#60094=CARTESIAN_POINT ( 'NONE',  ( 0.9762797500689124330, -0.8945891712298984499, -41.89897964629236782 ) ) ;
#60095=CARTESIAN_POINT ( 'NONE',  ( 3.238018933889920792, 6.194554405862141344, 11.87581525961341633 ) ) ;
#60097=CARTESIAN_POINT ( 'NONE',  ( 0.5806925824938499181, -35.14454992382352572, 31.04968555388990836 ) ) ;
#60098=( BOUNDED_SURFACE ( )  B_SPLINE_SURFACE ( 3, 1, ( 
 ( #33288, #38927 ),
 ( #5355, #5652 ),
 ( #24798, #43004 ),
 ( #38003, #14792 ) ),
 .UNSPECIFIED., .F., .F., .F. ) 
 B_SPLINE_SURFACE_WITH_KNOTS ( ( 4, 4 ),
 ( 2, 2 ),
 ( 0.000000000000000000, 1.000000000000000000 ),
 ( 0.000000000000000000, 1.000000000000000000 ),
 .UNSPECIFIED. ) 
 GEOMETRIC_REPRESENTATION_ITEM ( )  RATIONAL_B_SPLINE_SURFACE ( (
 ( 1.000000000000000000, 1.000000000000000000),
 ( 0.7282232189291693025, 0.9929344683865674037),
 ( 0.7282232189291693025, 0.9929344683865674037),
 ( 1.000000000000000000, 1.000000000000000000) ) ) 
 REPRESENTATION_ITEM ( '' )  SURFACE ( )  );
#60105=CARTESIAN_POINT ( 'NONE',  ( 0.8554163680231816613, -8.703479761964905137, -46.10265624825630937 ) ) ;
#60109=ORIENTED_EDGE ( 'NONE', *, *, #19960, .T. ) ;
#60111=CARTESIAN_POINT ( 'NONE',  ( 4.958415959904823644, -43.93947138327067137, -11.51202885600005210 ) ) ;
#60115=CARTESIAN_POINT ( 'NONE',  ( 5.895596859100789899, 16.58392706178521792, -11.37987462241457948 ) ) ;
#60118=ORIENTED_EDGE ( 'NONE', *, *, #13457, .F. ) ;
#60119=CARTESIAN_POINT ( 'NONE',  ( 5.910764540655177868, -15.77444817831453427, -12.47669920847786962 ) ) ;
#60121=CARTESIAN_POINT ( 'NONE',  ( 4.956445790443991584, 39.12691469763999663, 26.20348443209871903 ) ) ;
#60126=CARTESIAN_POINT ( 'NONE',  ( 0.9788927965476018622, -17.51217498749385371, 38.07440531169427089 ) ) ;
#60136=ORIENTED_EDGE ( 'NONE', *, *, #4638, .F. ) ;
#60141=CARTESIAN_POINT ( 'NONE',  ( 0.9783242366443560822, 9.975869637871808138, -40.70401104528534120 ) ) ;
#60146=CARTESIAN_POINT ( 'NONE',  ( 0.6845945791218023269, -44.02134436206650037, 16.20270845477079646 ) ) ;
#60155=FACE_OUTER_BOUND ( 'NONE', #37966, .T. ) ;
#60159=CARTESIAN_POINT ( 'NONE',  ( 0.5782707292762423457, 10.16715070324166881, -45.78608304152248110 ) ) ;
#60178=EDGE_LOOP ( 'NONE', ( #42530, #34571 ) ) ;
#60186=CARTESIAN_POINT ( 'NONE',  ( 5.896782393890504181, -19.39652907507979052, 5.319844614046219000 ) ) ;
#60193=EDGE_CURVE ( 'NONE', #60737, #19581, #27200, .T. ) ;
#60195=CARTESIAN_POINT ( 'NONE',  ( 0.5797568599927139799, -30.75502584278100215, 35.40273568639684498 ) ) ;
#60204=CARTESIAN_POINT ( 'NONE',  ( 0.8554163680231720024, -0.6539261334255729308, 46.91244881397518895 ) ) ;
#60210=CARTESIAN_POINT ( 'NONE',  ( 0.5824936645240084143, 5.056360923409078723, -46.62264893002680566 ) ) ;
#60211=CARTESIAN_POINT ( 'NONE',  ( 0.7764139734771229318, -24.48247842768736149, -40.00810819002430208 ) ) ;
#60213=CARTESIAN_POINT ( 'NONE',  ( 4.962356264823608143, 0.000000000000000000, 0.000000000000000000 ) ) ;
#60217=CARTESIAN_POINT ( 'NONE',  ( 0.5834584762367742705, -13.72010822659117046, -44.84411465581428047 ) ) ;
#60236=CARTESIAN_POINT ( 'NONE',  ( 4.958415959904820092, -38.82150677285500961, -23.58165739950888096 ) ) ;
#60237=EDGE_CURVE ( 'NONE', #52026, #40574, #8542, .T. ) ;
#60239=CARTESIAN_POINT ( 'NONE',  ( 0.5806925824938502512, 11.40214825760292250, 45.48860711711456872 ) ) ;
#60251=CARTESIAN_POINT ( 'NONE',  ( 0.5806925824938499181, 10.33919002968644385, 45.74192291403583965 ) ) ;
#60256=CARTESIAN_POINT ( 'NONE',  ( 5.894904586330512508, -2.014437969560491037, 20.01178282233833627 ) ) ;
#60261=CARTESIAN_POINT ( 'NONE',  ( 4.960386119450149955, 36.33710775634317258, -24.37316279386498863 ) ) ;
#60265=FACE_OUTER_BOUND ( 'NONE', #23133, .T. ) ;
#60266=CARTESIAN_POINT ( 'NONE',  ( 2.282803330402962239, 9.607084330193609745, 45.98043973397309259 ) ) ;
#60271=CARTESIAN_POINT ( 'NONE',  ( 1.000110580585048536, 20.71550333451957826, -36.43192836468320905 ) ) ;
#60276=( BOUNDED_SURFACE ( )  B_SPLINE_SURFACE ( 3, 1, ( 
 ( #58436, #34669 ),
 ( #15562, #59064 ),
 ( #6420, #10547 ),
 ( #44098, #11475 ) ),
 .UNSPECIFIED., .F., .F., .F. ) 
 B_SPLINE_SURFACE_WITH_KNOTS ( ( 4, 4 ),
 ( 2, 2 ),
 ( 0.000000000000000000, 1.000000000000000000 ),
 ( 0.000000000000000000, 1.000000000000000000 ),
 .UNSPECIFIED. ) 
 GEOMETRIC_REPRESENTATION_ITEM ( )  RATIONAL_B_SPLINE_SURFACE ( (
 ( 1.000000000000000000, 1.000000000000000000),
 ( 0.7282232189291693025, 0.9929344683865674037),
 ( 0.7282232189291693025, 0.9929344683865674037),
 ( 1.000000000000000000, 1.000000000000000000) ) ) 
 REPRESENTATION_ITEM ( '' )  SURFACE ( )  );
#60280=FACE_OUTER_BOUND ( 'NONE', #22533, .T. ) ;
#60281=CARTESIAN_POINT ( 'NONE',  ( 0.7056759521544949676, 11.69106431276068747, -45.42100664177186076 ) ) ;
#60288=CARTESIAN_POINT ( 'NONE',  ( 0.8554163680231738898, 28.56078411578483056, -37.22213163970264560 ) ) ;
#60289=CARTESIAN_POINT ( 'NONE',  ( 0.9790850452238870627, -31.04767048625561898, 28.14923600455417230 ) ) ;
#60292=DIRECTION ( 'NONE',  ( -0.07500201931887529039, -0.8144017028153767157, 0.5754342391181688221 ) ) ;
#60296=CARTESIAN_POINT ( 'NONE',  ( 5.910764540655177868, -18.51025558288800354, -7.865855117234652916 ) ) ;
#60300=CARTESIAN_POINT ( 'NONE',  ( 0.5830082357119548142, -8.069412620820072490, 46.19650002860918647 ) ) ;
#60303=CARTESIAN_POINT ( 'NONE',  ( 3.376099380956838925, -11.30600709870817688, 7.202956831470493704 ) ) ;
#60306=ORIENTED_EDGE ( 'NONE', *, *, #1042, .F. ) ;
#60312=CARTESIAN_POINT ( 'NONE',  ( 0.9787284016396613495, 32.77352223152413302, -26.11957579036502608 ) ) ;
#60320=EDGE_LOOP ( 'NONE', ( #24515, #50341, #53369, #902 ) ) ;
#60329=CIRCLE ( 'NONE', #28338, 42.08604991992415023 ) ;
#60332=CARTESIAN_POINT ( 'NONE',  ( 0.6845945791218023269, 36.27071225238075414, -29.74629310382962188 ) ) ;
#60335=CARTESIAN_POINT ( 'NONE',  ( 0.6845945791218034371, -18.95641467630732535, -42.90758514917641264 ) ) ;
#60339=CARTESIAN_POINT ( 'NONE',  ( 4.960386119450146403, -21.43901005587111541, -38.14191018416091339 ) ) ;
#60349=CARTESIAN_POINT ( 'NONE',  ( 4.958415959904823644, 24.01335991617007792, -38.55596580762981773 ) ) ;
#60354=CARTESIAN_POINT ( 'NONE',  ( 5.895596859100789899, -11.92767122914683675, -16.19440774656085935 ) ) ;
#60356=ORIENTED_EDGE ( 'NONE', *, *, #42592, .F. ) ;
#60357=EDGE_CURVE ( 'NONE', #37103, #39646, #28751, .T. ) ;
#60359=CARTESIAN_POINT ( 'NONE',  ( 0.9780106845699489959, -27.29611424684454235, 31.80021058858961069 ) ) ;
#60360=CARTESIAN_POINT ( 'NONE',  ( 0.9762797500689124330, -17.18051571332144434, 38.22505284509125545 ) ) ;
#60366=CARTESIAN_POINT ( 'NONE',  ( 3.376099380956842921, -2.682194557846140359, -13.13446671874909377 ) ) ;
#60373=CARTESIAN_POINT ( 'NONE',  ( 0.5848930533535030563, 40.25661832390738937, 24.05572205340763148 ) ) ;
#60382=EDGE_CURVE ( 'NONE', #45184, #1908, #34614, .T. ) ;
#60387=AXIS2_PLACEMENT_3D ( 'NONE', #22372, #27072, #9197 ) ;
#60391=ORIENTED_EDGE ( 'NONE', *, *, #46563, .F. ) ;
#60398=CARTESIAN_POINT ( 'NONE',  ( 5.917102823773431552, -18.51940219202224114, -7.843561722958756199 ) ) ;
#60400=ADVANCED_FACE ( 'NONE', ( #10584 ), #51604, .F. ) ;
#60404=ORIENTED_EDGE ( 'NONE', *, *, #23986, .T. ) ;
#60406=ADVANCED_FACE ( 'NONE', ( #5845 ), #18889, .F. ) ;
#60409=CARTESIAN_POINT ( 'NONE',  ( 5.917102823773431552, -15.77849770028341680, -12.47111576298980928 ) ) ;
#60411=CARTESIAN_POINT ( 'NONE',  ( 0.9762797500689124330, -7.469026406146330288, 41.23758515880862774 ) ) ;
#60413=CARTESIAN_POINT ( 'NONE',  ( 5.901463166500145796, 19.00451910135526390, -6.583777340316079751 ) ) ;
#60417=CARTESIAN_POINT ( 'NONE',  ( 5.896782393890504181, 17.94821721415859628, 9.076760749925794514 ) ) ;
#60419=VERTEX_POINT ( 'NONE', #34706 ) ;
#60424=CARTESIAN_POINT ( 'NONE',  ( 0.5817216825391126056, -44.14976101355541260, 15.81244935654816786 ) ) ;
#60428=ORIENTED_EDGE ( 'NONE', *, *, #46996, .F. ) ;
#60434=CARTESIAN_POINT ( 'NONE',  ( 0.9780303403264770656, 9.399973085119292193, -40.84091232323437737 ) ) ;
#60437=SURFACE_SIDE_STYLE ('',( #46687 ) ) ;
#60441=DIRECTION ( 'NONE',  ( 0.000000000000000000, 0.000000000000000000, 1.000000000000000000 ) ) ;
#60444=ADVANCED_FACE ( 'NONE', ( #42888 ), #48872, .F. ) ;
#60448=CARTESIAN_POINT ( 'NONE',  ( 0.5848930533535030563, -45.99261677209132415, 9.162547944927917243 ) ) ;
#60449=CARTESIAN_POINT ( 'NONE',  ( 0.5806925824938499181, -38.35106547415185929, -26.98922265166007861 ) ) ;
#60451=LINE ( 'NONE', #22883, #23666 ) ;
#60456=CARTESIAN_POINT ( 'NONE',  ( 3.238018933889920792, 12.22151767825371493, -5.481058110236103786 ) ) ;
#60457=VERTEX_POINT ( 'NONE', #40347 ) ;
#60462=ORIENTED_EDGE ( 'NONE', *, *, #46410, .F. ) ;
#60467=VERTEX_POINT ( 'NONE', #59408 ) ;
#60473=CARTESIAN_POINT ( 'NONE',  ( 5.896278296736517710, -2.007758883826791241, 20.01239325714938744 ) ) ;
#60474=AXIS2_PLACEMENT_3D ( 'NONE', #20495, #34294, #48999 ) ;
#60475=ORIENTED_EDGE ( 'NONE', *, *, #6403, .T. ) ;
#60476=ORIENTED_EDGE ( 'NONE', *, *, #22218, .T. ) ;
#60482=CARTESIAN_POINT ( 'NONE',  ( 5.910764540655177868, -7.214026563325304231, -18.77389302230093904 ) ) ;
#60485=ORIENTED_EDGE ( 'NONE', *, *, #14451, .F. ) ;
#60487=CARTESIAN_POINT ( 'NONE',  ( 0.8554163680231738898, -46.74230100997658610, -4.045092014350424314 ) ) ;
#60505=CARTESIAN_POINT ( 'NONE',  ( 4.956445790443996025, 13.43466403631381567, 45.13366650706556982 ) ) ;
#60509=EDGE_CURVE ( 'NONE', #51483, #14125, #36203, .T. ) ;
#60511=EDGE_CURVE ( 'NONE', #52112, #18772, #20656, .T. ) ;
#60512=CARTESIAN_POINT ( 'NONE',  ( 0.5835871038041838821, 4.829953511217432549, -46.64660761492717000 ) ) ;
#60517=EDGE_CURVE ( 'NONE', #57645, #25309, #39095, .T. ) ;
#60518=AXIS2_PLACEMENT_3D ( 'NONE', #31294, #20666, #55085 ) ;
#60531=FACE_OUTER_BOUND ( 'NONE', #58750, .T. ) ;
#60540=EDGE_CURVE ( 'NONE', #42210, #55527, #20425, .T. ) ;
#60550=( BOUNDED_SURFACE ( )  B_SPLINE_SURFACE ( 3, 1, ( 
 ( #24550, #28938 ),
 ( #38671, #4795 ),
 ( #14552, #57726 ),
 ( #19249, #10144 ) ),
 .UNSPECIFIED., .F., .F., .F. ) 
 B_SPLINE_SURFACE_WITH_KNOTS ( ( 4, 4 ),
 ( 2, 2 ),
 ( 0.000000000000000000, 1.000000000000000000 ),
 ( 0.000000000000000000, 1.000000000000000000 ),
 .UNSPECIFIED. ) 
 GEOMETRIC_REPRESENTATION_ITEM ( )  RATIONAL_B_SPLINE_SURFACE ( (
 ( 1.000000000000000000, 1.000000000000000000),
 ( 0.9952954269826590483, 0.8620686068821307169),
 ( 0.9952954269826590483, 0.8620686068821307169),
 ( 1.000000000000000000, 1.000000000000000000) ) ) 
 REPRESENTATION_ITEM ( '' )  SURFACE ( )  );
#60553=B_SPLINE_CURVE_WITH_KNOTS ( 'NONE', 3,
 ( #50964, #41594, #50350, #26861 ),
 .UNSPECIFIED., .F., .F.,
 ( 4, 4 ),
 ( 1.398578778534940505E-17, 0.005004948556313816577 ),
 .UNSPECIFIED. ) ;
#60563=CARTESIAN_POINT ( 'NONE',  ( 1.231276596079887264, -0.5545928549379750550, 41.91621640586514985 ) ) ;
#60565=CARTESIAN_POINT ( 'NONE',  ( 0.5835871038041862136, -38.74013687519667570, 26.42794444886935779 ) ) ;
#60569=ORIENTED_EDGE ( 'NONE', *, *, #9742, .F. ) ;
#60578=ORIENTED_EDGE ( 'NONE', *, *, #52188, .F. ) ;
#60581=CARTESIAN_POINT ( 'NONE',  ( 3.782625744892853525, -14.09172058606395872, -39.60633175414385931 ) ) ;
#60583=CARTESIAN_POINT ( 'NONE',  ( 0.9754292580325133466, -23.03905107044544565, 35.00756479216186534 ) ) ;
#60585=CARTESIAN_POINT ( 'NONE',  ( 4.962356264823609031, -24.61258717641066696, -34.13877780978592824 ) ) ;
#60590=CARTESIAN_POINT ( 'NONE',  ( 3.661921753702020332, -9.674343372738375635, -46.03301211240026447 ) ) ;
#60591=ORIENTED_EDGE ( 'NONE', *, *, #31173, .F. ) ;
#60592=ADVANCED_FACE ( 'NONE', ( #47191 ), #34082, .F. ) ;
#60594=CARTESIAN_POINT ( 'NONE',  ( 0.7056759521544968550, -25.94340635086248881, 39.07286137501344570 ) ) ;
#60602=CARTESIAN_POINT ( 'NONE',  ( 3.661933894777877452, -18.07631262299097941, -43.42669785866236509 ) ) ;
#60616=VERTEX_POINT ( 'NONE', #13679 ) ;
#60617=CARTESIAN_POINT ( 'NONE',  ( 0.9775691876210979014, 25.16245705919257603, -33.51394431776540017 ) ) ;
#60623=( BOUNDED_SURFACE ( )  B_SPLINE_SURFACE ( 3, 1, ( 
 ( #11968, #31049 ),
 ( #50158, #26343 ),
 ( #12885, #45474 ),
 ( #36390, #12577 ) ),
 .UNSPECIFIED., .F., .F., .F. ) 
 B_SPLINE_SURFACE_WITH_KNOTS ( ( 4, 4 ),
 ( 2, 2 ),
 ( 0.000000000000000000, 1.000000000000000000 ),
 ( 0.000000000000000000, 1.000000000000000000 ),
 .UNSPECIFIED. ) 
 GEOMETRIC_REPRESENTATION_ITEM ( )  RATIONAL_B_SPLINE_SURFACE ( (
 ( 1.000000000000000000, 1.000000000000000000),
 ( 0.7282232189291693025, 0.9929344683865674037),
 ( 0.7282232189291693025, 0.9929344683865674037),
 ( 1.000000000000000000, 1.000000000000000000) ) ) 
 REPRESENTATION_ITEM ( '' )  SURFACE ( )  );
#60633=CARTESIAN_POINT ( 'NONE',  ( 0.9783242366443551941, 4.461546119134775168, -41.67048231582345608 ) ) ;
#60636=ORIENTED_EDGE ( 'NONE', *, *, #48849, .F. ) ;
#60655=AXIS2_PLACEMENT_3D ( 'NONE', #2166, #36348, #45133 ) ;
#60656=CARTESIAN_POINT ( 'NONE',  ( 5.895596859100789899, -18.51552686702056150, -7.855154234585556949 ) ) ;
#60659=CARTESIAN_POINT ( 'NONE',  ( 4.291220156522060236, -27.13845918422007131, -38.50835013879611068 ) ) ;
#60671=CARTESIAN_POINT ( 'NONE',  ( 5.901463166500146684, 16.57349776239452055, -11.39460584050806347 ) ) ;
#60673=B_SPLINE_CURVE_WITH_KNOTS ( 'NONE', 3,
 ( #45863, #51437, #51755, #3515 ),
 .UNSPECIFIED., .F., .F.,
 ( 4, 4 ),
 ( 5.682377955034955683E-17, 0.005004948556313868618 ),
 .UNSPECIFIED. ) ;
#60675=CARTESIAN_POINT ( 'NONE',  ( 0.8560838555295223751, -45.77741231505103059, 10.23725333375835689 ) ) ;
#60679=B_SPLINE_CURVE_WITH_KNOTS ( 'NONE', 3,
 ( #8812, #53557, #24769, #11288, #54169, #53865 ),
 .UNSPECIFIED., .F., .F.,
 ( 4, 2, 4 ),
 ( 6.805474077711127748E-18, 0.0002291472222819931524, 0.0004582944445639795285 ),
 .UNSPECIFIED. ) ;
#60681=CARTESIAN_POINT ( 'NONE',  ( 1.231276596079881047, 19.39962232756238691, 37.16088568059176112 ) ) ;
#60682=DIRECTION ( 'NONE',  ( -1.000000000000000000, -0.000000000000000000, -0.000000000000000000 ) ) ;
#60685=CARTESIAN_POINT ( 'NONE',  ( 3.782625744892852637, -40.81794195064407660, 10.05652618993522651 ) ) ;
#60686=CARTESIAN_POINT ( 'NONE',  ( 5.894904586330512508, 16.58122937421121534, -11.38385894595667835 ) ) ;
#60687=EDGE_CURVE ( 'NONE', #25777, #39735, #18888, .T. ) ;
#60689=CARTESIAN_POINT ( 'NONE',  ( 0.5832655196449136881, 46.44668467208332174, 6.476161358813500968 ) ) ;
#60692=AXIS2_PLACEMENT_3D ( 'NONE', #25024, #57891, #29399 ) ;
#60693=CARTESIAN_POINT ( 'NONE',  ( 0.5806925824938494740, -38.35106547415225009, 26.98922265165951018 ) ) ;
#60696=CARTESIAN_POINT ( 'NONE',  ( 5.895596859100789899, 10.81936814621369969, 16.95492424427734690 ) ) ;
#60697=EDGE_LOOP ( 'NONE', ( #43957, #36375, #36433, #8879 ) ) ;
#60706=VERTEX_POINT ( 'NONE', #56866 ) ;
#60709=EDGE_LOOP ( 'NONE', ( #2789, #61030, #58493, #38519 ) ) ;
#60710=CARTESIAN_POINT ( 'NONE',  ( 0.5837799406558225046, -7.890001094198478171, -46.22760465685791331 ) ) ;
#60712=EDGE_CURVE ( 'NONE', #24826, #18401, #54806, .T. ) ;
#60713=VECTOR ( 'NONE', #58574, 999.9999999999998863 ) ;
#60715=B_SPLINE_CURVE_WITH_KNOTS ( 'NONE', 3,
 ( #48282, #57962, #32964, #61730 ),
 .UNSPECIFIED., .F., .F.,
 ( 4, 4 ),
 ( 0.001752131338475893668, 0.004041751736741000349 ),
 .UNSPECIFIED. ) ;
#60718=VERTEX_POINT ( 'NONE', #19299 ) ;
#60721=ADVANCED_FACE ( 'NONE', ( #468 ), #8426, .F. ) ;
#60723=CARTESIAN_POINT ( 'NONE',  ( 4.956445790444018229, -5.251077430595369577, -46.79705371022334504 ) ) ;
#60724=CARTESIAN_POINT ( 'NONE',  ( 0.9754292580325133466, -7.544321912686871023, 41.22390900656750290 ) ) ;
#60725=CARTESIAN_POINT ( 'NONE',  ( 0.7764139734771252632, -44.59376569072301777, 14.54085734844269062 ) ) ;
#60728=VERTEX_POINT ( 'NONE', #48109 ) ;
#60736=CARTESIAN_POINT ( 'NONE',  ( 1.231276596079881047, 40.19859528295886975, 11.88905834349143653 ) ) ;
#60737=VERTEX_POINT ( 'NONE', #52171 ) ;
#60738=CARTESIAN_POINT ( 'NONE',  ( 5.895596859100789899, -2.016778947467960048, -20.01151633159111043 ) ) ;
#60747=CARTESIAN_POINT ( 'NONE',  ( 0.5830082357119562575, -41.73162262790440735, -21.39401102599778426 ) ) ;
#60750=SURFACE_STYLE_USAGE ( .BOTH. , #60437 ) ;
#60755=CARTESIAN_POINT ( 'NONE',  ( 0.7056759521545009628, 28.49525089474759909, -37.25277849452807999 ) ) ;
#60758=CARTESIAN_POINT ( 'NONE',  ( 5.895596859100789899, 19.71057157537855176, 4.002693016503615198 ) ) ;
#60759=CARTESIAN_POINT ( 'NONE',  ( 3.782542959838397056, 31.89521442703278353, 27.38490734054377995 ) ) ;
#60761=CARTESIAN_POINT ( 'NONE',  ( 0.8560838555295223751, -8.701885300215751684, -46.09392613244852299 ) ) ;
#60762=AXIS2_PLACEMENT_3D ( 'NONE', #50579, #55579, #12707 ) ;
#60763=DIRECTION ( 'NONE',  ( -0.07500201931887527651, 0.2442817726706026926, 0.9667994169624839484 ) ) ;
#60783=CARTESIAN_POINT ( 'NONE',  ( 5.896782393890504181, -2.006887468070398750, 20.01245835894516389 ) ) ;
#60786=ORIENTED_EDGE ( 'NONE', *, *, #40976, .T. ) ;
#60788=EDGE_CURVE ( 'NONE', #12584, #16352, #21879, .T. ) ;
#60790=CARTESIAN_POINT ( 'NONE',  ( 5.896782393890504181, 5.952874097602693482, -19.21169895808549200 ) ) ;
#60791=ORIENTED_EDGE ( 'NONE', *, *, #49782, .T. ) ;
#60801=CARTESIAN_POINT ( 'NONE',  ( 0.5830082357119570347, -44.21081432357497221, -15.64084178632068500 ) ) ;
#60802=CARTESIAN_POINT ( 'NONE',  ( 0.5837799406558226156, -30.20780738208704719, 35.87104574366253473 ) ) ;
#60817=CARTESIAN_POINT ( 'NONE',  ( 0.5824935313925918567, -1.931035634062136630, -46.85626189138252329 ) ) ;
#60821=CARTESIAN_POINT ( 'NONE',  ( 0.9790850452238869517, -41.81167860008601167, 2.849712776106803958 ) ) ;
#60827=CARTESIAN_POINT ( 'NONE',  ( 0.5806925824938499181, 46.89268439822727430, -0.5463627657667492477 ) ) ;
#60832=DIRECTION ( 'NONE',  ( 0.000000000000000000, 0.000000000000000000, 1.000000000000000000 ) ) ;
#60835=EDGE_CURVE ( 'NONE', #59460, #15516, #993, .T. ) ;
#60837=CARTESIAN_POINT ( 'NONE',  ( 0.5848930533535030563, 46.50190038545817828, -6.070118856207339597 ) ) ;
#60845=CARTESIAN_POINT ( 'NONE',  ( 4.962356264823608143, 42.01891079680549268, -2.376285612557975213 ) ) ;
#60849=CARTESIAN_POINT ( 'NONE',  ( 0.5804410086790514622, 43.38796872094628299, -17.80460676694615785 ) ) ;
#60850=CARTESIAN_POINT ( 'NONE',  ( 0.7764139734771249302, -18.93147429300290341, -42.91433038042463721 ) ) ;
#60852=VERTEX_POINT ( 'NONE', #16139 ) ;
#60859=CARTESIAN_POINT ( 'NONE',  ( 1.231276596079887264, 19.39962232756291272, -37.16088568059149111 ) ) ;
#60869=EDGE_CURVE ( 'NONE', #34397, #15656, #45277, .T. ) ;
#60873=EDGE_CURVE ( 'NONE', #59710, #51483, #3983, .T. ) ;
#60878=CARTESIAN_POINT ( 'NONE',  ( 3.782625744892854414, 23.52694838945772915, -34.83849600047044248 ) ) ;
#60884=CARTESIAN_POINT ( 'NONE',  ( 0.7056759521544980762, 16.06728742641350394, 44.06348946547473133 ) ) ;
#60893=CARTESIAN_POINT ( 'NONE',  ( 4.956445790444004018, -43.56224489968086999, -17.88487823385623443 ) ) ;
#60904=CARTESIAN_POINT ( 'NONE',  ( 0.5806925824938494740, -46.75147433417404841, 3.677228565731047283 ) ) ;
#60907=CARTESIAN_POINT ( 'NONE',  ( 0.9788927965476020843, -1.541996045496603074, -41.88029203369348608 ) ) ;
#60912=CARTESIAN_POINT ( 'NONE',  ( 2.528100132419516477, -41.78722613136653763, 4.010175916105612970 ) ) ;
#60919=CARTESIAN_POINT ( 'NONE',  ( 0.5835871038041877679, -25.34891654652388837, 39.45461801638514743 ) ) ;
#60922=CARTESIAN_POINT ( 'NONE',  ( 5.910764540655177868, 16.57257352145941098, 11.39522028505748708 ) ) ;
#60925=( BOUNDED_SURFACE ( )  B_SPLINE_SURFACE ( 3, 1, ( 
 ( #50441, #40455 ),
 ( #2508, #21947 ),
 ( #7828, #45767 ),
 ( #2813, #59519 ) ),
 .UNSPECIFIED., .F., .F., .F. ) 
 B_SPLINE_SURFACE_WITH_KNOTS ( ( 4, 4 ),
 ( 2, 2 ),
 ( 0.000000000000000000, 1.000000000000000000 ),
 ( 0.000000000000000000, 1.000000000000000000 ),
 .UNSPECIFIED. ) 
 GEOMETRIC_REPRESENTATION_ITEM ( )  RATIONAL_B_SPLINE_SURFACE ( (
 ( 1.000000000000000000, 1.000000000000000000),
 ( 0.9952954269826590483, 0.8620686068821339365),
 ( 0.9952954269826590483, 0.8620686068821339365),
 ( 1.000000000000000000, 1.000000000000000000) ) ) 
 REPRESENTATION_ITEM ( '' )  SURFACE ( )  );
#60927=EDGE_LOOP ( 'NONE', ( #15301, #48995, #17848, #21623 ) ) ;
#60928=ORIENTED_EDGE ( 'NONE', *, *, #29335, .F. ) ;
#60931=DIRECTION ( 'NONE',  ( -1.000000000000000000, -0.000000000000000000, -0.000000000000000000 ) ) ;
#60935=CARTESIAN_POINT ( 'NONE',  ( 0.5830082357119558134, 22.29740569870308775, 41.25600240020573040 ) ) ;
#60945=CARTESIAN_POINT ( 'NONE',  ( 5.895596859100789899, -18.51552686702066808, 7.855154234585303819 ) ) ;
#60968=CARTESIAN_POINT ( 'NONE',  ( 4.962356264823608143, 0.000000000000000000, 0.000000000000000000 ) ) ;
#60979=CARTESIAN_POINT ( 'NONE',  ( 5.896782393890504181, 10.81700609697876736, 16.95636948099257424 ) ) ;
#60985=VECTOR ( 'NONE', #58509, 1000.000000000000000 ) ;
#60998=CARTESIAN_POINT ( 'NONE',  ( 1.000110580585049647, 19.56154407020022745, 37.06431540392340196 ) ) ;
#61001=CARTESIAN_POINT ( 'NONE',  ( 3.782542959838394392, 35.26067992111592275, 22.88934915844450657 ) ) ;
#61002=CARTESIAN_POINT ( 'NONE',  ( 1.231276596079887931, -40.90292846002456173, 9.177538581350681568 ) ) ;
#61014=FACE_OUTER_BOUND ( 'NONE', #2875, .T. ) ;
#61015=VERTEX_POINT ( 'NONE', #36181 ) ;
#61016=CARTESIAN_POINT ( 'NONE',  ( 5.838029081930955932, -4.708022006887727429, -46.99893176377076287 ) ) ;
#61017=CARTESIAN_POINT ( 'NONE',  ( 0.8554163680231738898, -38.15570339590799165, -27.30105806512478850 ) ) ;
#61029=EDGE_CURVE ( 'NONE', #58239, #49073, #55555, .T. ) ;
#61030=ORIENTED_EDGE ( 'NONE', *, *, #34652, .F. ) ;
#61031=CARTESIAN_POINT ( 'NONE',  ( 3.238018933889920792, -9.747366695765370181, 9.186747785039983683 ) ) ;
#61032=CARTESIAN_POINT ( 'NONE',  ( 0.6845945791218023269, -30.94166671083539910, -35.25648567100138564 ) ) ;
#61038=CARTESIAN_POINT ( 'NONE',  ( 0.5797568665920711517, -39.01551406077552997, -26.01951135542895344 ) ) ;
#61041=CARTESIAN_POINT ( 'NONE',  ( 4.958415959904818315, -5.049385427348107136, -45.14097540626171678 ) ) ;
#61043=CARTESIAN_POINT ( 'NONE',  ( 5.895596859100789899, -11.92767122914705880, 16.19440774656069237 ) ) ;
#61047=CARTESIAN_POINT ( 'NONE',  ( 0.9754292589017197201, -39.39482825664529742, 14.29597752952562040 ) ) ;
#61051=ORIENTED_EDGE ( 'NONE', *, *, #52038, .T. ) ;
#61067=CARTESIAN_POINT ( 'NONE',  ( 5.917102823773431552, 8.473612197389558176, -18.23972626932742358 ) ) ;
#61068=CARTESIAN_POINT ( 'NONE',  ( 5.895881250540457863, 3.349849349787696440, -19.83194874292559007 ) ) ;
#61071=EDGE_CURVE ( 'NONE', #58688, #57391, #17431, .T. ) ;
#61075=EDGE_CURVE ( 'NONE', #54614, #35968, #14533, .T. ) ;
#61080=CARTESIAN_POINT ( 'NONE',  ( 0.9769922540276050338, 19.75190663635009614, 36.96205810442694428 ) ) ;
#61085=CARTESIAN_POINT ( 'NONE',  ( 0.9790850452238877288, -41.81844294212524460, -2.748665159565954585 ) ) ;
#61090=ADVANCED_FACE ( 'NONE', ( #29220 ), #2616, .T. ) ;
#61091=ORIENTED_EDGE ( 'NONE', *, *, #36726, .F. ) ;
#61103=CARTESIAN_POINT ( 'NONE',  ( 1.231276596079881047, 8.892602616353681100, 40.96581977363184990 ) ) ;
#61106=CARTESIAN_POINT ( 'NONE',  ( 5.910764540655177868, 19.71228184310538367, -3.990887496176878102 ) ) ;
#61110=CARTESIAN_POINT ( 'NONE',  ( 4.962356264823608143, 0.000000000000000000, 0.000000000000000000 ) ) ;
#61113=ORIENTED_EDGE ( 'NONE', *, *, #47376, .F. ) ;
#61117=( BOUNDED_SURFACE ( )  B_SPLINE_SURFACE ( 3, 1, ( 
 ( #46753, #18864 ),
 ( #14468, #37986 ),
 ( #14165, #33271 ),
 ( #37349, #18537 ) ),
 .UNSPECIFIED., .F., .F., .F. ) 
 B_SPLINE_SURFACE_WITH_KNOTS ( ( 4, 4 ),
 ( 2, 2 ),
 ( 0.000000000000000000, 1.000000000000000000 ),
 ( 0.000000000000000000, 1.000000000000000000 ),
 .UNSPECIFIED. ) 
 GEOMETRIC_REPRESENTATION_ITEM ( )  RATIONAL_B_SPLINE_SURFACE ( (
 ( 1.000000000000000000, 1.000000000000000000),
 ( 0.9952954269826590483, 0.8620686068821339365),
 ( 0.9952954269826590483, 0.8620686068821339365),
 ( 1.000000000000000000, 1.000000000000000000) ) ) 
 REPRESENTATION_ITEM ( '' )  SURFACE ( )  );
#61119=VERTEX_POINT ( 'NONE', #4165 ) ;
#61121=CARTESIAN_POINT ( 'NONE',  ( 4.958415959904820092, -44.94704195038539751, 6.554950322689975906 ) ) ;
#61123=CARTESIAN_POINT ( 'NONE',  ( 0.5830082357119558134, -1.293980016005006339, -46.87811483684595970 ) ) ;
#61125=CARTESIAN_POINT ( 'NONE',  ( 4.962356264823593932, 31.50371261889118557, 27.90612278853270922 ) ) ;
#61129=B_SPLINE_CURVE_WITH_KNOTS ( 'NONE', 3,
 ( #5433, #15485, #34592, #33985 ),
 .UNSPECIFIED., .F., .F.,
 ( 4, 4 ),
 ( 8.673617379884035472E-19, 0.004042984057420973693 ),
 .UNSPECIFIED. ) ;
#61134=CARTESIAN_POINT ( 'NONE',  ( 0.9772918015221174759, -12.01962968694840406, 40.14804301506249118 ) ) ;
#61139=CARTESIAN_POINT ( 'NONE',  ( 0.5848930533535030563, 46.45334699384599020, -6.431145734385029122 ) ) ;
#61143=CIRCLE ( 'NONE', #53841, 47.09074272231896430 ) ;
#61144=CARTESIAN_POINT ( 'NONE',  ( 4.956445790443988031, 0.000000000000000000, 0.000000000000000000 ) ) ;
#61146=CARTESIAN_POINT ( 'NONE',  ( 0.6845945791218034371, 11.71498854670100975, -45.42208233959124897 ) ) ;
#61152=CARTESIAN_POINT ( 'NONE',  ( 5.896782393890504181, -18.51439742298342139, 7.857682542699045314 ) ) ;
#61154=EDGE_CURVE ( 'NONE', #50643, #26909, #59233, .T. ) ;
#61166=EDGE_CURVE ( 'NONE', #55841, #35106, #50262, .T. ) ;
#61168=CARTESIAN_POINT ( 'NONE',  ( 0.9754292589017224957, -1.982398212836277818, -41.86164789184748969 ) ) ;
#61178=( BOUNDED_SURFACE ( )  B_SPLINE_SURFACE ( 3, 1, ( 
 ( #53707, #10520 ),
 ( #52492, #34039 ),
 ( #14621, #10838 ),
 ( #39052, #53109 ) ),
 .UNSPECIFIED., .F., .F., .F. ) 
 B_SPLINE_SURFACE_WITH_KNOTS ( ( 4, 4 ),
 ( 2, 2 ),
 ( 0.000000000000000000, 1.000000000000000000 ),
 ( 0.000000000000000000, 1.000000000000000000 ),
 .UNSPECIFIED. ) 
 GEOMETRIC_REPRESENTATION_ITEM ( )  RATIONAL_B_SPLINE_SURFACE ( (
 ( 1.000000000000000000, 1.000000000000000000),
 ( 0.9952954269826590483, 0.8620686068821339365),
 ( 0.9952954269826590483, 0.8620686068821339365),
 ( 1.000000000000000000, 1.000000000000000000) ) ) 
 REPRESENTATION_ITEM ( '' )  SURFACE ( )  );
#61184=CARTESIAN_POINT ( 'NONE',  ( 0.7764139734771252632, -8.679346378251009853, 46.09457036737849478 ) ) ;
#61186=CARTESIAN_POINT ( 'NONE',  ( 0.7764139734771221546, -20.54893558373679596, 42.16374885232933423 ) ) ;
#61187=CARTESIAN_POINT ( 'NONE',  ( 0.5834584762367749367, -38.76579285815412845, 26.39032574811979970 ) ) ;
#61188=DIRECTION ( 'NONE',  ( -1.000000000000000000, 0.000000000000000000, 0.000000000000000000 ) ) ;
#61191=ORIENTED_EDGE ( 'NONE', *, *, #41614, .T. ) ;
#61193=VECTOR ( 'NONE', #57362, 1000.000000000000000 ) ;
#61200=CARTESIAN_POINT ( 'NONE',  ( 0.9762797500689124330, -22.12212327108586152, -35.59405072711710716 ) ) ;
#61207=CARTESIAN_POINT ( 'NONE',  ( 0.5806925824938499181, -29.85799195566266917, -36.16244846134105018 ) ) ;
#61211=CARTESIAN_POINT ( 'NONE',  ( 4.956445790444004018, -40.78973928653763181, -23.53157918788973291 ) ) ;
#61225=CARTESIAN_POINT ( 'NONE',  ( 5.910764540655177868, -4.677486889029990991, 19.56073502893272220 ) ) ;
#61233=CARTESIAN_POINT ( 'NONE',  ( 0.5817216825391123836, -7.350843310970423872, 46.31630441674961673 ) ) ;
#61234=EDGE_CURVE ( 'NONE', #1809, #29343, #23310, .T. ) ;
#61236=EDGE_LOOP ( 'NONE', ( #10127, #16133, #50085, #45040 ) ) ;
#61238=CARTESIAN_POINT ( 'NONE',  ( 0.5830082357119567016, -46.00988774283680982, 9.073161787926713018 ) ) ;
#61241=ORIENTED_EDGE ( 'NONE', *, *, #41401, .T. ) ;
#61246=CARTESIAN_POINT ( 'NONE',  ( 0.5824936645240067490, 46.89462130976617971, 0.3642406538733899413 ) ) ;
#61250=CARTESIAN_POINT ( 'NONE',  ( 5.838029081930957709, -10.96929503790485683, -45.94278642533902968 ) ) ;
#61251=ORIENTED_EDGE ( 'NONE', *, *, #38166, .T. ) ;
#61253=ORIENTED_EDGE ( 'NONE', *, *, #23071, .F. ) ;
#61255=CARTESIAN_POINT ( 'NONE',  ( 4.291220156522060236, 20.72764654176005195, -42.30548033228744487 ) ) ;
#61262=CARTESIAN_POINT ( 'NONE',  ( 4.962356264823596597, -3.779019546647577776, 41.91604238389407300 ) ) ;
#61268=CARTESIAN_POINT ( 'NONE',  ( 0.5806925824938499181, 27.37593026015182218, 38.07598724570208049 ) ) ;
#61269=( BOUNDED_SURFACE ( )  B_SPLINE_SURFACE ( 3, 1, ( 
 ( #29505, #23575 ),
 ( #18900, #42700 ),
 ( #5668, #43956 ),
 ( #59548, #1595 ) ),
 .UNSPECIFIED., .F., .F., .F. ) 
 B_SPLINE_SURFACE_WITH_KNOTS ( ( 4, 4 ),
 ( 2, 2 ),
 ( 0.000000000000000000, 1.000000000000000000 ),
 ( 0.000000000000000000, 1.000000000000000000 ),
 .UNSPECIFIED. ) 
 GEOMETRIC_REPRESENTATION_ITEM ( )  RATIONAL_B_SPLINE_SURFACE ( (
 ( 1.000000000000000000, 1.000000000000000000),
 ( 0.9952954269826590483, 0.8620686068821339365),
 ( 0.9952954269826590483, 0.8620686068821339365),
 ( 1.000000000000000000, 1.000000000000000000) ) ) 
 REPRESENTATION_ITEM ( '' )  SURFACE ( )  );
#61274=CARTESIAN_POINT ( 'NONE',  ( 0.5834584762367738264, -41.93739078247706686, 20.98788325131905452 ) ) ;
#61280=CARTESIAN_POINT ( 'NONE',  ( 5.901463166500145796, 10.81005692193063261, 16.96055835417148927 ) ) ;
#61286=ORIENTED_EDGE ( 'NONE', *, *, #16211, .T. ) ;
#61288=CARTESIAN_POINT ( 'NONE',  ( 5.896782393890504181, 10.82771479451271368, 16.94953330350728748 ) ) ;
#61289=CARTESIAN_POINT ( 'NONE',  ( 0.9788927965476030835, -26.94903577592939925, 32.09495417319448762 ) ) ;
#61292=CARTESIAN_POINT ( 'NONE',  ( 5.894904586330512508, -17.30455939762474671, 10.25093342655779338 ) ) ;
#61307=CARTESIAN_POINT ( 'NONE',  ( 0.8554163680231708922, 46.61139063278411498, -5.346376005279187993 ) ) ;
#61308=CARTESIAN_POINT ( 'NONE',  ( 1.231276596079881047, -21.83837404314779462, -35.78214904347746739 ) ) ;
#61309=CARTESIAN_POINT ( 'NONE',  ( 4.962356264823603702, 0.9708976703223142213, -42.07484944210863631 ) ) ;
#61311=B_SPLINE_CURVE_WITH_KNOTS ( 'NONE', 3,
 ( #18466, #37594, #53198, #53495 ),
 .UNSPECIFIED., .F., .F.,
 ( 4, 4 ),
 ( 0.000000000000000000, 0.002405070305343063371 ),
 .UNSPECIFIED. ) ;
#61317=VERTEX_POINT ( 'NONE', #26376 ) ;
#61318=EDGE_CURVE ( 'NONE', #33684, #4545, #9093, .T. ) ;
#61327=CARTESIAN_POINT ( 'NONE',  ( 4.962356264823602814, -29.56943756613081931, -29.94802096775409339 ) ) ;
#61330=CARTESIAN_POINT ( 'NONE',  ( 0.5830081025819929819, -8.069435828662605559, -46.19649596873491504 ) ) ;
#61334=ORIENTED_EDGE ( 'NONE', *, *, #35820, .F. ) ;
#61343=EDGE_LOOP ( 'NONE', ( #11467, #10610, #60462, #44291 ) ) ;
#61355=ORIENTED_EDGE ( 'NONE', *, *, #53770, .F. ) ;
#61362=( NAMED_UNIT ( * ) PLANE_ANGLE_UNIT ( ) SI_UNIT ( $, .RADIAN. ) );
#61364=( BOUNDED_SURFACE ( )  B_SPLINE_SURFACE ( 3, 1, ( 
 ( #27856, #31948 ),
 ( #36978, #31633 ),
 ( #7812, #56039 ),
 ( #51032, #13158 ) ),
 .UNSPECIFIED., .F., .F., .F. ) 
 B_SPLINE_SURFACE_WITH_KNOTS ( ( 4, 4 ),
 ( 2, 2 ),
 ( 0.000000000000000000, 1.000000000000000000 ),
 ( 0.000000000000000000, 1.000000000000000000 ),
 .UNSPECIFIED. ) 
 GEOMETRIC_REPRESENTATION_ITEM ( )  RATIONAL_B_SPLINE_SURFACE ( (
 ( 1.000000000000000000, 1.000000000000000000),
 ( 0.9729067724841187204, 0.9999501103223794596),
 ( 0.9729067724841187204, 0.9999501103223794596),
 ( 1.000000000000000000, 1.000000000000000000) ) ) 
 REPRESENTATION_ITEM ( '' )  SURFACE ( )  );
#61369=CARTESIAN_POINT ( 'NONE',  ( 4.962356264823603702, 12.05238263218972072, -40.32338863178092225 ) ) ;
#61371=CARTESIAN_POINT ( 'NONE',  ( 0.9787284016396619046, 29.26888682565846977, 29.99447053901143079 ) ) ;
#61377=FACE_OUTER_BOUND ( 'NONE', #9274, .T. ) ;
#61381=CARTESIAN_POINT ( 'NONE',  ( 0.9762797500689124330, 38.38274741215467145, 16.82526333465357382 ) ) ;
#61383=VERTEX_POINT ( 'NONE', #23226 ) ;
#61386=CARTESIAN_POINT ( 'NONE',  ( 0.8560838555295223751, 27.08392101972057731, -38.29926965725677235 ) ) ;
#61387=DIRECTION ( 'NONE',  ( 0.000000000000000000, 0.000000000000000000, 1.000000000000000000 ) ) ;
#61396=CARTESIAN_POINT ( 'NONE',  ( 5.895596859100789899, 8.469463536103054579, -18.24270732712412624 ) ) ;
#61414=CARTESIAN_POINT ( 'NONE',  ( 0.5837157313716018203, 43.21027797204915544, -18.22385637455116481 ) ) ;
#61419=ORIENTED_EDGE ( 'NONE', *, *, #12175, .F. ) ;
#61420=CARTESIAN_POINT ( 'NONE',  ( 0.9784957157296378938, -34.68241884430302235, -23.52579180603076736 ) ) ;
#61425=CARTESIAN_POINT ( 'NONE',  ( 0.6064782688330875304, 45.03780212049427689, 13.07405165103655165 ) ) ;
#61430=CARTESIAN_POINT ( 'NONE',  ( 3.782625744892853525, -41.50499360117703418, -6.676347074655189395 ) ) ;
#61432=EDGE_CURVE ( 'NONE', #61929, #24638, #38309, .T. ) ;
#61435=EDGE_CURVE ( 'NONE', #57834, #52026, #60679, .T. ) ;
#61440=CARTESIAN_POINT ( 'NONE',  ( 4.962356264823598373, -24.61258717641114657, 34.13877780978559429 ) ) ;
#61446=CARTESIAN_POINT ( 'NONE',  ( 0.5797568599927148680, -13.29195561999140018, -44.97276091666135756 ) ) ;
#61454=EDGE_CURVE ( 'NONE', #41141, #12584, #32299, .T. ) ;
#61460=EDGE_LOOP ( 'NONE', ( #45838, #13352, #3692, #16537 ) ) ;
#61463=CARTESIAN_POINT ( 'NONE',  ( 4.962356264823608143, 17.31942680647409460, 38.35717733303029320 ) ) ;
#61467=VERTEX_POINT ( 'NONE', #49807 ) ;
#61477=CARTESIAN_POINT ( 'NONE',  ( 0.9787284016396609054, -39.52800361071009405, 13.92382596417090390 ) ) ;
#61486=FACE_OUTER_BOUND ( 'NONE', #61236, .T. ) ;
#61490=CARTESIAN_POINT ( 'NONE',  ( 1.157644175074337811, 32.37803412471593134, 26.62076598631064783 ) ) ;
#61493=B_SPLINE_CURVE_WITH_KNOTS ( 'NONE', 3,
 ( #11317, #35449, #11634, #30719 ),
 .UNSPECIFIED., .F., .F.,
 ( 4, 4 ),
 ( 0.000000000000000000, 0.004447772540403806783 ),
 .UNSPECIFIED. ) ;
#61508=CARTESIAN_POINT ( 'NONE',  ( 0.8560838555295158248, -24.46533024579895610, -40.02274915652004239 ) ) ;
#61513=CARTESIAN_POINT ( 'NONE',  ( 5.917102823773431552, -17.30871814525818664, 10.24197218409383581 ) ) ;
#61515=CARTESIAN_POINT ( 'NONE',  ( 0.9787464366903563251, -1.223426366651767072, -41.89077727633904402 ) ) ;
#61525=CARTESIAN_POINT ( 'NONE',  ( 0.5837800005270550319, -25.23388577838564828, 39.52829704357589691 ) ) ;
#61528=CARTESIAN_POINT ( 'NONE',  ( 1.092182651088183576, -37.05014944566807600, 19.59713271108671506 ) ) ;
#61533=CARTESIAN_POINT ( 'NONE',  ( 4.291220156522059348, -16.00047830133278381, 44.30997282141206028 ) ) ;
#61540=B_SPLINE_CURVE_WITH_KNOTS ( 'NONE', 3,
 ( #40915, #60581, #36200, #55893 ),
 .UNSPECIFIED., .F., .F.,
 ( 4, 4 ),
 ( 1.734723475976807094E-18, 0.004042984057420974560 ),
 .UNSPECIFIED. ) ;
#61545=B_SPLINE_CURVE_WITH_KNOTS ( 'NONE', 3,
 ( #16141, #15833, #39654, #6377 ),
 .UNSPECIFIED., .F., .F.,
 ( 4, 4 ),
 ( 5.421010862427522170E-19, 0.004446298630425054611 ),
 .UNSPECIFIED. ) ;
#61547=CARTESIAN_POINT ( 'NONE',  ( 0.9790320750461904975, 24.92853536925881031, -33.68835491510091629 ) ) ;
#61549=CARTESIAN_POINT ( 'NONE',  ( 0.5835226383429297226, 46.89572792844976590, -0.1821444667875269929 ) ) ;
#61553=( BOUNDED_SURFACE ( )  B_SPLINE_SURFACE ( 3, 1, ( 
 ( #44478, #30963 ),
 ( #49445, #2439 ),
 ( #49141, #35688 ),
 ( #45092, #58829 ) ),
 .UNSPECIFIED., .F., .F., .F. ) 
 B_SPLINE_SURFACE_WITH_KNOTS ( ( 4, 4 ),
 ( 2, 2 ),
 ( 0.000000000000000000, 1.000000000000000000 ),
 ( 0.000000000000000000, 1.000000000000000000 ),
 .UNSPECIFIED. ) 
 GEOMETRIC_REPRESENTATION_ITEM ( )  RATIONAL_B_SPLINE_SURFACE ( (
 ( 1.000000000000000000, 1.000000000000000000),
 ( 0.7282232189291694135, 0.9929344683865672927),
 ( 0.7282232189291694135, 0.9929344683865672927),
 ( 1.000000000000000000, 1.000000000000000000) ) ) 
 REPRESENTATION_ITEM ( '' )  SURFACE ( )  );
#61561=CARTESIAN_POINT ( 'NONE',  ( 0.9762797500689124330, 4.697980241569248427, -41.64437257103928403 ) ) ;
#61567=DIRECTION ( 'NONE',  ( -0.07500201931887529039, -0.5478996815936019171, -0.8331750332359465494 ) ) ;
#61573=ORIENTED_EDGE ( 'NONE', *, *, #5446, .T. ) ;
#61575=CARTESIAN_POINT ( 'NONE',  ( 3.238018933889920792, -0.7223087070294264000, 13.37481822304147983 ) ) ;
#61577=ORIENTED_EDGE ( 'NONE', *, *, #46331, .T. ) ;
#61578=CARTESIAN_POINT ( 'NONE',  ( 4.956445790443988031, 0.000000000000000000, 0.000000000000000000 ) ) ;
#61583=DIRECTION ( 'NONE',  ( 0.000000000000000000, 0.000000000000000000, 1.000000000000000000 ) ) ;
#61590=DIRECTION ( 'NONE',  ( 0.000000000000000000, 0.000000000000000000, 1.000000000000000000 ) ) ;
#61593=DIRECTION ( 'NONE',  ( -1.000000000000000000, -0.000000000000000000, -0.000000000000000000 ) ) ;
#61595=CARTESIAN_POINT ( 'NONE',  ( 3.238018933889920792, -13.06836926121498443, -2.936872012904941265 ) ) ;
#61598=CARTESIAN_POINT ( 'NONE',  ( 0.5806925824938499181, -7.260877859416734026, -46.33035738103254175 ) ) ;
#61605=CARTESIAN_POINT ( 'NONE',  ( 0.5835871038041874348, 32.50343185804469215, 33.80475366499425860 ) ) ;
#61622=AXIS2_PLACEMENT_3D ( 'NONE', #61110, #36735, #46744 ) ;
#61628=CARTESIAN_POINT ( 'NONE',  ( 4.962356264823608143, 27.50309822711080443, -31.85616401533997077 ) ) ;
#61642=CARTESIAN_POINT ( 'NONE',  ( 0.9789889208857702751, -37.36078624453494257, 18.98701001296773327 ) ) ;
#61649=LINE ( 'NONE', #37585, #7852 ) ;
#61663=ORIENTED_EDGE ( 'NONE', *, *, #47676, .T. ) ;
#61664=EDGE_CURVE ( 'NONE', #24375, #5770, #19081, .T. ) ;
#61667=CARTESIAN_POINT ( 'NONE',  ( 0.5837157313716025975, -41.81444688234194018, -21.23179444855826858 ) ) ;
#61669=LINE ( 'NONE', #28478, #17823 ) ;
#61672=VECTOR ( 'NONE', #25943, 1000.000000000000114 ) ;
#61676=CARTESIAN_POINT ( 'NONE',  ( 5.894904586330512508, 19.71013252676728200, 4.005007845050151616 ) ) ;
#61688=CARTESIAN_POINT ( 'NONE',  ( 5.895596859100789899, 19.71057157537860149, -4.002693016503341639 ) ) ;
#61689=CARTESIAN_POINT ( 'NONE',  ( 3.661921753702024329, 26.36408909118086541, -38.95594858588754761 ) ) ;
#61700=CARTESIAN_POINT ( 'NONE',  ( 1.091591847532194626, -6.200834385736088805, -41.45248658255029994 ) ) ;
#61710=CARTESIAN_POINT ( 'NONE',  ( 5.896278296736517710, -19.93412839397019098, -2.675351339001139195 ) ) ;
#61713=CARTESIAN_POINT ( 'NONE',  ( 5.895881250540457863, -9.669871309367247036, 17.63579514704616358 ) ) ;
#61714=CARTESIAN_POINT ( 'NONE',  ( 5.895596859100789899, 17.94951300836817865, -9.074313526372616678 ) ) ;
#61716=CARTESIAN_POINT ( 'NONE',  ( 0.5837799406558213944, 16.93978989757854592, 43.72970463887332926 ) ) ;
#61725=CARTESIAN_POINT ( 'NONE',  ( 4.962356264823608143, 0.000000000000000000, 0.000000000000000000 ) ) ;
#61726=CARTESIAN_POINT ( 'NONE',  ( 0.5835871038041865466, 11.00424250131069748, -45.58663290783655242 ) ) ;
#61728=CARTESIAN_POINT ( 'NONE',  ( 0.9769922540276045897, -34.29921094923819425, -24.08102330354307341 ) ) ;
#61730=CARTESIAN_POINT ( 'NONE',  ( 4.962356264823603702, 0.9708976703223142213, -42.07484944210863631 ) ) ;
#61735=CARTESIAN_POINT ( 'NONE',  ( 0.9787464366903561030, -41.82650318302786729, 2.622522520517909683 ) ) ;
#61736=CARTESIAN_POINT ( 'NONE',  ( 0.5804410086790514622, 37.14246315962216016, 28.63489623329386191 ) ) ;
#61744=CARTESIAN_POINT ( 'NONE',  ( 0.5835226383429281682, 40.25633451856137413, -24.05556080567755473 ) ) ;
#61745=LINE ( 'NONE', #37369, #59394 ) ;
#61752=ADVANCED_FACE ( 'NONE', ( #17081 ), #49233, .F. ) ;
#61753=CARTESIAN_POINT ( 'NONE',  ( 2.282803330402960906, 15.64995782534825075, 44.28967969540766347 ) ) ;
#61754=CARTESIAN_POINT ( 'NONE',  ( 3.238018933889920792, -10.11627964985467010, 8.778859744499238005 ) ) ;
#61759=VECTOR ( 'NONE', #45140, 999.9999999999998863 ) ;
#61760=CARTESIAN_POINT ( 'NONE',  ( 0.8554163680231738898, 3.785871848716432453, 46.76401017296225149 ) ) ;
#61765=VERTEX_POINT ( 'NONE', #16150 ) ;
#61771=EDGE_LOOP ( 'NONE', ( #3404, #32839, #60591, #56385 ) ) ;
#61778=AXIS2_PLACEMENT_3D ( 'NONE', #27715, #46843, #13629 ) ;
#61782=CARTESIAN_POINT ( 'NONE',  ( 0.9775691876210993447, -39.71209476610986400, 13.38966908767717534 ) ) ;
#61790=CARTESIAN_POINT ( 'NONE',  ( 4.962356264823608143, 0.000000000000000000, 0.000000000000000000 ) ) ;
#61791=CARTESIAN_POINT ( 'NONE',  ( 0.7764139734771250412, -0.6759653311300753975, -46.89971792855448740 ) ) ;
#61794=CARTESIAN_POINT ( 'NONE',  ( 4.962356264823608143, -38.91448554252697534, 16.02805081171152324 ) ) ;
#61798=CARTESIAN_POINT ( 'NONE',  ( 0.5824936645240084143, 37.02860808157328165, -28.77708050830649356 ) ) ;
#61799=ORIENTED_EDGE ( 'NONE', *, *, #18176, .F. ) ;
#61800=CARTESIAN_POINT ( 'NONE',  ( 1.231276596079881047, -7.805643096902013411, 41.18675402191647805 ) ) ;
#61810=EDGE_CURVE ( 'NONE', #10199, #37874, #29475, .T. ) ;
#61818=CARTESIAN_POINT ( 'NONE',  ( 0.9787284016396602393, 41.90824429648411353, -0.1872402601951978218 ) ) ;
#61828=CARTESIAN_POINT ( 'NONE',  ( 4.958415959904820092, -35.33199410137683572, -28.54565022280822006 ) ) ;
#61835=CARTESIAN_POINT ( 'NONE',  ( 5.895596859100789899, 10.81936814621369969, 16.95492424427734690 ) ) ;
#61838=EDGE_CURVE ( 'NONE', #44257, #13798, #16860, .T. ) ;
#61839=ORIENTED_EDGE ( 'NONE', *, *, #29802, .F. ) ;
#61851=CARTESIAN_POINT ( 'NONE',  ( 0.5806925824938499181, 17.36345040154836994, -43.56297685531297503 ) ) ;
#61853=CARTESIAN_POINT ( 'NONE',  ( 4.956445790443998689, -11.44166143952028314, 45.67960632101629415 ) ) ;
#61859=CIRCLE ( 'NONE', #28841, 47.09074272231896430 ) ;
#61866=ORIENTED_EDGE ( 'NONE', *, *, #38672, .T. ) ;
#61869=CARTESIAN_POINT ( 'NONE',  ( 4.960386119450146403, 17.98972314615754087, -39.88491351121305684 ) ) ;
#61871=CARTESIAN_POINT ( 'NONE',  ( 2.282803330402976005, 18.10201666796580255, -43.34528694113895853 ) ) ;
#61881=DIRECTION ( 'NONE',  ( 0.000000000000000000, 0.000000000000000000, 1.000000000000000000 ) ) ;
#61882=ADVANCED_FACE ( 'NONE', ( #60265 ), #31682, .F. ) ;
#61887=CARTESIAN_POINT ( 'NONE',  ( 5.901463166500146684, -19.40182753204446442, -5.299713082558163535 ) ) ;
#61890=ORIENTED_EDGE ( 'NONE', *, *, #1260, .T. ) ;
#61894=AXIS2_PLACEMENT_3D ( 'NONE', #13864, #36749, #9439 ) ;
#61903=CARTESIAN_POINT ( 'NONE',  ( 0.5837800005270561421, 10.87146978434382838, 45.61848751734192575 ) ) ;
#61915=CARTESIAN_POINT ( 'NONE',  ( 4.962356264823608143, 0.000000000000000000, 0.000000000000000000 ) ) ;
#61918=( BOUNDED_SURFACE ( )  B_SPLINE_SURFACE ( 3, 1, ( 
 ( #6305, #39895 ),
 ( #44585, #30139 ),
 ( #39577, #58630 ),
 ( #58954, #15758 ) ),
 .UNSPECIFIED., .F., .F., .F. ) 
 B_SPLINE_SURFACE_WITH_KNOTS ( ( 4, 4 ),
 ( 2, 2 ),
 ( 0.000000000000000000, 1.000000000000000000 ),
 ( 0.000000000000000000, 1.000000000000000000 ),
 .UNSPECIFIED. ) 
 GEOMETRIC_REPRESENTATION_ITEM ( )  RATIONAL_B_SPLINE_SURFACE ( (
 ( 1.000000000000000000, 1.000000000000000000),
 ( 0.7282232189291694135, 0.9929344683865672927),
 ( 0.7282232189291694135, 0.9929344683865672927),
 ( 1.000000000000000000, 1.000000000000000000) ) ) 
 REPRESENTATION_ITEM ( '' )  SURFACE ( )  );
#61924=EDGE_CURVE ( 'NONE', #55528, #30663, #38493, .T. ) ;
#61929=VERTEX_POINT ( 'NONE', #50466 ) ;
#61931=EDGE_CURVE ( 'NONE', #18314, #13524, #56676, .T. ) ;
#61936=VECTOR ( 'NONE', #17135, 999.9999999999998863 ) ;
#61944=DIRECTION ( 'NONE',  ( 0.9990097760809873995, 5.448601141172495260E-18, 0.04449120468829072944 ) ) ;
#61950=CARTESIAN_POINT ( 'NONE',  ( 0.9780303403264775097, -37.25713683229096063, 19.18972038501425814 ) ) ;
#61953=VERTEX_POINT ( 'NONE', #54846 ) ;
#61954=DIRECTION ( 'NONE',  ( -0.07906939808003034253, -0.1737655548591644228, -0.9816076416938430693 ) ) ;
#61955=CARTESIAN_POINT ( 'NONE',  ( 4.291220156522060236, -21.76365521422027882, -41.78196152674308905 ) ) ;
#61957=EDGE_CURVE ( 'NONE', #30850, #56380, #45800, .T. ) ;
#61965=CARTESIAN_POINT ( 'NONE',  ( 0.9772918015221170318, 38.74329897262556699, 15.97791101703945138 ) ) ;
#61966=ORIENTED_EDGE ( 'NONE', *, *, #10650, .T. ) ;
#61968=PRODUCT_DEFINITION ( 'UNKNOWN', '', #50889, #6591 ) ;
#61970=CARTESIAN_POINT ( 'NONE',  ( 0.9789233960466718898, -41.09488416218491125, 8.218711731709811730 ) ) ;
#61972=CARTESIAN_POINT ( 'NONE',  ( 3.376099380956838925, 13.39763462305342756, 0.4601848967830198811 ) ) ;
#61973=CARTESIAN_POINT ( 'NONE',  ( 0.7056313189692619003, -35.34445970792710767, -30.83046888894615734 ) ) ;
ENDSEC;
END-ISO-10303-21;
